ISO-10303-21;
HEADER;
FILE_DESCRIPTION (('STEP AP214'),
    '1' );
FILE_NAME ('Injection Molded Chain Links 9.step',
    '2026-10-08T22:59:04',
    ( '' ),
    ( '' ),
    'SwSTEP 2.0',
    'SolidWorks 2020',
    '' );
FILE_SCHEMA (( 'AUTOMOTIVE_DESIGN' ));
ENDSEC;

DATA;
#28=CIRCLE ( 'NONE', #245740, 0.1000000000000032113 ) ;
#49=ORIENTED_EDGE ( 'NONE', *, *, #170481, .T. ) ;
#55=ORIENTED_EDGE ( 'NONE', *, *, #79678, .T. ) ;
#57=ORIENTED_EDGE ( 'NONE', *, *, #255744, .F. ) ;
#83=AXIS2_PLACEMENT_3D ( 'NONE', #206420, #107313, #246821 ) ;
#114=DIRECTION ( 'NONE',  ( 0.000000000000000000, -0.4088369013363280513, 0.9126074666063769270 ) ) ;
#123=CARTESIAN_POINT ( 'NONE',  ( -23.15000000000000213, 54.26389919992384137, -237.1169412515656632 ) ) ;
#127=DIRECTION ( 'NONE',  ( 0.000000000000000000, -0.9126074666065964180, -0.4088369013358383874 ) ) ;
#139=ORIENTED_EDGE ( 'NONE', *, *, #116118, .F. ) ;
#155=CIRCLE ( 'NONE', #224998, 12.77499999999999503 ) ;
#220=CIRCLE ( 'NONE', #212623, 0.1000000000000024342 ) ;
#222=ORIENTED_EDGE ( 'NONE', *, *, #184474, .T. ) ;
#223=EDGE_CURVE ( 'NONE', #25855, #57391, #222711, .T. ) ;
#226=LINE ( 'NONE', #155042, #92913 ) ;
#236=CARTESIAN_POINT ( 'NONE',  ( 21.00000000000000000, 51.97441255244040548, -232.0063394385699667 ) ) ;
#256=CARTESIAN_POINT ( 'NONE',  ( 18.49999999999999289, 55.04793976901535757, -229.8170162380219210 ) ) ;
#258=DIRECTION ( 'NONE',  ( 0.000000000000000000, -0.2818822000686205809, 0.9594490217226104845 ) ) ;
#263=VECTOR ( 'NONE', #242147, 1000.000000000000000 ) ;
#307=FACE_OUTER_BOUND ( 'NONE', #226701, .T. ) ;
#375=CARTESIAN_POINT ( 'NONE',  ( -23.15000000000000213, 54.09940989982483472, -238.8890605415484174 ) ) ;
#391=ORIENTED_EDGE ( 'NONE', *, *, #246071, .F. ) ;
#414=CARTESIAN_POINT ( 'NONE',  ( -21.05000000000000071, 56.46250644710310951, -240.6794019422471251 ) ) ;
#443=AXIS2_PLACEMENT_3D ( 'NONE', #84004, #106171, #207893 ) ;
#447=B_SPLINE_CURVE_WITH_KNOTS ( 'NONE', 3,
 ( #104583, #22530, #181601, #82451, #44648, #185439, #202431, #102011 ),
 .UNSPECIFIED., .F., .F.,
 ( 4, 2, 2, 4 ),
 ( 0.000000000000000000, 0.0002114466876441559802, 0.0003171700314662930322, 0.0004228933752884300843 ),
 .UNSPECIFIED. ) ;
#451=DIRECTION ( 'NONE',  ( 0.000000000000000000, 0.9126074666063545004, 0.4088369013363783999 ) ) ;
#461=FACE_OUTER_BOUND ( 'NONE', #189351, .T. ) ;
#477=CARTESIAN_POINT ( 'NONE',  ( -20.94999999999999929, 44.43513953521873106, -247.3415577889845736 ) ) ;
#515=EDGE_CURVE ( 'NONE', #206460, #129055, #226257, .T. ) ;
#574=CARTESIAN_POINT ( 'NONE',  ( 20.94999999999999574, 44.06250559941687328, -258.7395785465160429 ) ) ;
#595=ORIENTED_EDGE ( 'NONE', *, *, #102002, .T. ) ;
#607=EDGE_LOOP ( 'NONE', ( #13906, #218176, #236632, #54115 ) ) ;
#634=ORIENTED_EDGE ( 'NONE', *, *, #116099, .T. ) ;
#665=FACE_OUTER_BOUND ( 'NONE', #166817, .T. ) ;
#668=SURFACE_STYLE_USAGE ( .BOTH. , #22864 ) ;
#675=AXIS2_PLACEMENT_3D ( 'NONE', #77860, #154878, #178290 ) ;
#690=DIRECTION ( 'NONE',  ( 1.000000000000000000, 0.000000000000000000, -0.000000000000000000 ) ) ;
#705=EDGE_CURVE ( 'NONE', #15348, #228584, #142870, .T. ) ;
#710=DIRECTION ( 'NONE',  ( 1.000000000000000000, 0.000000000000000000, 0.000000000000000000 ) ) ;
#735=ORIENTED_EDGE ( 'NONE', *, *, #173041, .F. ) ;
#744=ADVANCED_FACE ( 'NONE', ( #222276 ), #93020, .T. ) ;
#755=EDGE_LOOP ( 'NONE', ( #182777, #183423, #9876, #121194 ) ) ;
#782=VERTEX_POINT ( 'NONE', #38545 ) ;
#785=VERTEX_POINT ( 'NONE', #120670 ) ;
#797=EDGE_CURVE ( 'NONE', #139213, #218531, #126331, .T. ) ;
#856=DIRECTION ( 'NONE',  ( 2.465190328815662439E-32, -0.9126074666063770380, -0.4088369013363282178 ) ) ;
#879=CARTESIAN_POINT ( 'NONE',  ( -18.59999999999999787, 77.44184265367995579, -241.6694879557322508 ) ) ;
#900=ORIENTED_EDGE ( 'NONE', *, *, #233229, .T. ) ;
#929=CARTESIAN_POINT ( 'NONE',  ( 22.59999999999999432, 31.76322370622491320, -238.8696546380523671 ) ) ;
#930=VECTOR ( 'NONE', #157455, 1000.000000000000000 ) ;
#932=VERTEX_POINT ( 'NONE', #64520 ) ;
#942=CARTESIAN_POINT ( 'NONE',  ( 21.13498764882293557, 34.00176438950338564, -243.6238902785767095 ) ) ;
#965=EDGE_CURVE ( 'NONE', #227768, #157652, #25810, .T. ) ;
#973=VERTEX_POINT ( 'NONE', #10661 ) ;
#979=CARTESIAN_POINT ( 'NONE',  ( -20.54999999999999716, 50.16665896658852120, -238.7333021241242079 ) ) ;
#1001=ORIENTED_EDGE ( 'NONE', *, *, #105577, .T. ) ;
#1007=ORIENTED_EDGE ( 'NONE', *, *, #156845, .F. ) ;
#1040=LINE ( 'NONE', #115896, #206521 ) ;
#1071=ORIENTED_EDGE ( 'NONE', *, *, #163341, .T. ) ;
#1108=EDGE_CURVE ( 'NONE', #224475, #57327, #209152, .T. ) ;
#1132=CARTESIAN_POINT ( 'NONE',  ( -23.15000000000000213, 61.88149656937975607, -248.1136133839584090 ) ) ;
#1161=AXIS2_PLACEMENT_3D ( 'NONE', #77695, #114274, #157280 ) ;
#1177=CIRCLE ( 'NONE', #121826, 0.6000000000000081934 ) ;
#1193=ORIENTED_EDGE ( 'NONE', *, *, #64693, .T. ) ;
#1196=CARTESIAN_POINT ( 'NONE',  ( -18.50000000000000000, 51.33926024308902925, -230.0993571250899379 ) ) ;
#1197=AXIS2_PLACEMENT_3D ( 'NONE', #36958, #101994, #116467 ) ;
#1248=AXIS2_PLACEMENT_3D ( 'NONE', #185662, #63124, #162264 ) ;
#1251=DIRECTION ( 'NONE',  ( -0.7071067811864931718, -0.2890913453341744099, 0.6453109281989217738 ) ) ;
#1269=ORIENTED_EDGE ( 'NONE', *, *, #30961, .F. ) ;
#1313=DIRECTION ( 'NONE',  ( 0.000000000000000000, 0.9126074666064236673, 0.4088369013362239679 ) ) ;
#1359=FACE_OUTER_BOUND ( 'NONE', #222216, .T. ) ;
#1392=CARTESIAN_POINT ( 'NONE',  ( -21.14999999999999858, 30.94729882110367569, -252.1099006007311232 ) ) ;
#1408=AXIS2_PLACEMENT_3D ( 'NONE', #143754, #31253, #208582 ) ;
#1411=ORIENTED_EDGE ( 'NONE', *, *, #194967, .F. ) ;
#1429=EDGE_LOOP ( 'NONE', ( #115752, #177221, #179062, #191512 ) ) ;
#1431=CIRCLE ( 'NONE', #64472, 11.79999999999999538 ) ;
#1440=CARTESIAN_POINT ( 'NONE',  ( -20.85000000000000142, 67.67657779757796277, -227.9615671787948372 ) ) ;
#1444=EDGE_LOOP ( 'NONE', ( #137862, #189832, #184078, #139307 ) ) ;
#1525=ORIENTED_EDGE ( 'NONE', *, *, #153889, .T. ) ;
#1543=CIRCLE ( 'NONE', #155719, 11.89999999999999858 ) ;
#1590=CARTESIAN_POINT ( 'NONE',  ( 18.59999999999999432, 43.52285900727589762, -245.0935880436369985 ) ) ;
#1599=CARTESIAN_POINT ( 'NONE',  ( -20.64999999999999858, 36.65892442174472876, -249.5511627012454596 ) ) ;
#1615=VERTEX_POINT ( 'NONE', #163984 ) ;
#1616=CARTESIAN_POINT ( 'NONE',  ( 18.59999999999999076, 51.87818942736608818, -231.5469534541122414 ) ) ;
#1622=AXIS2_PLACEMENT_3D ( 'NONE', #232633, #14868, #177796 ) ;
#1625=CARTESIAN_POINT ( 'NONE',  ( -18.59999999999999787, 64.02438395623025258, -266.2629958759080182 ) ) ;
#1655=AXIS2_PLACEMENT_3D ( 'NONE', #121304, #200804, #23483 ) ;
#1678=CARTESIAN_POINT ( 'NONE',  ( 23.24999999999999645, 36.65892442174472876, -249.5511627012454596 ) ) ;
#1697=CIRCLE ( 'NONE', #193452, 11.90000000000000213 ) ;
#1720=ORIENTED_EDGE ( 'NONE', *, *, #76106, .T. ) ;
#1744=CARTESIAN_POINT ( 'NONE',  ( 21.11833042828143192, 34.01722704040963663, -243.6717221766632804 ) ) ;
#1749=AXIS2_PLACEMENT_3D ( 'NONE', #28287, #25688, #229029 ) ;
#1752=ORIENTED_EDGE ( 'NONE', *, *, #166734, .T. ) ;
#1779=CARTESIAN_POINT ( 'NONE',  ( 21.05000000000000071, 40.72908339264471067, -238.0561209609712705 ) ) ;
#1782=CARTESIAN_POINT ( 'NONE',  ( -18.50000000000000000, 52.17883100310857003, -232.4626431718731396 ) ) ;
#1788=CARTESIAN_POINT ( 'NONE',  ( -21.05000000000000782, 34.10431353847246072, -243.7569376156651515 ) ) ;
#1827=VERTEX_POINT ( 'NONE', #123248 ) ;
#1840=CIRCLE ( 'NONE', #255900, 0.09999999999999939493 ) ;
#1847=VERTEX_POINT ( 'NONE', #201490 ) ;
#1862=EDGE_CURVE ( 'NONE', #182190, #197418, #184379, .T. ) ;
#1866=VECTOR ( 'NONE', #230453, 1000.000000000000000 ) ;
#1874=CARTESIAN_POINT ( 'NONE',  ( -21.08479644141222664, 34.01140125657141766, -243.7845722631506646 ) ) ;
#1892=CIRCLE ( 'NONE', #81008, 0.4999999999999944489 ) ;
#1972=CIRCLE ( 'NONE', #147752, 0.4999999999999944489 ) ;
#1983=EDGE_CURVE ( 'NONE', #206700, #26858, #206638, .T. ) ;
#2011=DIRECTION ( 'NONE',  ( -1.000000000000000000, -0.000000000000000000, 0.000000000000000000 ) ) ;
#2012=ORIENTED_EDGE ( 'NONE', *, *, #116816, .T. ) ;
#2024=VERTEX_POINT ( 'NONE', #17423 ) ;
#2074=DIRECTION ( 'NONE',  ( -1.000000000000000000, 0.000000000000000000, 0.000000000000000000 ) ) ;
#2077=CARTESIAN_POINT ( 'NONE',  ( 20.84451136049691655, 39.15603001675818007, -236.7953489976115407 ) ) ;
#2086=EDGE_CURVE ( 'NONE', #146851, #82665, #184745, .T. ) ;
#2091=EDGE_CURVE ( 'NONE', #32455, #139213, #97225, .T. ) ;
#2146=ORIENTED_EDGE ( 'NONE', *, *, #84330, .T. ) ;
#2149=ORIENTED_EDGE ( 'NONE', *, *, #223484, .T. ) ;
#2176=CARTESIAN_POINT ( 'NONE',  ( -18.48179518609297389, 77.41031392689789925, -241.7248553661750918 ) ) ;
#2191=EDGE_CURVE ( 'NONE', #47266, #177428, #26568, .T. ) ;
#2192=DIRECTION ( 'NONE',  ( 0.000000000000000000, 0.9126074666063660468, 0.4088369013363524762 ) ) ;
#2211=CARTESIAN_POINT ( 'NONE',  ( -21.05000000000000071, 43.57281345108133053, -239.9888335660389487 ) ) ;
#2212=DIRECTION ( 'NONE',  ( -0.000000000000000000, -0.9126074666063770380, -0.4088369013363281068 ) ) ;
#2213=CARTESIAN_POINT ( 'NONE',  ( -23.15000000000000213, 54.12082040172526831, -247.0224274369251134 ) ) ;
#2218=CYLINDRICAL_SURFACE ( 'NONE', #153849, 0.09999999999999609201 ) ;
#2239=EDGE_CURVE ( 'NONE', #9664, #124376, #197236, .T. ) ;
#2241=CARTESIAN_POINT ( 'NONE',  ( 20.94999999999999574, 44.06843597547144498, -258.9974126733343951 ) ) ;
#2251=DIRECTION ( 'NONE',  ( 0.000000000000000000, 0.9126074666063660468, 0.4088369013363524762 ) ) ;
#2253=VERTEX_POINT ( 'NONE', #414 ) ;
#2256=DIRECTION ( 'NONE',  ( 0.000000000000000000, 0.9126074666063660468, 0.4088369013363524762 ) ) ;
#2259=ORIENTED_EDGE ( 'NONE', *, *, #44511, .F. ) ;
#2277=EDGE_CURVE ( 'NONE', #149628, #150106, #83774, .T. ) ;
#2299=DIRECTION ( 'NONE',  ( 0.000000000000000000, -0.9126074666063773710, -0.4088369013363274962 ) ) ;
#2314=CARTESIAN_POINT ( 'NONE',  ( -20.64999999999999858, 61.88149656937975607, -248.1136133839584090 ) ) ;
#2335=DIRECTION ( 'NONE',  ( 0.000000000000000000, 0.5859227990963212784, 0.8103668758649578141 ) ) ;
#2339=AXIS2_PLACEMENT_3D ( 'NONE', #85200, #109930, #4409 ) ;
#2343=ORIENTED_EDGE ( 'NONE', *, *, #155700, .F. ) ;
#2361=DIRECTION ( 'NONE',  ( -1.000000000000000000, -0.000000000000000000, 0.000000000000000000 ) ) ;
#2403=B_SPLINE_CURVE_WITH_KNOTS ( 'NONE', 3,
 ( #238427, #53691, #151540, #172404 ),
 .UNSPECIFIED., .F., .F.,
 ( 4, 4 ),
 ( 0.000000000000000000, 0.0002118541922231967595 ),
 .UNSPECIFIED. ) ;
#2417=CARTESIAN_POINT ( 'NONE',  ( -20.91682497891423154, 68.08564185115264422, -224.1612363371343122 ) ) ;
#2425=AXIS2_PLACEMENT_3D ( 'NONE', #153513, #135160, #16531 ) ;
#2444=AXIS2_PLACEMENT_3D ( 'NONE', #49428, #91120, #185088 ) ;
#2457=AXIS2_PLACEMENT_3D ( 'NONE', #232503, #133388, #212919 ) ;
#2470=DIRECTION ( 'NONE',  ( 1.000000000000000000, 0.000000000000000000, -0.000000000000000000 ) ) ;
#2479=LINE ( 'NONE', #242382, #193880 ) ;
#2482=VECTOR ( 'NONE', #191935, 1000.000000000000000 ) ;
#2511=ADVANCED_FACE ( 'NONE', ( #122524 ), #134841, .F. ) ;
#2518=ADVANCED_FACE ( 'NONE', ( #22149 ), #239113, .F. ) ;
#2526=CARTESIAN_POINT ( 'NONE',  ( 20.46382478191414833, 40.81860725232441922, -237.9338882589013053 ) ) ;
#2530=TOROIDAL_SURFACE ( 'NONE', #143999, 0.4000000000000009104, 0.1000000000000000056 ) ;
#2573=ORIENTED_EDGE ( 'NONE', *, *, #145484, .F. ) ;
#2643=ORIENTED_EDGE ( 'NONE', *, *, #100367, .F. ) ;
#2651=CARTESIAN_POINT ( 'NONE',  ( -23.15000000000000213, 36.65892442174472876, -249.5511627012454596 ) ) ;
#2652=ADVANCED_FACE ( 'NONE', ( #85757 ), #246160, .T. ) ;
#2655=ORIENTED_EDGE ( 'NONE', *, *, #161876, .T. ) ;
#2658=CARTESIAN_POINT ( 'NONE',  ( -18.50000000000000711, 38.29773864426884700, -236.0513742605307925 ) ) ;
#2665=CIRCLE ( 'NONE', #36012, 6.258578643762701788 ) ;
#2668=ORIENTED_EDGE ( 'NONE', *, *, #5102, .F. ) ;
#2697=VERTEX_POINT ( 'NONE', #109196 ) ;
#2702=ORIENTED_EDGE ( 'NONE', *, *, #97833, .T. ) ;
#2728=CARTESIAN_POINT ( 'NONE',  ( 21.05000000000000071, 67.23127455305835554, -235.8551265064784559 ) ) ;
#2741=ORIENTED_EDGE ( 'NONE', *, *, #20241, .F. ) ;
#2748=FACE_OUTER_BOUND ( 'NONE', #33714, .T. ) ;
#2756=CIRCLE ( 'NONE', #211066, 4.049999999999999822 ) ;
#2783=EDGE_CURVE ( 'NONE', #47266, #80413, #231741, .T. ) ;
#2789=VERTEX_POINT ( 'NONE', #15265 ) ;
#2794=CARTESIAN_POINT ( 'NONE',  ( -23.25000000000000000, 25.97741635855165754, -254.4468634167653249 ) ) ;
#2816=DIRECTION ( 'NONE',  ( 1.000000000000000000, -1.207181226542539700E-16, 2.694675058168174199E-16 ) ) ;
#2845=ADVANCED_FACE ( 'NONE', ( #118198 ), #157359, .F. ) ;
#2859=ORIENTED_EDGE ( 'NONE', *, *, #236922, .T. ) ;
#2876=DIRECTION ( 'NONE',  ( 0.000000000000000000, 0.9126074666063561658, 0.4088369013363748472 ) ) ;
#2944=ADVANCED_FACE ( 'NONE', ( #206717 ), #245848, .T. ) ;
#2959=EDGE_LOOP ( 'NONE', ( #24213, #221751, #38225, #124983 ) ) ;
#2985=ORIENTED_EDGE ( 'NONE', *, *, #132465, .F. ) ;
#3032=CARTESIAN_POINT ( 'NONE',  ( 21.12802099929860944, 44.24690014139965655, -236.5304528060606231 ) ) ;
#3038=EDGE_CURVE ( 'NONE', #49355, #114960, #205984, .T. ) ;
#3050=CIRCLE ( 'NONE', #148844, 0.09999999999999108213 ) ;
#3073=AXIS2_PLACEMENT_3D ( 'NONE', #51849, #131403, #210956 ) ;
#3093=CARTESIAN_POINT ( 'NONE',  ( -18.59999999999999787, 46.62132166459547733, -243.0426574061995950 ) ) ;
#3102=EDGE_CURVE ( 'NONE', #44054, #24915, #254779, .T. ) ;
#3113=CIRCLE ( 'NONE', #182211, 12.97499999999999787 ) ;
#3155=VERTEX_POINT ( 'NONE', #90603 ) ;
#3204=ORIENTED_EDGE ( 'NONE', *, *, #117094, .T. ) ;
#3229=CARTESIAN_POINT ( 'NONE',  ( -20.54999999999999716, 62.04148992963929743, -247.7470044306132024 ) ) ;
#3244=ORIENTED_EDGE ( 'NONE', *, *, #4230, .F. ) ;
#3270=DIRECTION ( 'NONE',  ( 0.000000000000000000, 0.9126074666063772600, 0.4088369013363274962 ) ) ;
#3279=CARTESIAN_POINT ( 'NONE',  ( 22.49999999999999645, 25.99095500300091643, -254.2329670263966364 ) ) ;
#3280=LINE ( 'NONE', #159827, #249424 ) ;
#3283=CARTESIAN_POINT ( 'NONE',  ( -21.05000000000000071, 43.48442877397276618, -245.2193771921251084 ) ) ;
#3285=DIRECTION ( 'NONE',  ( 0.7071067811864846231, 0.2890913453341779626, -0.6453109281989296564 ) ) ;
#3302=ORIENTED_EDGE ( 'NONE', *, *, #217551, .F. ) ;
#3305=CARTESIAN_POINT ( 'NONE',  ( -18.59999999999999787, 47.89822068137787170, -246.3100470504847692 ) ) ;
#3320=ORIENTED_EDGE ( 'NONE', *, *, #171838, .T. ) ;
#3325=CARTESIAN_POINT ( 'NONE',  ( 18.49999999999999289, 53.32357432685029153, -235.0179440783709879 ) ) ;
#3346=ORIENTED_EDGE ( 'NONE', *, *, #240068, .T. ) ;
#3348=ORIENTED_EDGE ( 'NONE', *, *, #224270, .F. ) ;
#3358=CARTESIAN_POINT ( 'NONE',  ( 20.41140022480496796, 39.35226318247610067, -236.9372322472320320 ) ) ;
#3362=DIRECTION ( 'NONE',  ( 1.000000000000000000, 0.000000000000000000, 0.000000000000000000 ) ) ;
#3394=ORIENTED_EDGE ( 'NONE', *, *, #60215, .F. ) ;
#3399=ORIENTED_EDGE ( 'NONE', *, *, #228972, .F. ) ;
#3400=ORIENTED_EDGE ( 'NONE', *, *, #247327, .T. ) ;
#3401=ORIENTED_EDGE ( 'NONE', *, *, #73318, .T. ) ;
#3431=EDGE_LOOP ( 'NONE', ( #63263, #200596, #67160, #172659 ) ) ;
#3450=TOROIDAL_SURFACE ( 'NONE', #240798, 0.2000000000000000111, 0.1000000000000000056 ) ;
#3453=EDGE_CURVE ( 'NONE', #117897, #214500, #203837, .T. ) ;
#3457=CARTESIAN_POINT ( 'NONE',  ( -21.05000000000000071, 34.01125473724786730, -243.8802146427611888 ) ) ;
#3459=CARTESIAN_POINT ( 'NONE',  ( 18.49999999999999645, 23.98305617022077030, -253.3362246115443099 ) ) ;
#3467=CARTESIAN_POINT ( 'NONE',  ( -18.37151313414733522, 77.36519577919750645, -241.8028021193905204 ) ) ;
#3500=LINE ( 'NONE', #242117, #129013 ) ;
#3510=CARTESIAN_POINT ( 'NONE',  ( 20.94560253601876809, 56.04839098492278993, -227.9897245711965752 ) ) ;
#3525=CIRCLE ( 'NONE', #170183, 12.87499999999999112 ) ;
#3552=EDGE_CURVE ( 'NONE', #140123, #187124, #76972, .T. ) ;
#3599=ORIENTED_EDGE ( 'NONE', *, *, #207278, .T. ) ;
#3603=ADVANCED_FACE ( 'NONE', ( #73359 ), #209701, .T. ) ;
#3642=SPHERICAL_SURFACE ( 'NONE', #149609, 0.1000000000000000056 ) ;
#3648=CIRCLE ( 'NONE', #103591, 0.09999999999999609201 ) ;
#3658=DIRECTION ( 'NONE',  ( 0.000000000000000000, 0.4088369013363283844, -0.9126074666063769270 ) ) ;
#3679=DIRECTION ( 'NONE',  ( 0.000000000000000000, 0.9126074666063771490, 0.4088369013363281623 ) ) ;
#3693=CARTESIAN_POINT ( 'NONE',  ( -20.64999999999999858, 62.08148826970418099, -247.6553521922769221 ) ) ;
#3737=CARTESIAN_POINT ( 'NONE',  ( 18.46932045258622068, 77.27562233161933136, -241.9521456325934139 ) ) ;
#3742=CARTESIAN_POINT ( 'NONE',  ( 22.14074124539698829, 33.54719148015350072, -242.8474189545858053 ) ) ;
#3747=DIRECTION ( 'NONE',  ( 0.000000000000000000, 0.9126074666063769270, 0.4088369013363280513 ) ) ;
#3758=EDGE_LOOP ( 'NONE', ( #143290, #59485 ) ) ;
#3864=CARTESIAN_POINT ( 'NONE',  ( -18.45140287520616695, 77.16972416950922309, -241.7973009820151162 ) ) ;
#3898=VERTEX_POINT ( 'NONE', #75297 ) ;
#3923=CIRCLE ( 'NONE', #78891, 7.799999999999999822 ) ;
#3932=DIRECTION ( 'NONE',  ( -1.000000000000000000, 0.000000000000000000, 0.000000000000000000 ) ) ;
#3942=CARTESIAN_POINT ( 'NONE',  ( 21.05000000000000071, 44.06843597547144498, -258.9974126733343951 ) ) ;
#3971=CYLINDRICAL_SURFACE ( 'NONE', #113661, 0.09999999999999609201 ) ;
#3984=TOROIDAL_SURFACE ( 'NONE', #49779, 1.900000000000002576, 0.1000000000000000056 ) ;
#3985=CARTESIAN_POINT ( 'NONE',  ( -18.59999999999999787, 48.05114133249968944, -246.4758750954581785 ) ) ;
#3986=CARTESIAN_POINT ( 'NONE',  ( -18.50000000000000000, 51.38014393322265505, -230.1906178717505611 ) ) ;
#4018=CARTESIAN_POINT ( 'NONE',  ( 21.05000000000000426, 34.11496337544747348, -243.6628028815440530 ) ) ;
#4049=CYLINDRICAL_SURFACE ( 'NONE', #224627, 0.09999999999999771572 ) ;
#4109=CARTESIAN_POINT ( 'NONE',  ( -21.05000000000000071, 69.29728574394107454, -247.8047749431123918 ) ) ;
#4111=DIRECTION ( 'NONE',  ( 1.000000000000000000, -0.000000000000000000, -0.000000000000000000 ) ) ;
#4121=CARTESIAN_POINT ( 'NONE',  ( 21.05000000000000071, 43.57568952063339651, -245.1784935019914826 ) ) ;
#4128=CARTESIAN_POINT ( 'NONE',  ( -18.40000000000000213, 46.91436717984746707, -255.3877622108296634 ) ) ;
#4178=DIRECTION ( 'NONE',  ( 0.000000000000000000, 0.9126074666063769270, 0.4088369013363280513 ) ) ;
#4230=EDGE_CURVE ( 'NONE', #108499, #179534, #145500, .T. ) ;
#4240=CARTESIAN_POINT ( 'NONE',  ( -18.59999999999999787, 43.52285900727589762, -245.0935880436369985 ) ) ;
#4258=CARTESIAN_POINT ( 'NONE',  ( -21.02374657821576065, 56.16603649953788135, -228.1013850333971504 ) ) ;
#4261=CIRCLE ( 'NONE', #137536, 0.4999999999999944489 ) ;
#4269=EDGE_LOOP ( 'NONE', ( #127506, #27287, #231040, #171760 ) ) ;
#4314=CARTESIAN_POINT ( 'NONE',  ( 21.04999999999897042, 34.03633519070044855, -243.8225528959771680 ) ) ;
#4315=DIRECTION ( 'NONE',  ( 0.000000000000000000, 0.9126074666063660468, 0.4088369013363524762 ) ) ;
#4343=CARTESIAN_POINT ( 'NONE',  ( 21.05000000000000071, 40.81669639643743608, -238.0718206589051533 ) ) ;
#4366=VERTEX_POINT ( 'NONE', #252291 ) ;
#4374=DIRECTION ( 'NONE',  ( -1.000000000000000000, -0.000000000000000000, -0.000000000000000000 ) ) ;
#4376=VERTEX_POINT ( 'NONE', #177924 ) ;
#4380=ORIENTED_EDGE ( 'NONE', *, *, #156821, .T. ) ;
#4394=ORIENTED_EDGE ( 'NONE', *, *, #30246, .F. ) ;
#4395=DIRECTION ( 'NONE',  ( -5.603264701231745086E-32, 0.9126074666063770380, 0.4088369013363283289 ) ) ;
#4409=DIRECTION ( 'NONE',  ( 0.000000000000000000, -0.9126074666063660468, -0.4088369013363524762 ) ) ;
#4429=CARTESIAN_POINT ( 'NONE',  ( -20.54999999999999716, 49.53130139001177668, -254.0846532093228802 ) ) ;
#4474=EDGE_LOOP ( 'NONE', ( #236923, #257024, #23491, #250902 ) ) ;
#4502=ADVANCED_FACE ( 'NONE', ( #239168 ), #136558, .F. ) ;
#4516=ADVANCED_FACE ( 'NONE', ( #147781 ), #243006, .F. ) ;
#4540=AXIS2_PLACEMENT_3D ( 'NONE', #92996, #130840, #50020 ) ;
#4542=AXIS2_PLACEMENT_3D ( 'NONE', #211607, #72103, #195906 ) ;
#4545=AXIS2_PLACEMENT_3D ( 'NONE', #30449, #113816, #149115 ) ;
#4564=CARTESIAN_POINT ( 'NONE',  ( 21.14999999999999503, 44.10931966560507789, -259.0886734199950183 ) ) ;
#4570=AXIS2_PLACEMENT_3D ( 'NONE', #158414, #237910, #257415 ) ;
#4587=CYLINDRICAL_SURFACE ( 'NONE', #47816, 11.74999999999999822 ) ;
#4597=VERTEX_POINT ( 'NONE', #113770 ) ;
#4605=TOROIDAL_SURFACE ( 'NONE', #196159, 0.2000000000000000111, 0.1000000000000000056 ) ;
#4642=CARTESIAN_POINT ( 'NONE',  ( -20.54999999999999716, 67.23127455305835554, -235.8551265064784559 ) ) ;
#4653=FACE_OUTER_BOUND ( 'NONE', #73563, .T. ) ;
#4661=ORIENTED_EDGE ( 'NONE', *, *, #26163, .T. ) ;
#4666=CIRCLE ( 'NONE', #79505, 4.000000000000002665 ) ;
#4709=DIRECTION ( 'NONE',  ( 1.000000000000000000, 0.000000000000000000, 0.000000000000000000 ) ) ;
#4711=DIRECTION ( 'NONE',  ( 8.673617379884089115E-15, -0.9126074666063771490, -0.4088369013363281623 ) ) ;
#4719=AXIS2_PLACEMENT_3D ( 'NONE', #81751, #60931, #23123 ) ;
#4749=CARTESIAN_POINT ( 'NONE',  ( -21.05000000000000071, 44.15969672213208952, -258.9565289832007693 ) ) ;
#4765=AXIS2_PLACEMENT_3D ( 'NONE', #235255, #93177, #56589 ) ;
#4777=ORIENTED_EDGE ( 'NONE', *, *, #127089, .F. ) ;
#4795=AXIS2_PLACEMENT_3D ( 'NONE', #2213, #144278, #204268 ) ;
#4808=CARTESIAN_POINT ( 'NONE',  ( 20.04142135623730070, 51.28888318656201761, -230.2315015618842153 ) ) ;
#4813=CYLINDRICAL_SURFACE ( 'NONE', #8136, 0.09999999999999939493 ) ;
#4819=AXIS2_PLACEMENT_3D ( 'NONE', #225635, #224375, #10480 ) ;
#4832=CARTESIAN_POINT ( 'NONE',  ( 23.14999999999999858, 54.32225538558145672, -236.1594012422037281 ) ) ;
#4837=DIRECTION ( 'NONE',  ( 0.000000000000000000, 0.9126074666063777041, 0.4088369013363266080 ) ) ;
#4919=ORIENTED_EDGE ( 'NONE', *, *, #101395, .T. ) ;
#4943=CARTESIAN_POINT ( 'NONE',  ( -21.05000000000000071, 36.65892442174472876, -249.5511627012454596 ) ) ;
#4944=CARTESIAN_POINT ( 'NONE',  ( -21.14999999999999858, 34.01125473725046078, -243.8802146427659352 ) ) ;
#4959=CARTESIAN_POINT ( 'NONE',  ( -18.59999999999999787, 25.52560498759422103, -248.6860249505299407 ) ) ;
#5018=DIRECTION ( 'NONE',  ( 0.000000000000000000, 0.5859227990963212784, 0.8103668758649578141 ) ) ;
#5076=DIRECTION ( 'NONE',  ( -0.000000000000000000, 0.4088369013363276072, -0.9126074666063772600 ) ) ;
#5086=CARTESIAN_POINT ( 'NONE',  ( 20.95035502843362707, 39.28946691834322280, -236.8917208353130093 ) ) ;
#5089=ADVANCED_FACE ( 'NONE', ( #220296 ), #92822, .T. ) ;
#5102=EDGE_CURVE ( 'NONE', #104336, #84696, #96887, .T. ) ;
#5125=CARTESIAN_POINT ( 'NONE',  ( -21.30740335185486245, 30.63482136116474663, -252.1414780222814898 ) ) ;
#5126=VECTOR ( 'NONE', #238340, 1000.000000000000114 ) ;
#5152=CARTESIAN_POINT ( 'NONE',  ( -21.08621493067320785, 30.84153651989748823, -252.0957046748300456 ) ) ;
#5153=CARTESIAN_POINT ( 'NONE',  ( 23.24999999999999645, 65.63681063784667913, -232.2959573867136100 ) ) ;
#5159=DIRECTION ( 'NONE',  ( 0.000000000000000000, 0.9126074666063773710, 0.4088369013363269966 ) ) ;
#5178=EDGE_CURVE ( 'NONE', #81533, #219794, #242675, .T. ) ;
#5185=CARTESIAN_POINT ( 'NONE',  ( -23.15000000000000213, 56.16603649944111254, -228.1013850343386764 ) ) ;
#5195=CIRCLE ( 'NONE', #217579, 0.09999999999999609201 ) ;
#5219=EDGE_CURVE ( 'NONE', #4376, #65749, #82013, .T. ) ;
#5234=ORIENTED_EDGE ( 'NONE', *, *, #205645, .F. ) ;
#5240=VERTEX_POINT ( 'NONE', #165455 ) ;
#5275=CARTESIAN_POINT ( 'NONE',  ( 21.04999999999999716, 34.10062737184202319, -243.7890691661991696 ) ) ;
#5276=ORIENTED_EDGE ( 'NONE', *, *, #110552, .T. ) ;
#5297=DIRECTION ( 'NONE',  ( 0.000000000000000000, -0.9126074666063660468, -0.4088369013363524762 ) ) ;
#5298=ORIENTED_EDGE ( 'NONE', *, *, #26181, .T. ) ;
#5319=ORIENTED_EDGE ( 'NONE', *, *, #230682, .F. ) ;
#5333=CARTESIAN_POINT ( 'NONE',  ( 22.00411653889230834, 29.99888786984128330, -252.4262548924342013 ) ) ;
#5365=LINE ( 'NONE', #4109, #231437 ) ;
#5381=CARTESIAN_POINT ( 'NONE',  ( 18.39999999999999858, 46.96039402156216624, -255.3459641718773128 ) ) ;
#5386=CARTESIAN_POINT ( 'NONE',  ( -18.51555513499156902, 47.04900152148760384, -255.1448163970531766 ) ) ;
#5417=ORIENTED_EDGE ( 'NONE', *, *, #72508, .T. ) ;
#5442=VECTOR ( 'NONE', #97334, 1000.000000000000227 ) ;
#5449=AXIS2_PLACEMENT_3D ( 'NONE', #115099, #52541, #210357 ) ;
#5499=EDGE_CURVE ( 'NONE', #86809, #96525, #240038, .T. ) ;
#5505=CIRCLE ( 'NONE', #47202, 0.1000000000000024342 ) ;
#5513=EDGE_CURVE ( 'NONE', #25987, #78948, #201362, .T. ) ;
#5524=DIRECTION ( 'NONE',  ( -3.265361837132812600E-16, -0.4088369013363282178, 0.9126074666063768159 ) ) ;
#5573=TOROIDAL_SURFACE ( 'NONE', #184657, 0.2000000000000000111, 0.1000000000000000056 ) ;
#5585=CARTESIAN_POINT ( 'NONE',  ( 21.04999999999999716, 34.05155896670549254, -243.7673268003813973 ) ) ;
#5589=FACE_OUTER_BOUND ( 'NONE', #108619, .T. ) ;
#5590=EDGE_CURVE ( 'NONE', #157652, #184585, #173459, .T. ) ;
#5605=CARTESIAN_POINT ( 'NONE',  ( 18.52928932188133970, 54.95214567929435390, -230.0923768967488456 ) ) ;
#5616=DIRECTION ( 'NONE',  ( -0.000000000000000000, 0.8103668758649578141, -0.5859227990963212784 ) ) ;
#5619=AXIS2_PLACEMENT_3D ( 'NONE', #78324, #57471, #236128 ) ;
#5620=DIRECTION ( 'NONE',  ( 0.000000000000000000, 0.9126074666063660468, 0.4088369013363524762 ) ) ;
#5627=CARTESIAN_POINT ( 'NONE',  ( -21.05000000000000071, 48.05114133249968944, -246.4758750954581785 ) ) ;
#5633=CARTESIAN_POINT ( 'NONE',  ( 20.85000000000000142, 67.32498692201720303, -236.1680459564915679 ) ) ;
#5683=ORIENTED_EDGE ( 'NONE', *, *, #45182, .T. ) ;
#5684=ADVANCED_FACE ( 'NONE', ( #107395, #5704 ), #26604, .F. ) ;
#5704=FACE_BOUND ( 'NONE', #121045, .T. ) ;
#5717=AXIS2_PLACEMENT_3D ( 'NONE', #62953, #23861, #5524 ) ;
#5722=CIRCLE ( 'NONE', #205640, 0.1000000000000024342 ) ;
#5727=CARTESIAN_POINT ( 'NONE',  ( -20.85000000000000142, 69.34766280046808617, -247.6726305063181428 ) ) ;
#5729=VERTEX_POINT ( 'NONE', #66989 ) ;
#5731=CARTESIAN_POINT ( 'NONE',  ( -21.05000000000000071, 36.65892442174472876, -249.5511627012454596 ) ) ;
#5743=ORIENTED_EDGE ( 'NONE', *, *, #20973, .T. ) ;
#5755=DIRECTION ( 'NONE',  ( 0.000000000000000000, 0.9126074666063771490, 0.4088369013363276627 ) ) ;
#5784=ORIENTED_EDGE ( 'NONE', *, *, #101625, .T. ) ;
#5790=CARTESIAN_POINT ( 'NONE',  ( 22.60000000000000142, 31.76322370622491320, -238.8696546380523671 ) ) ;
#5816=CIRCLE ( 'NONE', #205744, 0.09999999999999939493 ) ;
#5860=CARTESIAN_POINT ( 'NONE',  ( -21.14999999999999858, 34.07612324756792077, -243.5412266404783566 ) ) ;
#5864=CARTESIAN_POINT ( 'NONE',  ( 20.94999999999999929, 68.00417547777207972, -224.2303273613012493 ) ) ;
#5873=EDGE_CURVE ( 'NONE', #84325, #105422, #111038, .T. ) ;
#5884=AXIS2_PLACEMENT_3D ( 'NONE', #209920, #151229, #31306 ) ;
#5885=VERTEX_POINT ( 'NONE', #97634 ) ;
#5899=CARTESIAN_POINT ( 'NONE',  ( 20.94999999999999929, 39.29335463311362275, -236.8946393634875278 ) ) ;
#5901=CIRCLE ( 'NONE', #97473, 0.1000000000000024342 ) ;
#5918=CARTESIAN_POINT ( 'NONE',  ( 20.04142135623731136, 54.45778349825307885, -228.7022971282791843 ) ) ;
#5960=EDGE_CURVE ( 'NONE', #62684, #109264, #73642, .T. ) ;
#6009=VECTOR ( 'NONE', #98401, 1000.000000000000000 ) ;
#6023=DIRECTION ( 'NONE',  ( -4.408576920032448588E-17, -0.9594490217226103734, -0.2818822000686205254 ) ) ;
#6082=EDGE_CURVE ( 'NONE', #57757, #57263, #165395, .T. ) ;
#6085=FACE_OUTER_BOUND ( 'NONE', #111620, .T. ) ;
#6116=CIRCLE ( 'NONE', #247737, 0.1000000000000024342 ) ;
#6124=EDGE_LOOP ( 'NONE', ( #162563, #54633, #136940, #122280 ) ) ;
#6130=ORIENTED_EDGE ( 'NONE', *, *, #191183, .T. ) ;
#6138=CARTESIAN_POINT ( 'NONE',  ( -23.15000000000000213, 63.67210543329348837, -237.4495904216901465 ) ) ;
#6143=DIRECTION ( 'NONE',  ( 3.265361837132813093E-16, 0.4088369013363281068, -0.9126074666063770380 ) ) ;
#6144=CARTESIAN_POINT ( 'NONE',  ( -21.00023020733502221, 30.82656943040777620, -252.1639858803266918 ) ) ;
#6153=EDGE_LOOP ( 'NONE', ( #75190, #141513, #8813 ) ) ;
#6206=ORIENTED_EDGE ( 'NONE', *, *, #232768, .F. ) ;
#6240=DIRECTION ( 'NONE',  ( -1.000000000000000000, 0.000000000000000000, 0.000000000000000000 ) ) ;
#6246=ORIENTED_EDGE ( 'NONE', *, *, #108852, .F. ) ;
#6278=B_SPLINE_CURVE_WITH_KNOTS ( 'NONE', 3,
 ( #237815, #158313, #59135, #56569, #17475, #77428, #157016, #236518, #38341, #138672, #159567, #22641, #124297, #3032, #31323, #170853 ),
 .UNSPECIFIED., .F., .F.,
 ( 4, 3, 3, 3, 3, 4 ),
 ( 0.000000000000000000, 2.372700795693357903E-05, 5.739057815866867708E-05, 9.073899019179633917E-05, 0.0001243544287365728779, 0.0001585386695601243641 ),
 .UNSPECIFIED. ) ;
#6287=DIRECTION ( 'NONE',  ( 1.000000000000000000, -1.335000415235278971E-16, 2.979993593738921214E-16 ) ) ;
#6298=B_SPLINE_CURVE_WITH_KNOTS ( 'NONE', 3,
 ( #12398, #206724, #47625, #209284, #185873, #7225, #8528 ),
 .UNSPECIFIED., .F., .F.,
 ( 4, 3, 4 ),
 ( 0.000000000000000000, 0.0009834301579439959709, 0.001767853679402671277 ),
 .UNSPECIFIED. ) ;
#6307=AXIS2_PLACEMENT_3D ( 'NONE', #178600, #241134, #135573 ) ;
#6320=ORIENTED_EDGE ( 'NONE', *, *, #82715, .F. ) ;
#6342=CARTESIAN_POINT ( 'NONE',  ( 20.85000000000000142, 74.98773774893902555, -233.8732236541320333 ) ) ;
#6401=CARTESIAN_POINT ( 'NONE',  ( 20.95566103547454517, 39.28266729857053008, -236.7406927167233164 ) ) ;
#6423=CARTESIAN_POINT ( 'NONE',  ( 23.15000000000000213, 48.79765034352288922, -253.5326144460178170 ) ) ;
#6427=CARTESIAN_POINT ( 'NONE',  ( -20.94999999999999929, 69.34766280046808617, -247.6726305063181428 ) ) ;
#6431=DIRECTION ( 'NONE',  ( -1.000000000000000000, -0.000000000000000000, 0.000000000000000000 ) ) ;
#6441=AXIS2_PLACEMENT_3D ( 'NONE', #57822, #177822, #216905 ) ;
#6465=FACE_OUTER_BOUND ( 'NONE', #213956, .T. ) ;
#6478=CARTESIAN_POINT ( 'NONE',  ( -21.15000000000000213, 33.98486250090727623, -243.5821103306120108 ) ) ;
#6485=CARTESIAN_POINT ( 'NONE',  ( 18.49999999999999289, 53.24180694658302571, -234.8354225850497130 ) ) ;
#6507=AXIS2_PLACEMENT_3D ( 'NONE', #60089, #40582, #100483 ) ;
#6510=AXIS2_PLACEMENT_3D ( 'NONE', #197917, #213641, #75448 ) ;
#6524=ORIENTED_EDGE ( 'NONE', *, *, #71085, .F. ) ;
#6530=CIRCLE ( 'NONE', #252226, 0.5000000000000001110 ) ;
#6535=ORIENTED_EDGE ( 'NONE', *, *, #6927, .T. ) ;
#6590=CYLINDRICAL_SURFACE ( 'NONE', #127416, 0.09999999999999108213 ) ;
#6638=DIRECTION ( 'NONE',  ( 0.000000000000000000, 0.4088369013363276072, -0.9126074666063773710 ) ) ;
#6643=ORIENTED_EDGE ( 'NONE', *, *, #222134, .T. ) ;
#6702=AXIS2_PLACEMENT_3D ( 'NONE', #205697, #101423, #24532 ) ;
#6705=CARTESIAN_POINT ( 'NONE',  ( -18.50000000000000000, 77.35494420175976416, -241.6200040285045532 ) ) ;
#6711=DIRECTION ( 'NONE',  ( 0.000000000000000000, 0.09425075112713275638, 0.9955484899852801162 ) ) ;
#6718=EDGE_LOOP ( 'NONE', ( #80451, #202088 ) ) ;
#6753=( BOUNDED_SURFACE ( )  B_SPLINE_SURFACE ( 3, 2, ( 
 ( #208599, #29969, #127767 ),
 ( #109460, #89899, #249008 ),
 ( #70386, #213708, #194174 ),
 ( #232011, #235831, #54628 ) ),
 .UNSPECIFIED., .F., .F., .F. ) 
 B_SPLINE_SURFACE_WITH_KNOTS ( ( 4, 4 ),
 ( 3, 3 ),
 ( -4.228388472693467293E-18, 0.0003124336600439479731 ),
 ( 0.000000000000000000, 1.000000000000000000 ),
 .UNSPECIFIED. ) 
 GEOMETRIC_REPRESENTATION_ITEM ( )  RATIONAL_B_SPLINE_SURFACE ( (
 ( 1.000000000000000000, 0.7071067811865363595, 1.000000000000000000),
 ( 1.000000000000000000, 0.7089187706047865856, 1.000000000000000000),
 ( 1.000000000000000000, 0.7039288185054065616, 1.000000000000000000),
 ( 1.000000000000000000, 0.7040654476015160146, 1.000000000000000000) ) ) 
 REPRESENTATION_ITEM ( '' )  SURFACE ( )  );
#6777=DIRECTION ( 'NONE',  ( 0.000000000000000000, 0.9126074666063771490, 0.4088369013363281623 ) ) ;
#6796=DIRECTION ( 'NONE',  ( 0.000000000000000000, -0.5859227990963362664, -0.8103668758649469339 ) ) ;
#6843=CARTESIAN_POINT ( 'NONE',  ( -21.05000000000000071, 56.16603649944111254, -228.1013850343386764 ) ) ;
#6852=CARTESIAN_POINT ( 'NONE',  ( -18.50000000000000000, 67.84340367245323478, -228.0791829662263410 ) ) ;
#6863=CARTESIAN_POINT ( 'NONE',  ( 19.81427058490526250, 54.47541967946905572, -228.7836307801017597 ) ) ;
#6874=CARTESIAN_POINT ( 'NONE',  ( 21.08489834409762764, 43.58682864821898306, -234.8080148706948478 ) ) ;
#6882=ORIENTED_EDGE ( 'NONE', *, *, #108623, .F. ) ;
#6905=ORIENTED_EDGE ( 'NONE', *, *, #59058, .T. ) ;
#6922=ADVANCED_FACE ( 'NONE', ( #27817 ), #15362, .T. ) ;
#6927=EDGE_CURVE ( 'NONE', #144623, #112954, #66902, .T. ) ;
#6968=CARTESIAN_POINT ( 'NONE',  ( 21.11345278033178374, 44.20339642523578050, -236.4386460197867166 ) ) ;
#6989=LINE ( 'NONE', #123103, #136643 ) ;
#6994=EDGE_CURVE ( 'NONE', #174500, #70441, #123486, .T. ) ;
#7025=ADVANCED_FACE ( 'NONE', ( #171193 ), #173613, .F. ) ;
#7031=ORIENTED_EDGE ( 'NONE', *, *, #116250, .F. ) ;
#7034=CARTESIAN_POINT ( 'NONE',  ( 18.59999999999999076, 44.47083028126615289, -247.4212268238128161 ) ) ;
#7052=VERTEX_POINT ( 'NONE', #250669 ) ;
#7063=VECTOR ( 'NONE', #62522, 1000.000000000000000 ) ;
#7067=STYLED_ITEM ( 'NONE', ( #12150 ), #181958 ) ;
#7087=CARTESIAN_POINT ( 'NONE',  ( 21.05000000000000071, 49.57218508014540959, -254.1759139559835035 ) ) ;
#7094=FACE_OUTER_BOUND ( 'NONE', #234507, .T. ) ;
#7103=CYLINDRICAL_SURFACE ( 'NONE', #36513, 0.1000000000000024342 ) ;
#7110=VERTEX_POINT ( 'NONE', #53764 ) ;
#7115=EDGE_LOOP ( 'NONE', ( #128642, #151182, #239024, #106601 ) ) ;
#7171=VERTEX_POINT ( 'NONE', #251962 ) ;
#7178=CYLINDRICAL_SURFACE ( 'NONE', #136916, 0.1000000000000024342 ) ;
#7225=CARTESIAN_POINT ( 'NONE',  ( -21.33487959338958362, 33.90926806716008457, -243.4133681147159223 ) ) ;
#7240=AXIS2_PLACEMENT_3D ( 'NONE', #191657, #76799, #194213 ) ;
#7264=DIRECTION ( 'NONE',  ( 1.000000000000000000, 0.000000000000000000, 0.000000000000000000 ) ) ;
#7313=CARTESIAN_POINT ( 'NONE',  ( -18.59999999999999787, 44.10700160683882132, -235.9691471569721841 ) ) ;
#7323=DIRECTION ( 'NONE',  ( 0.000000000000000000, -0.4088369013363280513, 0.9126074666063769270 ) ) ;
#7337=ORIENTED_EDGE ( 'NONE', *, *, #135925, .T. ) ;
#7361=CARTESIAN_POINT ( 'NONE',  ( -20.85000000000000142, 78.45218979564165807, -232.7313097695096076 ) ) ;
#7363=DIRECTION ( 'NONE',  ( 0.000000000000000000, 0.9594490217226103734, 0.2818822000686205254 ) ) ;
#7380=DIRECTION ( 'NONE',  ( -1.000000000000000000, -0.000000000000000000, 0.000000000000000000 ) ) ;
#7393=DIRECTION ( 'NONE',  ( -1.000000000000000000, -0.000000000000000000, -0.000000000000000000 ) ) ;
#7402=ORIENTED_EDGE ( 'NONE', *, *, #234234, .F. ) ;
#7417=VECTOR ( 'NONE', #132201, 1000.000000000000000 ) ;
#7444=CARTESIAN_POINT ( 'NONE',  ( 18.43473516226031350, 46.97094695037121426, -255.3356945386573500 ) ) ;
#7460=CARTESIAN_POINT ( 'NONE',  ( 23.15000000000000213, 69.09936979046463534, -247.6075824278584605 ) ) ;
#7467=VECTOR ( 'NONE', #160895, 1000.000000000000000 ) ;
#7472=CARTESIAN_POINT ( 'NONE',  ( 21.12230431290518951, 30.76357089822023738, -252.1864996923993090 ) ) ;
#7478=DIRECTION ( 'NONE',  ( -0.000000000000000000, -0.9126074666063769270, -0.4088369013363283844 ) ) ;
#7483=EDGE_LOOP ( 'NONE', ( #54960, #114811, #91244, #151208, #142864 ) ) ;
#7499=EDGE_LOOP ( 'NONE', ( #227090, #154755 ) ) ;
#7509=EDGE_CURVE ( 'NONE', #26148, #61043, #169504, .T. ) ;
#7510=FACE_OUTER_BOUND ( 'NONE', #154028, .T. ) ;
#7539=CARTESIAN_POINT ( 'NONE',  ( -20.64999999999999858, 54.18213181965657554, -236.9344197582443883 ) ) ;
#7541=ORIENTED_EDGE ( 'NONE', *, *, #146783, .F. ) ;
#7571=CARTESIAN_POINT ( 'NONE',  ( -23.15000000000000213, 24.23911354857403921, -250.5676753055308552 ) ) ;
#7581=EDGE_LOOP ( 'NONE', ( #15111, #148890, #27897, #112780 ) ) ;
#7624=CARTESIAN_POINT ( 'NONE',  ( 18.59999999999999076, 54.53338637621133955, -228.6684279704127789 ) ) ;
#7663=DIRECTION ( 'NONE',  ( 0.000000000000000000, 0.4088369013363322146, -0.9126074666063751506 ) ) ;
#7679=ORIENTED_EDGE ( 'NONE', *, *, #235995, .T. ) ;
#7701=DIRECTION ( 'NONE',  ( -1.000000000000000000, -0.000000000000000000, 0.000000000000000000 ) ) ;
#7706=CARTESIAN_POINT ( 'NONE',  ( 20.95556889135987788, 39.29078794878244452, -236.7330049007518085 ) ) ;
#7776=EDGE_LOOP ( 'NONE', ( #210936, #52274, #230403, #227395 ) ) ;
#7777=FACE_OUTER_BOUND ( 'NONE', #142440, .T. ) ;
#7783=CARTESIAN_POINT ( 'NONE',  ( -21.05000000000000071, 34.07612324756792077, -243.5412266404783566 ) ) ;
#7789=FACE_BOUND ( 'NONE', #83184, .T. ) ;
#7795=EDGE_CURVE ( 'NONE', #64123, #131079, #232213, .T. ) ;
#7819=ORIENTED_EDGE ( 'NONE', *, *, #229517, .T. ) ;
#7829=VERTEX_POINT ( 'NONE', #102832 ) ;
#7858=DIRECTION ( 'NONE',  ( 0.000000000000000000, 0.9955484899852913294, -0.09425075112701486457 ) ) ;
#7863=AXIS2_PLACEMENT_3D ( 'NONE', #10554, #112228, #90061 ) ;
#7902=CARTESIAN_POINT ( 'NONE',  ( -21.05000000000000071, 69.65930857908919904, -248.3682875362397340 ) ) ;
#7905=CARTESIAN_POINT ( 'NONE',  ( -21.05000000000000071, 44.06250559941687328, -258.7395785465160429 ) ) ;
#7959=VERTEX_POINT ( 'NONE', #128853 ) ;
#7972=ORIENTED_EDGE ( 'NONE', *, *, #96609, .F. ) ;
#7981=CARTESIAN_POINT ( 'NONE',  ( 23.14999999999999503, 53.32357432685029153, -235.0179440783709879 ) ) ;
#7992=EDGE_CURVE ( 'NONE', #10114, #167448, #186598, .T. ) ;
#8000=CARTESIAN_POINT ( 'NONE',  ( -23.25000000000000000, 32.96286418198890544, -251.2069521516576174 ) ) ;
#8067=AXIS2_PLACEMENT_3D ( 'NONE', #217961, #75912, #141030 ) ;
#8075=DIRECTION ( 'NONE',  ( -1.000000000000000000, 1.207181226542539700E-16, -2.694675058168174199E-16 ) ) ;
#8106=EDGE_CURVE ( 'NONE', #170250, #20995, #163252, .T. ) ;
#8129=ADVANCED_FACE ( 'NONE', ( #236921 ), #135240, .T. ) ;
#8136=AXIS2_PLACEMENT_3D ( 'NONE', #64809, #85622, #68676 ) ;
#8144=DIRECTION ( 'NONE',  ( 0.000000000000000000, 0.9126074666063771490, 0.4088369013363281623 ) ) ;
#8160=ORIENTED_EDGE ( 'NONE', *, *, #219294, .F. ) ;
#8178=EDGE_CURVE ( 'NONE', #143511, #40310, #124050, .T. ) ;
#8188=CARTESIAN_POINT ( 'NONE',  ( -18.59999999999999787, 67.23127455305835554, -235.8551265064784559 ) ) ;
#8235=CARTESIAN_POINT ( 'NONE',  ( 20.94999999999999929, 62.04148992963929032, -247.7470044306132024 ) ) ;
#8258=ORIENTED_EDGE ( 'NONE', *, *, #194341, .F. ) ;
#8261=CARTESIAN_POINT ( 'NONE',  ( -18.59999999999999787, 46.50671693017397246, -243.2369495081682942 ) ) ;
#8264=EDGE_CURVE ( 'NONE', #13269, #162201, #108954, .T. ) ;
#8272=CARTESIAN_POINT ( 'NONE',  ( 20.95512820512820440, 44.11820694106862106, -236.4833523840365217 ) ) ;
#8350=CARTESIAN_POINT ( 'NONE',  ( -23.25000000000000000, 61.88149656937975607, -248.1136133839584090 ) ) ;
#8373=DIRECTION ( 'NONE',  ( -0.000000000000000000, -0.9126074666063770380, -0.4088369013363281068 ) ) ;
#8406=ORIENTED_EDGE ( 'NONE', *, *, #238472, .F. ) ;
#8420=AXIS2_PLACEMENT_3D ( 'NONE', #47549, #63273, #3285 ) ;
#8431=CIRCLE ( 'NONE', #137580, 12.87499999999999822 ) ;
#8475=EDGE_CURVE ( 'NONE', #70449, #95060, #32689, .T. ) ;
#8497=DIRECTION ( 'NONE',  ( 0.000000000000000000, 0.9126074666063545004, 0.4088369013363783999 ) ) ;
#8516=ORIENTED_EDGE ( 'NONE', *, *, #9222, .T. ) ;
#8528=CARTESIAN_POINT ( 'NONE',  ( -21.14999999999999858, 33.98486250090727623, -243.5821103306120108 ) ) ;
#8537=EDGE_CURVE ( 'NONE', #4597, #235986, #45107, .T. ) ;
#8552=AXIS2_PLACEMENT_3D ( 'NONE', #234448, #233206, #134064 ) ;
#8563=CIRCLE ( 'NONE', #175205, 0.5000000000000031086 ) ;
#8644=DIRECTION ( 'NONE',  ( 0.000000000000000000, 0.9126074666063545004, 0.4088369013363783999 ) ) ;
#8646=DIRECTION ( 'NONE',  ( 6.938893903907225222E-15, 0.4088369013363283844, -0.9126074666063769270 ) ) ;
#8654=CYLINDRICAL_SURFACE ( 'NONE', #64915, 0.1000000000000076245 ) ;
#8668=FACE_OUTER_BOUND ( 'NONE', #237529, .T. ) ;
#8813=ORIENTED_EDGE ( 'NONE', *, *, #145025, .F. ) ;
#8858=ORIENTED_EDGE ( 'NONE', *, *, #9550, .F. ) ;
#8868=ORIENTED_EDGE ( 'NONE', *, *, #118669, .F. ) ;
#8898=DIRECTION ( 'NONE',  ( 1.000000000000000000, 0.000000000000000000, 0.000000000000000000 ) ) ;
#8913=CARTESIAN_POINT ( 'NONE',  ( 18.41416235934317314, 77.13860723519889007, -241.8264964602988982 ) ) ;
#8928=DIRECTION ( 'NONE',  ( 0.000000000000000000, -0.4088369013363205573, 0.9126074666063803686 ) ) ;
#8930=EDGE_CURVE ( 'NONE', #1827, #118580, #216151, .T. ) ;
#8947=ORIENTED_EDGE ( 'NONE', *, *, #224270, .T. ) ;
#8974=CARTESIAN_POINT ( 'NONE',  ( -20.00857864376270001, 52.21971469324220294, -232.5539039185337913 ) ) ;
#8989=DIRECTION ( 'NONE',  ( 0.000000000000000000, -0.9126074666063770380, -0.4088369013363281068 ) ) ;
#8991=EDGE_CURVE ( 'NONE', #155744, #13290, #45289, .T. ) ;
#8992=ORIENTED_EDGE ( 'NONE', *, *, #86129, .T. ) ;
#9000=CARTESIAN_POINT ( 'NONE',  ( 23.14999999999998437, 32.96286418198891255, -251.2069521516576174 ) ) ;
#9024=DIRECTION ( 'NONE',  ( 0.000000000000000000, 0.9126074666063772600, 0.4088369013363274407 ) ) ;
#9026=VERTEX_POINT ( 'NONE', #183732 ) ;
#9056=EDGE_LOOP ( 'NONE', ( #161483, #191140, #135960, #227489, #70748 ) ) ;
#9069=PLANE ( 'NONE',  #111726 ) ;
#9079=ORIENTED_EDGE ( 'NONE', *, *, #3038, .T. ) ;
#9084=EDGE_CURVE ( 'NONE', #124831, #48342, #28963, .T. ) ;
#9089=AXIS2_PLACEMENT_3D ( 'NONE', #212083, #30897, #191247 ) ;
#9090=EDGE_CURVE ( 'NONE', #47325, #144142, #33064, .T. ) ;
#9091=VERTEX_POINT ( 'NONE', #128895 ) ;
#9111=EDGE_CURVE ( 'NONE', #13670, #12655, #20553, .T. ) ;
#9129=EDGE_CURVE ( 'NONE', #206263, #171099, #217385, .T. ) ;
#9173=AXIS2_PLACEMENT_3D ( 'NONE', #14393, #93893, #54761 ) ;
#9180=DIRECTION ( 'NONE',  ( -0.000000000000000000, -0.9126074666063771490, -0.4088369013363281623 ) ) ;
#9181=DIRECTION ( 'NONE',  ( -0.000000000000000000, 0.9126074666063770380, 0.4088369013363281068 ) ) ;
#9193=LINE ( 'NONE', #30074, #75767 ) ;
#9200=DIRECTION ( 'NONE',  ( -0.000000000000000000, -0.4088369013363281068, 0.9126074666063770380 ) ) ;
#9217=EDGE_CURVE ( 'NONE', #198468, #23132, #24843, .T. ) ;
#9222=EDGE_CURVE ( 'NONE', #221888, #61043, #41398, .T. ) ;
#9226=DIRECTION ( 'NONE',  ( 5.603264701231746180E-32, -0.9126074666063769270, -0.4088369013363282733 ) ) ;
#9236=EDGE_CURVE ( 'NONE', #170976, #73589, #213543, .T. ) ;
#9243=CYLINDRICAL_SURFACE ( 'NONE', #69136, 0.09999999999999939493 ) ;
#9259=CYLINDRICAL_SURFACE ( 'NONE', #190463, 0.1000000000000024342 ) ;
#9375=EDGE_CURVE ( 'NONE', #176131, #94408, #108029, .T. ) ;
#9391=ORIENTED_EDGE ( 'NONE', *, *, #63587, .T. ) ;
#9419=DIRECTION ( 'NONE',  ( -2.578261006436900068E-14, 0.8490545835447238510, 0.5283051335749973099 ) ) ;
#9454=ADVANCED_FACE ( 'NONE', ( #245964 ), #216528, .F. ) ;
#9477=DIRECTION ( 'NONE',  ( -1.000000000000000000, 1.207181226542539700E-16, -2.694675058168174199E-16 ) ) ;
#9508=LINE ( 'NONE', #224697, #110051 ) ;
#9522=VERTEX_POINT ( 'NONE', #256152 ) ;
#9531=DIRECTION ( 'NONE',  ( 0.000000000000000000, 0.9126074666063770380, 0.4088369013363281068 ) ) ;
#9532=CARTESIAN_POINT ( 'NONE',  ( 21.08804582317323906, 44.29990453334584544, -236.3997463056264792 ) ) ;
#9550=EDGE_CURVE ( 'NONE', #19155, #133755, #33368, .T. ) ;
#9567=DIRECTION ( 'NONE',  ( 0.000000000000000000, -0.4088369013363276072, 0.9126074666063772600 ) ) ;
#9578=DIRECTION ( 'NONE',  ( -1.000000000000000000, 1.207181226542539946E-16, -2.694675058168174692E-16 ) ) ;
#9594=EDGE_CURVE ( 'NONE', #55978, #251464, #257992, .T. ) ;
#9596=AXIS2_PLACEMENT_3D ( 'NONE', #211519, #53720, #14622 ) ;
#9598=VERTEX_POINT ( 'NONE', #232832 ) ;
#9619=ORIENTED_EDGE ( 'NONE', *, *, #125816, .T. ) ;
#9636=TOROIDAL_SURFACE ( 'NONE', #109391, 6.258578643762712446, 0.1000000000000000056 ) ;
#9639=AXIS2_PLACEMENT_3D ( 'NONE', #97579, #38940, #256629 ) ;
#9664=VERTEX_POINT ( 'NONE', #177985 ) ;
#9668=CARTESIAN_POINT ( 'NONE',  ( 22.47071067811865319, 29.57301391503007082, -252.6169816238249552 ) ) ;
#9682=EDGE_CURVE ( 'NONE', #112295, #72558, #162279, .T. ) ;
#9683=DIRECTION ( 'NONE',  ( 0.000000000000000000, 0.9126074666063660468, 0.4088369013363524762 ) ) ;
#9698=DIRECTION ( 'NONE',  ( -0.000000000000000000, 0.9579639084728132081, 0.2868887416116073230 ) ) ;
#9708=EDGE_CURVE ( 'NONE', #57757, #248466, #225787, .T. ) ;
#9709=CIRCLE ( 'NONE', #142970, 0.09999999999999609201 ) ;
#9721=EDGE_CURVE ( 'NONE', #173891, #186873, #183214, .T. ) ;
#9724=DIRECTION ( 'NONE',  ( 0.000000000000000000, 0.9126074666063772600, 0.4088369013363274407 ) ) ;
#9741=CARTESIAN_POINT ( 'NONE',  ( -2.995603634470829482E-16, 53.33306769324366314, -234.7945388949160872 ) ) ;
#9758=VERTEX_POINT ( 'NONE', #249516 ) ;
#9774=EDGE_LOOP ( 'NONE', ( #117510, #3401, #180048 ) ) ;
#9780=B_SPLINE_CURVE_WITH_KNOTS ( 'NONE', 3,
 ( #74471, #233524, #95276, #135670, #215227, #167783 ),
 .UNSPECIFIED., .F., .F.,
 ( 4, 2, 4 ),
 ( 0.000000000000000000, 0.0001891491689349690151, 0.0003782983378699380302 ),
 .UNSPECIFIED. ) ;
#9786=AXIS2_PLACEMENT_3D ( 'NONE', #40422, #44246, #101598 ) ;
#9817=( BOUNDED_CURVE ( )  B_SPLINE_CURVE ( 3, ( #226244, #5918, #104994, #163743 ),
 .UNSPECIFIED., .F., .F. ) 
 B_SPLINE_CURVE_WITH_KNOTS ( ( 4, 4 ),
 ( 0.000000000000000000, 1.570796326794908992 ),
 .UNSPECIFIED. ) 
 CURVE ( )  GEOMETRIC_REPRESENTATION_ITEM ( )  RATIONAL_B_SPLINE_CURVE ( ( 1.000000000000000000, 0.8047378541243619399, 0.8047378541243619399, 1.000000000000000000 ) ) 
 REPRESENTATION_ITEM ( '' )  );
#9835=VECTOR ( 'NONE', #51367, 1000.000000000000114 ) ;
#9840=CARTESIAN_POINT ( 'NONE',  ( -18.59999999999999787, 74.93036000061670165, -233.6816308724374949 ) ) ;
#9848=ORIENTED_EDGE ( 'NONE', *, *, #230354, .F. ) ;
#9866=CARTESIAN_POINT ( 'NONE',  ( 20.94999999999999929, 46.45388641681647357, -243.1520440498138385 ) ) ;
#9875=CIRCLE ( 'NONE', #110019, 11.74999999999999822 ) ;
#9876=ORIENTED_EDGE ( 'NONE', *, *, #164398, .T. ) ;
#9879=LINE ( 'NONE', #103826, #200227 ) ;
#9880=ORIENTED_EDGE ( 'NONE', *, *, #43647, .T. ) ;
#9883=CARTESIAN_POINT ( 'NONE',  ( 18.59999999999999787, 60.94692742449272771, -251.5456325903398067 ) ) ;
#9903=DIRECTION ( 'NONE',  ( 1.000000000000000000, 0.000000000000000000, 0.000000000000000000 ) ) ;
#9931=DIRECTION ( 'NONE',  ( 0.000000000000000000, -0.4088369013363280513, 0.9126074666063769270 ) ) ;
#9936=DIRECTION ( 'NONE',  ( 0.000000000000000000, -0.4088369013363281623, 0.9126074666063771490 ) ) ;
#9945=ADVANCED_FACE ( 'NONE', ( #153009 ), #214234, .T. ) ;
#9978=EDGE_LOOP ( 'NONE', ( #42815, #8868, #194436, #92022 ) ) ;
#10001=CARTESIAN_POINT ( 'NONE',  ( -21.05000000000000071, 32.73471231533735448, -251.3091613769916535 ) ) ;
#10020=CARTESIAN_POINT ( 'NONE',  ( 18.43579564894488954, 46.91436734373925077, -255.3877619228566687 ) ) ;
#10071=FACE_BOUND ( 'NONE', #23826, .T. ) ;
#10081=AXIS2_PLACEMENT_3D ( 'NONE', #102528, #227640, #25610 ) ;
#10082=CARTESIAN_POINT ( 'NONE',  ( -23.25000000000000000, 36.65892442174472876, -249.5511627012454596 ) ) ;
#10111=CARTESIAN_POINT ( 'NONE',  ( 21.07888907270776002, 43.42727287605945463, -234.7669095404490065 ) ) ;
#10114=VERTEX_POINT ( 'NONE', #43205 ) ;
#10129=CARTESIAN_POINT ( 'NONE',  ( -20.94999999999999929, 56.45527679911575802, -225.2871936083021467 ) ) ;
#10177=AXIS2_PLACEMENT_3D ( 'NONE', #65927, #145446, #224971 ) ;
#10192=LINE ( 'NONE', #169295, #236204 ) ;
#10217=DIRECTION ( 'NONE',  ( 1.000000000000000000, 0.000000000000000000, 0.000000000000000000 ) ) ;
#10229=ORIENTED_EDGE ( 'NONE', *, *, #232167, .T. ) ;
#10244=AXIS2_PLACEMENT_3D ( 'NONE', #220052, #239622, #41437 ) ;
#10296=ADVANCED_FACE ( 'NONE', ( #194293 ), #192237, .F. ) ;
#10321=AXIS2_PLACEMENT_3D ( 'NONE', #7460, #30917, #204371 ) ;
#10326=CARTESIAN_POINT ( 'NONE',  ( 20.94999999999999929, 67.85909929089923764, -227.8797997985275856 ) ) ;
#10364=SPHERICAL_SURFACE ( 'NONE', #151715, 0.1000000000000000056 ) ;
#10384=DIRECTION ( 'NONE',  ( 0.000000000000000000, 0.9126074666063813678, 0.4088369013363182813 ) ) ;
#10386=AXIS2_PLACEMENT_3D ( 'NONE', #120163, #38043, #39326 ) ;
#10405=CARTESIAN_POINT ( 'NONE',  ( -22.50875500270930019, 25.97741616883209659, -254.4468630028325435 ) ) ;
#10413=DIRECTION ( 'NONE',  ( 0.000000000000000000, 0.8371762388950346745, 0.5469332180710581026 ) ) ;
#10431=VERTEX_POINT ( 'NONE', #212560 ) ;
#10457=EDGE_CURVE ( 'NONE', #24438, #60871, #113441, .T. ) ;
#10480=DIRECTION ( 'NONE',  ( 0.000000000000000000, 0.9126074666063660468, 0.4088369013363524762 ) ) ;
#10481=AXIS2_PLACEMENT_3D ( 'NONE', #23807, #241535, #158196 ) ;
#10492=ORIENTED_EDGE ( 'NONE', *, *, #165815, .F. ) ;
#10500=CARTESIAN_POINT ( 'NONE',  ( -21.05000000000000071, 40.58313652815211015, -247.7931640254992658 ) ) ;
#10514=CARTESIAN_POINT ( 'NONE',  ( 21.07016717457009847, 30.89038661691666121, -252.1353965670249977 ) ) ;
#10516=B_SPLINE_CURVE_WITH_KNOTS ( 'NONE', 3,
 ( #138293, #255649, #57476, #159194 ),
 .UNSPECIFIED., .F., .F.,
 ( 4, 4 ),
 ( 0.000000000000000000, 0.001767853679387106471 ),
 .UNSPECIFIED. ) ;
#10524=AXIS2_PLACEMENT_3D ( 'NONE', #231963, #248951, #70336 ) ;
#10549=DIRECTION ( 'NONE',  ( 1.000000000000000000, 0.000000000000000000, 0.000000000000000000 ) ) ;
#10554=CARTESIAN_POINT ( 'NONE',  ( 23.15000000000000213, 69.09936979046463534, -247.6075824278584605 ) ) ;
#10564=PLANE ( 'NONE',  #144981 ) ;
#10572=EDGE_LOOP ( 'NONE', ( #235321, #69640, #203389 ) ) ;
#10580=DIRECTION ( 'NONE',  ( -1.000000000000000000, -0.000000000000000000, -0.000000000000000000 ) ) ;
#10584=ORIENTED_EDGE ( 'NONE', *, *, #25542, .F. ) ;
#10588=DIRECTION ( 'NONE',  ( 1.000000000000000000, 0.000000000000000000, -0.000000000000000000 ) ) ;
#10633=CARTESIAN_POINT ( 'NONE',  ( -23.25000000000000000, 74.93036000061670165, -233.6816308724374949 ) ) ;
#10646=CARTESIAN_POINT ( 'NONE',  ( -21.05000000000000071, 36.65892442174472876, -249.5511627012454596 ) ) ;
#10647=CARTESIAN_POINT ( 'NONE',  ( 21.14999999999999858, 31.98723526783714988, -238.8784020251475511 ) ) ;
#10656=ORIENTED_EDGE ( 'NONE', *, *, #117554, .F. ) ;
#10661=CARTESIAN_POINT ( 'NONE',  ( 20.94999999999999574, 44.55458850188623643, -247.3966190010231969 ) ) ;
#10702=AXIS2_PLACEMENT_3D ( 'NONE', #109098, #170426, #249911 ) ;
#10724=CARTESIAN_POINT ( 'NONE',  ( 19.83283456528358002, 54.53338637568176495, -228.6684279706500433 ) ) ;
#10735=VERTEX_POINT ( 'NONE', #193971 ) ;
#10748=DIRECTION ( 'NONE',  ( 1.000000000000000000, 0.000000000000000000, -0.000000000000000000 ) ) ;
#10786=CARTESIAN_POINT ( 'NONE',  ( -22.39999999999999858, 36.61804073161109585, -249.4599019545848364 ) ) ;
#10799=CARTESIAN_POINT ( 'NONE',  ( -21.05000000000000071, 31.98723526783714988, -238.8784020251475511 ) ) ;
#10809=AXIS2_PLACEMENT_3D ( 'NONE', #250107, #45481, #151010 ) ;
#10837=CARTESIAN_POINT ( 'NONE',  ( 21.05000000000000071, 33.07085611758234478, -241.5418614019517065 ) ) ;
#10846=SHAPE_REPRESENTATION_RELATIONSHIP ( 'NONE' , 'NONE' ,  #90142, #181958 ) ;
#10879=CARTESIAN_POINT ( 'NONE',  ( -23.25000000000000000, 62.42744096235649920, -225.1319887738535499 ) ) ;
#10901=AXIS2_PLACEMENT_3D ( 'NONE', #184833, #162730, #101402 ) ;
#10902=DIRECTION ( 'NONE',  ( -1.000000000000000000, -0.000000000000000000, -0.000000000000000000 ) ) ;
#10909=AXIS2_PLACEMENT_3D ( 'NONE', #241768, #158422, #200087 ) ;
#10921=ORIENTED_EDGE ( 'NONE', *, *, #247804, .T. ) ;
#10933=ORIENTED_EDGE ( 'NONE', *, *, #22271, .F. ) ;
#10934=DIRECTION ( 'NONE',  ( 1.000000000000000000, 0.000000000000000000, 0.000000000000000000 ) ) ;
#10943=ORIENTED_EDGE ( 'NONE', *, *, #12046, .T. ) ;
#10961=DIRECTION ( 'NONE',  ( 1.000000000000000000, 0.000000000000000000, 0.000000000000000000 ) ) ;
#10984=ORIENTED_EDGE ( 'NONE', *, *, #163631, .F. ) ;
#10991=CARTESIAN_POINT ( 'NONE',  ( -18.59999999999999787, 74.86109765932731364, -233.8067614591677454 ) ) ;
#10992=EDGE_LOOP ( 'NONE', ( #95386, #85100, #215684, #195435 ) ) ;
#11073=DIRECTION ( 'NONE',  ( -1.000000000000000000, -0.000000000000000000, -0.000000000000000000 ) ) ;
#11074=VERTEX_POINT ( 'NONE', #112824 ) ;
#11130=LINE ( 'NONE', #90645, #240907 ) ;
#11159=CIRCLE ( 'NONE', #123585, 1.999999999999994893 ) ;
#11176=CARTESIAN_POINT ( 'NONE',  ( 22.49231231312463208, 31.84026337202740820, -238.9442601656825786 ) ) ;
#11190=AXIS2_PLACEMENT_3D ( 'NONE', #74722, #154262, #16014 ) ;
#11202=CARTESIAN_POINT ( 'NONE',  ( -21.14999999893415250, 38.10142838669770526, -236.0297427011622631 ) ) ;
#11240=AXIS2_PLACEMENT_3D ( 'NONE', #12020, #151536, #165964 ) ;
#11276=CIRCLE ( 'NONE', #52953, 0.09999999999999950595 ) ;
#11344=CIRCLE ( 'NONE', #165481, 0.5000000000000001110 ) ;
#11349=VECTOR ( 'NONE', #64822, 1000.000000000000000 ) ;
#11350=VECTOR ( 'NONE', #242001, 1000.000000000000000 ) ;
#11351=ORIENTED_EDGE ( 'NONE', *, *, #5219, .T. ) ;
#11361=EDGE_CURVE ( 'NONE', #41121, #256883, #140063, .T. ) ;
#11369=CARTESIAN_POINT ( 'NONE',  ( -20.64999999999999858, 55.48145342050125350, -241.1189016111836736 ) ) ;
#11385=AXIS2_PLACEMENT_3D ( 'NONE', #225510, #208568, #29934 ) ;
#11418=FACE_OUTER_BOUND ( 'NONE', #252579, .T. ) ;
#11437=ORIENTED_EDGE ( 'NONE', *, *, #106782, .F. ) ;
#11471=AXIS2_PLACEMENT_3D ( 'NONE', #199841, #81137, #181561 ) ;
#11476=ORIENTED_EDGE ( 'NONE', *, *, #31096, .F. ) ;
#11572=CARTESIAN_POINT ( 'NONE',  ( -22.59999999999999787, 31.76322370622491320, -238.8696546380523671 ) ) ;
#11591=DIRECTION ( 'NONE',  ( 6.938893903907499746E-14, -0.9126074666063545004, -0.4088369013363783999 ) ) ;
#11606=FACE_OUTER_BOUND ( 'NONE', #10992, .T. ) ;
#11614=VERTEX_POINT ( 'NONE', #117337 ) ;
#11678=ORIENTED_EDGE ( 'NONE', *, *, #36566, .T. ) ;
#11693=AXIS2_PLACEMENT_3D ( 'NONE', #120454, #179139, #451 ) ;
#11719=ORIENTED_EDGE ( 'NONE', *, *, #4230, .T. ) ;
#11724=CARTESIAN_POINT ( 'NONE',  ( 18.60000000000000497, 36.65892442174472876, -249.5511627012454596 ) ) ;
#11731=LINE ( 'NONE', #130357, #40214 ) ;
#11737=CARTESIAN_POINT ( 'NONE',  ( -23.25000000000000000, 78.57744179526842743, -232.8011145694030972 ) ) ;
#11802=LINE ( 'NONE', #10500, #65105 ) ;
#11823=AXIS2_PLACEMENT_3D ( 'NONE', #252310, #114090, #94523 ) ;
#11878=CARTESIAN_POINT ( 'NONE',  ( -21.44999999999999929, 53.08776555244186568, -234.2469744149522626 ) ) ;
#11880=LINE ( 'NONE', #247893, #153596 ) ;
#11943=DIRECTION ( 'NONE',  ( 0.000000000000000000, -0.4088369013363783999, 0.9126074666063545004 ) ) ;
#11949=CIRCLE ( 'NONE', #220222, 0.1000000000000117045 ) ;
#11975=DIRECTION ( 'NONE',  ( 7.304098846218134667E-16, 0.4088369013363281068, -0.9126074666063770380 ) ) ;
#11983=AXIS2_PLACEMENT_3D ( 'NONE', #173543, #59932, #139479 ) ;
#12020=CARTESIAN_POINT ( 'NONE',  ( 23.14999999999999503, 42.98415524044398950, -233.9519173640447889 ) ) ;
#12046=EDGE_CURVE ( 'NONE', #9522, #110542, #38249, .T. ) ;
#12063=CIRCLE ( 'NONE', #37004, 0.09999999999999939493 ) ;
#12123=ORIENTED_EDGE ( 'NONE', *, *, #150110, .F. ) ;
#12133=AXIS2_PLACEMENT_3D ( 'NONE', #176075, #239881, #75681 ) ;
#12150=PRESENTATION_STYLE_ASSIGNMENT (( #193341 ) ) ;
#12171=ORIENTED_EDGE ( 'NONE', *, *, #223484, .F. ) ;
#12173=AXIS2_PLACEMENT_3D ( 'NONE', #155777, #76192, #131041 ) ;
#12219=VERTEX_POINT ( 'NONE', #124733 ) ;
#12262=DIRECTION ( 'NONE',  ( -1.000000000000000000, -0.000000000000000000, 0.000000000000000000 ) ) ;
#12273=EDGE_CURVE ( 'NONE', #168786, #85846, #130776, .T. ) ;
#12310=ORIENTED_EDGE ( 'NONE', *, *, #73318, .F. ) ;
#12314=AXIS2_PLACEMENT_3D ( 'NONE', #40301, #136784, #196758 ) ;
#12315=ORIENTED_EDGE ( 'NONE', *, *, #24174, .T. ) ;
#12319=ORIENTED_EDGE ( 'NONE', *, *, #117934, .F. ) ;
#12392=CARTESIAN_POINT ( 'NONE',  ( 18.49999999999998934, 45.21086124044690280, -238.4331873168094091 ) ) ;
#12398=CARTESIAN_POINT ( 'NONE',  ( -22.39999999999999858, 33.47376623175146904, -242.4412390690852703 ) ) ;
#12405=AXIS2_PLACEMENT_3D ( 'NONE', #44782, #184281, #5620 ) ;
#12461=CARTESIAN_POINT ( 'NONE',  ( 23.15000000000000213, 62.12148660976905745, -247.5636999539406133 ) ) ;
#12465=DIRECTION ( 'NONE',  ( 0.000000000000000000, 0.4088369013363280513, -0.9126074666063769270 ) ) ;
#12469=CARTESIAN_POINT ( 'NONE',  ( -21.05000000000000071, 44.05869416168422958, -258.6139110589941197 ) ) ;
#12486=EDGE_LOOP ( 'NONE', ( #61567, #186808, #7031, #168361 ) ) ;
#12520=LINE ( 'NONE', #192424, #248789 ) ;
#12586=AXIS2_PLACEMENT_3D ( 'NONE', #21218, #218079, #100684 ) ;
#12589=AXIS2_PLACEMENT_3D ( 'NONE', #94165, #18502, #231148 ) ;
#12609=CONICAL_SURFACE ( 'NONE', #195779, 4.299999999999953637, 0.7853981633974466137 ) ;
#12655=VERTEX_POINT ( 'NONE', #125699 ) ;
#12671=CARTESIAN_POINT ( 'NONE',  ( -18.59999999999999787, 52.22920805963557456, -232.3304987350788906 ) ) ;
#12689=FACE_OUTER_BOUND ( 'NONE', #244722, .T. ) ;
#12708=FACE_OUTER_BOUND ( 'NONE', #755, .T. ) ;
#12715=EDGE_LOOP ( 'NONE', ( #234551, #161143, #37177, #142301 ) ) ;
#12736=CARTESIAN_POINT ( 'NONE',  ( 20.04142135623730070, 51.33926024308902925, -230.0993571250899379 ) ) ;
#12760=CARTESIAN_POINT ( 'NONE',  ( 18.59999999999999076, 67.65998959290219261, -227.8609496483021530 ) ) ;
#12808=ORIENTED_EDGE ( 'NONE', *, *, #80041, .F. ) ;
#12813=CARTESIAN_POINT ( 'NONE',  ( -20.94999999999999929, 44.00266445878927613, -258.8505972146074896 ) ) ;
#12817=EDGE_CURVE ( 'NONE', #155744, #213386, #100663, .T. ) ;
#12894=DIRECTION ( 'NONE',  ( -1.000000000000000000, 0.000000000000000000, 0.000000000000000000 ) ) ;
#12905=DIRECTION ( 'NONE',  ( 1.000000000000000000, -1.207181226542539700E-16, 2.694675058168174199E-16 ) ) ;
#12910=LINE ( 'NONE', #131543, #179910 ) ;
#12938=AXIS2_PLACEMENT_3D ( 'NONE', #117163, #155029, #137979 ) ;
#12970=EDGE_CURVE ( 'NONE', #128733, #78948, #155566, .T. ) ;
#12975=EDGE_CURVE ( 'NONE', #54257, #242821, #130391, .T. ) ;
#12987=DIRECTION ( 'NONE',  ( -3.265361837132813093E-16, -0.4088369013363280513, 0.9126074666063769270 ) ) ;
#12988=LINE ( 'NONE', #153810, #92804 ) ;
#13024=ORIENTED_EDGE ( 'NONE', *, *, #192089, .T. ) ;
#13102=LINE ( 'NONE', #207449, #107642 ) ;
#13127=VECTOR ( 'NONE', #129671, 1000.000000000000000 ) ;
#13143=CARTESIAN_POINT ( 'NONE',  ( 20.94999999999999929, 53.86595165227826243, -236.3638196928718855 ) ) ;
#13154=DIRECTION ( 'NONE',  ( 0.000000000000000000, -0.7203564749500614983, 0.6936040289657504632 ) ) ;
#13157=LINE ( 'NONE', #129251, #52045 ) ;
#13205=ORIENTED_EDGE ( 'NONE', *, *, #248751, .F. ) ;
#13257=AXIS2_PLACEMENT_3D ( 'NONE', #237295, #252991, #92627 ) ;
#13267=EDGE_CURVE ( 'NONE', #231005, #97895, #26539, .T. ) ;
#13269=VERTEX_POINT ( 'NONE', #247260 ) ;
#13271=ORIENTED_EDGE ( 'NONE', *, *, #23112, .T. ) ;
#13290=VERTEX_POINT ( 'NONE', #245999 ) ;
#13354=DIRECTION ( 'NONE',  ( -1.000000000000000000, 0.000000000000000000, 0.000000000000000000 ) ) ;
#13364=CARTESIAN_POINT ( 'NONE',  ( 21.05000000000000071, 36.65892442174472876, -249.5511627012454596 ) ) ;
#13434=DIRECTION ( 'NONE',  ( 1.000000000000000000, -1.335000415235278971E-16, 2.979993593738921214E-16 ) ) ;
#13436=DIRECTION ( 'NONE',  ( 1.000000000000000000, 0.000000000000000000, -0.000000000000000000 ) ) ;
#13441=DIRECTION ( 'NONE',  ( 0.000000000000000000, -0.1022405907414166287, -0.9947597004326452774 ) ) ;
#13489=ORIENTED_EDGE ( 'NONE', *, *, #237504, .T. ) ;
#13509=VERTEX_POINT ( 'NONE', #41098 ) ;
#13532=DIRECTION ( 'NONE',  ( 0.000000000000000000, 0.9126074666063660468, 0.4088369013363524762 ) ) ;
#13563=ORIENTED_EDGE ( 'NONE', *, *, #85972, .F. ) ;
#13571=ORIENTED_EDGE ( 'NONE', *, *, #125718, .F. ) ;
#13572=CYLINDRICAL_SURFACE ( 'NONE', #1622, 0.09999999999999939493 ) ;
#13600=ORIENTED_EDGE ( 'NONE', *, *, #243476, .F. ) ;
#13609=VERTEX_POINT ( 'NONE', #14677 ) ;
#13622=CARTESIAN_POINT ( 'NONE',  ( 23.14999999999999503, 51.38014393322265505, -230.1906178717505327 ) ) ;
#13650=CARTESIAN_POINT ( 'NONE',  ( -23.25000000000000000, 36.65892442174472876, -249.5511627012454596 ) ) ;
#13670=VERTEX_POINT ( 'NONE', #254510 ) ;
#13679=CARTESIAN_POINT ( 'NONE',  ( -21.05000000000000071, 30.78834561061718489, -252.2906857787774015 ) ) ;
#13696=CYLINDRICAL_SURFACE ( 'NONE', #142159, 0.4999999999999944489 ) ;
#13715=ADVANCED_FACE ( 'NONE', ( #115031 ), #255797, .T. ) ;
#13725=VECTOR ( 'NONE', #185006, 1000.000000000000114 ) ;
#13762=CARTESIAN_POINT ( 'NONE',  ( 18.59999999999999787, 36.65892442174472876, -249.5511627012454596 ) ) ;
#13766=FACE_OUTER_BOUND ( 'NONE', #91373, .T. ) ;
#13787=EDGE_LOOP ( 'NONE', ( #214229, #209524, #30269, #191254 ) ) ;
#13815=CARTESIAN_POINT ( 'NONE',  ( -23.25000000000000000, 30.69873658968802488, -264.9868732779115703 ) ) ;
#13837=DIRECTION ( 'NONE',  ( 1.000000000000000000, 0.000000000000000000, 0.000000000000000000 ) ) ;
#13840=EDGE_LOOP ( 'NONE', ( #76855, #236453, #216190, #31231 ) ) ;
#13846=EDGE_CURVE ( 'NONE', #197595, #201532, #199528, .T. ) ;
#13857=CARTESIAN_POINT ( 'NONE',  ( 21.11825140030044423, 30.77385224628299198, -252.1797090801663046 ) ) ;
#13878=EDGE_CURVE ( 'NONE', #168134, #39096, #59970, .T. ) ;
#13895=AXIS2_PLACEMENT_3D ( 'NONE', #112720, #154449, #232680 ) ;
#13906=ORIENTED_EDGE ( 'NONE', *, *, #19128, .F. ) ;
#13970=CARTESIAN_POINT ( 'NONE',  ( 21.05933563467872105, 43.40235695101777225, -234.7786682115255985 ) ) ;
#14015=ORIENTED_EDGE ( 'NONE', *, *, #123473, .T. ) ;
#14026=DIRECTION ( 'NONE',  ( 0.000000000000000000, -0.4088369013363281623, 0.9126074666063771490 ) ) ;
#14035=EDGE_CURVE ( 'NONE', #114879, #227981, #139288, .T. ) ;
#14061=CARTESIAN_POINT ( 'NONE',  ( -20.94999999999999929, 43.44873802792533724, -245.1397081572968659 ) ) ;
#14068=CYLINDRICAL_SURFACE ( 'NONE', #41907, 4.049999999999994493 ) ;
#14107=ORIENTED_EDGE ( 'NONE', *, *, #9217, .T. ) ;
#14112=DIRECTION ( 'NONE',  ( 0.000000000000000000, -0.9579639084728132081, -0.2868887416116073230 ) ) ;
#14122=EDGE_CURVE ( 'NONE', #139949, #25924, #245051, .T. ) ;
#14125=ORIENTED_EDGE ( 'NONE', *, *, #73612, .F. ) ;
#14132=CIRCLE ( 'NONE', #22507, 11.79999999999999716 ) ;
#14152=CARTESIAN_POINT ( 'NONE',  ( -23.15000000000000213, 21.17283678855157802, -243.7231193059830332 ) ) ;
#14160=DIRECTION ( 'NONE',  ( 0.000000000000000000, 0.9126074666063765939, 0.4088369013363291060 ) ) ;
#14168=LINE ( 'NONE', #114527, #199504 ) ;
#14193=ORIENTED_EDGE ( 'NONE', *, *, #32389, .F. ) ;
#14205=AXIS2_PLACEMENT_3D ( 'NONE', #78289, #255602, #198242 ) ;
#14208=DIRECTION ( 'NONE',  ( 1.000000000000000000, 0.000000000000000000, 0.000000000000000000 ) ) ;
#14220=DIRECTION ( 'NONE',  ( -1.000000000000000000, -0.000000000000000000, 0.000000000000000000 ) ) ;
#14242=TOROIDAL_SURFACE ( 'NONE', #230712, 0.4000000000000005773, 0.1000000000000000056 ) ;
#14251=DIRECTION ( 'NONE',  ( 2.952720810173289112E-16, 0.4088369013363278848, -0.9126074666063770380 ) ) ;
#14266=CARTESIAN_POINT ( 'NONE',  ( -22.39999999999999858, 26.02743912001966464, -254.3139371321002216 ) ) ;
#14311=AXIS2_PLACEMENT_3D ( 'NONE', #252529, #190008, #68777 ) ;
#14313=DIRECTION ( 'NONE',  ( 1.000000000000000000, 0.000000000000000000, 0.000000000000000000 ) ) ;
#14332=DIRECTION ( 'NONE',  ( 1.734723475976817823E-14, 0.4088369013363281623, -0.9126074666063771490 ) ) ;
#14364=DIRECTION ( 'NONE',  ( 1.224646799147353207E-16, -0.4088369013363281623, 0.9126074666063771490 ) ) ;
#14368=ADVANCED_FACE ( 'NONE', ( #46520 ), #242164, .T. ) ;
#14371=DIRECTION ( 'NONE',  ( 0.000000000000000000, -0.9126074666063773710, -0.4088369013363272741 ) ) ;
#14385=VERTEX_POINT ( 'NONE', #144323 ) ;
#14393=CARTESIAN_POINT ( 'NONE',  ( 21.30000000000002558, 36.65892442174472876, -249.5511627012454596 ) ) ;
#14395=DIRECTION ( 'NONE',  ( 0.000000000000000000, -0.4088369013363280513, 0.9126074666063769270 ) ) ;
#14415=CARTESIAN_POINT ( 'NONE',  ( -18.50000000000000000, 52.36135249642984490, -232.3808757916058880 ) ) ;
#14419=SPHERICAL_SURFACE ( 'NONE', #54630, 0.1000000000000000056 ) ;
#14425=AXIS2_PLACEMENT_3D ( 'NONE', #246091, #128708, #208250 ) ;
#14437=CARTESIAN_POINT ( 'NONE',  ( 20.94999999999999574, 43.48442877397276618, -245.2193771921251084 ) ) ;
#14449=CARTESIAN_POINT ( 'NONE',  ( 21.05000000000000071, 67.23127455305835554, -235.8551265064784559 ) ) ;
#14473=AXIS2_PLACEMENT_3D ( 'NONE', #243275, #21689, #145464 ) ;
#14513=LINE ( 'NONE', #253080, #241938 ) ;
#14533=CARTESIAN_POINT ( 'NONE',  ( -21.05000000000000071, 63.58084468663284383, -237.4904741118237723 ) ) ;
#14546=CARTESIAN_POINT ( 'NONE',  ( -23.15000000000000213, 69.16514130714681130, -247.7543978865853660 ) ) ;
#14555=ORIENTED_EDGE ( 'NONE', *, *, #24193, .F. ) ;
#14564=VERTEX_POINT ( 'NONE', #90781 ) ;
#14588=AXIS2_PLACEMENT_3D ( 'NONE', #256503, #85285, #77920 ) ;
#14599=ORIENTED_EDGE ( 'NONE', *, *, #200446, .T. ) ;
#14622=DIRECTION ( 'NONE',  ( 0.000000000000000000, 0.9126074666063772600, 0.4088369013363273852 ) ) ;
#14667=CARTESIAN_POINT ( 'NONE',  ( 18.59999999999998721, 30.62437029989165893, -230.5032680968432715 ) ) ;
#14677=CARTESIAN_POINT ( 'NONE',  ( -18.50000000000000000, 43.63140573099096287, -239.9077968784524444 ) ) ;
#14712=ORIENTED_EDGE ( 'NONE', *, *, #252639, .T. ) ;
#14716=DIRECTION ( 'NONE',  ( 0.000000000000000000, 0.9126074666063770380, 0.4088369013363281068 ) ) ;
#14720=FACE_OUTER_BOUND ( 'NONE', #156973, .T. ) ;
#14729=VERTEX_POINT ( 'NONE', #227102 ) ;
#14731=CARTESIAN_POINT ( 'NONE',  ( -18.59999999999999787, 78.45218979564165807, -232.7313097695096076 ) ) ;
#14761=DIRECTION ( 'NONE',  ( 0.000000000000000000, -0.4088369013363282733, 0.9126074666063771490 ) ) ;
#14763=ORIENTED_EDGE ( 'NONE', *, *, #180906, .F. ) ;
#14814=DIRECTION ( 'NONE',  ( 0.000000000000000000, 0.4088369013362748716, -0.9126074666064009078 ) ) ;
#14821=AXIS2_PLACEMENT_3D ( 'NONE', #176155, #155318, #40515 ) ;
#14846=CARTESIAN_POINT ( 'NONE',  ( -21.05000000000000071, 41.42187432231295219, -260.1830396872097140 ) ) ;
#14856=EDGE_CURVE ( 'NONE', #118580, #93087, #191875, .T. ) ;
#14868=DIRECTION ( 'NONE',  ( 0.000000000000000000, 0.9126074666063769270, 0.4088369013363280513 ) ) ;
#14903=ADVANCED_FACE ( 'NONE', ( #254358 ), #252108, .F. ) ;
#14905=ORIENTED_EDGE ( 'NONE', *, *, #211785, .T. ) ;
#14911=ADVANCED_FACE ( 'NONE', ( #22212 ), #138264, .T. ) ;
#14937=EDGE_CURVE ( 'NONE', #246752, #198869, #89786, .T. ) ;
#14941=DIRECTION ( 'NONE',  ( 0.000000000000000000, 0.9126074666063753726, 0.4088369013363316040 ) ) ;
#14969=CARTESIAN_POINT ( 'NONE',  ( -20.94999999999999929, 44.47083028126616000, -247.4212268238128161 ) ) ;
#14987=CARTESIAN_POINT ( 'NONE',  ( -21.05000000000000071, 30.84055724867796044, -252.2517348665298016 ) ) ;
#15019=ORIENTED_EDGE ( 'NONE', *, *, #167949, .T. ) ;
#15031=VECTOR ( 'NONE', #131070, 1000.000000000000000 ) ;
#15040=CARTESIAN_POINT ( 'NONE',  ( 20.94999999999999574, 44.18518595211054389, -258.7688298343402380 ) ) ;
#15058=VERTEX_POINT ( 'NONE', #24794 ) ;
#15067=ORIENTED_EDGE ( 'NONE', *, *, #186875, .F. ) ;
#15111=ORIENTED_EDGE ( 'NONE', *, *, #153417, .T. ) ;
#15141=CARTESIAN_POINT ( 'NONE',  ( 21.04999999999965254, 30.88828517705548649, -252.0799250334554813 ) ) ;
#15147=( BOUNDED_CURVE ( )  B_SPLINE_CURVE ( 3, ( #109227, #193927, #174400, #153554 ),
 .UNSPECIFIED., .F., .F. ) 
 B_SPLINE_CURVE_WITH_KNOTS ( ( 4, 4 ),
 ( 3.141592653589793116, 4.712388980384689674 ),
 .UNSPECIFIED. ) 
 CURVE ( )  GEOMETRIC_REPRESENTATION_ITEM ( )  RATIONAL_B_SPLINE_CURVE ( ( 1.000000000000000000, 0.8047378541243649375, 0.8047378541243649375, 1.000000000000000000 ) ) 
 REPRESENTATION_ITEM ( '' )  );
#15164=ORIENTED_EDGE ( 'NONE', *, *, #183292, .T. ) ;
#15188=DIRECTION ( 'NONE',  ( -1.000000000000000000, -0.000000000000000000, 0.000000000000000000 ) ) ;
#15226=EDGE_CURVE ( 'NONE', #203555, #250586, #252275, .T. ) ;
#15245=CARTESIAN_POINT ( 'NONE',  ( 21.13461538461538680, 43.58999342716159475, -234.8150793036844846 ) ) ;
#15248=CYLINDRICAL_SURFACE ( 'NONE', #161476, 11.74999999999999822 ) ;
#15249=ADVANCED_FACE ( 'NONE', ( #31227 ), #212401, .T. ) ;
#15263=CARTESIAN_POINT ( 'NONE',  ( 20.58091095332318332, 40.65476404443996472, -237.8789846480217705 ) ) ;
#15265=CARTESIAN_POINT ( 'NONE',  ( -21.05000000000000071, 44.06843597547145208, -258.9974126733344519 ) ) ;
#15285=ADVANCED_FACE ( 'NONE', ( #157590 ), #106516, .F. ) ;
#15348=VERTEX_POINT ( 'NONE', #100103 ) ;
#15357=DIRECTION ( 'NONE',  ( 1.000000000000000000, 0.000000000000000000, 0.000000000000000000 ) ) ;
#15362=TOROIDAL_SURFACE ( 'NONE', #106906, 0.2000000000000000111, 0.1000000000000000056 ) ;
#15390=CARTESIAN_POINT ( 'NONE',  ( -23.15000000000000213, 43.03453229697098692, -233.8197729272505114 ) ) ;
#15463=CIRCLE ( 'NONE', #123785, 0.09999999999999939493 ) ;
#15485=EDGE_CURVE ( 'NONE', #12655, #226018, #165174, .T. ) ;
#15517=ORIENTED_EDGE ( 'NONE', *, *, #125789, .T. ) ;
#15534=ORIENTED_EDGE ( 'NONE', *, *, #77722, .F. ) ;
#15535=CIRCLE ( 'NONE', #44739, 0.1000000000000024342 ) ;
#15556=CARTESIAN_POINT ( 'NONE',  ( -22.45437739390952459, 26.02743911632091312, -254.3139371337572072 ) ) ;
#15579=DIRECTION ( 'NONE',  ( 1.000000000000000000, 0.000000000000000000, 0.000000000000000000 ) ) ;
#15591=CARTESIAN_POINT ( 'NONE',  ( 21.17356465864818560, 30.75698776691031000, -252.0867744921908695 ) ) ;
#15623=AXIS2_PLACEMENT_3D ( 'NONE', #190578, #173616, #11943 ) ;
#15625=CARTESIAN_POINT ( 'NONE',  ( -20.85000000000000142, 66.90607807833499976, -235.8243394455619182 ) ) ;
#15650=DIRECTION ( 'NONE',  ( -1.000000000000000000, 0.000000000000000000, 0.000000000000000000 ) ) ;
#15670=CARTESIAN_POINT ( 'NONE',  ( 19.88284271247461632, 54.46607474075112520, -228.7627709682279260 ) ) ;
#15680=CARTESIAN_POINT ( 'NONE',  ( 21.30000000000002558, 32.96286418198891255, -251.2069521516576174 ) ) ;
#15698=CARTESIAN_POINT ( 'NONE',  ( -22.48660254037844552, 31.80946045771259634, -238.8484668136873381 ) ) ;
#15704=VERTEX_POINT ( 'NONE', #76388 ) ;
#15705=CARTESIAN_POINT ( 'NONE',  ( -23.15000000000000213, 69.09936979046463534, -247.6075824278584605 ) ) ;
#15709=VECTOR ( 'NONE', #179548, 1000.000000000000000 ) ;
#15800=DIRECTION ( 'NONE',  ( 0.000000000000000000, 0.9126074666063771490, 0.4088369013363281623 ) ) ;
#15852=VERTEX_POINT ( 'NONE', #205320 ) ;
#15907=ADVANCED_FACE ( 'NONE', ( #167529 ), #71000, .F. ) ;
#15910=CARTESIAN_POINT ( 'NONE',  ( 23.25000000000000000, 48.79765034352288922, -253.5326144460178170 ) ) ;
#15939=CARTESIAN_POINT ( 'NONE',  ( 20.94999999999999929, 67.23127455305835554, -235.8551265064784559 ) ) ;
#15950=ORIENTED_EDGE ( 'NONE', *, *, #34747, .F. ) ;
#15956=CARTESIAN_POINT ( 'NONE',  ( 18.41832399655356411, 77.26488349376249687, -241.9697967040461322 ) ) ;
#15967=DIRECTION ( 'NONE',  ( 0.000000000000000000, 0.9126074666063769270, 0.4088369013363280513 ) ) ;
#16008=CARTESIAN_POINT ( 'NONE',  ( -20.64999999999999858, 47.70572087816298534, -241.8629305864830030 ) ) ;
#16010=LINE ( 'NONE', #100614, #203481 ) ;
#16014=DIRECTION ( 'NONE',  ( 0.000000000000000000, 0.9126074666063660468, 0.4088369013363524762 ) ) ;
#16062=EDGE_CURVE ( 'NONE', #52763, #203994, #194798, .T. ) ;
#16083=ORIENTED_EDGE ( 'NONE', *, *, #71997, .T. ) ;
#16119=ADVANCED_FACE ( 'NONE', ( #176508 ), #190316, .T. ) ;
#16157=FACE_OUTER_BOUND ( 'NONE', #48609, .T. ) ;
#16176=CYLINDRICAL_SURFACE ( 'NONE', #6441, 0.09999999999999939493 ) ;
#16190=ORIENTED_EDGE ( 'NONE', *, *, #131233, .F. ) ;
#16225=ADVANCED_FACE ( 'NONE', ( #83766 ), #181642, .F. ) ;
#16269=AXIS2_PLACEMENT_3D ( 'NONE', #254789, #132323, #112770 ) ;
#16277=ADVANCED_FACE ( 'NONE', ( #88929 ), #35112, .F. ) ;
#16354=CARTESIAN_POINT ( 'NONE',  ( -21.14999999999999858, 38.04609728753135300, -236.0545303518866547 ) ) ;
#16394=LINE ( 'NONE', #230274, #183808 ) ;
#16401=ORIENTED_EDGE ( 'NONE', *, *, #198553, .F. ) ;
#16418=CARTESIAN_POINT ( 'NONE',  ( 21.05000000000000071, 53.86595165227826243, -236.3638196928718855 ) ) ;
#16440=CARTESIAN_POINT ( 'NONE',  ( 21.15000000000000213, 30.68987205111127281, -252.2252246220829193 ) ) ;
#16474=DIRECTION ( 'NONE',  ( 1.000000000000000000, -0.000000000000000000, -0.000000000000000000 ) ) ;
#16489=ORIENTED_EDGE ( 'NONE', *, *, #152020, .T. ) ;
#16499=AXIS2_PLACEMENT_3D ( 'NONE', #176713, #77564, #141413 ) ;
#16509=DIRECTION ( 'NONE',  ( 1.000000000000000000, 0.000000000000000000, 0.000000000000000000 ) ) ;
#16511=DIRECTION ( 'NONE',  ( 0.000000000000000000, -0.9126074666063622720, -0.4088369013363611360 ) ) ;
#16531=DIRECTION ( 'NONE',  ( 1.000000000000000000, 0.000000000000000000, 0.000000000000000000 ) ) ;
#16543=AXIS2_PLACEMENT_3D ( 'NONE', #125581, #145129, #160879 ) ;
#16547=ORIENTED_EDGE ( 'NONE', *, *, #185462, .T. ) ;
#16623=CARTESIAN_POINT ( 'NONE',  ( 18.59999999999999432, 74.73788286442776041, -233.7359682632885267 ) ) ;
#16678=CARTESIAN_POINT ( 'NONE',  ( 20.94999999999999574, 36.65892442174472876, -249.5511627012454596 ) ) ;
#16703=CARTESIAN_POINT ( 'NONE',  ( 21.14999999999999858, 43.54959646497384540, -234.7249050332107458 ) ) ;
#16719=EDGE_CURVE ( 'NONE', #241241, #14564, #230392, .T. ) ;
#16726=ORIENTED_EDGE ( 'NONE', *, *, #51374, .F. ) ;
#16727=AXIS2_PLACEMENT_3D ( 'NONE', #206882, #182196, #42669 ) ;
#16763=FACE_OUTER_BOUND ( 'NONE', #216797, .T. ) ;
#16773=ORIENTED_EDGE ( 'NONE', *, *, #141590, .T. ) ;
#16836=ORIENTED_EDGE ( 'NONE', *, *, #74002, .T. ) ;
#16850=CARTESIAN_POINT ( 'NONE',  ( 20.94999999999999929, 47.95459712139159336, -246.5019368548292675 ) ) ;
#16853=CARTESIAN_POINT ( 'NONE',  ( 21.05000000000000071, 61.88149656937974896, -248.1136133839584090 ) ) ;
#16913=CARTESIAN_POINT ( 'NONE',  ( 20.02499999999999858, 51.97441255244040548, -232.0063394385699667 ) ) ;
#16975=FACE_OUTER_BOUND ( 'NONE', #208904, .T. ) ;
#17014=AXIS2_PLACEMENT_3D ( 'NONE', #224376, #24925, #139691 ) ;
#17020=DIRECTION ( 'NONE',  ( -1.000000000000000000, -6.834672213024256725E-16, 4.941700349840508052E-16 ) ) ;
#17053=CIRCLE ( 'NONE', #83624, 11.65000000000000213 ) ;
#17062=CIRCLE ( 'NONE', #4545, 0.09999999999999326095 ) ;
#17082=DIRECTION ( 'NONE',  ( 0.000000000000000000, -0.8103668758649498205, 0.5859227990963324917 ) ) ;
#17088=EDGE_CURVE ( 'NONE', #24027, #210045, #245019, .T. ) ;
#17104=LINE ( 'NONE', #215280, #180989 ) ;
#17115=DIRECTION ( 'NONE',  ( 0.000000000000000000, 0.9126074666063768159, 0.4088369013363282178 ) ) ;
#17142=AXIS2_PLACEMENT_3D ( 'NONE', #35876, #191104, #17557 ) ;
#17184=ORIENTED_EDGE ( 'NONE', *, *, #5513, .F. ) ;
#17206=ORIENTED_EDGE ( 'NONE', *, *, #130251, .T. ) ;
#17213=ORIENTED_EDGE ( 'NONE', *, *, #188524, .T. ) ;
#17221=ORIENTED_EDGE ( 'NONE', *, *, #85558, .T. ) ;
#17223=B_SPLINE_CURVE_WITH_KNOTS ( 'NONE', 3,
 ( #105559, #146000, #229407, #209840, #225513, #208572, #89872, #169469 ),
 .UNSPECIFIED., .F., .F.,
 ( 4, 2, 2, 4 ),
 ( 0.000000000000000000, 0.0001049670497870137855, 0.0002099340995740275710, 0.0004198681991480551420 ),
 .UNSPECIFIED. ) ;
#17232=DIRECTION ( 'NONE',  ( 0.000000000000000000, -0.4088369013363281068, 0.9126074666063770380 ) ) ;
#17252=CARTESIAN_POINT ( 'NONE',  ( -23.25000000000000000, 56.02567683926420727, -227.9999002286038774 ) ) ;
#17263=AXIS2_PLACEMENT_3D ( 'NONE', #87196, #23425, #83331 ) ;
#17271=CARTESIAN_POINT ( 'NONE',  ( -23.25000000000000000, 67.23127455305835554, -235.8551265064784559 ) ) ;
#17282=PLANE ( 'NONE',  #78572 ) ;
#17286=DIRECTION ( 'NONE',  ( 1.000000000000000000, 0.000000000000000000, -0.000000000000000000 ) ) ;
#17289=DIRECTION ( 'NONE',  ( -3.265361837132813093E-16, -0.4088369013363053472, 0.9126074666063872520 ) ) ;
#17290=CYLINDRICAL_SURFACE ( 'NONE', #149113, 0.1000000000000024342 ) ;
#17297=ORIENTED_EDGE ( 'NONE', *, *, #239817, .F. ) ;
#17304=FACE_OUTER_BOUND ( 'NONE', #194484, .T. ) ;
#17340=VERTEX_POINT ( 'NONE', #245537 ) ;
#17357=EDGE_CURVE ( 'NONE', #182190, #41483, #202937, .T. ) ;
#17358=VECTOR ( 'NONE', #256084, 1000.000000000000000 ) ;
#17372=CARTESIAN_POINT ( 'NONE',  ( -18.59999999999999787, 74.83909925395606422, -233.7225145625711491 ) ) ;
#17396=AXIS2_PLACEMENT_3D ( 'NONE', #94308, #130872, #248261 ) ;
#17411=EDGE_LOOP ( 'NONE', ( #172090, #174480, #101206 ) ) ;
#17423=CARTESIAN_POINT ( 'NONE',  ( 21.14999999999998082, 41.46275801244657799, -260.2743004338703940 ) ) ;
#17428=CARTESIAN_POINT ( 'NONE',  ( 21.05000000000000071, 30.73075574124490217, -252.3164853687435709 ) ) ;
#17441=DIRECTION ( 'NONE',  ( 0.000000000000000000, 0.4088369013363281068, -0.9126074666063770380 ) ) ;
#17473=DIRECTION ( 'NONE',  ( 0.000000000000000000, 0.9126074666063772600, 0.4088369013363274962 ) ) ;
#17475=CARTESIAN_POINT ( 'NONE',  ( 21.05543885634738643, 44.19062562409153117, -236.5609025269668848 ) ) ;
#17491=ORIENTED_EDGE ( 'NONE', *, *, #130543, .F. ) ;
#17495=DIRECTION ( 'NONE',  ( 0.000000000000000000, -0.9126074666063545004, -0.4088369013363783999 ) ) ;
#17515=CARTESIAN_POINT ( 'NONE',  ( 18.59999999999999076, 67.74990736105834799, -227.9721689390126755 ) ) ;
#17557=DIRECTION ( 'NONE',  ( -1.000000000000000000, 0.000000000000000000, 0.000000000000000000 ) ) ;
#17563=LINE ( 'NONE', #180512, #132649 ) ;
#17577=EDGE_LOOP ( 'NONE', ( #63159, #50175, #253092, #255822, #198391 ) ) ;
#17615=DIRECTION ( 'NONE',  ( 0.000000000000000000, -0.9126074666063765939, -0.4088369013363289950 ) ) ;
#17616=TOROIDAL_SURFACE ( 'NONE', #163394, 0.2000000000000000111, 0.1000000000000000056 ) ;
#17618=ORIENTED_EDGE ( 'NONE', *, *, #245437, .F. ) ;
#17674=LINE ( 'NONE', #37273, #200812 ) ;
#17678=LINE ( 'NONE', #38546, #57108 ) ;
#17686=ORIENTED_EDGE ( 'NONE', *, *, #198802, .F. ) ;
#17687=CARTESIAN_POINT ( 'NONE',  ( 18.57399277249656322, 68.10911674539558192, -224.1414149070238864 ) ) ;
#17705=DIRECTION ( 'NONE',  ( 0.000000000000000000, 0.9654421110809058293, 0.2606175937108693996 ) ) ;
#17727=AXIS2_PLACEMENT_3D ( 'NONE', #126406, #242503, #66442 ) ;
#17745=CARTESIAN_POINT ( 'NONE',  ( 22.59999999999999076, 25.91621630664725728, -254.3113660372828804 ) ) ;
#17752=EDGE_CURVE ( 'NONE', #3898, #26858, #186392, .T. ) ;
#17766=CARTESIAN_POINT ( 'NONE',  ( -23.15000000000000213, 56.46250644710310951, -240.6794019422471251 ) ) ;
#17768=ORIENTED_EDGE ( 'NONE', *, *, #112644, .F. ) ;
#17772=ORIENTED_EDGE ( 'NONE', *, *, #64320, .T. ) ;
#17793=CARTESIAN_POINT ( 'NONE',  ( -21.93340585971078838, 33.66454284798572161, -242.8670914416577773 ) ) ;
#17803=DIRECTION ( 'NONE',  ( 0.000000000000000000, 0.9126074666063660468, 0.4088369013363524762 ) ) ;
#17817=AXIS2_PLACEMENT_3D ( 'NONE', #223485, #44869, #184362 ) ;
#17818=CIRCLE ( 'NONE', #146987, 0.09999999999999939493 ) ;
#17847=CARTESIAN_POINT ( 'NONE',  ( -23.25000000000000000, 51.38014393322265505, -230.1906178717505611 ) ) ;
#17849=EDGE_CURVE ( 'NONE', #36016, #168134, #217619, .T. ) ;
#17861=EDGE_CURVE ( 'NONE', #19219, #78948, #86381, .T. ) ;
#17878=CARTESIAN_POINT ( 'NONE',  ( -22.47120815636973390, 26.01529255436784993, -254.2877069526234948 ) ) ;
#17943=CARTESIAN_POINT ( 'NONE',  ( 20.96428641293985962, 56.19879751615954433, -227.9223442982753625 ) ) ;
#17978=ORIENTED_EDGE ( 'NONE', *, *, #122954, .T. ) ;
#17982=EDGE_LOOP ( 'NONE', ( #112617, #195850, #181578, #80466, #119256, #245111, #90958 ) ) ;
#17986=TOROIDAL_SURFACE ( 'NONE', #113666, 0.4000000000000003553, 0.1000000000000000056 ) ;
#17998=EDGE_LOOP ( 'NONE', ( #175306, #196932, #154323, #46991, #83207, #96275, #218169, #53147, #74169, #144698, #228350, #176031, #206038, #167880, #237174, #93757, #104266, #23591 ) ) ;
#18020=DIRECTION ( 'NONE',  ( 0.000000000000000000, 0.9126074666063772600, 0.4088369013363274962 ) ) ;
#18024=EDGE_LOOP ( 'NONE', ( #104683, #130053, #92776, #246641 ) ) ;
#18047=DIRECTION ( 'NONE',  ( 1.000000000000000000, 0.000000000000000000, 0.000000000000000000 ) ) ;
#18063=AXIS2_PLACEMENT_3D ( 'NONE', #160120, #158838, #146603 ) ;
#18070=ORIENTED_EDGE ( 'NONE', *, *, #80659, .F. ) ;
#18074=VERTEX_POINT ( 'NONE', #28477 ) ;
#18075=EDGE_LOOP ( 'NONE', ( #40777, #81483, #99974, #63599 ) ) ;
#18098=EDGE_CURVE ( 'NONE', #191031, #143511, #82294, .T. ) ;
#18114=EDGE_LOOP ( 'NONE', ( #211316, #58507, #160223, #247767 ) ) ;
#18121=EDGE_CURVE ( 'NONE', #77834, #18296, #203312, .T. ) ;
#18125=CARTESIAN_POINT ( 'NONE',  ( -21.05000000000000071, 67.23127455305835554, -235.8551265064784559 ) ) ;
#18152=CARTESIAN_POINT ( 'NONE',  ( -23.25000000000000000, 51.28888318656201761, -230.2315015618842153 ) ) ;
#18154=AXIS2_PLACEMENT_3D ( 'NONE', #158049, #79718, #180144 ) ;
#18255=CARTESIAN_POINT ( 'NONE',  ( -23.15000000000000213, 36.65892442174472876, -249.5511627012454596 ) ) ;
#18296=VERTEX_POINT ( 'NONE', #256393 ) ;
#18322=ORIENTED_EDGE ( 'NONE', *, *, #127089, .T. ) ;
#18340=CARTESIAN_POINT ( 'NONE',  ( 21.14999999999999503, 31.85509083104287598, -238.8280249686205536 ) ) ;
#18364=EDGE_LOOP ( 'NONE', ( #183795, #244428, #228169, #251987 ) ) ;
#18427=PLANE ( 'NONE',  #213241 ) ;
#18465=VECTOR ( 'NONE', #148120, 1000.000000000000000 ) ;
#18472=VECTOR ( 'NONE', #204899, 1000.000000000000114 ) ;
#18483=CIRCLE ( 'NONE', #201637, 0.09999999999999609201 ) ;
#18487=EDGE_CURVE ( 'NONE', #102676, #227500, #11130, .T. ) ;
#18502=DIRECTION ( 'NONE',  ( -1.000000000000000000, 0.000000000000000000, 0.000000000000000000 ) ) ;
#18513=ORIENTED_EDGE ( 'NONE', *, *, #105712, .F. ) ;
#18523=CIRCLE ( 'NONE', #235009, 4.049999999999999822 ) ;
#18543=CARTESIAN_POINT ( 'NONE',  ( 18.59999999999999076, 62.46832465249013921, -225.2232495205141731 ) ) ;
#18554=CARTESIAN_POINT ( 'NONE',  ( 20.94999999999999574, 44.43513953521873106, -247.3415577889845736 ) ) ;
#18556=DIRECTION ( 'NONE',  ( 1.000000000000000000, 0.000000000000000000, 0.000000000000000000 ) ) ;
#18558=EDGE_LOOP ( 'NONE', ( #173327, #149018, #65673, #2573 ) ) ;
#18570=CARTESIAN_POINT ( 'NONE',  ( 20.94999999999999929, 45.06922343725926083, -238.6062154437373124 ) ) ;
#18577=AXIS2_PLACEMENT_3D ( 'NONE', #221898, #100660, #219351 ) ;
#18591=CARTESIAN_POINT ( 'NONE',  ( -22.50000000000000000, 31.80488924422933295, -238.9605610896540213 ) ) ;
#18594=ORIENTED_EDGE ( 'NONE', *, *, #36566, .F. ) ;
#18598=VERTEX_POINT ( 'NONE', #200040 ) ;
#18605=DIRECTION ( 'NONE',  ( 0.000000000000000000, 0.9126074666063660468, 0.4088369013363524762 ) ) ;
#18656=DIRECTION ( 'NONE',  ( 0.000000000000000000, 0.9126074666063660468, 0.4088369013363524762 ) ) ;
#18661=CIRCLE ( 'NONE', #14588, 0.09999999999999939493 ) ;
#18662=CARTESIAN_POINT ( 'NONE',  ( -23.15000000000000213, 31.85509083104287598, -238.8280249686205536 ) ) ;
#18679=ADVANCED_FACE ( 'NONE', ( #103475 ), #106039, .T. ) ;
#18684=ADVANCED_FACE ( 'NONE', ( #143901 ), #66937, .F. ) ;
#18696=CIRCLE ( 'NONE', #131126, 0.1999999999999987899 ) ;
#18705=AXIS2_PLACEMENT_3D ( 'NONE', #79615, #97880, #216577 ) ;
#18715=CARTESIAN_POINT ( 'NONE',  ( -23.15000000000000213, 54.31427625645084589, -236.9847968147713857 ) ) ;
#18817=VECTOR ( 'NONE', #256664, 1000.000000000000114 ) ;
#18848=DIRECTION ( 'NONE',  ( 0.000000000000000000, 0.9126074666063660468, 0.4088369013363524762 ) ) ;
#18850=ADVANCED_FACE ( 'NONE', ( #252957 ), #153663, .T. ) ;
#18875=AXIS2_PLACEMENT_3D ( 'NONE', #23150, #126057, #2256 ) ;
#18882=CARTESIAN_POINT ( 'NONE',  ( 23.14999999999999858, 45.51971589178210564, -240.3486087337583399 ) ) ;
#18887=AXIS2_PLACEMENT_3D ( 'NONE', #79426, #23357, #20779 ) ;
#18901=DIRECTION ( 'NONE',  ( 0.000000000000000000, -0.9126074666063660468, -0.4088369013363524762 ) ) ;
#18903=DIRECTION ( 'NONE',  ( -4.336808689941752679E-15, -0.8103668758649498205, 0.5859227990963324917 ) ) ;
#18918=DIRECTION ( 'NONE',  ( 0.000000000000000000, 0.9955484899852913294, -0.09425075112701486457 ) ) ;
#18930=EDGE_CURVE ( 'NONE', #89024, #120435, #220265, .T. ) ;
#18931=ORIENTED_EDGE ( 'NONE', *, *, #73852, .F. ) ;
#18950=DIRECTION ( 'NONE',  ( 1.000000000000000000, 0.000000000000000000, 0.000000000000000000 ) ) ;
#18955=ORIENTED_EDGE ( 'NONE', *, *, #32733, .F. ) ;
#19019=VERTEX_POINT ( 'NONE', #147131 ) ;
#19042=VERTEX_POINT ( 'NONE', #105407 ) ;
#19047=DIRECTION ( 'NONE',  ( 1.000000000000000000, 0.000000000000000000, 0.000000000000000000 ) ) ;
#19087=CARTESIAN_POINT ( 'NONE',  ( -21.53752568617673191, 33.79390208800049322, -243.3979355726113738 ) ) ;
#19128=EDGE_CURVE ( 'NONE', #57537, #250431, #107804, .T. ) ;
#19129=ORIENTED_EDGE ( 'NONE', *, *, #7509, .T. ) ;
#19153=CIRCLE ( 'NONE', #152461, 0.2000000000000118627 ) ;
#19155=VERTEX_POINT ( 'NONE', #196525 ) ;
#19169=DIRECTION ( 'NONE',  ( 0.000000000000000000, 0.9126074666063769270, 0.4088369013363280513 ) ) ;
#19174=DIRECTION ( 'NONE',  ( 0.000000000000000000, 0.9126074666063769270, 0.4088369013363280513 ) ) ;
#19187=PLANE ( 'NONE',  #675 ) ;
#19193=CARTESIAN_POINT ( 'NONE',  ( -18.39999999999999858, 77.26488334054519669, -241.9697969554615611 ) ) ;
#19218=DIRECTION ( 'NONE',  ( 0.000000000000000000, -0.4088369013362687654, 0.9126074666064034613 ) ) ;
#19219=VERTEX_POINT ( 'NONE', #102526 ) ;
#19228=DIRECTION ( 'NONE',  ( 1.000000000000000000, 0.000000000000000000, 0.000000000000000000 ) ) ;
#19251=CARTESIAN_POINT ( 'NONE',  ( 22.49999999999999645, 31.76322370622490965, -238.8696546380523955 ) ) ;
#19303=DIRECTION ( 'NONE',  ( 1.000000000000000000, 0.000000000000000000, 0.000000000000000000 ) ) ;
#19344=EDGE_CURVE ( 'NONE', #157687, #215487, #133582, .T. ) ;
#19350=DIRECTION ( 'NONE',  ( 0.000000000000000000, -0.9126074666063660468, -0.4088369013363524762 ) ) ;
#19361=EDGE_CURVE ( 'NONE', #243903, #241027, #9879, .T. ) ;
#19379=FACE_BOUND ( 'NONE', #196060, .T. ) ;
#19420=ORIENTED_EDGE ( 'NONE', *, *, #45505, .T. ) ;
#19434=EDGE_CURVE ( 'NONE', #119565, #103333, #187776, .T. ) ;
#19443=CARTESIAN_POINT ( 'NONE',  ( -20.93975676684922504, 68.05374558910872906, -224.1882283518532120 ) ) ;
#19450=DIRECTION ( 'NONE',  ( 0.000000000000000000, 0.9126074666063132002, 0.4088369013364708815 ) ) ;
#19465=ORIENTED_EDGE ( 'NONE', *, *, #153417, .F. ) ;
#19531=DIRECTION ( 'NONE',  ( 1.000000000000000000, 0.000000000000000000, -0.000000000000000000 ) ) ;
#19539=CIRCLE ( 'NONE', #256791, 0.09999999999999609201 ) ;
#19561=CARTESIAN_POINT ( 'NONE',  ( 23.24999999999999645, 67.23127455305835554, -235.8551265064784559 ) ) ;
#19602=CARTESIAN_POINT ( 'NONE',  ( 20.94999999999999929, 62.04503132991427350, -248.4786563706009588 ) ) ;
#19615=EDGE_CURVE ( 'NONE', #212825, #77135, #66956, .T. ) ;
#19669=DIRECTION ( 'NONE',  ( 0.000000000000000000, 0.9126074666063545004, 0.4088369013363783999 ) ) ;
#19675=AXIS2_PLACEMENT_3D ( 'NONE', #203245, #145825, #63731 ) ;
#19695=CIRCLE ( 'NONE', #165443, 0.09999999999999695244 ) ;
#19698=EDGE_LOOP ( 'NONE', ( #60673, #37912, #194931, #109236, #253158 ) ) ;
#19717=ORIENTED_EDGE ( 'NONE', *, *, #218107, .F. ) ;
#19738=DIRECTION ( 'NONE',  ( 0.000000000000000000, 0.9126074666063660468, 0.4088369013363524762 ) ) ;
#19818=ADVANCED_FACE ( 'NONE', ( #43574 ), #200415, .T. ) ;
#19819=DIRECTION ( 'NONE',  ( -4.336808689942053235E-15, 0.8103668758649498205, -0.5859227990963324917 ) ) ;
#19847=DIRECTION ( 'NONE',  ( 0.000000000000000000, -0.9992764785629962843, -0.03803313543132441632 ) ) ;
#19856=CARTESIAN_POINT ( 'NONE',  ( -23.25000000000000000, 63.67210543329348837, -237.4495904216901181 ) ) ;
#19895=CARTESIAN_POINT ( 'NONE',  ( 20.94999999999999574, 46.53760404070597900, -243.0973507280067167 ) ) ;
#19896=CARTESIAN_POINT ( 'NONE',  ( -21.55000000000000426, 52.90028168070691095, -233.8284721206281915 ) ) ;
#19942=CARTESIAN_POINT ( 'NONE',  ( -20.54999999999999716, 47.70572087816298534, -241.8629305864830030 ) ) ;
#19957=DIRECTION ( 'NONE',  ( 1.000000000000000000, 0.000000000000000000, 0.000000000000000000 ) ) ;
#20000=DIRECTION ( 'NONE',  ( -2.952720810173289112E-16, -0.4088369013363281068, 0.9126074666063770380 ) ) ;
#20051=DIRECTION ( 'NONE',  ( -1.000000000000000000, -0.000000000000000000, -0.000000000000000000 ) ) ;
#20062=AXIS2_PLACEMENT_3D ( 'NONE', #121595, #163269, #177715 ) ;
#20070=ORIENTED_EDGE ( 'NONE', *, *, #84983, .T. ) ;
#20083=DIRECTION ( 'NONE',  ( 0.000000000000000000, 0.4088369013363280513, -0.9126074666063769270 ) ) ;
#20105=ORIENTED_EDGE ( 'NONE', *, *, #62846, .T. ) ;
#20130=CARTESIAN_POINT ( 'NONE',  ( -18.54270223418606633, 77.31779168390137613, -241.8822140496988595 ) ) ;
#20196=ORIENTED_EDGE ( 'NONE', *, *, #36727, .T. ) ;
#20200=ADVANCED_FACE ( 'NONE', ( #127944 ), #94766, .F. ) ;
#20207=ORIENTED_EDGE ( 'NONE', *, *, #244651, .F. ) ;
#20241=EDGE_CURVE ( 'NONE', #217929, #97383, #88785, .T. ) ;
#20284=CARTESIAN_POINT ( 'NONE',  ( 18.59999999999999787, 36.65892442174472876, -249.5511627012454596 ) ) ;
#20304=DIRECTION ( 'NONE',  ( 0.000000000000000000, 0.9126074666063660468, 0.4088369013363524762 ) ) ;
#20335=ORIENTED_EDGE ( 'NONE', *, *, #66408, .F. ) ;
#20342=EDGE_CURVE ( 'NONE', #91403, #256883, #136436, .T. ) ;
#20345=EDGE_CURVE ( 'NONE', #15058, #33224, #78203, .T. ) ;
#20348=DIRECTION ( 'NONE',  ( 0.000000000000000000, 0.8103668758649577031, -0.5859227990963212784 ) ) ;
#20356=VERTEX_POINT ( 'NONE', #85753 ) ;
#20362=EDGE_CURVE ( 'NONE', #104038, #58341, #219846, .T. ) ;
#20379=LINE ( 'NONE', #223356, #125165 ) ;
#20385=VECTOR ( 'NONE', #37255, 1000.000000000000114 ) ;
#20413=AXIS2_PLACEMENT_3D ( 'NONE', #45740, #104404, #26194 ) ;
#20428=AXIS2_PLACEMENT_3D ( 'NONE', #51737, #171748, #208290 ) ;
#20438=EDGE_CURVE ( 'NONE', #5729, #83103, #212675, .T. ) ;
#20478=CARTESIAN_POINT ( 'NONE',  ( -22.45372860728439690, 26.02113247230217752, -254.3004129941882638 ) ) ;
#20493=VERTEX_POINT ( 'NONE', #251268 ) ;
#20496=CARTESIAN_POINT ( 'NONE',  ( -18.39999999999999858, 77.43243075322048696, -241.6948671442531520 ) ) ;
#20512=ORIENTED_EDGE ( 'NONE', *, *, #65515, .T. ) ;
#20514=DIRECTION ( 'NONE',  ( 0.000000000000000000, 0.9126074666063770380, 0.4088369013363281068 ) ) ;
#20523=EDGE_CURVE ( 'NONE', #61601, #241398, #107431, .T. ) ;
#20553=CIRCLE ( 'NONE', #228828, 0.09999999999999277522 ) ;
#20568=CARTESIAN_POINT ( 'NONE',  ( 21.11927991906888025, 34.01425264317992969, -243.6699334763191871 ) ) ;
#20608=CARTESIAN_POINT ( 'NONE',  ( 23.15000000000000213, 69.16514130714681130, -247.7543978865853660 ) ) ;
#20625=DIRECTION ( 'NONE',  ( 1.000000000000000000, 0.000000000000000000, 0.000000000000000000 ) ) ;
#20660=AXIS2_PLACEMENT_3D ( 'NONE', #14449, #10580, #93949 ) ;
#20669=AXIS2_PLACEMENT_3D ( 'NONE', #101273, #180876, #182160 ) ;
#20681=DIRECTION ( 'NONE',  ( 0.000000000000000000, -0.9126074666063622720, -0.4088369013363611360 ) ) ;
#20711=CARTESIAN_POINT ( 'NONE',  ( 23.14999999999999858, 68.82573846827003194, -239.4142956262433302 ) ) ;
#20738=CARTESIAN_POINT ( 'NONE',  ( -20.94999999999999929, 68.00417547777207972, -224.2303273613012777 ) ) ;
#20754=ADVANCED_FACE ( 'NONE', ( #206311 ), #192854, .F. ) ;
#20770=AXIS2_PLACEMENT_3D ( 'NONE', #88194, #51632, #32132 ) ;
#20773=CARTESIAN_POINT ( 'NONE',  ( 20.94999999999999929, 43.12265650693429819, -239.4782534460092052 ) ) ;
#20779=DIRECTION ( 'NONE',  ( 0.000000000000000000, -0.9126074666063773710, -0.4088369013363274962 ) ) ;
#20812=LINE ( 'NONE', #256775, #219556 ) ;
#20827=DIRECTION ( 'NONE',  ( 0.000000000000000000, 0.9126074666063545004, 0.4088369013363783999 ) ) ;
#20847=FACE_OUTER_BOUND ( 'NONE', #56797, .T. ) ;
#20886=CIRCLE ( 'NONE', #74681, 0.2000000000000048683 ) ;
#20962=ORIENTED_EDGE ( 'NONE', *, *, #126176, .T. ) ;
#20973=EDGE_CURVE ( 'NONE', #183601, #61130, #105242, .T. ) ;
#20983=ORIENTED_EDGE ( 'NONE', *, *, #218872, .T. ) ;
#20995=VERTEX_POINT ( 'NONE', #154713 ) ;
#21005=ORIENTED_EDGE ( 'NONE', *, *, #27338, .F. ) ;
#21046=ORIENTED_EDGE ( 'NONE', *, *, #252511, .T. ) ;
#21070=EDGE_LOOP ( 'NONE', ( #163947, #254500, #30415, #236531 ) ) ;
#21075=DIRECTION ( 'NONE',  ( 0.000000000000000000, 0.9177795674685970129, 0.3970902486049678326 ) ) ;
#21085=CARTESIAN_POINT ( 'NONE',  ( -23.25000000000000000, 47.40541193113006813, -242.6436572752161283 ) ) ;
#21104=DIRECTION ( 'NONE',  ( -0.000000000000000000, -0.9126074666063769270, -0.4088369013363283844 ) ) ;
#21113=EDGE_CURVE ( 'NONE', #250431, #65749, #193819, .T. ) ;
#21123=DIRECTION ( 'NONE',  ( -1.000000000000000000, -0.000000000000000000, 0.000000000000000000 ) ) ;
#21124=EDGE_CURVE ( 'NONE', #71259, #120435, #140539, .T. ) ;
#21148=VERTEX_POINT ( 'NONE', #256275 ) ;
#21205=DIRECTION ( 'NONE',  ( 1.000000000000000000, 0.000000000000000000, 0.000000000000000000 ) ) ;
#21218=CARTESIAN_POINT ( 'NONE',  ( 18.49999999999998934, 55.05538098155519577, -230.0782228604559805 ) ) ;
#21219=AXIS2_PLACEMENT_3D ( 'NONE', #148755, #14395, #32696 ) ;
#21247=AXIS2_PLACEMENT_3D ( 'NONE', #53163, #201656, #98662 ) ;
#21252=ORIENTED_EDGE ( 'NONE', *, *, #67679, .F. ) ;
#21289=CARTESIAN_POINT ( 'NONE',  ( -23.15000000000000213, 47.45383559552795560, -242.5236527704543334 ) ) ;
#21322=AXIS2_PLACEMENT_3D ( 'NONE', #1678, #179082, #60372 ) ;
#21323=VERTEX_POINT ( 'NONE', #124555 ) ;
#21329=ORIENTED_EDGE ( 'NONE', *, *, #256621, .T. ) ;
#21338=CIRCLE ( 'NONE', #17396, 0.1000000000000062367 ) ;
#21343=EDGE_CURVE ( 'NONE', #147844, #248466, #232713, .T. ) ;
#21355=FACE_OUTER_BOUND ( 'NONE', #156614, .T. ) ;
#21358=FACE_OUTER_BOUND ( 'NONE', #607, .T. ) ;
#21378=AXIS2_PLACEMENT_3D ( 'NONE', #173814, #91652, #132060 ) ;
#21383=CARTESIAN_POINT ( 'NONE',  ( 20.95512820512820440, 40.84069494668059264, -237.9516373772122506 ) ) ;
#21407=ORIENTED_EDGE ( 'NONE', *, *, #223, .T. ) ;
#21455=DIRECTION ( 'NONE',  ( 0.000000000000000000, 0.9126074666063772600, 0.4088369013363276627 ) ) ;
#21490=ADVANCED_FACE ( 'NONE', ( #220777 ), #121697, .T. ) ;
#21519=VERTEX_POINT ( 'NONE', #99512 ) ;
#21526=DIRECTION ( 'NONE',  ( 1.000000000000000000, 0.000000000000000000, -0.000000000000000000 ) ) ;
#21542=AXIS2_PLACEMENT_3D ( 'NONE', #250384, #112182, #151307 ) ;
#21593=VECTOR ( 'NONE', #152594, 1000.000000000000000 ) ;
#21596=CARTESIAN_POINT ( 'NONE',  ( 23.25000000000000000, 49.36776662947724503, -253.7196102226803021 ) ) ;
#21602=ORIENTED_EDGE ( 'NONE', *, *, #171245, .F. ) ;
#21608=CARTESIAN_POINT ( 'NONE',  ( 20.93302460841143287, 68.06642993404715014, -224.1774859612004036 ) ) ;
#21645=CARTESIAN_POINT ( 'NONE',  ( 22.39999999999999503, 30.91424406532124181, -252.0151325879369040 ) ) ;
#21674=ORIENTED_EDGE ( 'NONE', *, *, #35523, .F. ) ;
#21687=DIRECTION ( 'NONE',  ( 0.000000000000000000, 0.9126074666063770380, 0.4088369013363281068 ) ) ;
#21689=DIRECTION ( 'NONE',  ( -1.000000000000000000, -0.000000000000000000, -0.000000000000000000 ) ) ;
#21700=EDGE_CURVE ( 'NONE', #84696, #20356, #190646, .T. ) ;
#21738=AXIS2_PLACEMENT_3D ( 'NONE', #48056, #225395, #29820 ) ;
#21768=DIRECTION ( 'NONE',  ( -1.000000000000000000, 0.000000000000000000, 0.000000000000000000 ) ) ;
#21774=CARTESIAN_POINT ( 'NONE',  ( -18.43459694179565744, 77.15158635572022661, -241.8143376528992405 ) ) ;
#21806=FACE_OUTER_BOUND ( 'NONE', #106533, .T. ) ;
#21814=FACE_OUTER_BOUND ( 'NONE', #221731, .T. ) ;
#21837=CARTESIAN_POINT ( 'NONE',  ( 21.08621493067296271, 34.01181478797902713, -243.7797238474834387 ) ) ;
#21841=AXIS2_PLACEMENT_3D ( 'NONE', #257316, #256030, #235240 ) ;
#21856=CIRCLE ( 'NONE', #17727, 0.1999999999999893807 ) ;
#21889=CARTESIAN_POINT ( 'NONE',  ( 18.59999994388910238, 47.04063701600456682, -255.1605173984034423 ) ) ;
#21929=VERTEX_POINT ( 'NONE', #101764 ) ;
#21936=EDGE_LOOP ( 'NONE', ( #141099, #165432, #41584, #142019 ) ) ;
#21974=ADVANCED_FACE ( 'NONE', ( #171380 ), #172671, .T. ) ;
#21987=VECTOR ( 'NONE', #22447, 1000.000000000000000 ) ;
#21988=FACE_OUTER_BOUND ( 'NONE', #239432, .T. ) ;
#22010=ORIENTED_EDGE ( 'NONE', *, *, #171325, .T. ) ;
#22038=CARTESIAN_POINT ( 'NONE',  ( 18.44206774312971220, 77.15870146463355184, -241.8076626181645281 ) ) ;
#22079=CARTESIAN_POINT ( 'NONE',  ( -20.64999999999999858, 36.65892442174472876, -249.5511627012454596 ) ) ;
#22149=FACE_OUTER_BOUND ( 'NONE', #249280, .T. ) ;
#22174=EDGE_LOOP ( 'NONE', ( #88346, #33867, #46568, #71950, #167575, #9880, #24608 ) ) ;
#22207=AXIS2_PLACEMENT_3D ( 'NONE', #198854, #21526, #99730 ) ;
#22212=FACE_OUTER_BOUND ( 'NONE', #120991, .T. ) ;
#22214=ORIENTED_EDGE ( 'NONE', *, *, #95556, .T. ) ;
#22271=EDGE_CURVE ( 'NONE', #101872, #77834, #121646, .T. ) ;
#22286=VECTOR ( 'NONE', #38282, 1000.000000000000114 ) ;
#22305=LINE ( 'NONE', #62697, #38652 ) ;
#22314=ORIENTED_EDGE ( 'NONE', *, *, #199964, .F. ) ;
#22323=AXIS2_PLACEMENT_3D ( 'NONE', #100610, #101904, #221850 ) ;
#22354=CARTESIAN_POINT ( 'NONE',  ( 21.30000000000002558, 36.65892442174472876, -249.5511627012454596 ) ) ;
#22382=TOROIDAL_SURFACE ( 'NONE', #134749, 11.65000000000000036, 0.1000000000000000056 ) ;
#22447=DIRECTION ( 'NONE',  ( 1.000000000000000000, 0.000000000000000000, 0.000000000000000000 ) ) ;
#22449=ORIENTED_EDGE ( 'NONE', *, *, #174102, .T. ) ;
#22507=AXIS2_PLACEMENT_3D ( 'NONE', #13762, #108993, #170317 ) ;
#22530=CARTESIAN_POINT ( 'NONE',  ( 18.60000000000001208, 47.04012343383972450, -255.1614814433716845 ) ) ;
#22531=CARTESIAN_POINT ( 'NONE',  ( 18.59999999999999787, 46.53760404070597900, -243.0973507280067167 ) ) ;
#22538=ADVANCED_FACE ( 'NONE', ( #61232 ), #198171, .F. ) ;
#22546=ORIENTED_EDGE ( 'NONE', *, *, #229832, .F. ) ;
#22554=ORIENTED_EDGE ( 'NONE', *, *, #12273, .T. ) ;
#22556=ORIENTED_EDGE ( 'NONE', *, *, #39750, .T. ) ;
#22566=CIRCLE ( 'NONE', #122527, 12.87499999999999112 ) ;
#22568=CARTESIAN_POINT ( 'NONE',  ( -20.99551997958471361, 56.17759395754637808, -227.9318432312958294 ) ) ;
#22575=ADVANCED_FACE ( 'NONE', ( #100330 ), #96484, .T. ) ;
#22626=DIRECTION ( 'NONE',  ( 0.000000000000000000, -0.9126074666063770380, -0.4088369013363281068 ) ) ;
#22629=CARTESIAN_POINT ( 'NONE',  ( 21.05000000000000071, 26.06832281015329755, -254.4051978787608732 ) ) ;
#22641=CARTESIAN_POINT ( 'NONE',  ( 21.10710606213542206, 44.24183109435373495, -236.5367325923057251 ) ) ;
#22671=CARTESIAN_POINT ( 'NONE',  ( -21.05000000000000071, 31.98723526783714988, -238.8784020251475511 ) ) ;
#22681=CARTESIAN_POINT ( 'NONE',  ( -21.05000000000000071, 34.01125473725046078, -243.8802146427659352 ) ) ;
#22682=CARTESIAN_POINT ( 'NONE',  ( 20.95512820512820440, 40.84069494668059264, -237.9516373772122222 ) ) ;
#22725=LINE ( 'NONE', #220884, #191557 ) ;
#22737=CARTESIAN_POINT ( 'NONE',  ( -18.59999999999999787, 74.44087353924872730, -232.6253149859214773 ) ) ;
#22771=ORIENTED_EDGE ( 'NONE', *, *, #205952, .T. ) ;
#22782=AXIS2_PLACEMENT_3D ( 'NONE', #108100, #143361, #83362 ) ;
#22854=ADVANCED_FACE ( 'NONE', ( #169363 ), #50633, .T. ) ;
#22864=SURFACE_SIDE_STYLE ('',( #240597 ) ) ;
#22890=DIRECTION ( 'NONE',  ( 0.000000000000000000, 0.4088369013363322146, -0.9126074666063751506 ) ) ;
#22927=EDGE_CURVE ( 'NONE', #24913, #148383, #3923, .T. ) ;
#22954=VERTEX_POINT ( 'NONE', #256491 ) ;
#22969=CIRCLE ( 'NONE', #97745, 0.09999999999999609201 ) ;
#23026=ORIENTED_EDGE ( 'NONE', *, *, #8264, .T. ) ;
#23035=VECTOR ( 'NONE', #45638, 1000.000000000000000 ) ;
#23038=ORIENTED_EDGE ( 'NONE', *, *, #84330, .F. ) ;
#23053=CARTESIAN_POINT ( 'NONE',  ( -22.49756042579671700, 25.99526245069998254, -254.2428317230260291 ) ) ;
#23061=CARTESIAN_POINT ( 'NONE',  ( -21.05000000000000071, 34.07086262126583875, -243.8523844785541428 ) ) ;
#23085=CARTESIAN_POINT ( 'NONE',  ( -18.49499033040906681, 47.08667629969059476, -255.2216170810507947 ) ) ;
#23088=CARTESIAN_POINT ( 'NONE',  ( -18.50000000000000000, 36.65892442174472876, -249.5511627012454596 ) ) ;
#23112=EDGE_CURVE ( 'NONE', #56338, #207268, #3500, .T. ) ;
#23123=DIRECTION ( 'NONE',  ( 0.000000000000000000, 0.8412123295017488456, 0.5407049257166434142 ) ) ;
#23132=VERTEX_POINT ( 'NONE', #7361 ) ;
#23136=CARTESIAN_POINT ( 'NONE',  ( 21.07971444708685738, 33.99092351726255856, -243.8104526470560813 ) ) ;
#23143=DIRECTION ( 'NONE',  ( 0.000000000000000000, 0.9126074666063545004, 0.4088369013363783999 ) ) ;
#23150=CARTESIAN_POINT ( 'NONE',  ( -18.59999999999999787, 53.17902629910250312, -234.2060907248186368 ) ) ;
#23161=EDGE_CURVE ( 'NONE', #179534, #215487, #249834, .T. ) ;
#23176=LINE ( 'NONE', #102654, #5126 ) ;
#23184=CARTESIAN_POINT ( 'NONE',  ( -22.39999999999999503, 29.54900078958453236, -252.7363208912387620 ) ) ;
#23193=CARTESIAN_POINT ( 'NONE',  ( 18.50000000000000000, 47.16152503674115337, -255.1462838189583806 ) ) ;
#23212=ADVANCED_FACE ( 'NONE', ( #69933 ), #228780, .F. ) ;
#23294=CARTESIAN_POINT ( 'NONE',  ( 20.94999999999999574, 46.45388641681647357, -243.1520440498138385 ) ) ;
#23300=CIRCLE ( 'NONE', #10809, 0.09999999999999609201 ) ;
#23311=CARTESIAN_POINT ( 'NONE',  ( 23.14999999999999503, 56.06656052939784729, -228.0911609752645290 ) ) ;
#23317=DIRECTION ( 'NONE',  ( 0.000000000000000000, -0.9126074666063844765, -0.4088369013363114535 ) ) ;
#23337=CARTESIAN_POINT ( 'NONE',  ( 18.47135592147650840, 77.20290371986166633, -241.7660124468425522 ) ) ;
#23357=DIRECTION ( 'NONE',  ( 1.000000000000000000, 0.000000000000000000, -0.000000000000000000 ) ) ;
#23407=CIRCLE ( 'NONE', #48313, 0.09999999999999741040 ) ;
#23425=DIRECTION ( 'NONE',  ( -1.000000000000000000, -0.000000000000000000, -0.000000000000000000 ) ) ;
#23435=DIRECTION ( 'NONE',  ( -1.000000000000000000, -0.000000000000000000, 0.000000000000000000 ) ) ;
#23466=CYLINDRICAL_SURFACE ( 'NONE', #58418, 0.09999999999999609201 ) ;
#23481=ORIENTED_EDGE ( 'NONE', *, *, #254008, .T. ) ;
#23483=DIRECTION ( 'NONE',  ( -1.000000000000000000, 0.000000000000000000, 0.000000000000000000 ) ) ;
#23486=EDGE_CURVE ( 'NONE', #105957, #227500, #154171, .T. ) ;
#23491=ORIENTED_EDGE ( 'NONE', *, *, #110843, .F. ) ;
#23502=FACE_OUTER_BOUND ( 'NONE', #184526, .T. ) ;
#23520=ORIENTED_EDGE ( 'NONE', *, *, #197703, .F. ) ;
#23528=( BOUNDED_CURVE ( )  B_SPLINE_CURVE ( 3, ( #163172, #116638, #55336, #155792 ),
 .UNSPECIFIED., .F., .F. ) 
 B_SPLINE_CURVE_WITH_KNOTS ( ( 4, 4 ),
 ( 3.141592653589706519, 4.712388980384571546 ),
 .UNSPECIFIED. ) 
 CURVE ( )  GEOMETRIC_REPRESENTATION_ITEM ( )  RATIONAL_B_SPLINE_CURVE ( ( 1.000000000000000000, 0.8047378541243723760, 0.8047378541243723760, 1.000000000000000000 ) ) 
 REPRESENTATION_ITEM ( '' )  );
#23537=ORIENTED_EDGE ( 'NONE', *, *, #167891, .T. ) ;
#23557=VECTOR ( 'NONE', #255036, 1000.000000000000114 ) ;
#23584=ADVANCED_FACE ( 'NONE', ( #26653 ), #75715, .T. ) ;
#23591=ORIENTED_EDGE ( 'NONE', *, *, #145650, .F. ) ;
#23632=CARTESIAN_POINT ( 'NONE',  ( -23.25000000000000000, 54.26389919992384137, -237.1169412515656632 ) ) ;
#23675=DIRECTION ( 'NONE',  ( 0.000000000000000000, -0.4088369013363783999, 0.9126074666063545004 ) ) ;
#23712=ADVANCED_FACE ( 'NONE', ( #241211 ), #23466, .F. ) ;
#23725=EDGE_CURVE ( 'NONE', #206012, #124831, #121020, .T. ) ;
#23759=ADVANCED_FACE ( 'NONE', ( #130798 ), #29442, .F. ) ;
#23772=EDGE_CURVE ( 'NONE', #14564, #56338, #216664, .T. ) ;
#23797=ORIENTED_EDGE ( 'NONE', *, *, #106100, .F. ) ;
#23807=CARTESIAN_POINT ( 'NONE',  ( 21.14999999999999503, 36.65892442174472876, -249.5511627012454596 ) ) ;
#23812=VECTOR ( 'NONE', #14716, 1000.000000000000114 ) ;
#23826=EDGE_LOOP ( 'NONE', ( #149908, #110448 ) ) ;
#23831=ORIENTED_EDGE ( 'NONE', *, *, #147397, .F. ) ;
#23861=DIRECTION ( 'NONE',  ( 1.000000000000000000, -1.335000415235278971E-16, 2.979993593738921214E-16 ) ) ;
#23870=CARTESIAN_POINT ( 'NONE',  ( -21.04386569057474432, 56.16954312985654241, -227.9354499029107046 ) ) ;
#23875=EDGE_CURVE ( 'NONE', #139949, #92460, #187645, .T. ) ;
#23908=CIRCLE ( 'NONE', #173954, 0.2000000000000048683 ) ;
#23921=DIRECTION ( 'NONE',  ( 0.000000000000000000, 0.9126074666063772600, 0.4088369013363274407 ) ) ;
#23941=LINE ( 'NONE', #83840, #195894 ) ;
#23943=ORIENTED_EDGE ( 'NONE', *, *, #215986, .F. ) ;
#23966=CIRCLE ( 'NONE', #19675, 0.1000000000000033501 ) ;
#23972=ORIENTED_EDGE ( 'NONE', *, *, #36727, .F. ) ;
#24026=DIRECTION ( 'NONE',  ( 1.000000000000000000, 0.000000000000000000, 0.000000000000000000 ) ) ;
#24027=VERTEX_POINT ( 'NONE', #242823 ) ;
#24053=AXIS2_PLACEMENT_3D ( 'NONE', #197349, #216909, #38295 ) ;
#24063=EDGE_CURVE ( 'NONE', #251832, #19019, #183534, .T. ) ;
#24073=ORIENTED_EDGE ( 'NONE', *, *, #38507, .F. ) ;
#24089=DIRECTION ( 'NONE',  ( 0.000000000000000000, -0.4088369013363283289, 0.9126074666063768159 ) ) ;
#24102=CARTESIAN_POINT ( 'NONE',  ( 21.05000000000000426, 39.14562251533264003, -236.8628884932207654 ) ) ;
#24109=AXIS2_PLACEMENT_3D ( 'NONE', #79110, #158704, #162545 ) ;
#24149=ADVANCED_FACE ( 'NONE', ( #208844 ), #204360, .F. ) ;
#24168=CARTESIAN_POINT ( 'NONE',  ( 22.44352723754030166, 26.02350891930491272, -254.3055323313045903 ) ) ;
#24174=EDGE_CURVE ( 'NONE', #153695, #46950, #159168, .T. ) ;
#24183=VECTOR ( 'NONE', #141230, 1000.000000000000000 ) ;
#24193=EDGE_CURVE ( 'NONE', #241192, #14385, #91934, .T. ) ;
#24209=CARTESIAN_POINT ( 'NONE',  ( 18.59999999999999076, 53.33306769324366314, -234.7945388949160872 ) ) ;
#24213=ORIENTED_EDGE ( 'NONE', *, *, #156055, .F. ) ;
#24229=AXIS2_PLACEMENT_3D ( 'NONE', #88566, #209827, #149864 ) ;
#24276=CARTESIAN_POINT ( 'NONE',  ( -23.25000000000000000, 69.20602499728043711, -247.8456586332460176 ) ) ;
#24307=ORIENTED_EDGE ( 'NONE', *, *, #206006, .T. ) ;
#24362=ORIENTED_EDGE ( 'NONE', *, *, #88738, .F. ) ;
#24402=DIRECTION ( 'NONE',  ( 1.000000000000000000, 0.000000000000000000, 0.000000000000000000 ) ) ;
#24404=VECTOR ( 'NONE', #108374, 1000.000000000000114 ) ;
#24438=VERTEX_POINT ( 'NONE', #152445 ) ;
#24446=DIRECTION ( 'NONE',  ( 0.000000000000000000, -0.9126074666063770380, -0.4088369013363281068 ) ) ;
#24454=VERTEX_POINT ( 'NONE', #186422 ) ;
#24456=CIRCLE ( 'NONE', #11983, 0.09999999999999351075 ) ;
#24474=AXIS2_PLACEMENT_3D ( 'NONE', #138918, #81518, #22890 ) ;
#24480=DIRECTION ( 'NONE',  ( 0.000000000000000000, -0.2868887416115947775, 0.9579639084728169829 ) ) ;
#24525=CARTESIAN_POINT ( 'NONE',  ( -21.98333005346336932, 29.92928821712972720, -252.5659568089976403 ) ) ;
#24528=FACE_OUTER_BOUND ( 'NONE', #29959, .T. ) ;
#24532=DIRECTION ( 'NONE',  ( 0.000000000000000000, -0.9126074666063660468, -0.4088369013363524762 ) ) ;
#24540=ORIENTED_EDGE ( 'NONE', *, *, #172587, .F. ) ;
#24554=ORIENTED_EDGE ( 'NONE', *, *, #256244, .T. ) ;
#24561=DIRECTION ( 'NONE',  ( 0.000000000000000000, 0.9126074666064177832, 0.4088369013362369020 ) ) ;
#24576=AXIS2_PLACEMENT_3D ( 'NONE', #167542, #210499, #91829 ) ;
#24577=AXIS2_PLACEMENT_3D ( 'NONE', #64696, #47685, #258041 ) ;
#24608=ORIENTED_EDGE ( 'NONE', *, *, #104895, .F. ) ;
#24621=CARTESIAN_POINT ( 'NONE',  ( 18.46163235739467368, 77.18289512160934862, -241.7849060539989807 ) ) ;
#24626=CARTESIAN_POINT ( 'NONE',  ( 21.07928932188134397, 33.98134083355422774, -243.8161431329846778 ) ) ;
#24630=DIRECTION ( 'NONE',  ( 0.000000000000000000, 0.9126074666063771490, 0.4088369013363281623 ) ) ;
#24634=AXIS2_PLACEMENT_3D ( 'NONE', #237939, #37199, #140107 ) ;
#24635=EDGE_LOOP ( 'NONE', ( #96474, #205634, #177585, #244611 ) ) ;
#24659=CARTESIAN_POINT ( 'NONE',  ( -20.94999999999999929, 47.95459712139159336, -246.5019368548292675 ) ) ;
#24678=ADVANCED_FACE ( 'NONE', ( #76711 ), #192115, .T. ) ;
#24693=ORIENTED_EDGE ( 'NONE', *, *, #61789, .T. ) ;
#24711=CARTESIAN_POINT ( 'NONE',  ( 21.05000000000000071, 55.59258605799641373, -234.6589115948038966 ) ) ;
#24716=ADVANCED_FACE ( 'NONE', ( #218784 ), #40197, .T. ) ;
#24782=CARTESIAN_POINT ( 'NONE',  ( -21.14250536705909056, 30.71039182449740679, -252.2160320164180689 ) ) ;
#24788=CARTESIAN_POINT ( 'NONE',  ( 21.05000000000000071, 43.39316802731212874, -245.2602608822587342 ) ) ;
#24791=EDGE_CURVE ( 'NONE', #238120, #84325, #105483, .T. ) ;
#24794=CARTESIAN_POINT ( 'NONE',  ( -23.25000000000000000, 49.61306877027904250, -254.2671747026441551 ) ) ;
#24815=EDGE_LOOP ( 'NONE', ( #202486, #8406, #109703, #164949 ) ) ;
#24821=CARTESIAN_POINT ( 'NONE',  ( -21.14999999999999858, 26.06832281015329755, -254.4051978787608732 ) ) ;
#24840=EDGE_LOOP ( 'NONE', ( #53075, #107350, #136682, #35365 ) ) ;
#24843=CIRCLE ( 'NONE', #132984, 0.09999999999999854838 ) ;
#24861=CARTESIAN_POINT ( 'NONE',  ( -20.94999999999999929, 44.09392520544991356, -258.8097135244738638 ) ) ;
#24913=VERTEX_POINT ( 'NONE', #27051 ) ;
#24915=VERTEX_POINT ( 'NONE', #169134 ) ;
#24925=DIRECTION ( 'NONE',  ( 1.000000000000000000, 0.000000000000000000, -0.000000000000000000 ) ) ;
#24976=DIRECTION ( 'NONE',  ( -1.000000000000000000, -0.000000000000000000, -0.000000000000000000 ) ) ;
#25018=CARTESIAN_POINT ( 'NONE',  ( 20.94999999999999929, 54.32225538558144962, -236.1594012422037281 ) ) ;
#25051=AXIS2_PLACEMENT_3D ( 'NONE', #220700, #42082, #103290 ) ;
#25078=ORIENTED_EDGE ( 'NONE', *, *, #79689, .F. ) ;
#25082=VECTOR ( 'NONE', #128892, 1000.000000000000114 ) ;
#25098=DIRECTION ( 'NONE',  ( 0.000000000000000000, -0.9126074666063660468, -0.4088369013363524762 ) ) ;
#25132=EDGE_CURVE ( 'NONE', #139340, #114526, #251447, .T. ) ;
#25149=AXIS2_PLACEMENT_3D ( 'NONE', #163481, #202606, #26554 ) ;
#25153=EDGE_CURVE ( 'NONE', #37046, #257664, #76463, .T. ) ;
#25169=EDGE_CURVE ( 'NONE', #7171, #183348, #105675, .T. ) ;
#25177=ORIENTED_EDGE ( 'NONE', *, *, #85815, .F. ) ;
#25187=ORIENTED_EDGE ( 'NONE', *, *, #54465, .F. ) ;
#25193=DIRECTION ( 'NONE',  ( -2.602085213965227050E-14, -0.9126074666063771490, -0.4088369013363281623 ) ) ;
#25226=DIRECTION ( 'NONE',  ( 0.000000000000000000, 0.9126074666063660468, 0.4088369013363524762 ) ) ;
#25231=DIRECTION ( 'NONE',  ( 1.000000000000000000, 0.000000000000000000, 0.000000000000000000 ) ) ;
#25241=DIRECTION ( 'NONE',  ( -1.000000000000000000, -0.000000000000000000, -0.000000000000000000 ) ) ;
#25249=CYLINDRICAL_SURFACE ( 'NONE', #143366, 0.09999999999999854838 ) ;
#25262=ORIENTED_EDGE ( 'NONE', *, *, #138459, .F. ) ;
#25278=ORIENTED_EDGE ( 'NONE', *, *, #86129, .F. ) ;
#25293=EDGE_CURVE ( 'NONE', #172262, #155744, #213044, .T. ) ;
#25325=SPHERICAL_SURFACE ( 'NONE', #1248, 0.1000000000000000056 ) ;
#25331=DIRECTION ( 'NONE',  ( -0.000000000000000000, 0.9594490217226103734, 0.2818822000686205254 ) ) ;
#25342=CARTESIAN_POINT ( 'NONE',  ( -21.10257677756356998, 34.02025961620756078, -243.7221525359516079 ) ) ;
#25354=CARTESIAN_POINT ( 'NONE',  ( 23.24999999999999645, 36.65892442174472876, -249.5511627012454596 ) ) ;
#25357=EDGE_LOOP ( 'NONE', ( #151001, #204439, #225467, #167651, #184226 ) ) ;
#25362=CARTESIAN_POINT ( 'NONE',  ( 21.05000000000000071, 44.34387878855809362, -247.3824414791181994 ) ) ;
#25369=AXIS2_PLACEMENT_3D ( 'NONE', #151492, #250556, #234863 ) ;
#25375=EDGE_CURVE ( 'NONE', #191992, #62719, #226478, .T. ) ;
#25399=DIRECTION ( 'NONE',  ( 0.000000000000000000, 0.5283051335750404975, -0.8490545835446967615 ) ) ;
#25413=CARTESIAN_POINT ( 'NONE',  ( -21.05000000000000071, 43.57568952063339651, -245.1784935019914826 ) ) ;
#25458=CARTESIAN_POINT ( 'NONE',  ( 21.14999999999999858, 36.65892442174472876, -249.5511627012454596 ) ) ;
#25484=ORIENTED_EDGE ( 'NONE', *, *, #170319, .F. ) ;
#25496=CARTESIAN_POINT ( 'NONE',  ( 21.05000000000002558, 39.30856869743859505, -236.7176136696176627 ) ) ;
#25501=VECTOR ( 'NONE', #202936, 1000.000000000000000 ) ;
#25523=CARTESIAN_POINT ( 'NONE',  ( -18.59999999999999787, 43.57281345108133053, -239.9888335660389487 ) ) ;
#25542=EDGE_CURVE ( 'NONE', #7829, #20356, #234153, .T. ) ;
#25547=ORIENTED_EDGE ( 'NONE', *, *, #77097, .T. ) ;
#25557=EDGE_CURVE ( 'NONE', #73589, #12219, #172584, .T. ) ;
#25559=EDGE_LOOP ( 'NONE', ( #6130, #188189, #113366, #144589 ) ) ;
#25564=ORIENTED_EDGE ( 'NONE', *, *, #206006, .F. ) ;
#25604=EDGE_CURVE ( 'NONE', #136568, #238120, #35012, .T. ) ;
#25610=DIRECTION ( 'NONE',  ( -1.000000000000000000, 0.000000000000000000, 0.000000000000000000 ) ) ;
#25640=ORIENTED_EDGE ( 'NONE', *, *, #43795, .T. ) ;
#25674=DIRECTION ( 'NONE',  ( -1.000000000000000000, -0.000000000000000000, 0.000000000000000000 ) ) ;
#25675=DIRECTION ( 'NONE',  ( 0.000000000000000000, -0.9126074666063660468, -0.4088369013363524762 ) ) ;
#25680=AXIS2_PLACEMENT_3D ( 'NONE', #16913, #14364, #55996 ) ;
#25688=DIRECTION ( 'NONE',  ( 0.000000000000000000, 0.4088369013363283289, -0.9126074666063768159 ) ) ;
#25706=CARTESIAN_POINT ( 'NONE',  ( -23.25000000000000000, 68.11287320386161070, -224.1382462126928488 ) ) ;
#25726=ADVANCED_FACE ( 'NONE', ( #81356 ), #231199, .F. ) ;
#25736=CARTESIAN_POINT ( 'NONE',  ( 18.45036689428352616, 46.93870047321756545, -255.3449267777946829 ) ) ;
#25737=CARTESIAN_POINT ( 'NONE',  ( -18.59999999999999787, 67.23127455305835554, -235.8551265064784559 ) ) ;
#25745=DIRECTION ( 'NONE',  ( 1.000000000000000000, 0.000000000000000000, 0.000000000000000000 ) ) ;
#25776=ORIENTED_EDGE ( 'NONE', *, *, #166640, .F. ) ;
#25810=CIRCLE ( 'NONE', #217512, 0.09999999999999609201 ) ;
#25819=EDGE_LOOP ( 'NONE', ( #45338, #125956, #172459, #1007 ) ) ;
#25828=DIRECTION ( 'NONE',  ( 0.000000000000000000, -0.9126074666063660468, -0.4088369013363524762 ) ) ;
#25830=DIRECTION ( 'NONE',  ( 0.000000000000000000, -0.9126074666063770380, -0.4088369013363281068 ) ) ;
#25855=VERTEX_POINT ( 'NONE', #16008 ) ;
#25859=EDGE_CURVE ( 'NONE', #130019, #227981, #95511, .T. ) ;
#25879=EDGE_LOOP ( 'NONE', ( #110430, #115190, #69627, #33630 ) ) ;
#25896=DIRECTION ( 'NONE',  ( 0.000000000000000000, -0.4088369013363296611, 0.9126074666063762608 ) ) ;
#25905=CARTESIAN_POINT ( 'NONE',  ( -21.55000000000000071, 44.92467540951147953, -237.7943620901849613 ) ) ;
#25924=VERTEX_POINT ( 'NONE', #18554 ) ;
#25931=LINE ( 'NONE', #144567, #89691 ) ;
#25934=CARTESIAN_POINT ( 'NONE',  ( -20.15000000000000568, 44.03968997137859986, -236.0634901547873312 ) ) ;
#25954=ADVANCED_FACE ( 'NONE', ( #193350 ), #130449, .T. ) ;
#25978=CARTESIAN_POINT ( 'NONE',  ( -18.50000000000000000, 45.53758419368699606, -241.2860287061636768 ) ) ;
#25981=ADVANCED_FACE ( 'NONE', ( #56368 ), #47158, .T. ) ;
#25982=CARTESIAN_POINT ( 'NONE',  ( 20.95568717954149562, 39.26254392658486125, -236.7675178030809207 ) ) ;
#25985=EDGE_CURVE ( 'NONE', #26858, #72558, #217731, .T. ) ;
#25987=VERTEX_POINT ( 'NONE', #40719 ) ;
#25991=EDGE_LOOP ( 'NONE', ( #188133, #126825, #126216, #40834 ) ) ;
#26014=DIRECTION ( 'NONE',  ( 0.000000000000000000, -0.9126074666063660468, -0.4088369013363524762 ) ) ;
#26067=DIRECTION ( 'NONE',  ( 0.000000000000000000, 0.4088369013363281623, -0.9126074666063771490 ) ) ;
#26078=ORIENTED_EDGE ( 'NONE', *, *, #108852, .T. ) ;
#26092=EDGE_CURVE ( 'NONE', #222344, #15852, #30701, .T. ) ;
#26104=EDGE_LOOP ( 'NONE', ( #191098, #134889, #24362, #128907 ) ) ;
#26107=EDGE_LOOP ( 'NONE', ( #67551, #227466, #210412, #220654 ) ) ;
#26110=ADVANCED_FACE ( 'NONE', ( #212290 ), #167081, .T. ) ;
#26130=ADVANCED_FACE ( 'NONE', ( #213542 ), #246571, .T. ) ;
#26148=VERTEX_POINT ( 'NONE', #174486 ) ;
#26149=DIRECTION ( 'NONE',  ( -1.000000000000000000, -0.000000000000000000, -0.000000000000000000 ) ) ;
#26150=CARTESIAN_POINT ( 'NONE',  ( -18.59999999999999787, 44.10700160683882132, -235.9691471569721841 ) ) ;
#26163=EDGE_CURVE ( 'NONE', #232311, #120786, #68085, .T. ) ;
#26181=EDGE_CURVE ( 'NONE', #178795, #217944, #111906, .T. ) ;
#26183=ORIENTED_EDGE ( 'NONE', *, *, #102992, .T. ) ;
#26192=DIRECTION ( 'NONE',  ( -1.000000000000000000, 1.207181226542539700E-16, -2.694675058168174199E-16 ) ) ;
#26194=DIRECTION ( 'NONE',  ( 0.000000000000000000, -0.4088369013363494231, 0.9126074666063672680 ) ) ;
#26195=ORIENTED_EDGE ( 'NONE', *, *, #12046, .F. ) ;
#26235=VECTOR ( 'NONE', #78504, 1000.000000000000114 ) ;
#26315=CARTESIAN_POINT ( 'NONE',  ( 23.14999999999999858, 63.58084468663284383, -237.4904741118237723 ) ) ;
#26320=EDGE_LOOP ( 'NONE', ( #228500, #22449, #203016, #229326 ) ) ;
#26367=EDGE_LOOP ( 'NONE', ( #127040, #160237, #174950, #99860 ) ) ;
#26372=DIRECTION ( 'NONE',  ( 0.000000000000000000, -0.9126074666063660468, -0.4088369013363524762 ) ) ;
#26376=DIRECTION ( 'NONE',  ( 0.000000000000000000, 0.2868887416115947775, -0.9579639084728169829 ) ) ;
#26385=EDGE_CURVE ( 'NONE', #124376, #97342, #251227, .T. ) ;
#26446=ORIENTED_EDGE ( 'NONE', *, *, #163341, .F. ) ;
#26456=CARTESIAN_POINT ( 'NONE',  ( 21.13461538461538325, 43.58999342716158765, -234.8150793036844846 ) ) ;
#26462=AXIS2_PLACEMENT_3D ( 'NONE', #108402, #10588, #148821 ) ;
#26478=DIRECTION ( 'NONE',  ( -0.000000000000000000, 0.9594490217226113726, 0.2818822000686178608 ) ) ;
#26480=VECTOR ( 'NONE', #248211, 1000.000000000000000 ) ;
#26481=CARTESIAN_POINT ( 'NONE',  ( -20.64999999999999858, 54.34471204062663219, -239.4366250215122420 ) ) ;
#26482=DIRECTION ( 'NONE',  ( 0.000000000000000000, -0.09425075112713271475, -0.9955484899852801162 ) ) ;
#26488=EDGE_CURVE ( 'NONE', #142241, #52160, #14132, .T. ) ;
#26495=CYLINDRICAL_SURFACE ( 'NONE', #73899, 4.000000000000002665 ) ;
#26506=DIRECTION ( 'NONE',  ( 0.000000000000000000, -0.9126074666063770380, -0.4088369013363281068 ) ) ;
#26516=DIRECTION ( 'NONE',  ( -1.000000000000000000, -0.000000000000000000, 0.000000000000000000 ) ) ;
#26518=ORIENTED_EDGE ( 'NONE', *, *, #219294, .T. ) ;
#26539=CIRCLE ( 'NONE', #118100, 0.1000000000000091788 ) ;
#26554=DIRECTION ( 'NONE',  ( 1.000000000000000000, 0.000000000000000000, 0.000000000000000000 ) ) ;
#26568=CIRCLE ( 'NONE', #172351, 0.09999999999999771572 ) ;
#26584=CARTESIAN_POINT ( 'NONE',  ( 20.94999999999999929, 61.88149656937974896, -248.1136133839584090 ) ) ;
#26604=PLANE ( 'NONE',  #235927 ) ;
#26609=CYLINDRICAL_SURFACE ( 'NONE', #98975, 0.09999999999999950595 ) ;
#26618=AXIS2_PLACEMENT_3D ( 'NONE', #127054, #206588, #106182 ) ;
#26653=FACE_OUTER_BOUND ( 'NONE', #22174, .T. ) ;
#26659=AXIS2_PLACEMENT_3D ( 'NONE', #96209, #36273, #175781 ) ;
#26692=FACE_OUTER_BOUND ( 'NONE', #25879, .T. ) ;
#26704=ADVANCED_FACE ( 'NONE', ( #85251 ), #81397, .F. ) ;
#26709=AXIS2_PLACEMENT_3D ( 'NONE', #131579, #136696, #92434 ) ;
#26717=ORIENTED_EDGE ( 'NONE', *, *, #51948, .T. ) ;
#26736=EDGE_LOOP ( 'NONE', ( #65313, #113511, #229067, #173693 ) ) ;
#26773=CARTESIAN_POINT ( 'NONE',  ( 23.14999999999999858, 36.65892442174472876, -249.5511627012454596 ) ) ;
#26787=EDGE_CURVE ( 'NONE', #78569, #139340, #230791, .T. ) ;
#26797=CARTESIAN_POINT ( 'NONE',  ( 20.95595624212449692, 39.27834562703553445, -236.7364447859425525 ) ) ;
#26808=EDGE_CURVE ( 'NONE', #28183, #116722, #68305, .T. ) ;
#26833=ORIENTED_EDGE ( 'NONE', *, *, #3552, .F. ) ;
#26849=VERTEX_POINT ( 'NONE', #90416 ) ;
#26855=EDGE_CURVE ( 'NONE', #34297, #207268, #35179, .T. ) ;
#26858=VERTEX_POINT ( 'NONE', #229938 ) ;
#26862=ORIENTED_EDGE ( 'NONE', *, *, #121659, .F. ) ;
#26875=CARTESIAN_POINT ( 'NONE',  ( -18.50000000000000000, 43.07541598710462694, -233.9110336739111631 ) ) ;
#26962=AXIS2_PLACEMENT_3D ( 'NONE', #98254, #138671, #137413 ) ;
#27002=ORIENTED_EDGE ( 'NONE', *, *, #117044, .F. ) ;
#27022=EDGE_LOOP ( 'NONE', ( #118967, #26518, #158540, #114645 ) ) ;
#27038=VERTEX_POINT ( 'NONE', #19895 ) ;
#27050=CARTESIAN_POINT ( 'NONE',  ( 18.48536876927967398, 46.96058523626525272, -255.3059130797066985 ) ) ;
#27051=CARTESIAN_POINT ( 'NONE',  ( 20.94999999999999929, 74.73788286442776041, -233.7359682632885267 ) ) ;
#27054=AXIS2_PLACEMENT_3D ( 'NONE', #24821, #27398, #147298 ) ;
#27063=DIRECTION ( 'NONE',  ( 0.000000000000000000, 0.9126074666063791474, 0.4088369013363231663 ) ) ;
#27096=DIRECTION ( 'NONE',  ( 0.000000000000000000, -0.9126074666063771490, -0.4088369013363281623 ) ) ;
#27097=ORIENTED_EDGE ( 'NONE', *, *, #194826, .F. ) ;
#27113=EDGE_CURVE ( 'NONE', #34297, #229408, #43297, .T. ) ;
#27133=EDGE_CURVE ( 'NONE', #59699, #24915, #122643, .T. ) ;
#27154=ORIENTED_EDGE ( 'NONE', *, *, #184749, .F. ) ;
#27198=ORIENTED_EDGE ( 'NONE', *, *, #235822, .T. ) ;
#27220=DIRECTION ( 'NONE',  ( 0.000000000000000000, 0.9126074666063844765, 0.4088369013363114535 ) ) ;
#27222=EDGE_CURVE ( 'NONE', #214984, #223215, #240225, .T. ) ;
#27225=AXIS2_PLACEMENT_3D ( 'NONE', #28647, #31203, #88540 ) ;
#27250=EDGE_LOOP ( 'NONE', ( #115617, #145014, #8516, #173070 ) ) ;
#27267=CIRCLE ( 'NONE', #89755, 0.09999999999999735489 ) ;
#27287=ORIENTED_EDGE ( 'NONE', *, *, #178761, .F. ) ;
#27301=ORIENTED_EDGE ( 'NONE', *, *, #132632, .T. ) ;
#27338=EDGE_CURVE ( 'NONE', #74869, #220667, #13157, .T. ) ;
#27339=CARTESIAN_POINT ( 'NONE',  ( -22.32929514600008503, 29.70208827356600523, -252.5591762845882329 ) ) ;
#27398=DIRECTION ( 'NONE',  ( 0.000000000000000000, 0.4166553800442402977, -0.9090645160164321226 ) ) ;
#27412=ORIENTED_EDGE ( 'NONE', *, *, #126195, .T. ) ;
#27430=EDGE_CURVE ( 'NONE', #79169, #19155, #126906, .T. ) ;
#27441=DIRECTION ( 'NONE',  ( 1.000000000000000000, 0.000000000000000000, 0.000000000000000000 ) ) ;
#27448=ORIENTED_EDGE ( 'NONE', *, *, #173474, .F. ) ;
#27455=ORIENTED_EDGE ( 'NONE', *, *, #160543, .F. ) ;
#27480=DIRECTION ( 'NONE',  ( -1.000000000000000000, 1.207181226542539700E-16, -2.694675058168174199E-16 ) ) ;
#27491=CYLINDRICAL_SURFACE ( 'NONE', #32255, 0.09999999999999609201 ) ;
#27494=AXIS2_PLACEMENT_3D ( 'NONE', #40194, #218781, #235786 ) ;
#27496=DIRECTION ( 'NONE',  ( 0.000000000000000000, -0.9126074666063660468, -0.4088369013363524762 ) ) ;
#27575=AXIS2_PLACEMENT_3D ( 'NONE', #68138, #171136, #130668 ) ;
#27586=CARTESIAN_POINT ( 'NONE',  ( -20.94999999999999929, 78.57896856393121254, -232.7977304333149675 ) ) ;
#27589=AXIS2_PLACEMENT_3D ( 'NONE', #220619, #121548, #199792 ) ;
#27626=CARTESIAN_POINT ( 'NONE',  ( -18.55121869061588669, 68.09900309800710261, -224.1499508721967686 ) ) ;
#27696=TOROIDAL_SURFACE ( 'NONE', #31783, 0.2000000000000000111, 0.1000000000000000056 ) ;
#27698=DIRECTION ( 'NONE',  ( -3.265361837132813093E-16, -0.4088369013363283844, 0.9126074666063769270 ) ) ;
#27701=ORIENTED_EDGE ( 'NONE', *, *, #237427, .T. ) ;
#27706=DIRECTION ( 'NONE',  ( 0.000000000000000000, -0.9126074666063769270, -0.4088369013363280513 ) ) ;
#27714=CIRCLE ( 'NONE', #173492, 0.09999999999999939493 ) ;
#27715=ORIENTED_EDGE ( 'NONE', *, *, #133541, .F. ) ;
#27723=DIRECTION ( 'NONE',  ( -0.000000000000000000, 0.9126074666063771490, 0.4088369013363281623 ) ) ;
#27725=DIRECTION ( 'NONE',  ( 0.000000000000000000, -0.9126074666063765939, -0.4088369013363289950 ) ) ;
#27729=ORIENTED_EDGE ( 'NONE', *, *, #227876, .F. ) ;
#27731=CIRCLE ( 'NONE', #244343, 11.70000000000000462 ) ;
#27744=DIRECTION ( 'NONE',  ( -1.000000000000000000, -0.000000000000000000, 0.000000000000000000 ) ) ;
#27750=CARTESIAN_POINT ( 'NONE',  ( 20.04142135623731136, 54.35086488289006468, -228.7501953506800589 ) ) ;
#27753=ORIENTED_EDGE ( 'NONE', *, *, #15485, .T. ) ;
#27757=CARTESIAN_POINT ( 'NONE',  ( -23.15000000000000213, 69.25640205380744874, -247.7135141964517402 ) ) ;
#27766=ORIENTED_EDGE ( 'NONE', *, *, #187125, .T. ) ;
#27785=ADVANCED_FACE ( 'NONE', ( #63177 ), #131354, .T. ) ;
#27793=CARTESIAN_POINT ( 'NONE',  ( -20.94999999999999929, 44.29184115892635987, -259.0069060397277667 ) ) ;
#27817=FACE_OUTER_BOUND ( 'NONE', #113040, .T. ) ;
#27835=ORIENTED_EDGE ( 'NONE', *, *, #155743, .T. ) ;
#27874=B_SPLINE_CURVE_WITH_KNOTS ( 'NONE', 3,
 ( #256306, #17745, #236803, #244182, #141253, #136395 ),
 .UNSPECIFIED., .F., .F.,
 ( 4, 2, 4 ),
 ( 0.000000000000000000, 0.0001569047307838634909, 0.0003138094615677269818 ),
 .UNSPECIFIED. ) ;
#27897=ORIENTED_EDGE ( 'NONE', *, *, #74526, .F. ) ;
#27921=DIRECTION ( 'NONE',  ( -0.000000000000000000, 0.9126074666063771490, 0.4088369013363281623 ) ) ;
#27925=DIRECTION ( 'NONE',  ( -0.000000000000000000, 0.9579639084728132081, 0.2868887416116073230 ) ) ;
#27934=DIRECTION ( 'NONE',  ( 0.000000000000000000, 0.9126074666063813678, 0.4088369013363182813 ) ) ;
#27962=DIRECTION ( 'NONE',  ( 0.000000000000000000, -0.9126074666063545004, -0.4088369013363783999 ) ) ;
#27986=FACE_OUTER_BOUND ( 'NONE', #183626, .T. ) ;
#28010=EDGE_CURVE ( 'NONE', #168551, #37194, #56452, .T. ) ;
#28025=ORIENTED_EDGE ( 'NONE', *, *, #215549, .T. ) ;
#28055=CARTESIAN_POINT ( 'NONE',  ( -21.05000000000000071, 44.15969672213208952, -258.9565289832007693 ) ) ;
#28097=CARTESIAN_POINT ( 'NONE',  ( 20.94999999999999929, 70.97296516614450468, -234.1788952109995137 ) ) ;
#28113=ORIENTED_EDGE ( 'NONE', *, *, #127301, .T. ) ;
#28168=DIRECTION ( 'NONE',  ( 1.000000000000000000, 0.000000000000000000, 0.000000000000000000 ) ) ;
#28183=VERTEX_POINT ( 'NONE', #1616 ) ;
#28231=DIRECTION ( 'NONE',  ( 1.000000000000000000, 0.000000000000000000, 0.000000000000000000 ) ) ;
#28240=DIRECTION ( 'NONE',  ( 1.000000000000000000, 0.000000000000000000, 0.000000000000000000 ) ) ;
#28287=CARTESIAN_POINT ( 'NONE',  ( -18.59999999999999787, 51.63105570370733233, -253.2535652827696424 ) ) ;
#28355=DIRECTION ( 'NONE',  ( 0.000000000000000000, -0.4088369013363281068, 0.9126074666063770380 ) ) ;
#28357=CYLINDRICAL_SURFACE ( 'NONE', #65037, 0.09999999999999939493 ) ;
#28384=AXIS2_PLACEMENT_3D ( 'NONE', #182985, #164697, #4315 ) ;
#28390=EDGE_CURVE ( 'NONE', #118038, #151518, #94305, .T. ) ;
#28430=DIRECTION ( 'NONE',  ( -1.000000000000000000, 1.335000415235278971E-16, -2.979993593738921214E-16 ) ) ;
#28431=CARTESIAN_POINT ( 'NONE',  ( -23.15000000000000213, 49.61306877027904250, -254.2671747026441551 ) ) ;
#28436=DIRECTION ( 'NONE',  ( 0.000000000000000000, 0.9126074666063660468, 0.4088369013363524762 ) ) ;
#28439=VERTEX_POINT ( 'NONE', #53596 ) ;
#28465=CARTESIAN_POINT ( 'NONE',  ( 18.59999999999999076, 54.95667902235472013, -229.8578999281555753 ) ) ;
#28473=CIRCLE ( 'NONE', #249203, 4.299999999999953637 ) ;
#28477=CARTESIAN_POINT ( 'NONE',  ( -23.15000000000000213, 70.88170441948386724, -234.2197789011331679 ) ) ;
#28503=ORIENTED_EDGE ( 'NONE', *, *, #150151, .T. ) ;
#28508=DIRECTION ( 'NONE',  ( 0.000000000000000000, 0.9126074666063769270, 0.4088369013363280513 ) ) ;
#28517=DIRECTION ( 'NONE',  ( 0.000000000000000000, -0.4088369013363281623, 0.9126074666063771490 ) ) ;
#28552=DIRECTION ( 'NONE',  ( -1.000000000000000000, 1.207181226542539700E-16, -2.694675058168174199E-16 ) ) ;
#28554=DIRECTION ( 'NONE',  ( 0.000000000000000000, 0.9126074666064696306, 0.4088369013361213278 ) ) ;
#28601=ORIENTED_EDGE ( 'NONE', *, *, #9375, .T. ) ;
#28605=CIRCLE ( 'NONE', #24474, 0.5999999999999934275 ) ;
#28628=ORIENTED_EDGE ( 'NONE', *, *, #204201, .F. ) ;
#28641=DIRECTION ( 'NONE',  ( 1.000000000000000000, 0.000000000000000000, 0.000000000000000000 ) ) ;
#28647=CARTESIAN_POINT ( 'NONE',  ( -21.29999999999995808, 36.65892442174472876, -249.5511627012454596 ) ) ;
#28677=CARTESIAN_POINT ( 'NONE',  ( 21.14999999999999858, 30.68987205111126926, -252.2252246220829193 ) ) ;
#28684=FACE_OUTER_BOUND ( 'NONE', #48234, .T. ) ;
#28778=CARTESIAN_POINT ( 'NONE',  ( 21.05000000000000071, 39.26973050389061370, -236.6309188891183055 ) ) ;
#28786=CARTESIAN_POINT ( 'NONE',  ( -20.94999999999999929, 69.09936979046463534, -247.6075824278584889 ) ) ;
#28790=EDGE_LOOP ( 'NONE', ( #51492, #99945, #47170, #255793 ) ) ;
#28795=DIRECTION ( 'NONE',  ( -1.000000000000000000, -1.387778780781454006E-13, 2.775557561562908012E-13 ) ) ;
#28796=ADVANCED_FACE ( 'NONE', ( #11606 ), #231891, .F. ) ;
#28820=DIRECTION ( 'NONE',  ( 0.7071067811865487940, 0.6453109281988437251, 0.2890913453342125461 ) ) ;
#28826=DIRECTION ( 'NONE',  ( 0.000000000000000000, -0.9126074666063769270, -0.4088369013363280513 ) ) ;
#28851=LINE ( 'NONE', #147458, #32690 ) ;
#28856=ORIENTED_EDGE ( 'NONE', *, *, #27133, .F. ) ;
#28870=B_SPLINE_CURVE_WITH_KNOTS ( 'NONE', 3,
 ( #191119, #228939, #91983, #131110, #11176, #171560, #209367 ),
 .UNSPECIFIED., .F., .F.,
 ( 4, 3, 4 ),
 ( 0.000000000000000000, 3.357501770815118507E-05, 5.199112466349255934E-05 ),
 .UNSPECIFIED. ) ;
#28882=CARTESIAN_POINT ( 'NONE',  ( -22.59999999999999787, 31.76322370622491320, -238.8696546380523671 ) ) ;
#28907=CARTESIAN_POINT ( 'NONE',  ( -21.45000000000000284, 44.77807522791015060, -237.4671205425215135 ) ) ;
#28921=CARTESIAN_POINT ( 'NONE',  ( -18.50211644919735932, 68.02921119886117651, -224.2090419302654141 ) ) ;
#28963=CIRCLE ( 'NONE', #191245, 0.09999999999999108213 ) ;
#28981=CARTESIAN_POINT ( 'NONE',  ( -18.50000000000000000, 44.52640028187936849, -247.3006740988509193 ) ) ;
#29020=ORIENTED_EDGE ( 'NONE', *, *, #5960, .T. ) ;
#29027=EDGE_CURVE ( 'NONE', #53966, #171512, #69384, .T. ) ;
#29107=FACE_OUTER_BOUND ( 'NONE', #213870, .T. ) ;
#29122=DIRECTION ( 'NONE',  ( -1.000000000000000000, -0.000000000000000000, 0.000000000000000000 ) ) ;
#29158=EDGE_CURVE ( 'NONE', #86618, #84696, #128008, .T. ) ;
#29185=DIRECTION ( 'NONE',  ( 0.000000000000000000, 0.9126074666063771490, 0.4088369013363278293 ) ) ;
#29196=DIRECTION ( 'NONE',  ( 1.000000000000000000, 0.000000000000000000, 0.000000000000000000 ) ) ;
#29225=CIRCLE ( 'NONE', #33318, 1.900000000000004574 ) ;
#29287=DIRECTION ( 'NONE',  ( 0.000000000000000000, -0.4088369013363280513, 0.9126074666063772600 ) ) ;
#29313=LINE ( 'NONE', #10991, #80722 ) ;
#29338=CIRCLE ( 'NONE', #179168, 3.899999999999999023 ) ;
#29343=ORIENTED_EDGE ( 'NONE', *, *, #219864, .T. ) ;
#29352=EDGE_LOOP ( 'NONE', ( #82610, #134913, #240621 ) ) ;
#29372=EDGE_LOOP ( 'NONE', ( #155404, #195529, #108678, #220039 ) ) ;
#29421=AXIS2_PLACEMENT_3D ( 'NONE', #141765, #144315, #23143 ) ;
#29431=CARTESIAN_POINT ( 'NONE',  ( -23.15000000000000213, 56.02567683926420727, -227.9999002286038774 ) ) ;
#29438=EDGE_CURVE ( 'NONE', #70783, #175048, #115508, .T. ) ;
#29442=TOROIDAL_SURFACE ( 'NONE', #204169, 7.791421356237316687, 0.1000000000000000056 ) ;
#29449=DIRECTION ( 'NONE',  ( 0.000000000000000000, -0.9126074666063622720, -0.4088369013363611360 ) ) ;
#29457=EDGE_CURVE ( 'NONE', #14729, #1615, #151474, .T. ) ;
#29488=DIRECTION ( 'NONE',  ( 0.000000000000000000, -0.9126074666063660468, -0.4088369013363524762 ) ) ;
#29495=DIRECTION ( 'NONE',  ( 0.000000000000000000, 0.9126074666063844765, 0.4088369013363114535 ) ) ;
#29505=TOROIDAL_SURFACE ( 'NONE', #191993, 0.2000000000000000111, 0.1000000000000000056 ) ;
#29514=CARTESIAN_POINT ( 'NONE',  ( -20.64999999999999858, 62.24653955602229871, -247.9500786234238490 ) ) ;
#29574=ORIENTED_EDGE ( 'NONE', *, *, #132722, .F. ) ;
#29582=CARTESIAN_POINT ( 'NONE',  ( -20.54999999999999716, 47.91013932883114990, -242.3192343197862044 ) ) ;
#29650=TOROIDAL_SURFACE ( 'NONE', #158825, 0.2000000000000000111, 0.1000000000000000056 ) ;
#29688=CARTESIAN_POINT ( 'NONE',  ( 21.06280952165534259, 43.45167128181677185, -234.8632948402907914 ) ) ;
#29707=ADVANCED_FACE ( 'NONE', ( #140881 ), #160470, .F. ) ;
#29720=TOROIDAL_SURFACE ( 'NONE', #175456, 11.65000000000000036, 0.1000000000000000056 ) ;
#29731=ORIENTED_EDGE ( 'NONE', *, *, #797, .T. ) ;
#29813=EDGE_CURVE ( 'NONE', #71022, #37046, #17223, .T. ) ;
#29820=DIRECTION ( 'NONE',  ( 1.000000000000000000, 0.000000000000000000, 0.000000000000000000 ) ) ;
#29842=DIRECTION ( 'NONE',  ( -5.603264701231745086E-32, 0.9126074666063769270, 0.4088369013363282733 ) ) ;
#29852=CARTESIAN_POINT ( 'NONE',  ( 20.95325940946048249, 39.25995885369344762, -236.8548070915221047 ) ) ;
#29868=EDGE_CURVE ( 'NONE', #57391, #45859, #105762, .T. ) ;
#29885=EDGE_LOOP ( 'NONE', ( #130432, #58220, #54009, #221694 ) ) ;
#29899=DIRECTION ( 'NONE',  ( 1.000000000000000000, 0.000000000000000000, 0.000000000000000000 ) ) ;
#29907=CARTESIAN_POINT ( 'NONE',  ( 23.24999999999999645, 68.08983204586466798, -237.7716021863518563 ) ) ;
#29919=ADVANCED_FACE ( 'NONE', ( #33808 ), #153766, .F. ) ;
#29934=DIRECTION ( 'NONE',  ( 0.000000000000000000, 0.9126074666063769270, 0.4088369013363280513 ) ) ;
#29957=AXIS2_PLACEMENT_3D ( 'NONE', #173131, #169268, #251317 ) ;
#29959=EDGE_LOOP ( 'NONE', ( #112820, #33566, #112019, #243181, #194787, #105028, #69831, #138111, #43145, #230486, #107683, #135926 ) ) ;
#29967=CARTESIAN_POINT ( 'NONE',  ( -20.85000000000000142, 78.48087866980282001, -232.8271061603568910 ) ) ;
#29969=CARTESIAN_POINT ( 'NONE',  ( 22.49999999999999289, 25.89494711235934687, -254.2627752153468350 ) ) ;
#30012=DIRECTION ( 'NONE',  ( 0.000000000000000000, -0.9501938099239353175, 0.3116596277708039708 ) ) ;
#30029=DIRECTION ( 'NONE',  ( 0.000000000000000000, 0.9126074666064236673, 0.4088369013362239679 ) ) ;
#30059=CARTESIAN_POINT ( 'NONE',  ( 23.14999999999999858, 55.49311008795314137, -234.6486875357297492 ) ) ;
#30060=CARTESIAN_POINT ( 'NONE',  ( -20.85000000000000142, 62.46832465249013921, -225.2232495205141731 ) ) ;
#30073=DIRECTION ( 'NONE',  ( 0.000000000000000000, -0.9126074666063660468, -0.4088369013363524762 ) ) ;
#30074=CARTESIAN_POINT ( 'NONE',  ( 18.49999999999999645, 46.50671693017397246, -243.2369495081682942 ) ) ;
#30079=CARTESIAN_POINT ( 'NONE',  ( -20.85000000000000142, 74.93036000061670165, -233.6816308724374949 ) ) ;
#30102=ORIENTED_EDGE ( 'NONE', *, *, #35523, .T. ) ;
#30127=SPHERICAL_SURFACE ( 'NONE', #7863, 0.1000000000000000056 ) ;
#30129=ORIENTED_EDGE ( 'NONE', *, *, #248744, .T. ) ;
#30136=EDGE_CURVE ( 'NONE', #120786, #85465, #81013, .T. ) ;
#30176=CARTESIAN_POINT ( 'NONE',  ( -18.50000972452446035, 68.00519115550238780, -224.2294631537215821 ) ) ;
#30179=ADVANCED_FACE ( 'NONE', ( #49155 ), #184812, .F. ) ;
#30212=CARTESIAN_POINT ( 'NONE',  ( 18.59999999999999432, 44.43513953521873106, -247.3415577889845736 ) ) ;
#30246=EDGE_CURVE ( 'NONE', #124831, #228315, #213351, .T. ) ;
#30260=ORIENTED_EDGE ( 'NONE', *, *, #102982, .F. ) ;
#30269=ORIENTED_EDGE ( 'NONE', *, *, #233798, .F. ) ;
#30294=CARTESIAN_POINT ( 'NONE',  ( 19.94784844284934877, 54.41359201945252266, -228.7625389915575056 ) ) ;
#30297=AXIS2_PLACEMENT_3D ( 'NONE', #101251, #81699, #161300 ) ;
#30321=ADVANCED_FACE ( 'NONE', ( #135094 ), #76406, .F. ) ;
#30398=ORIENTED_EDGE ( 'NONE', *, *, #101447, .F. ) ;
#30406=CARTESIAN_POINT ( 'NONE',  ( 20.97462148592277487, 44.21428412855883749, -236.4418601092407926 ) ) ;
#30409=LINE ( 'NONE', #10837, #79372 ) ;
#30415=ORIENTED_EDGE ( 'NONE', *, *, #20241, .T. ) ;
#30449=CARTESIAN_POINT ( 'NONE',  ( 23.14999999999999503, 53.24180694658302571, -234.8354225850497130 ) ) ;
#30454=DIRECTION ( 'NONE',  ( 2.952720810173289112E-16, 0.4088369013363280513, -0.9126074666063769270 ) ) ;
#30467=ORIENTED_EDGE ( 'NONE', *, *, #173041, .T. ) ;
#30501=VECTOR ( 'NONE', #91645, 1000.000000000000114 ) ;
#30510=AXIS2_PLACEMENT_3D ( 'NONE', #157961, #100474, #237449 ) ;
#30512=ORIENTED_EDGE ( 'NONE', *, *, #228926, .T. ) ;
#30517=AXIS2_PLACEMENT_3D ( 'NONE', #149090, #169966, #129512 ) ;
#30564=CIRCLE ( 'NONE', #180959, 0.1000000000000091788 ) ;
#30565=EDGE_CURVE ( 'NONE', #199454, #101237, #222661, .T. ) ;
#30612=LINE ( 'NONE', #232664, #34752 ) ;
#30639=DIRECTION ( 'NONE',  ( 0.000000000000000000, 0.9126074666063660468, 0.4088369013363524762 ) ) ;
#30653=ORIENTED_EDGE ( 'NONE', *, *, #87062, .F. ) ;
#30667=PRODUCT ( 'Injection Molded Chain Links 9', 'Injection Molded Chain Links 9', '', ( #170944 ) ) ;
#30668=EDGE_CURVE ( 'NONE', #62507, #138284, #36706, .T. ) ;
#30701=CIRCLE ( 'NONE', #22323, 0.09999999999999939493 ) ;
#30714=ORIENTED_EDGE ( 'NONE', *, *, #64305, .F. ) ;
#30734=DIRECTION ( 'NONE',  ( 0.000000000000000000, 0.9126074666063660468, 0.4088369013363524762 ) ) ;
#30735=DIRECTION ( 'NONE',  ( 2.557131231893037478E-16, -0.1022405907414166287, -0.9947597004326451664 ) ) ;
#30750=CARTESIAN_POINT ( 'NONE',  ( -23.25000000000000000, 42.98415524044399660, -233.9519173640447889 ) ) ;
#30786=EDGE_CURVE ( 'NONE', #126059, #67538, #81362, .T. ) ;
#30792=DIRECTION ( 'NONE',  ( 0.000000000000000000, 0.9126074666063774821, 0.4088369013363273297 ) ) ;
#30804=VECTOR ( 'NONE', #195740, 1000.000000000000000 ) ;
#30822=CARTESIAN_POINT ( 'NONE',  ( -23.15000000000000213, 69.09936979046463534, -247.6075824278584605 ) ) ;
#30839=DIRECTION ( 'NONE',  ( -1.000000000000000000, -0.000000000000000000, 0.000000000000000000 ) ) ;
#30874=AXIS2_PLACEMENT_3D ( 'NONE', #144127, #145422, #46317 ) ;
#30887=AXIS2_PLACEMENT_3D ( 'NONE', #104813, #244350, #223500 ) ;
#30897=DIRECTION ( 'NONE',  ( 0.000000000000000000, 0.4088369013363281623, -0.9126074666063771490 ) ) ;
#30904=VERTEX_POINT ( 'NONE', #79188 ) ;
#30911=CARTESIAN_POINT ( 'NONE',  ( -21.05000000000000071, 43.47002849391839874, -245.0086825852825143 ) ) ;
#30917=DIRECTION ( 'NONE',  ( -4.801466763864314121E-15, 0.9876013379310922824, 0.1569827930593562515 ) ) ;
#30930=DIRECTION ( 'NONE',  ( -0.000000000000000000, 0.4701782451859590206, 0.8825714802517993229 ) ) ;
#30961=EDGE_CURVE ( 'NONE', #111477, #23132, #123105, .T. ) ;
#30972=ORIENTED_EDGE ( 'NONE', *, *, #2191, .F. ) ;
#30976=CARTESIAN_POINT ( 'NONE',  ( 22.40000000000001279, 33.47376623175148325, -242.4412390690852703 ) ) ;
#31012=CARTESIAN_POINT ( 'NONE',  ( 20.94999999999999574, 46.54514716347711101, -243.1111603596801842 ) ) ;
#31034=AXIS2_PLACEMENT_3D ( 'NONE', #87277, #228108, #131559 ) ;
#31046=VERTEX_POINT ( 'NONE', #84278 ) ;
#31080=CIRCLE ( 'NONE', #214375, 11.74999999999999822 ) ;
#31096=EDGE_CURVE ( 'NONE', #177620, #70690, #122197, .T. ) ;
#31113=ADVANCED_FACE ( 'NONE', ( #83019 ), #91398, .T. ) ;
#31163=CYLINDRICAL_SURFACE ( 'NONE', #210212, 0.09999999999999939493 ) ;
#31170=TOROIDAL_SURFACE ( 'NONE', #64456, 11.65000000000000036, 0.1000000000000000056 ) ;
#31197=CIRCLE ( 'NONE', #176920, 0.1000000000000024342 ) ;
#31203=DIRECTION ( 'NONE',  ( 1.000000000000000000, 0.000000000000000000, 0.000000000000000000 ) ) ;
#31227=FACE_OUTER_BOUND ( 'NONE', #247709, .T. ) ;
#31231=ORIENTED_EDGE ( 'NONE', *, *, #79678, .F. ) ;
#31239=DIRECTION ( 'NONE',  ( 0.000000000000000000, -0.9126074666063660468, -0.4088369013363524762 ) ) ;
#31251=ORIENTED_EDGE ( 'NONE', *, *, #137353, .T. ) ;
#31253=DIRECTION ( 'NONE',  ( 3.469446951953635646E-14, -0.9126074666063771490, -0.4088369013363281623 ) ) ;
#31270=ORIENTED_EDGE ( 'NONE', *, *, #68139, .F. ) ;
#31306=DIRECTION ( 'NONE',  ( 0.000000000000000000, -0.9126074666063742624, -0.4088369013363343241 ) ) ;
#31314=EDGE_CURVE ( 'NONE', #57244, #215487, #102389, .T. ) ;
#31323=CARTESIAN_POINT ( 'NONE',  ( 21.13920837816993270, 44.24745038003037934, -236.5272538208875801 ) ) ;
#31325=ORIENTED_EDGE ( 'NONE', *, *, #198005, .T. ) ;
#31336=CARTESIAN_POINT ( 'NONE',  ( -21.05000000000000071, 39.30548607490320734, -248.3655356873701123 ) ) ;
#31354=DIRECTION ( 'NONE',  ( 0.000000000000000000, -0.2606175937107792495, 0.9654421110809303652 ) ) ;
#31359=DIRECTION ( 'NONE',  ( -1.000000000000000000, -0.000000000000000000, -0.000000000000000000 ) ) ;
#31375=DIRECTION ( 'NONE',  ( 0.000000000000000000, 0.4088369013363280513, -0.9126074666063769270 ) ) ;
#31379=VECTOR ( 'NONE', #108782, 1000.000000000000114 ) ;
#31385=DIRECTION ( 'NONE',  ( 1.000000000000000000, 0.000000000000000000, 0.000000000000000000 ) ) ;
#31469=DIRECTION ( 'NONE',  ( -0.8660254037843529984, 0.4563037333032838316, 0.2044184506683135449 ) ) ;
#31569=CARTESIAN_POINT ( 'NONE',  ( 22.59999999999999432, 25.98655542988603173, -254.2226763854395983 ) ) ;
#31570=ORIENTED_EDGE ( 'NONE', *, *, #154558, .F. ) ;
#31572=AXIS2_PLACEMENT_3D ( 'NONE', #177448, #196963, #237394 ) ;
#31580=ORIENTED_EDGE ( 'NONE', *, *, #200676, .T. ) ;
#31612=LINE ( 'NONE', #207664, #123209 ) ;
#31675=CARTESIAN_POINT ( 'NONE',  ( -18.59999999999999787, 67.85909929089923764, -227.8797997985275856 ) ) ;
#31677=CARTESIAN_POINT ( 'NONE',  ( -20.64999999999999858, 67.23127455305835554, -235.8551265064784559 ) ) ;
#31701=CARTESIAN_POINT ( 'NONE',  ( -21.44999999999999929, 53.03738849591485405, -234.3791188517465400 ) ) ;
#31725=ADVANCED_FACE ( 'NONE', ( #137883 ), #31170, .T. ) ;
#31748=EDGE_CURVE ( 'NONE', #230182, #21519, #18661, .T. ) ;
#31774=DIRECTION ( 'NONE',  ( 1.000000000000000000, 0.000000000000000000, 0.000000000000000000 ) ) ;
#31783=AXIS2_PLACEMENT_3D ( 'NONE', #236313, #257112, #122811 ) ;
#31898=ORIENTED_EDGE ( 'NONE', *, *, #90839, .F. ) ;
#31906=ORIENTED_EDGE ( 'NONE', *, *, #72680, .F. ) ;
#31918=CARTESIAN_POINT ( 'NONE',  ( -20.64999999999999858, 67.23127455305835554, -235.8551265064784559 ) ) ;
#31947=VECTOR ( 'NONE', #78213, 1000.000000000000114 ) ;
#31975=CARTESIAN_POINT ( 'NONE',  ( -23.25000000000000000, 54.34471204062663219, -239.4366250215122420 ) ) ;
#31989=TOROIDAL_SURFACE ( 'NONE', #186092, 11.70000000000000107, 0.1000000000000000056 ) ;
#32020=DIRECTION ( 'NONE',  ( 1.000000000000000000, 0.000000000000000000, 0.000000000000000000 ) ) ;
#32027=DIRECTION ( 'NONE',  ( -0.000000000000000000, -0.9594490217226103734, -0.2818822000686205254 ) ) ;
#32035=FACE_OUTER_BOUND ( 'NONE', #37043, .T. ) ;
#32036=CARTESIAN_POINT ( 'NONE',  ( 21.14999999999999858, 47.74710514101221293, -244.5837943500090716 ) ) ;
#32037=EDGE_CURVE ( 'NONE', #62010, #61601, #255893, .T. ) ;
#32047=FACE_OUTER_BOUND ( 'NONE', #139363, .T. ) ;
#32088=CARTESIAN_POINT ( 'NONE',  ( -18.50000000000000000, 74.98773774893902555, -233.8732236541320333 ) ) ;
#32110=AXIS2_PLACEMENT_3D ( 'NONE', #30079, #249117, #170901 ) ;
#32132=DIRECTION ( 'NONE',  ( 1.000000000000000000, 0.000000000000000000, 0.000000000000000000 ) ) ;
#32144=VECTOR ( 'NONE', #138818, 1000.000000000000114 ) ;
#32234=CARTESIAN_POINT ( 'NONE',  ( 21.05000000000000071, 54.23099463892081928, -236.2002849323373255 ) ) ;
#32255=AXIS2_PLACEMENT_3D ( 'NONE', #7902, #186529, #87403 ) ;
#32256=ORIENTED_EDGE ( 'NONE', *, *, #89458, .F. ) ;
#32260=AXIS2_PLACEMENT_3D ( 'NONE', #34260, #118598, #40366 ) ;
#32264=CARTESIAN_POINT ( 'NONE',  ( 21.05000000000000071, 43.37306621509043225, -234.7926750453023601 ) ) ;
#32274=CARTESIAN_POINT ( 'NONE',  ( -23.25000000000000000, 41.46275801244657799, -260.2743004338703940 ) ) ;
#32284=FACE_OUTER_BOUND ( 'NONE', #91430, .T. ) ;
#32287=LINE ( 'NONE', #251291, #59770 ) ;
#32389=EDGE_CURVE ( 'NONE', #121176, #227768, #52323, .T. ) ;
#32422=AXIS2_PLACEMENT_3D ( 'NONE', #88186, #107779, #169081 ) ;
#32448=DIRECTION ( 'NONE',  ( 0.000000000000000000, 0.9177795674685970129, 0.3970902486049678326 ) ) ;
#32453=CARTESIAN_POINT ( 'NONE',  ( -23.15000000000000213, 29.86062094194855376, -263.1160279713685100 ) ) ;
#32455=VERTEX_POINT ( 'NONE', #220379 ) ;
#32467=DIRECTION ( 'NONE',  ( -0.000000000000000000, 0.9126074666063771490, 0.4088369013363281623 ) ) ;
#32478=ORIENTED_EDGE ( 'NONE', *, *, #178307, .T. ) ;
#32484=ORIENTED_EDGE ( 'NONE', *, *, #175385, .F. ) ;
#32513=CARTESIAN_POINT ( 'NONE',  ( 23.14999999999999858, 53.66153320161009788, -235.9075159595686841 ) ) ;
#32515=ORIENTED_EDGE ( 'NONE', *, *, #194208, .T. ) ;
#32520=CARTESIAN_POINT ( 'NONE',  ( 18.50000000000000000, 29.81973725181491730, -263.0247672247078867 ) ) ;
#32521=ORIENTED_EDGE ( 'NONE', *, *, #44968, .F. ) ;
#32534=CYLINDRICAL_SURFACE ( 'NONE', #154553, 2.000000000000012879 ) ;
#32594=ADVANCED_FACE ( 'NONE', ( #147239 ), #207234, .T. ) ;
#32621=CARTESIAN_POINT ( 'NONE',  ( 20.85000000000000142, 67.23127455305835554, -235.8551265064784559 ) ) ;
#32689=CIRCLE ( 'NONE', #11823, 0.09999999999999609201 ) ;
#32690=VECTOR ( 'NONE', #9226, 1000.000000000000114 ) ;
#32696=DIRECTION ( 'NONE',  ( 1.000000000000000000, 0.000000000000000000, 0.000000000000000000 ) ) ;
#32697=AXIS2_PLACEMENT_3D ( 'NONE', #121695, #129060, #148634 ) ;
#32720=VERTEX_POINT ( 'NONE', #175811 ) ;
#32722=DIRECTION ( 'NONE',  ( 0.000000000000000000, -0.4088369013363280513, 0.9126074666063769270 ) ) ;
#32733=EDGE_CURVE ( 'NONE', #76006, #173652, #53285, .T. ) ;
#32748=DIRECTION ( 'NONE',  ( 0.000000000000000000, 0.9126074666063660468, 0.4088369013363524762 ) ) ;
#32764=CARTESIAN_POINT ( 'NONE',  ( 20.94999999999999574, 44.25095746879271985, -258.9156452930671435 ) ) ;
#32776=CARTESIAN_POINT ( 'NONE',  ( 23.24999999999999289, 42.98415524044398950, -233.9519173640447889 ) ) ;
#32804=DIRECTION ( 'NONE',  ( -1.000000000000000000, 0.000000000000000000, 0.000000000000000000 ) ) ;
#32849=TOROIDAL_SURFACE ( 'NONE', #132781, 0.6000000000000006439, 0.1000000000000000056 ) ;
#32853=EDGE_CURVE ( 'NONE', #75688, #144175, #33765, .T. ) ;
#32873=CARTESIAN_POINT ( 'NONE',  ( -23.25000000000000000, 44.29184115892635987, -259.0069060397277667 ) ) ;
#32874=ORIENTED_EDGE ( 'NONE', *, *, #22927, .F. ) ;
#32878=EDGE_CURVE ( 'NONE', #95060, #14729, #254032, .T. ) ;
#32915=AXIS2_PLACEMENT_3D ( 'NONE', #62793, #24976, #100592 ) ;
#32925=DIRECTION ( 'NONE',  ( 0.000000000000000000, 0.9126074666063771490, 0.4088369013363278848 ) ) ;
#32932=CIRCLE ( 'NONE', #45348, 0.1999999999999987899 ) ;
#32971=ORIENTED_EDGE ( 'NONE', *, *, #30668, .F. ) ;
#33010=CARTESIAN_POINT ( 'NONE',  ( -20.12071067811865888, 44.11897616243903286, -235.9958768108129448 ) ) ;
#33038=CARTESIAN_POINT ( 'NONE',  ( 18.59999999999998366, 67.85909929089923764, -227.8797997985275856 ) ) ;
#33041=DIRECTION ( 'NONE',  ( 0.000000000000000000, 0.9126074666064696306, 0.4088369013361213278 ) ) ;
#33053=DIRECTION ( 'NONE',  ( 1.000000000000000000, 0.000000000000000000, 0.000000000000000000 ) ) ;
#33062=EDGE_LOOP ( 'NONE', ( #77755, #120401, #161246, #254096 ) ) ;
#33064=CIRCLE ( 'NONE', #74751, 0.09999999999999939493 ) ;
#33147=ORIENTED_EDGE ( 'NONE', *, *, #78505, .T. ) ;
#33169=ORIENTED_EDGE ( 'NONE', *, *, #19434, .T. ) ;
#33224=VERTEX_POINT ( 'NONE', #222275 ) ;
#33242=TOROIDAL_SURFACE ( 'NONE', #25051, 0.6000000000000015321, 0.1000000000000000056 ) ;
#33268=LINE ( 'NONE', #214421, #241126 ) ;
#33290=CARTESIAN_POINT ( 'NONE',  ( -21.05000000000000071, 30.91400355739106942, -252.1479406582309366 ) ) ;
#33309=FACE_OUTER_BOUND ( 'NONE', #17998, .T. ) ;
#33318=AXIS2_PLACEMENT_3D ( 'NONE', #43955, #246013, #162632 ) ;
#33368=LINE ( 'NONE', #56699, #137404 ) ;
#33378=ORIENTED_EDGE ( 'NONE', *, *, #104895, .T. ) ;
#33392=CIRCLE ( 'NONE', #195700, 0.1000000000000024342 ) ;
#33409=CARTESIAN_POINT ( 'NONE',  ( 20.12500000000000355, 39.64491763323097473, -236.9907406594410588 ) ) ;
#33440=ORIENTED_EDGE ( 'NONE', *, *, #144736, .T. ) ;
#33442=DIRECTION ( 'NONE',  ( -1.000000000000000000, -0.000000000000000000, -0.000000000000000000 ) ) ;
#33471=FACE_OUTER_BOUND ( 'NONE', #75577, .T. ) ;
#33490=ADVANCED_FACE ( 'NONE', ( #51338 ), #132200, .F. ) ;
#33518=ORIENTED_EDGE ( 'NONE', *, *, #82243, .T. ) ;
#33566=ORIENTED_EDGE ( 'NONE', *, *, #201556, .T. ) ;
#33578=EDGE_LOOP ( 'NONE', ( #28113, #15067, #222911, #77711 ) ) ;
#33588=DIRECTION ( 'NONE',  ( 1.000000000000000000, 0.000000000000000000, 0.000000000000000000 ) ) ;
#33607=CARTESIAN_POINT ( 'NONE',  ( 18.59999999999999076, 54.98105481382776816, -230.1569079895687366 ) ) ;
#33626=ORIENTED_EDGE ( 'NONE', *, *, #219086, .F. ) ;
#33628=ORIENTED_EDGE ( 'NONE', *, *, #38925, .F. ) ;
#33630=ORIENTED_EDGE ( 'NONE', *, *, #35368, .F. ) ;
#33662=ORIENTED_EDGE ( 'NONE', *, *, #181224, .F. ) ;
#33663=AXIS2_PLACEMENT_3D ( 'NONE', #129824, #51543, #93266 ) ;
#33714=EDGE_LOOP ( 'NONE', ( #77207, #232223, #201615, #93773 ) ) ;
#33763=EDGE_CURVE ( 'NONE', #166897, #125226, #62625, .T. ) ;
#33765=LINE ( 'NONE', #252745, #115071 ) ;
#33783=VERTEX_POINT ( 'NONE', #187720 ) ;
#33808=FACE_OUTER_BOUND ( 'NONE', #195247, .T. ) ;
#33814=DIRECTION ( 'NONE',  ( 0.000000000000000000, -0.4088369013363280513, 0.9126074666063769270 ) ) ;
#33816=EDGE_CURVE ( 'NONE', #241398, #41988, #108174, .T. ) ;
#33825=ORIENTED_EDGE ( 'NONE', *, *, #40825, .T. ) ;
#33850=ADVANCED_FACE ( 'NONE', ( #7789, #92432 ), #245106, .T. ) ;
#33866=CIRCLE ( 'NONE', #100428, 11.79999999999999538 ) ;
#33867=ORIENTED_EDGE ( 'NONE', *, *, #194371, .T. ) ;
#33870=ORIENTED_EDGE ( 'NONE', *, *, #155725, .F. ) ;
#33891=CARTESIAN_POINT ( 'NONE',  ( 22.01447462590973814, 29.98943614194342189, -252.4304903617178297 ) ) ;
#33894=ORIENTED_EDGE ( 'NONE', *, *, #189924, .F. ) ;
#33919=CARTESIAN_POINT ( 'NONE',  ( 18.59999999999999432, 44.52640028187936849, -247.3006740988509193 ) ) ;
#33927=CIRCLE ( 'NONE', #17142, 0.09999999999999939493 ) ;
#33954=CARTESIAN_POINT ( 'NONE',  ( 20.94999999999999929, 49.36776662947724503, -253.7196102226803021 ) ) ;
#33994=AXIS2_PLACEMENT_3D ( 'NONE', #63793, #247563, #85888 ) ;
#34013=CARTESIAN_POINT ( 'NONE',  ( -18.50000000000000355, 47.16152503674115337, -255.1462838189583806 ) ) ;
#34019=DIRECTION ( 'NONE',  ( 1.000000000000000000, 0.000000000000000000, 0.000000000000000000 ) ) ;
#34056=ORIENTED_EDGE ( 'NONE', *, *, #244234, .T. ) ;
#34062=VERTEX_POINT ( 'NONE', #161426 ) ;
#34161=VERTEX_POINT ( 'NONE', #30911 ) ;
#34193=DIRECTION ( 'NONE',  ( 0.000000000000000000, -0.9126074666063767049, -0.4088369013363286619 ) ) ;
#34203=CARTESIAN_POINT ( 'NONE',  ( -21.37071067811865532, 52.75222874190619393, -233.4979877221775837 ) ) ;
#34204=CARTESIAN_POINT ( 'NONE',  ( 21.51976009735019346, 33.83367400564330296, -243.2446267297141844 ) ) ;
#34209=ORIENTED_EDGE ( 'NONE', *, *, #184749, .T. ) ;
#34234=CARTESIAN_POINT ( 'NONE',  ( 18.39999999999999858, 77.26488334054521090, -241.9697969554615611 ) ) ;
#34260=CARTESIAN_POINT ( 'NONE',  ( -21.05000000000000071, 67.23127455305835554, -235.8551265064784559 ) ) ;
#34297=VERTEX_POINT ( 'NONE', #58110 ) ;
#34357=EDGE_CURVE ( 'NONE', #140623, #58126, #257214, .T. ) ;
#34379=FACE_OUTER_BOUND ( 'NONE', #104960, .T. ) ;
#34430=AXIS2_PLACEMENT_3D ( 'NONE', #117184, #96309, #14251 ) ;
#34446=CARTESIAN_POINT ( 'NONE',  ( -23.15000000000000213, 67.23127455305835554, -235.8551265064784559 ) ) ;
#34472=DIRECTION ( 'NONE',  ( 1.000000000000000000, 2.986185139342071370E-16, -6.665775143889693760E-16 ) ) ;
#34513=ORIENTED_EDGE ( 'NONE', *, *, #144169, .T. ) ;
#34529=VECTOR ( 'NONE', #248612, 999.9999999999998863 ) ;
#34550=ORIENTED_EDGE ( 'NONE', *, *, #56733, .T. ) ;
#34553=CARTESIAN_POINT ( 'NONE',  ( -21.05000000000000071, 30.93406981821913604, -252.0810274548579457 ) ) ;
#34570=FACE_OUTER_BOUND ( 'NONE', #200914, .T. ) ;
#34572=FACE_BOUND ( 'NONE', #236036, .T. ) ;
#34594=AXIS2_PLACEMENT_3D ( 'NONE', #79467, #39098, #78185 ) ;
#34598=FACE_OUTER_BOUND ( 'NONE', #209020, .T. ) ;
#34605=ORIENTED_EDGE ( 'NONE', *, *, #217815, .T. ) ;
#34639=FACE_OUTER_BOUND ( 'NONE', #136829, .T. ) ;
#34675=LINE ( 'NONE', #52923, #38086 ) ;
#34678=CIRCLE ( 'NONE', #22207, 0.1999999999999985401 ) ;
#34690=CARTESIAN_POINT ( 'NONE',  ( 21.05000000000000071, 47.74710514101221293, -244.5837943500090716 ) ) ;
#34691=FACE_OUTER_BOUND ( 'NONE', #149359, .T. ) ;
#34703=CARTESIAN_POINT ( 'NONE',  ( -23.15000000000000213, 67.23127455305835554, -235.8551265064784559 ) ) ;
#34724=FACE_OUTER_BOUND ( 'NONE', #253832, .T. ) ;
#34735=LINE ( 'NONE', #51673, #142155 ) ;
#34747=EDGE_CURVE ( 'NONE', #197418, #109819, #132552, .T. ) ;
#34752=VECTOR ( 'NONE', #211807, 1000.000000000000000 ) ;
#34798=DIRECTION ( 'NONE',  ( 1.000000000000000000, 0.000000000000000000, -0.000000000000000000 ) ) ;
#34809=DIRECTION ( 'NONE',  ( 1.000000000000000000, 0.000000000000000000, 0.000000000000000000 ) ) ;
#34810=AXIS2_PLACEMENT_3D ( 'NONE', #64858, #25745, #105226 ) ;
#34893=DIRECTION ( 'NONE',  ( 0.000000000000000000, -0.9126074666063660468, -0.4088369013363524762 ) ) ;
#34899=DIRECTION ( 'NONE',  ( 0.000000000000000000, 0.9955484899852913294, -0.09425075112701486457 ) ) ;
#34927=DIRECTION ( 'NONE',  ( 0.000000000000000000, 0.5859227990963362664, 0.8103668758649469339 ) ) ;
#34946=VECTOR ( 'NONE', #36284, 1000.000000000000000 ) ;
#34949=EDGE_LOOP ( 'NONE', ( #139320, #252150, #45876, #104980 ) ) ;
#34951=DIRECTION ( 'NONE',  ( 1.000000000000000000, 0.000000000000000000, 0.000000000000000000 ) ) ;
#34955=DIRECTION ( 'NONE',  ( 1.000000000000000000, 0.000000000000000000, 0.000000000000000000 ) ) ;
#34994=CARTESIAN_POINT ( 'NONE',  ( -21.64999999999999858, 52.99650480578122824, -234.2878581050858884 ) ) ;
#35012=CIRCLE ( 'NONE', #85005, 7.899999999999995914 ) ;
#35034=DIRECTION ( 'NONE',  ( 0.000000000000000000, 0.9126074666063660468, 0.4088369013363524762 ) ) ;
#35037=CARTESIAN_POINT ( 'NONE',  ( -20.07928932188135107, 52.19080555870878158, -232.4893728257138719 ) ) ;
#35043=CARTESIAN_POINT ( 'NONE',  ( 21.14999999999999503, 31.89597452117651244, -238.9192857152811484 ) ) ;
#35067=CIRCLE ( 'NONE', #222427, 11.79999999999999005 ) ;
#35072=CIRCLE ( 'NONE', #189344, 0.1000000000000024342 ) ;
#35109=ADVANCED_FACE ( 'NONE', ( #21355 ), #55054, .T. ) ;
#35112=CYLINDRICAL_SURFACE ( 'NONE', #127957, 0.1000000000000024342 ) ;
#35157=ORIENTED_EDGE ( 'NONE', *, *, #57421, .T. ) ;
#35167=CARTESIAN_POINT ( 'NONE',  ( 21.40925344232282868, 30.54185590562371999, -252.1831082382518048 ) ) ;
#35179=CIRCLE ( 'NONE', #193377, 0.09999999999999939493 ) ;
#35200=ORIENTED_EDGE ( 'NONE', *, *, #255430, .F. ) ;
#35211=CARTESIAN_POINT ( 'NONE',  ( 18.49999999999999645, 36.65892442174472876, -249.5511627012454596 ) ) ;
#35239=AXIS2_PLACEMENT_3D ( 'NONE', #248790, #25896, #148403 ) ;
#35248=DIRECTION ( 'NONE',  ( 1.000000000000000000, 0.000000000000000000, 0.000000000000000000 ) ) ;
#35249=VECTOR ( 'NONE', #133907, 1000.000000000000114 ) ;
#35264=CARTESIAN_POINT ( 'NONE',  ( -22.59999999999999787, 31.76322370622491320, -238.8696546380523671 ) ) ;
#35333=DIRECTION ( 'NONE',  ( 1.000000000000000000, 0.000000000000000000, 0.000000000000000000 ) ) ;
#35358=EDGE_CURVE ( 'NONE', #5240, #176861, #216655, .T. ) ;
#35365=ORIENTED_EDGE ( 'NONE', *, *, #25604, .T. ) ;
#35368=EDGE_CURVE ( 'NONE', #178487, #1827, #177573, .T. ) ;
#35383=ORIENTED_EDGE ( 'NONE', *, *, #24174, .F. ) ;
#35400=AXIS2_PLACEMENT_3D ( 'NONE', #138948, #20348, #60715 ) ;
#35418=ORIENTED_EDGE ( 'NONE', *, *, #128526, .F. ) ;
#35428=DIRECTION ( 'NONE',  ( 0.000000000000000000, 0.9594490217226103734, 0.2818822000686205254 ) ) ;
#35442=ORIENTED_EDGE ( 'NONE', *, *, #79127, .F. ) ;
#35447=AXIS2_PLACEMENT_3D ( 'NONE', #39523, #201122, #143712 ) ;
#35457=ORIENTED_EDGE ( 'NONE', *, *, #174891, .F. ) ;
#35480=ORIENTED_EDGE ( 'NONE', *, *, #105279, .T. ) ;
#35482=CARTESIAN_POINT ( 'NONE',  ( -18.59999999999999787, 38.29773864426884700, -236.0513742605307925 ) ) ;
#35507=CARTESIAN_POINT ( 'NONE',  ( -22.39999999999999858, 25.97741635855165754, -254.4468634167653249 ) ) ;
#35514=CIRCLE ( 'NONE', #52023, 12.87499999999999112 ) ;
#35523=EDGE_CURVE ( 'NONE', #215121, #150106, #82991, .T. ) ;
#35527=CIRCLE ( 'NONE', #118718, 0.09999999999999939493 ) ;
#35542=EDGE_LOOP ( 'NONE', ( #155032, #65219, #202465, #63570, #225009 ) ) ;
#35562=CARTESIAN_POINT ( 'NONE',  ( -18.50000000000000355, 74.95904887477786360, -233.7774272632847783 ) ) ;
#35566=( NAMED_UNIT ( * ) SI_UNIT ( $, .STERADIAN. ) SOLID_ANGLE_UNIT ( ) );
#35569=LINE ( 'NONE', #115078, #40390 ) ;
#35597=AXIS2_PLACEMENT_3D ( 'NONE', #224384, #147429, #207420 ) ;
#35624=ORIENTED_EDGE ( 'NONE', *, *, #191305, .T. ) ;
#35627=CARTESIAN_POINT ( 'NONE',  ( 20.85000000000000142, 78.48087866980282001, -232.8271061603568910 ) ) ;
#35655=CARTESIAN_POINT ( 'NONE',  ( 19.99999999999998934, 51.28888318656201761, -230.2315015618842153 ) ) ;
#35686=CARTESIAN_POINT ( 'NONE',  ( 19.58285714285715073, 39.37606100570253886, -236.9544388824136831 ) ) ;
#35721=CARTESIAN_POINT ( 'NONE',  ( 18.59999999999999432, 44.55458850188623643, -247.3966190010231969 ) ) ;
#35736=EDGE_CURVE ( 'NONE', #51036, #28439, #249811, .T. ) ;
#35819=DIRECTION ( 'NONE',  ( -1.000000000000000000, -0.000000000000000000, -0.000000000000000000 ) ) ;
#35847=CARTESIAN_POINT ( 'NONE',  ( -18.58735405345342784, 77.36886435760402492, -241.7961888098465408 ) ) ;
#35851=ORIENTED_EDGE ( 'NONE', *, *, #117340, .F. ) ;
#35853=CARTESIAN_POINT ( 'NONE',  ( 23.24999999999997513, 56.06656052939784729, -228.0911609752645290 ) ) ;
#35854=DIRECTION ( 'NONE',  ( 1.000000000000000000, 0.000000000000000000, -0.000000000000000000 ) ) ;
#35870=EDGE_CURVE ( 'NONE', #200814, #36945, #197740, .T. ) ;
#35876=CARTESIAN_POINT ( 'NONE',  ( 21.05000000000000071, 45.77234354862702048, -239.5513518621457365 ) ) ;
#35891=CARTESIAN_POINT ( 'NONE',  ( 18.39999999999999858, 77.26488334054519669, -241.9697969554615611 ) ) ;
#35893=EDGE_CURVE ( 'NONE', #2024, #223475, #185876, .T. ) ;
#35901=CARTESIAN_POINT ( 'NONE',  ( 20.94999999999999929, 69.34766280046808617, -247.6726305063181144 ) ) ;
#35906=VECTOR ( 'NONE', #99300, 1000.000000000000114 ) ;
#35916=CARTESIAN_POINT ( 'NONE',  ( -18.50000000000000000, 67.23127455305835554, -235.8551265064784559 ) ) ;
#35934=DIRECTION ( 'NONE',  ( -1.000000000000000000, -0.000000000000000000, 0.000000000000000000 ) ) ;
#35936=EDGE_LOOP ( 'NONE', ( #33662, #73742, #57156, #112401 ) ) ;
#35948=ADVANCED_FACE ( 'NONE', ( #145460 ), #84156, .T. ) ;
#35984=TOROIDAL_SURFACE ( 'NONE', #69308, 0.2000000000000000111, 0.1000000000000000056 ) ;
#35995=CARTESIAN_POINT ( 'NONE',  ( 21.09107601085606021, 30.83513164543635909, -252.1170788411612023 ) ) ;
#36000=CARTESIAN_POINT ( 'NONE',  ( 18.51024323315077069, 68.05374558910872906, -224.1882283518531835 ) ) ;
#36012=AXIS2_PLACEMENT_3D ( 'NONE', #141838, #201817, #73896 ) ;
#36016=VERTEX_POINT ( 'NONE', #48931 ) ;
#36026=CARTESIAN_POINT ( 'NONE',  ( -22.50000000000000000, 36.65892442174472876, -249.5511627012454596 ) ) ;
#36033=AXIS2_PLACEMENT_3D ( 'NONE', #4121, #125365, #246581 ) ;
#36039=CARTESIAN_POINT ( 'NONE',  ( 20.86777300164945004, 68.11153784908182729, -224.1393723182492579 ) ) ;
#36050=EDGE_CURVE ( 'NONE', #97383, #247446, #233081, .T. ) ;
#36056=EDGE_LOOP ( 'NONE', ( #144054, #178883, #53229, #77289 ) ) ;
#36066=DIRECTION ( 'NONE',  ( 1.000000000000000000, -7.510212038922846022E-17, 1.676432719286211941E-16 ) ) ;
#36106=CARTESIAN_POINT ( 'NONE',  ( 20.97438252431638972, 40.74183068305447364, -237.9419367875085527 ) ) ;
#36154=CARTESIAN_POINT ( 'NONE',  ( 21.05000000000000071, 45.93587830916155212, -239.9163948487882863 ) ) ;
#36181=CARTESIAN_POINT ( 'NONE',  ( 23.24999999999999289, 21.13195309841794867, -243.6318585593223816 ) ) ;
#36193=LINE ( 'NONE', #14061, #257297 ) ;
#36198=CARTESIAN_POINT ( 'NONE',  ( -20.64999999999999858, 54.34471204062663219, -239.4366250215122420 ) ) ;
#36206=DIRECTION ( 'NONE',  ( -1.000000000000000000, 1.207181226542539700E-16, -2.694675058168174199E-16 ) ) ;
#36209=CARTESIAN_POINT ( 'NONE',  ( 23.15000000000000213, 69.08367151115869831, -247.5088222940653679 ) ) ;
#36216=ADVANCED_FACE ( 'NONE', ( #143870 ), #211830, .T. ) ;
#36231=AXIS2_PLACEMENT_3D ( 'NONE', #18125, #153841, #233352 ) ;
#36256=DIRECTION ( 'NONE',  ( -1.000000000000000000, 1.207181226542539700E-16, -2.694675058168174199E-16 ) ) ;
#36265=CARTESIAN_POINT ( 'NONE',  ( 22.60000000000000142, 25.89494711235935043, -254.2627752153468350 ) ) ;
#36270=CIRCLE ( 'NONE', #181996, 0.1000000000000033501 ) ;
#36273=DIRECTION ( 'NONE',  ( 0.000000000000000000, 0.4088369013363281623, -0.9126074666063771490 ) ) ;
#36276=EDGE_CURVE ( 'NONE', #257664, #71259, #60476, .T. ) ;
#36284=DIRECTION ( 'NONE',  ( -1.000000000000000000, -0.000000000000000000, -0.000000000000000000 ) ) ;
#36335=ADVANCED_FACE ( 'NONE', ( #102152 ), #103449, .F. ) ;
#36346=CARTESIAN_POINT ( 'NONE',  ( -20.64999999999999858, 53.03738849591485405, -234.3791188517465400 ) ) ;
#36347=EDGE_CURVE ( 'NONE', #1827, #15704, #220214, .T. ) ;
#36389=CIRCLE ( 'NONE', #11240, 0.1000000000000024342 ) ;
#36417=EDGE_CURVE ( 'NONE', #102676, #39096, #20886, .T. ) ;
#36435=CARTESIAN_POINT ( 'NONE',  ( -18.59999999999999787, 78.48087866980282001, -232.8271061603568910 ) ) ;
#36467=CIRCLE ( 'NONE', #111272, 0.09999999999999609201 ) ;
#36475=DIRECTION ( 'NONE',  ( 1.000000000000000000, -1.207181226542539700E-16, 2.694675058168174199E-16 ) ) ;
#36476=DIRECTION ( 'NONE',  ( -1.000000000000000000, 0.000000000000000000, 0.000000000000000000 ) ) ;
#36495=ORIENTED_EDGE ( 'NONE', *, *, #144830, .T. ) ;
#36496=DIRECTION ( 'NONE',  ( 0.000000000000000000, -0.9188841341108708871, -0.3945274997757635127 ) ) ;
#36510=DIRECTION ( 'NONE',  ( 0.000000000000000000, 0.9126074666063769270, 0.4088369013363284399 ) ) ;
#36513=AXIS2_PLACEMENT_3D ( 'NONE', #25413, #67090, #47507 ) ;
#36531=VECTOR ( 'NONE', #14112, 1000.000000000000114 ) ;
#36549=CARTESIAN_POINT ( 'NONE',  ( -22.49544290803669000, 31.79553970091675907, -238.8548453295646823 ) ) ;
#36566=EDGE_CURVE ( 'NONE', #71259, #125186, #174645, .T. ) ;
#36574=CARTESIAN_POINT ( 'NONE',  ( -18.50000000000000000, 21.13195309841794867, -243.6318585593224100 ) ) ;
#36617=ORIENTED_EDGE ( 'NONE', *, *, #8178, .F. ) ;
#36627=CARTESIAN_POINT ( 'NONE',  ( -20.94999999999999929, 46.45388641681647357, -243.1520440498138385 ) ) ;
#36635=ORIENTED_EDGE ( 'NONE', *, *, #176831, .T. ) ;
#36636=AXIS2_PLACEMENT_3D ( 'NONE', #9866, #252311, #132386 ) ;
#36653=DIRECTION ( 'NONE',  ( 1.000000000000000000, 0.000000000000000000, 0.000000000000000000 ) ) ;
#36673=CARTESIAN_POINT ( 'NONE',  ( 23.24999999999999289, 31.94635157770351341, -238.7871412784868710 ) ) ;
#36679=VECTOR ( 'NONE', #178325, 1000.000000000000114 ) ;
#36687=DIRECTION ( 'NONE',  ( 0.000000000000000000, -0.1022405907414443982, -0.9947597004326425019 ) ) ;
#36706=LINE ( 'NONE', #54928, #243524 ) ;
#36724=ORIENTED_EDGE ( 'NONE', *, *, #11361, .T. ) ;
#36726=EDGE_CURVE ( 'NONE', #79169, #171172, #132906, .T. ) ;
#36727=EDGE_CURVE ( 'NONE', #69371, #188456, #81021, .T. ) ;
#36761=AXIS2_PLACEMENT_3D ( 'NONE', #243915, #64006, #105672 ) ;
#36807=FACE_OUTER_BOUND ( 'NONE', #171134, .T. ) ;
#36822=VECTOR ( 'NONE', #202318, 1000.000000000000114 ) ;
#36830=ADVANCED_FACE ( 'NONE', ( #226976 ), #127882, .F. ) ;
#36864=CARTESIAN_POINT ( 'NONE',  ( 18.49999999999999289, 54.98105481382776816, -230.1569079895687366 ) ) ;
#36891=FACE_OUTER_BOUND ( 'NONE', #148241, .T. ) ;
#36893=ORIENTED_EDGE ( 'NONE', *, *, #59158, .T. ) ;
#36915=VECTOR ( 'NONE', #242633, 1000.000000000000114 ) ;
#36936=B_SPLINE_CURVE_WITH_KNOTS ( 'NONE', 3,
 ( #128324, #85298, #24102, #184425, #147885, #227404 ),
 .UNSPECIFIED., .F., .F.,
 ( 4, 2, 4 ),
 ( 0.000000000000000000, 0.0002113392456165965911, 0.0004226784912331931821 ),
 .UNSPECIFIED. ) ;
#36945=VERTEX_POINT ( 'NONE', #95166 ) ;
#36958=CARTESIAN_POINT ( 'NONE',  ( 23.14999999999999858, 55.39363411790989034, -234.6384634766556303 ) ) ;
#36972=DIRECTION ( 'NONE',  ( 1.000000000000000000, 0.000000000000000000, 0.000000000000000000 ) ) ;
#36985=EDGE_LOOP ( 'NONE', ( #107971, #24693, #17297, #55050 ) ) ;
#37004=AXIS2_PLACEMENT_3D ( 'NONE', #207401, #9180, #28795 ) ;
#37043=EDGE_LOOP ( 'NONE', ( #221408, #47836, #33378, #68936, #72954, #24554, #15517 ) ) ;
#37046=VERTEX_POINT ( 'NONE', #92583 ) ;
#37135=LINE ( 'NONE', #174103, #50061 ) ;
#37177=ORIENTED_EDGE ( 'NONE', *, *, #123537, .F. ) ;
#37193=EDGE_LOOP ( 'NONE', ( #246796, #8858, #101149, #45944 ) ) ;
#37194=VERTEX_POINT ( 'NONE', #7624 ) ;
#37199=DIRECTION ( 'NONE',  ( 0.000000000000000000, -0.9126074666063769270, -0.4088369013363280513 ) ) ;
#37255=DIRECTION ( 'NONE',  ( -0.000000000000000000, 0.4088369013363276072, -0.9126074666063772600 ) ) ;
#37261=FACE_OUTER_BOUND ( 'NONE', #216819, .T. ) ;
#37269=ORIENTED_EDGE ( 'NONE', *, *, #34357, .T. ) ;
#37273=CARTESIAN_POINT ( 'NONE',  ( -21.05000000000000071, 48.04585786805223080, -246.4610531646956417 ) ) ;
#37332=CARTESIAN_POINT ( 'NONE',  ( -20.94999999999999929, 46.54514716347711101, -243.1111603596801842 ) ) ;
#37361=LINE ( 'NONE', #133869, #115212 ) ;
#37373=ORIENTED_EDGE ( 'NONE', *, *, #102002, .F. ) ;
#37392=ORIENTED_EDGE ( 'NONE', *, *, #221852, .T. ) ;
#37394=CARTESIAN_POINT ( 'NONE',  ( -22.00411653962173730, 33.60306640061016026, -242.9721070132478076 ) ) ;
#37410=DIRECTION ( 'NONE',  ( 0.000000000000000000, 0.3999834006488773852, 0.9165223833629813077 ) ) ;
#37455=DIRECTION ( 'NONE',  ( 0.000000000000000000, 0.9126074666063660468, 0.4088369013363524762 ) ) ;
#37480=EDGE_CURVE ( 'NONE', #62294, #77834, #22725, .T. ) ;
#37490=CARTESIAN_POINT ( 'NONE',  ( -18.49372193242259499, 77.26530055437073941, -241.7067161772392865 ) ) ;
#37499=DIRECTION ( 'NONE',  ( 1.000000000000000000, -2.986185139342070877E-16, 6.665775143889692774E-16 ) ) ;
#37501=DIRECTION ( 'NONE',  ( 0.000000000000000000, 0.9623856809447771665, 0.2716869542551821892 ) ) ;
#37509=CIRCLE ( 'NONE', #41623, 0.09999999999999939493 ) ;
#37550=CARTESIAN_POINT ( 'NONE',  ( -20.94999999999999929, 36.52237217006333481, -249.3317055962219229 ) ) ;
#37597=EDGE_CURVE ( 'NONE', #199454, #9026, #70843, .T. ) ;
#37619=ORIENTED_EDGE ( 'NONE', *, *, #182516, .T. ) ;
#37628=FACE_OUTER_BOUND ( 'NONE', #64729, .T. ) ;
#37667=EDGE_CURVE ( 'NONE', #139340, #49350, #155, .T. ) ;
#37686=ORIENTED_EDGE ( 'NONE', *, *, #104860, .F. ) ;
#37690=CARTESIAN_POINT ( 'NONE',  ( 23.25000000000000000, 41.42187432231295219, -260.1830396872097140 ) ) ;
#37707=FACE_OUTER_BOUND ( 'NONE', #97001, .T. ) ;
#37743=CARTESIAN_POINT ( 'NONE',  ( -20.89878130938411616, 68.09900309800710261, -224.1499508721967970 ) ) ;
#37778=CARTESIAN_POINT ( 'NONE',  ( -21.05000000000000071, 46.54514716347711101, -243.1111603596801842 ) ) ;
#37795=ADVANCED_FACE ( 'NONE', ( #14720 ), #233751, .T. ) ;
#37808=TOROIDAL_SURFACE ( 'NONE', #208494, 2.100000000000002309, 0.1000000000000000056 ) ;
#37857=CIRCLE ( 'NONE', #112656, 0.1999999999999985401 ) ;
#37860=ORIENTED_EDGE ( 'NONE', *, *, #40124, .F. ) ;
#37893=CARTESIAN_POINT ( 'NONE',  ( 18.50000000000000000, 77.13860723519891849, -241.8264964602988982 ) ) ;
#37912=ORIENTED_EDGE ( 'NONE', *, *, #186669, .T. ) ;
#37962=ORIENTED_EDGE ( 'NONE', *, *, #20345, .T. ) ;
#37976=CIRCLE ( 'NONE', #183708, 0.1000000000000024342 ) ;
#37979=CARTESIAN_POINT ( 'NONE',  ( 20.94999999999999929, 62.46832465249013921, -225.2232495205141731 ) ) ;
#37985=ORIENTED_EDGE ( 'NONE', *, *, #212566, .F. ) ;
#38043=DIRECTION ( 'NONE',  ( 1.000000000000000000, 0.000000000000000000, 0.000000000000000000 ) ) ;
#38063=DIRECTION ( 'NONE',  ( 0.000000000000000000, 0.9126074666063660468, 0.4088369013363524762 ) ) ;
#38081=CARTESIAN_POINT ( 'NONE',  ( 20.94999999999999574, 44.58277672189309015, -247.4925639031954745 ) ) ;
#38086=VECTOR ( 'NONE', #212024, 1000.000000000000114 ) ;
#38119=ORIENTED_EDGE ( 'NONE', *, *, #150110, .T. ) ;
#38143=DIRECTION ( 'NONE',  ( 0.000000000000000000, 0.5283051335749160415, -0.8490545835447742551 ) ) ;
#38157=DIRECTION ( 'NONE',  ( 0.000000000000000000, 0.9126074666063844765, 0.4088369013363114535 ) ) ;
#38161=DIRECTION ( 'NONE',  ( -1.000000000000000000, 7.510212038922846022E-17, -1.676432719286211941E-16 ) ) ;
#38186=DIRECTION ( 'NONE',  ( 1.000000000000000000, 0.000000000000000000, 0.000000000000000000 ) ) ;
#38190=ORIENTED_EDGE ( 'NONE', *, *, #22927, .T. ) ;
#38225=ORIENTED_EDGE ( 'NONE', *, *, #9111, .F. ) ;
#38249=B_SPLINE_CURVE_WITH_KNOTS ( 'NONE', 3,
 ( #58309, #80421, #43906, #217388, #62194, #137851, #60889, #23085, #158749, #79161 ),
 .UNSPECIFIED., .F., .F.,
 ( 4, 2, 2, 2, 4 ),
 ( 0.000000000000000000, 3.990160268009109807E-05, 7.980320536018219613E-05, 0.0001596064107204557634, 0.0003192128214410053103 ),
 .UNSPECIFIED. ) ;
#38250=CIRCLE ( 'NONE', #150673, 0.09999999999999939493 ) ;
#38256=LINE ( 'NONE', #181623, #156302 ) ;
#38282=DIRECTION ( 'NONE',  ( -0.000000000000000000, -0.9126074666063770380, -0.4088369013363281068 ) ) ;
#38295=DIRECTION ( 'NONE',  ( -1.000000000000000000, 0.000000000000000000, 0.000000000000000000 ) ) ;
#38307=VERTEX_POINT ( 'NONE', #196407 ) ;
#38310=ORIENTED_EDGE ( 'NONE', *, *, #23725, .F. ) ;
#38322=ORIENTED_EDGE ( 'NONE', *, *, #70900, .T. ) ;
#38341=CARTESIAN_POINT ( 'NONE',  ( 21.07964655665547582, 44.22523807184186495, -236.5463624157991944 ) ) ;
#38357=FACE_OUTER_BOUND ( 'NONE', #117722, .T. ) ;
#38382=ADVANCED_FACE ( 'NONE', ( #77730 ), #236816, .T. ) ;
#38398=CARTESIAN_POINT ( 'NONE',  ( -18.59999999999999787, 77.44184265367995579, -241.6694879557322508 ) ) ;
#38433=CARTESIAN_POINT ( 'NONE',  ( 20.85000000000000142, 74.93036000061670165, -233.6816308724374949 ) ) ;
#38507=EDGE_CURVE ( 'NONE', #56413, #79382, #226008, .T. ) ;
#38545=CARTESIAN_POINT ( 'NONE',  ( -23.25000000000000000, 41.42187432231295219, -260.1830396872097140 ) ) ;
#38546=CARTESIAN_POINT ( 'NONE',  ( -23.25000000000000000, 62.12679871018153932, -248.6611778639222337 ) ) ;
#38559=VERTEX_POINT ( 'NONE', #12469 ) ;
#38585=VECTOR ( 'NONE', #78716, 1000.000000000000227 ) ;
#38628=EDGE_CURVE ( 'NONE', #49350, #15058, #1177, .T. ) ;
#38652=VECTOR ( 'NONE', #83501, 1000.000000000000000 ) ;
#38664=ORIENTED_EDGE ( 'NONE', *, *, #192882, .T. ) ;
#38745=CYLINDRICAL_SURFACE ( 'NONE', #54527, 0.09999999999999939493 ) ;
#38757=CARTESIAN_POINT ( 'NONE',  ( -23.15000000000000213, 46.15118611352045974, -240.5321844900040844 ) ) ;
#38759=CARTESIAN_POINT ( 'NONE',  ( -18.59999999999999787, 44.55458850188623643, -247.3966190010231969 ) ) ;
#38769=ORIENTED_EDGE ( 'NONE', *, *, #146101, .F. ) ;
#38776=CARTESIAN_POINT ( 'NONE',  ( -20.85000000000000142, 74.73788286442776041, -233.7359682632885267 ) ) ;
#38789=DIRECTION ( 'NONE',  ( -1.000000000000000000, 1.335000415235278971E-16, -2.979993593738921214E-16 ) ) ;
#38831=ORIENTED_EDGE ( 'NONE', *, *, #245208, .T. ) ;
#38840=CARTESIAN_POINT ( 'NONE',  ( 21.14999999999999858, 33.98486250090727623, -243.5821103306120108 ) ) ;
#38843=DIRECTION ( 'NONE',  ( -1.000000000000000000, -0.000000000000000000, -0.000000000000000000 ) ) ;
#38844=CARTESIAN_POINT ( 'NONE',  ( 21.05000000000000071, 49.36776662947724503, -253.7196102226803021 ) ) ;
#38846=CIRCLE ( 'NONE', #147165, 2.000000000000012879 ) ;
#38866=AXIS2_PLACEMENT_3D ( 'NONE', #41135, #63219, #159781 ) ;
#38881=AXIS2_PLACEMENT_3D ( 'NONE', #152327, #154897, #125356 ) ;
#38891=DIRECTION ( 'NONE',  ( 0.000000000000000000, 0.9126074666063791474, 0.4088369013363231663 ) ) ;
#38913=CARTESIAN_POINT ( 'NONE',  ( 23.15000000000000213, 60.94692742449272771, -251.5456325903398067 ) ) ;
#38924=CARTESIAN_POINT ( 'NONE',  ( -18.59999999999999787, 47.95459712139159336, -246.5019368548292675 ) ) ;
#38925=EDGE_CURVE ( 'NONE', #206263, #220667, #121995, .T. ) ;
#38928=EDGE_CURVE ( 'NONE', #227981, #248454, #94432, .T. ) ;
#38940=DIRECTION ( 'NONE',  ( -0.000000000000000000, 0.4088369013363281623, -0.9126074666063771490 ) ) ;
#38941=ORIENTED_EDGE ( 'NONE', *, *, #247649, .T. ) ;
#38952=CARTESIAN_POINT ( 'NONE',  ( 21.14999999999999858, 34.01125473725045367, -243.8802146427659352 ) ) ;
#38954=CIRCLE ( 'NONE', #72272, 0.09999999999999854838 ) ;
#38956=CARTESIAN_POINT ( 'NONE',  ( -18.59999999999999787, 74.93036000061670165, -233.6816308724374949 ) ) ;
#38989=DIRECTION ( 'NONE',  ( 0.000000000000000000, 0.1022405907414316584, 0.9947597004326437231 ) ) ;
#39054=DIRECTION ( 'NONE',  ( 0.000000000000000000, -0.3945274997758418944, 0.9188841341108372474 ) ) ;
#39073=ORIENTED_EDGE ( 'NONE', *, *, #78103, .T. ) ;
#39077=AXIS2_PLACEMENT_3D ( 'NONE', #168732, #10902, #248223 ) ;
#39096=VERTEX_POINT ( 'NONE', #18570 ) ;
#39098=DIRECTION ( 'NONE',  ( -1.000000000000000000, -0.000000000000000000, -0.000000000000000000 ) ) ;
#39125=DIRECTION ( 'NONE',  ( 1.000000000000000000, 2.986185139342070877E-16, -6.665775143889692774E-16 ) ) ;
#39134=ORIENTED_EDGE ( 'NONE', *, *, #6994, .F. ) ;
#39140=DIRECTION ( 'NONE',  ( 0.7071067811865475727, -0.2890913453342130457, 0.6453109281988448354 ) ) ;
#39236=VECTOR ( 'NONE', #53083, 1000.000000000000000 ) ;
#39246=CYLINDRICAL_SURFACE ( 'NONE', #126634, 0.09999999999999939493 ) ;
#39249=TOROIDAL_SURFACE ( 'NONE', #60056, 0.6000000000000009770, 0.1000000000000000056 ) ;
#39254=ADVANCED_FACE ( 'NONE', ( #66684 ), #215484, .T. ) ;
#39260=ORIENTED_EDGE ( 'NONE', *, *, #117340, .T. ) ;
#39261=VERTEX_POINT ( 'NONE', #233479 ) ;
#39274=AXIS2_PLACEMENT_3D ( 'NONE', #228435, #125474, #26376 ) ;
#39326=DIRECTION ( 'NONE',  ( 0.000000000000000000, 0.9126074666063773710, 0.4088369013363274407 ) ) ;
#39341=AXIS2_PLACEMENT_3D ( 'NONE', #239689, #2335, #161450 ) ;
#39370=DIRECTION ( 'NONE',  ( -2.827886303505249259E-16, -0.8103668758649578141, 0.5859227990963213895 ) ) ;
#39380=CARTESIAN_POINT ( 'NONE',  ( 18.47654891039377389, 47.03189691987548571, -255.2758813845442774 ) ) ;
#39390=ORIENTED_EDGE ( 'NONE', *, *, #244456, .F. ) ;
#39396=DIRECTION ( 'NONE',  ( 0.000000000000000000, 0.9126074666063545004, 0.4088369013363783999 ) ) ;
#39435=DIRECTION ( 'NONE',  ( 0.000000000000000000, -0.9126074666063767049, -0.4088369013363286619 ) ) ;
#39447=ORIENTED_EDGE ( 'NONE', *, *, #27338, .T. ) ;
#39458=CARTESIAN_POINT ( 'NONE',  ( -21.05000000000000071, 44.18518595211054389, -258.7688298343402380 ) ) ;
#39472=ORIENTED_EDGE ( 'NONE', *, *, #193644, .T. ) ;
#39487=CARTESIAN_POINT ( 'NONE',  ( 21.00000000000000000, 43.94346684630428967, -235.6041041703296344 ) ) ;
#39505=ADVANCED_FACE ( 'NONE', ( #243727 ), #162929, .F. ) ;
#39523=CARTESIAN_POINT ( 'NONE',  ( 21.05000000000000071, 68.96522873961046685, -235.0783363939394235 ) ) ;
#39546=DIRECTION ( 'NONE',  ( 0.000000000000000000, 0.9126074666064812879, 0.4088369013360954596 ) ) ;
#39575=DIRECTION ( 'NONE',  ( 0.000000000000000000, 0.4088369013363287729, -0.9126074666063767049 ) ) ;
#39604=FACE_OUTER_BOUND ( 'NONE', #7581, .T. ) ;
#39618=ORIENTED_EDGE ( 'NONE', *, *, #97223, .T. ) ;
#39630=CIRCLE ( 'NONE', #77006, 0.09999999999999609201 ) ;
#39640=DIRECTION ( 'NONE',  ( 0.000000000000000000, -0.9126074666063844765, -0.4088369013363114535 ) ) ;
#39679=DIRECTION ( 'NONE',  ( 0.000000000000000000, -0.9126074666063660468, -0.4088369013363524762 ) ) ;
#39683=AXIS2_PLACEMENT_3D ( 'NONE', #136980, #93993, #138246 ) ;
#39713=DIRECTION ( 'NONE',  ( 0.000000000000000000, -0.4088369013363783999, 0.9126074666063545004 ) ) ;
#39737=CIRCLE ( 'NONE', #60713, 2.099999999999990763 ) ;
#39750=EDGE_CURVE ( 'NONE', #235986, #119433, #207139, .T. ) ;
#39794=LINE ( 'NONE', #98398, #32144 ) ;
#39801=CARTESIAN_POINT ( 'NONE',  ( -20.54999999999999716, 47.45383559552796271, -242.5236527704543334 ) ) ;
#39822=ORIENTED_EDGE ( 'NONE', *, *, #20438, .T. ) ;
#39832=DIRECTION ( 'NONE',  ( 1.000000000000000000, 0.000000000000000000, 0.000000000000000000 ) ) ;
#39844=DIRECTION ( 'NONE',  ( 0.000000000000000000, 0.9126074666063768159, 0.4088369013363282178 ) ) ;
#39853=EDGE_LOOP ( 'NONE', ( #27154, #87091, #246094, #41802, #210762 ) ) ;
#39879=CARTESIAN_POINT ( 'NONE',  ( 23.24999999999999645, 68.82573846827003194, -239.4142956262433302 ) ) ;
#39884=EDGE_CURVE ( 'NONE', #151518, #118038, #203013, .T. ) ;
#39905=DIRECTION ( 'NONE',  ( 1.000000000000000000, -1.207181226542539700E-16, 2.694675058168174199E-16 ) ) ;
#39963=ORIENTED_EDGE ( 'NONE', *, *, #221267, .T. ) ;
#39984=ADVANCED_FACE ( 'NONE', ( #125707 ), #226064, .F. ) ;
#39986=ORIENTED_EDGE ( 'NONE', *, *, #174044, .T. ) ;
#39995=VECTOR ( 'NONE', #252097, 1000.000000000000114 ) ;
#40006=CARTESIAN_POINT ( 'NONE',  ( -21.64999999999999858, 44.92467540951147953, -237.7943620901849613 ) ) ;
#40023=DIRECTION ( 'NONE',  ( 0.000000000000000000, -0.9160831752668552319, -0.4009882990724247809 ) ) ;
#40029=CARTESIAN_POINT ( 'NONE',  ( 18.59999999999999076, 54.57427006634497957, -228.7596887170734306 ) ) ;
#40038=CARTESIAN_POINT ( 'NONE',  ( -23.15000000000000213, 30.73962027982165779, -265.0781340245722504 ) ) ;
#40047=CARTESIAN_POINT ( 'NONE',  ( 21.05000000000000071, 45.58907629467868361, -240.2765730862633404 ) ) ;
#40049=EDGE_LOOP ( 'NONE', ( #114709, #192207, #40723, #256982 ) ) ;
#40050=CARTESIAN_POINT ( 'NONE',  ( -20.94999999999999929, 44.34387878855809362, -247.3824414791181994 ) ) ;
#40054=DIRECTION ( 'NONE',  ( 0.000000000000000000, -0.09425075112712516523, -0.9955484899852807823 ) ) ;
#40073=CARTESIAN_POINT ( 'NONE',  ( -18.44232395689850534, 77.38089040410972075, -241.7752457915469506 ) ) ;
#40079=EDGE_LOOP ( 'NONE', ( #138867, #80124, #234792, #120152 ) ) ;
#40111=B_SPLINE_CURVE_WITH_KNOTS ( 'NONE', 3,
 ( #186343, #204596, #5086, #45536, #88483, #166802, #49391, #29852, #106779, #168098, #224160, #247586, #85911, #68972, #225432, #25982, #185042, #148494, #6401, #7706, #165497, #108086 ),
 .UNSPECIFIED., .F., .F.,
 ( 4, 3, 3, 3, 3, 3, 3, 4 ),
 ( 0.000000000000000000, 7.307836821075696998E-06, 4.161455748547338501E-05, 7.576591810648398973E-05, 0.0001098090429817408253, 0.0001438003617351054644, 0.0001777914035423563022, 0.0002117966137402873411 ),
 .UNSPECIFIED. ) ;
#40117=ADVANCED_FACE ( 'NONE', ( #99403 ), #40773, .T. ) ;
#40119=CARTESIAN_POINT ( 'NONE',  ( 20.85000000106584750, 56.18110340670159530, -227.9302710413118689 ) ) ;
#40124=EDGE_CURVE ( 'NONE', #101872, #177565, #53363, .T. ) ;
#40174=CIRCLE ( 'NONE', #190191, 0.5000000000000031086 ) ;
#40187=CARTESIAN_POINT ( 'NONE',  ( -21.07016717457009136, 30.89038661691667542, -252.1353965670249693 ) ) ;
#40194=CARTESIAN_POINT ( 'NONE',  ( -21.05000000000000071, 67.23127455305835554, -235.8551265064784559 ) ) ;
#40197=CYLINDRICAL_SURFACE ( 'NONE', #101186, 0.09999999999999854838 ) ;
#40201=AXIS2_PLACEMENT_3D ( 'NONE', #105498, #169405, #207220 ) ;
#40214=VECTOR ( 'NONE', #209926, 1000.000000000000114 ) ;
#40219=EDGE_CURVE ( 'NONE', #192641, #239804, #158167, .T. ) ;
#40220=CARTESIAN_POINT ( 'NONE',  ( -20.54999999999999716, 46.15118611352045974, -240.5321844900040844 ) ) ;
#40222=VERTEX_POINT ( 'NONE', #199835 ) ;
#40230=PLANE ( 'NONE',  #39341 ) ;
#40231=CARTESIAN_POINT ( 'NONE',  ( 20.94999999999999929, 43.36285386911620776, -234.7972500504784534 ) ) ;
#40261=EDGE_CURVE ( 'NONE', #45859, #206465, #65825, .T. ) ;
#40291=ADVANCED_FACE ( 'NONE', ( #204929 ), #167140, .T. ) ;
#40301=CARTESIAN_POINT ( 'NONE',  ( -20.54999999999999716, 53.03738849591485405, -234.3791188517465400 ) ) ;
#40303=VECTOR ( 'NONE', #241957, 1000.000000000000114 ) ;
#40310=VERTEX_POINT ( 'NONE', #168445 ) ;
#40366=DIRECTION ( 'NONE',  ( 0.000000000000000000, -0.9126074666063772600, -0.4088369013363274407 ) ) ;
#40390=VECTOR ( 'NONE', #172539, 1000.000000000000114 ) ;
#40391=CARTESIAN_POINT ( 'NONE',  ( -20.54999999999999716, 54.73010456436290383, -239.3295147855486107 ) ) ;
#40422=CARTESIAN_POINT ( 'NONE',  ( -20.64999999999999858, 47.91013932883114990, -242.3192343197862044 ) ) ;
#40437=TOROIDAL_SURFACE ( 'NONE', #65899, 0.4000000000000010214, 0.1000000000000000056 ) ;
#40438=DIRECTION ( 'NONE',  ( -1.000000000000000000, -0.000000000000000000, 0.000000000000000000 ) ) ;
#40473=CARTESIAN_POINT ( 'NONE',  ( 20.85000000000000142, 67.74990736105834799, -227.9721689390126755 ) ) ;
#40477=CIRCLE ( 'NONE', #252801, 0.09999999999999939493 ) ;
#40479=LINE ( 'NONE', #57413, #61709 ) ;
#40501=CARTESIAN_POINT ( 'NONE',  ( -21.05000000000000071, 69.06797323185276127, -247.4100621602722470 ) ) ;
#40515=DIRECTION ( 'NONE',  ( 0.000000000000000000, 0.9126074666063770380, 0.4088369013363281068 ) ) ;
#40536=VECTOR ( 'NONE', #230584, 1000.000000000000000 ) ;
#40582=DIRECTION ( 'NONE',  ( -0.000000000000000000, 0.4088369013363281623, -0.9126074666063771490 ) ) ;
#40620=EDGE_LOOP ( 'NONE', ( #39447, #107649, #31251, #111667 ) ) ;
#40621=EDGE_LOOP ( 'NONE', ( #20070, #186766, #170897 ) ) ;
#40629=CARTESIAN_POINT ( 'NONE',  ( 23.14999999999999858, 56.06656052939784729, -228.0911609752645290 ) ) ;
#40641=AXIS2_PLACEMENT_3D ( 'NONE', #251417, #72812, #113190 ) ;
#40651=EDGE_CURVE ( 'NONE', #215460, #1615, #74626, .T. ) ;
#40654=DIRECTION ( 'NONE',  ( 1.000000000000000000, 0.000000000000000000, 0.000000000000000000 ) ) ;
#40664=AXIS2_PLACEMENT_3D ( 'NONE', #103216, #107081, #124103 ) ;
#40674=CARTESIAN_POINT ( 'NONE',  ( 18.42555734704284376, 46.96631509381553116, -255.3401978472650740 ) ) ;
#40719=CARTESIAN_POINT ( 'NONE',  ( 20.94999999999999574, 44.15969672213208241, -258.9565289832007693 ) ) ;
#40723=ORIENTED_EDGE ( 'NONE', *, *, #239867, .F. ) ;
#40758=ADVANCED_FACE ( 'NONE', ( #188930 ), #187037, .T. ) ;
#40769=DIRECTION ( 'NONE',  ( -1.000000000000000000, 0.000000000000000000, 0.000000000000000000 ) ) ;
#40773=PLANE ( 'NONE',  #132473 ) ;
#40777=ORIENTED_EDGE ( 'NONE', *, *, #222705, .F. ) ;
#40783=PLANE ( 'NONE',  #12586 ) ;
#40815=DIRECTION ( 'NONE',  ( 0.000000000000000000, -0.9126074666063660468, -0.4088369013363524762 ) ) ;
#40825=EDGE_CURVE ( 'NONE', #41411, #184585, #111974, .T. ) ;
#40830=AXIS2_PLACEMENT_3D ( 'NONE', #7539, #83191, #25828 ) ;
#40833=EDGE_CURVE ( 'NONE', #241985, #13269, #3648, .T. ) ;
#40834=ORIENTED_EDGE ( 'NONE', *, *, #134216, .T. ) ;
#40877=ORIENTED_EDGE ( 'NONE', *, *, #6994, .T. ) ;
#40894=EDGE_CURVE ( 'NONE', #225601, #74869, #14168, .T. ) ;
#40923=CARTESIAN_POINT ( 'NONE',  ( 21.07954763557290079, 34.01115785052155616, -243.8019369918546317 ) ) ;
#40956=ORIENTED_EDGE ( 'NONE', *, *, #54609, .F. ) ;
#40989=AXIS2_PLACEMENT_3D ( 'NONE', #170096, #228755, #94347 ) ;
#41025=ORIENTED_EDGE ( 'NONE', *, *, #201726, .F. ) ;
#41043=AXIS2_PLACEMENT_3D ( 'NONE', #236, #159342, #137185 ) ;
#41084=FACE_OUTER_BOUND ( 'NONE', #7115, .T. ) ;
#41098=CARTESIAN_POINT ( 'NONE',  ( -20.94999999999999929, 67.67657779757796277, -227.9615671787948372 ) ) ;
#41103=ADVANCED_FACE ( 'NONE', ( #227733 ), #4813, .T. ) ;
#41121=VERTEX_POINT ( 'NONE', #126056 ) ;
#41135=CARTESIAN_POINT ( 'NONE',  ( 20.94999999999999574, 44.06843597547144498, -258.9974126733343951 ) ) ;
#41140=FILL_AREA_STYLE_COLOUR ( '', #152476 ) ;
#41145=CARTESIAN_POINT ( 'NONE',  ( 18.55121869061587958, 68.09900309800710261, -224.1499508721967686 ) ) ;
#41164=CARTESIAN_POINT ( 'NONE',  ( -18.59999999999999787, 36.65892442174472876, -249.5511627012454596 ) ) ;
#41175=CARTESIAN_POINT ( 'NONE',  ( 22.50000000000000000, 25.98655542988603173, -254.2226763854395983 ) ) ;
#41255=CARTESIAN_POINT ( 'NONE',  ( 20.19326291201523205, 39.59028495805256398, -237.1093300823515619 ) ) ;
#41268=ORIENTED_EDGE ( 'NONE', *, *, #26488, .F. ) ;
#41380=LINE ( 'NONE', #251087, #86862 ) ;
#41384=DIRECTION ( 'NONE',  ( 2.915501640297155269E-16, 0.4088369013363274962, -0.9126074666063773710 ) ) ;
#41398=CIRCLE ( 'NONE', #187144, 0.09999999999999481526 ) ;
#41403=CARTESIAN_POINT ( 'NONE',  ( 22.59066674512252604, 31.82725254005531212, -238.8404961800036688 ) ) ;
#41410=FACE_OUTER_BOUND ( 'NONE', #97877, .T. ) ;
#41411=VERTEX_POINT ( 'NONE', #46224 ) ;
#41424=ORIENTED_EDGE ( 'NONE', *, *, #190414, .F. ) ;
#41425=ORIENTED_EDGE ( 'NONE', *, *, #208626, .F. ) ;
#41437=DIRECTION ( 'NONE',  ( 0.000000000000000000, 0.9126074666063783702, 0.4088369013363252757 ) ) ;
#41461=LINE ( 'NONE', #235778, #154476 ) ;
#41471=ORIENTED_EDGE ( 'NONE', *, *, #256119, .T. ) ;
#41472=CARTESIAN_POINT ( 'NONE',  ( 18.59999999999999787, 47.07326788871596790, -255.0992659944397758 ) ) ;
#41483=VERTEX_POINT ( 'NONE', #146592 ) ;
#41494=FACE_OUTER_BOUND ( 'NONE', #202125, .T. ) ;
#41512=ADVANCED_FACE ( 'NONE', ( #164902 ), #127059, .F. ) ;
#41515=LINE ( 'NONE', #83140, #80516 ) ;
#41565=EDGE_CURVE ( 'NONE', #251832, #81533, #68376, .T. ) ;
#41566=DIRECTION ( 'NONE',  ( 0.000000000000000000, 0.4088369013363281623, -0.9126074666063771490 ) ) ;
#41583=ORIENTED_EDGE ( 'NONE', *, *, #228926, .F. ) ;
#41584=ORIENTED_EDGE ( 'NONE', *, *, #2086, .F. ) ;
#41588=ORIENTED_EDGE ( 'NONE', *, *, #73547, .T. ) ;
#41589=ADVANCED_FACE ( 'NONE', ( #50083 ), #255614, .F. ) ;
#41609=CARTESIAN_POINT ( 'NONE',  ( 18.59999999999999787, 47.95459712139159336, -246.5019368548292675 ) ) ;
#41614=ORIENTED_EDGE ( 'NONE', *, *, #212395, .T. ) ;
#41623=AXIS2_PLACEMENT_3D ( 'NONE', #201136, #125467, #146296 ) ;
#41650=CARTESIAN_POINT ( 'NONE',  ( -22.47071067811865319, 33.41224047107334627, -242.5462774987836383 ) ) ;
#41668=ORIENTED_EDGE ( 'NONE', *, *, #167821, .T. ) ;
#41682=DIRECTION ( 'NONE',  ( 0.000000000000000000, 0.1569827930593259702, -0.9876013379310970564 ) ) ;
#41716=CIRCLE ( 'NONE', #45971, 0.09999999999999328870 ) ;
#41737=DIRECTION ( 'NONE',  ( -1.000000000000000000, 0.000000000000000000, 0.000000000000000000 ) ) ;
#41742=VERTEX_POINT ( 'NONE', #200835 ) ;
#41758=DIRECTION ( 'NONE',  ( 0.000000000000000000, -0.4088369013363280513, 0.9126074666063769270 ) ) ;
#41771=CARTESIAN_POINT ( 'NONE',  ( -21.08134388332232589, 30.84685005410138103, -252.0718209705130164 ) ) ;
#41797=( BOUNDED_SURFACE ( )  B_SPLINE_SURFACE ( 3, 2, ( 
 ( #14266, #212460, #155072 ),
 ( #15556, #71671, #10405 ),
 ( #234569, #151198, #173368 ),
 ( #70403, #91221, #190331 ) ),
 .UNSPECIFIED., .F., .F., .F. ) 
 B_SPLINE_SURFACE_WITH_KNOTS ( ( 4, 4 ),
 ( 3, 3 ),
 ( 4.282598581317742514E-18, 0.0003124336117480847335 ),
 ( 0.000000000000000000, 1.000000000000000000 ),
 .UNSPECIFIED. ) 
 GEOMETRIC_REPRESENTATION_ITEM ( )  RATIONAL_B_SPLINE_SURFACE ( (
 ( 1.000000000000000000, 0.7040654476015048013, 1.000000000000000000),
 ( 1.000000000000000000, 0.7039193538783653503, 1.000000000000000000),
 ( 1.000000000000000000, 0.7089171279144677040, 1.000000000000000000),
 ( 1.000000000000000000, 0.7071067811865137109, 1.000000000000000000) ) ) 
 REPRESENTATION_ITEM ( '' )  SURFACE ( )  );
#41799=DIRECTION ( 'NONE',  ( 1.000000000000000000, 0.000000000000000000, 0.000000000000000000 ) ) ;
#41802=ORIENTED_EDGE ( 'NONE', *, *, #116143, .F. ) ;
#41817=AXIS2_PLACEMENT_3D ( 'NONE', #92700, #131835, #227076 ) ;
#41839=EDGE_LOOP ( 'NONE', ( #113298, #18955, #116629, #120693 ) ) ;
#41874=ADVANCED_FACE ( 'NONE', ( #134109 ), #12609, .F. ) ;
#41901=DIRECTION ( 'NONE',  ( -1.000000000000000000, -0.000000000000000000, -0.000000000000000000 ) ) ;
#41907=AXIS2_PLACEMENT_3D ( 'NONE', #250099, #10217, #251371 ) ;
#41908=AXIS2_PLACEMENT_3D ( 'NONE', #182527, #115095, #33041 ) ;
#41939=FACE_OUTER_BOUND ( 'NONE', #65859, .T. ) ;
#41979=CARTESIAN_POINT ( 'NONE',  ( -21.05000000000000071, 43.86852340793510763, -246.3213511806884810 ) ) ;
#41983=CARTESIAN_POINT ( 'NONE',  ( -20.07928932188135107, 52.28206630536941901, -232.4484891355802461 ) ) ;
#41985=EDGE_CURVE ( 'NONE', #28439, #51036, #100036, .T. ) ;
#41988=VERTEX_POINT ( 'NONE', #156076 ) ;
#42028=EDGE_LOOP ( 'NONE', ( #63165, #115313, #183566, #92146 ) ) ;
#42043=EDGE_LOOP ( 'NONE', ( #111940, #190056, #59931, #36495 ) ) ;
#42082=DIRECTION ( 'NONE',  ( 1.000000000000000000, 0.000000000000000000, 0.000000000000000000 ) ) ;
#42096=CARTESIAN_POINT ( 'NONE',  ( 22.39999999999999858, 33.38250548509083870, -242.4821227592188961 ) ) ;
#42138=ADVANCED_FACE ( 'NONE', ( #200304 ), #75154, .T. ) ;
#42140=EDGE_LOOP ( 'NONE', ( #152284, #192627, #114710, #63277, #162262 ) ) ;
#42212=CIRCLE ( 'NONE', #187972, 0.09999999999999854838 ) ;
#42264=EDGE_LOOP ( 'NONE', ( #100498, #110486, #236582, #243709, #161663 ) ) ;
#42307=TOROIDAL_SURFACE ( 'NONE', #221338, 4.149999999999999467, 0.1000000000000000056 ) ;
#42343=CARTESIAN_POINT ( 'NONE',  ( -23.15000000000000213, 42.94327155031035659, -233.8606566173841372 ) ) ;
#42344=EDGE_LOOP ( 'NONE', ( #139516, #92490, #145439, #92046 ) ) ;
#42347=CYLINDRICAL_SURFACE ( 'NONE', #73340, 0.09999999999999681366 ) ;
#42355=ORIENTED_EDGE ( 'NONE', *, *, #182801, .F. ) ;
#42387=VECTOR ( 'NONE', #96456, 1000.000000000000114 ) ;
#42408=ORIENTED_EDGE ( 'NONE', *, *, #12975, .T. ) ;
#42462=EDGE_CURVE ( 'NONE', #9026, #256883, #174577, .T. ) ;
#42474=DIRECTION ( 'NONE',  ( 1.000000000000000000, 0.000000000000000000, 0.000000000000000000 ) ) ;
#42497=CARTESIAN_POINT ( 'NONE',  ( 20.86036036209906186, 39.31301701234226442, -236.7240336282158353 ) ) ;
#42505=ADVANCED_FACE ( 'NONE', ( #2748 ), #116272, .F. ) ;
#42513=DIRECTION ( 'NONE',  ( 0.000000000000000000, 0.9126074666063745955, 0.4088369013363334359 ) ) ;
#42533=EDGE_CURVE ( 'NONE', #13290, #7110, #132840, .T. ) ;
#42588=CIRCLE ( 'NONE', #138426, 0.09999999999999763245 ) ;
#42589=ORIENTED_EDGE ( 'NONE', *, *, #212731, .F. ) ;
#42598=AXIS2_PLACEMENT_3D ( 'NONE', #244315, #83920, #163513 ) ;
#42669=DIRECTION ( 'NONE',  ( 0.000000000000000000, 0.9126074666063844765, 0.4088369013363113980 ) ) ;
#42733=DIRECTION ( 'NONE',  ( 0.000000000000000000, 0.9126074666063757057, 0.4088369013363309379 ) ) ;
#42749=FACE_OUTER_BOUND ( 'NONE', #194374, .T. ) ;
#42791=DIRECTION ( 'NONE',  ( 0.000000000000000000, 0.2716869542551192951, -0.9623856809447951521 ) ) ;
#42805=ORIENTED_EDGE ( 'NONE', *, *, #80041, .T. ) ;
#42815=ORIENTED_EDGE ( 'NONE', *, *, #218107, .T. ) ;
#42816=CYLINDRICAL_SURFACE ( 'NONE', #123795, 11.74999999999999822 ) ;
#42827=DIRECTION ( 'NONE',  ( 1.000000000000000000, 0.000000000000000000, 0.000000000000000000 ) ) ;
#42847=ORIENTED_EDGE ( 'NONE', *, *, #172760, .T. ) ;
#42852=DIRECTION ( 'NONE',  ( -1.000000000000000000, -0.000000000000000000, 0.000000000000000000 ) ) ;
#42871=CARTESIAN_POINT ( 'NONE',  ( 18.37172112093938026, 77.36523961789227144, -241.8027249817224629 ) ) ;
#42880=AXIS2_PLACEMENT_3D ( 'NONE', #213773, #76822, #195522 ) ;
#42962=EDGE_CURVE ( 'NONE', #188456, #232621, #53134, .T. ) ;
#42981=DIRECTION ( 'NONE',  ( 0.000000000000000000, 0.9126074666063769270, 0.4088369013363283844 ) ) ;
#42991=ADVANCED_FACE ( 'NONE', ( #133947 ), #234332, .T. ) ;
#43038=EDGE_CURVE ( 'NONE', #36945, #9091, #166736, .T. ) ;
#43095=EDGE_LOOP ( 'NONE', ( #14599, #3599, #107542, #27701 ) ) ;
#43118=ORIENTED_EDGE ( 'NONE', *, *, #141590, .F. ) ;
#43132=ORIENTED_EDGE ( 'NONE', *, *, #68311, .F. ) ;
#43145=ORIENTED_EDGE ( 'NONE', *, *, #47852, .T. ) ;
#43171=VERTEX_POINT ( 'NONE', #17847 ) ;
#43205=CARTESIAN_POINT ( 'NONE',  ( -20.94999999999999929, 67.65998959290219261, -227.8609496483021530 ) ) ;
#43221=EDGE_CURVE ( 'NONE', #235820, #69009, #158353, .T. ) ;
#43231=CARTESIAN_POINT ( 'NONE',  ( -18.59999999999999787, 67.85909929089923764, -227.8797997985275856 ) ) ;
#43249=CARTESIAN_POINT ( 'NONE',  ( 18.49999999999999289, 55.06386612490207000, -230.0864074704206246 ) ) ;
#43268=DIRECTION ( 'NONE',  ( 0.000000000000000000, 0.9126074666063768159, 0.4088369013363282178 ) ) ;
#43297=LINE ( 'NONE', #65416, #130991 ) ;
#43320=VECTOR ( 'NONE', #53337, 1000.000000000000000 ) ;
#43339=AXIS2_PLACEMENT_3D ( 'NONE', #204754, #163096, #175291 ) ;
#43404=CARTESIAN_POINT ( 'NONE',  ( -20.96428641294048489, 56.19879751616013408, -227.9223442982746803 ) ) ;
#43412=CARTESIAN_POINT ( 'NONE',  ( 21.05000000000000071, 43.47002849391839874, -245.0086825852825143 ) ) ;
#43442=CIRCLE ( 'NONE', #143394, 0.2000000000000048683 ) ;
#43448=ORIENTED_EDGE ( 'NONE', *, *, #209876, .F. ) ;
#43458=AXIS2_PLACEMENT_3D ( 'NONE', #77178, #177606, #257055 ) ;
#43478=ADVANCED_FACE ( 'NONE', ( #34570 ), #114074, .T. ) ;
#43511=CARTESIAN_POINT ( 'NONE',  ( 20.95289811251229750, 40.78188399555352817, -237.9593377293462027 ) ) ;
#43514=DIRECTION ( 'NONE',  ( 0.000000000000000000, 0.9579639084728133192, 0.2868887416116073785 ) ) ;
#43536=ORIENTED_EDGE ( 'NONE', *, *, #122993, .T. ) ;
#43564=DIRECTION ( 'NONE',  ( 1.000000000000000000, 0.000000000000000000, 0.000000000000000000 ) ) ;
#43574=FACE_OUTER_BOUND ( 'NONE', #113045, .T. ) ;
#43587=EDGE_LOOP ( 'NONE', ( #192226, #211990, #32521, #25484, #208304 ) ) ;
#43633=CYLINDRICAL_SURFACE ( 'NONE', #142382, 12.87499999999999822 ) ;
#43647=EDGE_CURVE ( 'NONE', #74878, #242431, #66916, .T. ) ;
#43659=EDGE_CURVE ( 'NONE', #64123, #230182, #30409, .T. ) ;
#43668=DIRECTION ( 'NONE',  ( 0.000000000000000000, 0.9126074666063781482, 0.4088369013363253313 ) ) ;
#43686=PRESENTATION_STYLE_ASSIGNMENT (( #668 ) ) ;
#43699=DIRECTION ( 'NONE',  ( -0.7071067811864846231, -0.2890913453341779626, 0.6453109281989296564 ) ) ;
#43793=DIRECTION ( 'NONE',  ( -0.000000000000000000, -0.9126074666063771490, -0.4088369013363281623 ) ) ;
#43795=EDGE_CURVE ( 'NONE', #176943, #174581, #104485, .T. ) ;
#43796=CIRCLE ( 'NONE', #189562, 11.70000000000000462 ) ;
#43867=CARTESIAN_POINT ( 'NONE',  ( 18.59999999999999076, 43.16354019706792400, -239.5695141926698284 ) ) ;
#43889=ORIENTED_EDGE ( 'NONE', *, *, #225232, .T. ) ;
#43906=CARTESIAN_POINT ( 'NONE',  ( -18.42554971533678909, 46.96631235741502053, -255.3402005058479460 ) ) ;
#43940=DIRECTION ( 'NONE',  ( 1.000000000000000000, 0.000000000000000000, -0.000000000000000000 ) ) ;
#43954=EDGE_CURVE ( 'NONE', #223215, #168134, #175288, .T. ) ;
#43955=CARTESIAN_POINT ( 'NONE',  ( 20.94999999999999929, 67.23127455305835554, -235.8551265064784559 ) ) ;
#43965=CARTESIAN_POINT ( 'NONE',  ( -20.94999999999999929, 44.10931966560507789, -259.0886734199950183 ) ) ;
#43994=DIRECTION ( 'NONE',  ( -1.000000000000000000, -0.000000000000000000, -0.000000000000000000 ) ) ;
#44003=CARTESIAN_POINT ( 'NONE',  ( -21.53752568622177677, 30.42476846892962072, -252.2355353702321850 ) ) ;
#44004=AXIS2_PLACEMENT_3D ( 'NONE', #177804, #257261, #59074 ) ;
#44009=ORIENTED_EDGE ( 'NONE', *, *, #186560, .F. ) ;
#44054=VERTEX_POINT ( 'NONE', #47063 ) ;
#44070=CARTESIAN_POINT ( 'NONE',  ( -21.14999999999999858, 30.68987205111127281, -252.2252246220829193 ) ) ;
#44083=VECTOR ( 'NONE', #253666, 1000.000000000000000 ) ;
#44135=ORIENTED_EDGE ( 'NONE', *, *, #140931, .T. ) ;
#44150=ORIENTED_EDGE ( 'NONE', *, *, #94197, .T. ) ;
#44156=CARTESIAN_POINT ( 'NONE',  ( -18.50000000000000000, 46.45388641681647357, -243.1520440498138385 ) ) ;
#44158=CARTESIAN_POINT ( 'NONE',  ( -23.15000000000000213, 54.34471204062663219, -239.4366250215122420 ) ) ;
#44164=CARTESIAN_POINT ( 'NONE',  ( 18.50000000000000355, 77.44184265367995579, -241.6694879557322793 ) ) ;
#44173=ORIENTED_EDGE ( 'NONE', *, *, #205971, .F. ) ;
#44206=DIRECTION ( 'NONE',  ( 1.000000000000000000, 0.000000000000000000, 0.000000000000000000 ) ) ;
#44239=ORIENTED_EDGE ( 'NONE', *, *, #221267, .F. ) ;
#44246=DIRECTION ( 'NONE',  ( 1.000000000000000000, 0.000000000000000000, 0.000000000000000000 ) ) ;
#44287=CARTESIAN_POINT ( 'NONE',  ( -18.49999999999999289, 77.31516873553810854, -241.6587350081051113 ) ) ;
#44309=ORIENTED_EDGE ( 'NONE', *, *, #76106, .F. ) ;
#44326=CARTESIAN_POINT ( 'NONE',  ( -21.12757541349819590, 30.74915888275712206, -252.1930093910820290 ) ) ;
#44341=EDGE_CURVE ( 'NONE', #104038, #43171, #46437, .T. ) ;
#44345=DIRECTION ( 'NONE',  ( 0.000000000000000000, 0.9126074666063545004, 0.4088369013363783999 ) ) ;
#44357=EDGE_CURVE ( 'NONE', #209494, #99525, #45163, .T. ) ;
#44359=ORIENTED_EDGE ( 'NONE', *, *, #184474, .F. ) ;
#44362=CIRCLE ( 'NONE', #198279, 0.2000000000000048683 ) ;
#44368=CONICAL_SURFACE ( 'NONE', #248353, 6.250000000000000888, 0.7853981633974431720 ) ;
#44382=ORIENTED_EDGE ( 'NONE', *, *, #53541, .T. ) ;
#44424=CIRCLE ( 'NONE', #198346, 0.09999999999999108213 ) ;
#44437=ADVANCED_FACE ( 'NONE', ( #152001 ), #227644, .T. ) ;
#44438=ORIENTED_EDGE ( 'NONE', *, *, #163631, .T. ) ;
#44440=VECTOR ( 'NONE', #193606, 1000.000000000000000 ) ;
#44446=ORIENTED_EDGE ( 'NONE', *, *, #193634, .F. ) ;
#44464=ORIENTED_EDGE ( 'NONE', *, *, #6082, .F. ) ;
#44472=DIRECTION ( 'NONE',  ( 1.000000000000000000, 0.000000000000000000, 0.000000000000000000 ) ) ;
#44511=EDGE_CURVE ( 'NONE', #239535, #108899, #217284, .T. ) ;
#44512=CIRCLE ( 'NONE', #190253, 0.09999999999999939493 ) ;
#44528=VECTOR ( 'NONE', #60033, 1000.000000000000000 ) ;
#44598=DIRECTION ( 'NONE',  ( 0.000000000000000000, 0.9126074666063769270, 0.4088369013363280513 ) ) ;
#44618=ORIENTED_EDGE ( 'NONE', *, *, #129281, .T. ) ;
#44627=DIRECTION ( 'NONE',  ( 0.000000000000000000, -0.9955484899852913294, 0.09425075112701486457 ) ) ;
#44628=CARTESIAN_POINT ( 'NONE',  ( 23.14999999999998437, 36.65892442174472876, -249.5511627012454596 ) ) ;
#44641=ORIENTED_EDGE ( 'NONE', *, *, #178076, .F. ) ;
#44648=CARTESIAN_POINT ( 'NONE',  ( 18.52130828395272033, 46.94588606482535909, -255.3320774683811010 ) ) ;
#44668=EDGE_CURVE ( 'NONE', #212825, #144138, #104846, .T. ) ;
#44670=AXIS2_PLACEMENT_3D ( 'NONE', #86551, #146534, #44894 ) ;
#44706=DIRECTION ( 'NONE',  ( -1.000000000000000000, -0.000000000000000000, -0.000000000000000000 ) ) ;
#44709=ORIENTED_EDGE ( 'NONE', *, *, #223, .F. ) ;
#44714=DIRECTION ( 'NONE',  ( 0.000000000000000000, -0.9126074666063660468, -0.4088369013363524762 ) ) ;
#44739=AXIS2_PLACEMENT_3D ( 'NONE', #32234, #253809, #191320 ) ;
#44777=CARTESIAN_POINT ( 'NONE',  ( 22.39999999999999503, 31.80471377451587500, -238.9601694054147742 ) ) ;
#44782=CARTESIAN_POINT ( 'NONE',  ( 23.14999999999999503, 42.98415524044398950, -233.9519173640447889 ) ) ;
#44790=PLANE ( 'NONE',  #240908 ) ;
#44800=VERTEX_POINT ( 'NONE', #52554 ) ;
#44817=CARTESIAN_POINT ( 'NONE',  ( -20.64999999999999858, 49.36776662947724503, -253.7196102226803021 ) ) ;
#44825=ORIENTED_EDGE ( 'NONE', *, *, #67567, .F. ) ;
#44839=DIRECTION ( 'NONE',  ( -0.000000000000000000, -0.9126074666063770380, -0.4088369013363281068 ) ) ;
#44867=CARTESIAN_POINT ( 'NONE',  ( -20.85000000000000142, 74.98773774893902555, -233.8732236541320333 ) ) ;
#44869=DIRECTION ( 'NONE',  ( 0.000000000000000000, 0.9126074666063769270, 0.4088369013363280513 ) ) ;
#44875=LINE ( 'NONE', #61873, #183474 ) ;
#44887=FACE_OUTER_BOUND ( 'NONE', #183879, .T. ) ;
#44894=DIRECTION ( 'NONE',  ( 0.000000000000000000, 0.2818822000686317941, -0.9594490217226071538 ) ) ;
#44948=EDGE_CURVE ( 'NONE', #26849, #33224, #237632, .T. ) ;
#44952=CARTESIAN_POINT ( 'NONE',  ( 20.94999999999999574, 43.57281345108133053, -239.9888335660389487 ) ) ;
#44957=EDGE_LOOP ( 'NONE', ( #59405, #46129, #116523, #81207 ) ) ;
#44968=EDGE_CURVE ( 'NONE', #109005, #214500, #88470, .T. ) ;
#44999=CARTESIAN_POINT ( 'NONE',  ( 22.45301702632625762, 26.02101828454447485, -254.3001460930269673 ) ) ;
#45045=CARTESIAN_POINT ( 'NONE',  ( 21.04999999999999716, 39.24426575657115279, -236.8395263841964038 ) ) ;
#45049=DIRECTION ( 'NONE',  ( 2.879366945564059217E-14, 0.2599159095383297702, -0.9656312546561770516 ) ) ;
#45097=CIRCLE ( 'NONE', #190882, 2.000000000000001776 ) ;
#45107=CIRCLE ( 'NONE', #245023, 11.64999999999999680 ) ;
#45143=DIRECTION ( 'NONE',  ( 1.000000000000000000, 0.000000000000000000, 0.000000000000000000 ) ) ;
#45163=LINE ( 'NONE', #3459, #167275 ) ;
#45179=DIRECTION ( 'NONE',  ( 1.000000000000000000, 0.000000000000000000, 0.000000000000000000 ) ) ;
#45182=EDGE_CURVE ( 'NONE', #233399, #51812, #247440, .T. ) ;
#45207=LINE ( 'NONE', #249837, #44083 ) ;
#45215=AXIS2_PLACEMENT_3D ( 'NONE', #18255, #116082, #117359 ) ;
#45260=DIRECTION ( 'NONE',  ( 2.694716079187273932E-16, 0.4088369013363286064, -0.9126074666063768159 ) ) ;
#45269=CARTESIAN_POINT ( 'NONE',  ( -22.48660254037843487, 31.85034414784621148, -238.9397275603479898 ) ) ;
#45273=CARTESIAN_POINT ( 'NONE',  ( -20.94999999999999929, 63.58084468663284383, -237.4904741118237723 ) ) ;
#45289=CIRCLE ( 'NONE', #191063, 0.1000000000000024342 ) ;
#45291=CARTESIAN_POINT ( 'NONE',  ( -21.46681500598551651, 30.40070853532066408, -252.3547663145424451 ) ) ;
#45305=DIRECTION ( 'NONE',  ( 0.000000000000000000, 0.9126074666064696306, 0.4088369013361212723 ) ) ;
#45331=FACE_OUTER_BOUND ( 'NONE', #204207, .T. ) ;
#45338=ORIENTED_EDGE ( 'NONE', *, *, #705, .F. ) ;
#45348=AXIS2_PLACEMENT_3D ( 'NONE', #65300, #163138, #44472 ) ;
#45375=EDGE_LOOP ( 'NONE', ( #32256, #31580, #130456, #48097 ) ) ;
#45436=CARTESIAN_POINT ( 'NONE',  ( 18.50000000000000355, 77.31102155260600739, -241.6627732871349963 ) ) ;
#45460=AXIS2_PLACEMENT_3D ( 'NONE', #215125, #54758, #134284 ) ;
#45467=CARTESIAN_POINT ( 'NONE',  ( 18.39999999999999858, 77.13860723519891849, -241.8264964602989266 ) ) ;
#45481=DIRECTION ( 'NONE',  ( 0.000000000000000000, 0.4088369013363281068, -0.9126074666063770380 ) ) ;
#45483=ADVANCED_FACE ( 'NONE', ( #225284 ), #88335, .T. ) ;
#45494=EDGE_CURVE ( 'NONE', #60194, #45673, #148343, .T. ) ;
#45505=EDGE_CURVE ( 'NONE', #238500, #23132, #130043, .T. ) ;
#45506=CYLINDRICAL_SURFACE ( 'NONE', #245371, 4.000000000000002665 ) ;
#45536=CARTESIAN_POINT ( 'NONE',  ( 20.95052659398289308, 39.28760495060160451, -236.8901595946551311 ) ) ;
#45583=ORIENTED_EDGE ( 'NONE', *, *, #25153, .F. ) ;
#45609=DIRECTION ( 'NONE',  ( 1.000000000000000000, 0.000000000000000000, 0.000000000000000000 ) ) ;
#45623=AXIS2_PLACEMENT_3D ( 'NONE', #230454, #127504, #87065 ) ;
#45638=DIRECTION ( 'NONE',  ( -1.000000000000000000, -0.000000000000000000, 0.000000000000000000 ) ) ;
#45651=ORIENTED_EDGE ( 'NONE', *, *, #256209, .T. ) ;
#45655=CARTESIAN_POINT ( 'NONE',  ( -22.39999999999999858, 26.02743912001966464, -254.3139371321002216 ) ) ;
#45673=VERTEX_POINT ( 'NONE', #170294 ) ;
#45712=CARTESIAN_POINT ( 'NONE',  ( -23.15000000000000213, 54.22301550979020845, -237.0256805049050115 ) ) ;
#45725=FACE_OUTER_BOUND ( 'NONE', #241970, .T. ) ;
#45740=CARTESIAN_POINT ( 'NONE',  ( -21.45000000000000284, 44.68681448124952027, -237.5080042326551393 ) ) ;
#45746=DIRECTION ( 'NONE',  ( 0.000000000000000000, -0.9947597004326491632, 0.1022405907413782566 ) ) ;
#45765=DIRECTION ( 'NONE',  ( 2.952720810173289112E-16, 0.4088369013363281068, -0.9126074666063770380 ) ) ;
#45844=CARTESIAN_POINT ( 'NONE',  ( 23.24999999999999289, 42.98415524044398950, -233.9519173640447889 ) ) ;
#45847=ORIENTED_EDGE ( 'NONE', *, *, #160066, .F. ) ;
#45859=VERTEX_POINT ( 'NONE', #83929 ) ;
#45876=ORIENTED_EDGE ( 'NONE', *, *, #79127, .T. ) ;
#45903=DIRECTION ( 'NONE',  ( 0.000000000000000000, 0.9126074666063545004, 0.4088369013363783999 ) ) ;
#45922=ORIENTED_EDGE ( 'NONE', *, *, #187492, .F. ) ;
#45934=CARTESIAN_POINT ( 'NONE',  ( 23.14999999999999858, 53.86595165227826243, -236.3638196928718855 ) ) ;
#45944=ORIENTED_EDGE ( 'NONE', *, *, #82268, .F. ) ;
#45961=LINE ( 'NONE', #198609, #197267 ) ;
#45965=DIRECTION ( 'NONE',  ( 1.000000000000000000, 0.000000000000000000, 0.000000000000000000 ) ) ;
#45966=CARTESIAN_POINT ( 'NONE',  ( -20.94999999999999929, 56.27731819600170837, -227.9967441372480721 ) ) ;
#45971=AXIS2_PLACEMENT_3D ( 'NONE', #47028, #225655, #246526 ) ;
#45990=ORIENTED_EDGE ( 'NONE', *, *, #87384, .T. ) ;
#45998=EDGE_CURVE ( 'NONE', #21929, #231005, #1543, .T. ) ;
#46025=AXIS2_PLACEMENT_3D ( 'NONE', #143817, #25193, #145103 ) ;
#46026=ADVANCED_FACE ( 'NONE', ( #248201 ), #64103, .F. ) ;
#46060=DIRECTION ( 'NONE',  ( 2.952720810173289112E-16, 0.4088369013363246096, -0.9126074666063785923 ) ) ;
#46129=ORIENTED_EDGE ( 'NONE', *, *, #154558, .T. ) ;
#46151=ORIENTED_EDGE ( 'NONE', *, *, #87384, .F. ) ;
#46205=CIRCLE ( 'NONE', #12938, 0.1000000000000032113 ) ;
#46224=CARTESIAN_POINT ( 'NONE',  ( 20.84999999999998721, 72.03510814376021187, -246.5782642391033903 ) ) ;
#46236=DIRECTION ( 'NONE',  ( -3.265361837132813093E-16, -0.4088369013363281068, 0.9126074666063770380 ) ) ;
#46252=DIRECTION ( 'NONE',  ( 0.000000000000000000, -0.9126074666063770380, -0.4088369013363281068 ) ) ;
#46277=CARTESIAN_POINT ( 'NONE',  ( 20.92356734117541706, 68.07764576057049055, -224.1679995073710359 ) ) ;
#46317=DIRECTION ( 'NONE',  ( 0.000000000000000000, -0.4088369013362748716, 0.9126074666064009078 ) ) ;
#46339=DIRECTION ( 'NONE',  ( 0.000000000000000000, 0.9126074666063844765, 0.4088369013363114535 ) ) ;
#46362=ORIENTED_EDGE ( 'NONE', *, *, #97929, .T. ) ;
#46369=DIRECTION ( 'NONE',  ( 0.000000000000000000, 0.9126074666063771490, 0.4088369013363281623 ) ) ;
#46394=EDGE_CURVE ( 'NONE', #65298, #241398, #5816, .T. ) ;
#46437=LINE ( 'NONE', #201667, #146371 ) ;
#46442=ORIENTED_EDGE ( 'NONE', *, *, #183670, .T. ) ;
#46457=FACE_OUTER_BOUND ( 'NONE', #25357, .T. ) ;
#46466=FACE_OUTER_BOUND ( 'NONE', #227400, .T. ) ;
#46468=DIRECTION ( 'NONE',  ( 0.000000000000000000, 0.9594490217226104845, 0.2818822000686205254 ) ) ;
#46472=CARTESIAN_POINT ( 'NONE',  ( 18.59999999999999076, 55.07231556048840559, -230.1160242994351108 ) ) ;
#46483=ORIENTED_EDGE ( 'NONE', *, *, #80063, .T. ) ;
#46514=DIRECTION ( 'NONE',  ( 1.836970198721030427E-16, 0.4088369013363281623, -0.9126074666063771490 ) ) ;
#46520=FACE_OUTER_BOUND ( 'NONE', #116178, .T. ) ;
#46522=ORIENTED_EDGE ( 'NONE', *, *, #73466, .F. ) ;
#46552=DIRECTION ( 'NONE',  ( 1.000000000000000000, 0.000000000000000000, 0.000000000000000000 ) ) ;
#46568=ORIENTED_EDGE ( 'NONE', *, *, #249066, .T. ) ;
#46574=DIRECTION ( 'NONE',  ( 1.000000000000000000, 0.000000000000000000, 0.000000000000000000 ) ) ;
#46579=EDGE_LOOP ( 'NONE', ( #126097, #172052, #30972, #251760 ) ) ;
#46620=ORIENTED_EDGE ( 'NONE', *, *, #153324, .T. ) ;
#46640=AXIS2_PLACEMENT_3D ( 'NONE', #216422, #147154, #224120 ) ;
#46657=AXIS2_PLACEMENT_3D ( 'NONE', #44158, #124976, #244908 ) ;
#46662=ADVANCED_FACE ( 'NONE', ( #49046 ), #14242, .F. ) ;
#46666=CARTESIAN_POINT ( 'NONE',  ( 23.15000000000000213, 41.42187432231295219, -260.1830396872097140 ) ) ;
#46679=CIRCLE ( 'NONE', #192443, 12.87499999999999112 ) ;
#46724=DIRECTION ( 'NONE',  ( 0.000000000000000000, -0.4088369013363282178, 0.9126074666063770380 ) ) ;
#46747=CARTESIAN_POINT ( 'NONE',  ( -21.55000000000000071, 44.96555909964510533, -237.8856228368455845 ) ) ;
#46750=EDGE_LOOP ( 'NONE', ( #27753, #113127, #127471, #147072, #20196, #79643, #36893 ) ) ;
#46763=CARTESIAN_POINT ( 'NONE',  ( -21.55000000000000426, 44.77807522791015060, -237.4671205425215135 ) ) ;
#46801=ORIENTED_EDGE ( 'NONE', *, *, #116816, .F. ) ;
#46805=EDGE_CURVE ( 'NONE', #123266, #116784, #56716, .T. ) ;
#46826=ORIENTED_EDGE ( 'NONE', *, *, #112974, .F. ) ;
#46827=DIRECTION ( 'NONE',  ( 0.000000000000000000, 0.9126074666063771490, 0.4088369013363276627 ) ) ;
#46828=CARTESIAN_POINT ( 'NONE',  ( -21.05000000000000071, 44.43513953521873106, -247.3415577889845736 ) ) ;
#46832=ORIENTED_EDGE ( 'NONE', *, *, #91621, .T. ) ;
#46847=EDGE_LOOP ( 'NONE', ( #97130, #106771, #205278, #206668 ) ) ;
#46850=ORIENTED_EDGE ( 'NONE', *, *, #215560, .T. ) ;
#46899=CIRCLE ( 'NONE', #130112, 4.049999999999974953 ) ;
#46950=VERTEX_POINT ( 'NONE', #25362 ) ;
#46952=EDGE_LOOP ( 'NONE', ( #220514, #137935, #173632, #164873 ) ) ;
#46991=ORIENTED_EDGE ( 'NONE', *, *, #248291, .T. ) ;
#46993=EDGE_LOOP ( 'NONE', ( #21407, #103259, #247104, #193102 ) ) ;
#47001=DIRECTION ( 'NONE',  ( 0.000000000000000000, -0.9126074666063757057, -0.4088369013363309379 ) ) ;
#47003=VECTOR ( 'NONE', #91363, 1000.000000000000000 ) ;
#47007=DIRECTION ( 'NONE',  ( 0.000000000000000000, 0.9126074666063660468, 0.4088369013363524762 ) ) ;
#47028=CARTESIAN_POINT ( 'NONE',  ( -22.39999999999999858, 29.50811709945089945, -252.6450601445781103 ) ) ;
#47037=CARTESIAN_POINT ( 'NONE',  ( 21.53699400388664031, 30.46440795807615132, -252.3262297578936568 ) ) ;
#47058=ORIENTED_EDGE ( 'NONE', *, *, #68582, .F. ) ;
#47063=CARTESIAN_POINT ( 'NONE',  ( 21.05000000000000071, 45.73145985849338047, -239.4600911154851133 ) ) ;
#47078=CARTESIAN_POINT ( 'NONE',  ( 22.50000000000000000, 31.80488924422933295, -238.9605610896540213 ) ) ;
#47115=CARTESIAN_POINT ( 'NONE',  ( 22.60000000000000142, 36.65892442174472876, -249.5511627012454596 ) ) ;
#47144=ORIENTED_EDGE ( 'NONE', *, *, #202580, .F. ) ;
#47150=EDGE_CURVE ( 'NONE', #50249, #9758, #126445, .T. ) ;
#47158=( BOUNDED_SURFACE ( )  B_SPLINE_SURFACE ( 3, 2, ( 
 ( #215457, #98046, #36864 ),
 ( #74715, #116377, #195921 ),
 ( #177655, #158106, #43249 ),
 ( #141070, #118948, #202317 ),
 ( #64091, #143621, #201035 ),
 ( #124082, #223151, #256 ) ),
 .UNSPECIFIED., .F., .F., .T. ) 
 B_SPLINE_SURFACE_WITH_KNOTS ( ( 4, 2, 4 ),
 ( 3, 3 ),
 ( 3.141592653589804662, 3.926990816987256494, 4.712388980384708326 ),
 ( 0.000000000000000000, 1.000000000000000000 ),
 .UNSPECIFIED. ) 
 GEOMETRIC_REPRESENTATION_ITEM ( )  RATIONAL_B_SPLINE_SURFACE ( (
 ( 1.000000000000000000, 0.9238795325113159373, 1.000000000000000000),
 ( 1.000000000000000000, 0.9240297172245346413, 1.000000000000000000),
 ( 1.000000000000000000, 0.9038128468036756846, 1.000000000000000000),
 ( 1.000000000000000000, 0.8282379607651599862, 1.000000000000000000),
 ( 1.000000000000000000, 0.7727932973488951252, 1.000000000000000000),
 ( 1.000000000000000000, 0.7071067811865977548, 1.000000000000000000) ) ) 
 REPRESENTATION_ITEM ( '' )  SURFACE ( )  );
#47170=ORIENTED_EDGE ( 'NONE', *, *, #36347, .F. ) ;
#47191=CIRCLE ( 'NONE', #205402, 7.899999999999995914 ) ;
#47202=AXIS2_PLACEMENT_3D ( 'NONE', #31701, #211599, #188183 ) ;
#47213=CIRCLE ( 'NONE', #147199, 0.09999999999999939493 ) ;
#47252=CARTESIAN_POINT ( 'NONE',  ( 20.01093837587850288, 54.44613876119747431, -228.7075138270121215 ) ) ;
#47265=CARTESIAN_POINT ( 'NONE',  ( 20.97224591636398827, 43.49434346882816271, -234.8463466113539653 ) ) ;
#47266=VERTEX_POINT ( 'NONE', #116444 ) ;
#47295=ORIENTED_EDGE ( 'NONE', *, *, #71953, .F. ) ;
#47298=CARTESIAN_POINT ( 'NONE',  ( -20.00857864376270001, 52.17883100310857003, -232.4626431718731396 ) ) ;
#47320=LINE ( 'NONE', #224681, #73154 ) ;
#47325=VERTEX_POINT ( 'NONE', #184102 ) ;
#47368=CARTESIAN_POINT ( 'NONE',  ( 21.05000000000000071, 53.66153320161009788, -235.9075159595686841 ) ) ;
#47417=ORIENTED_EDGE ( 'NONE', *, *, #172587, .T. ) ;
#47464=CARTESIAN_POINT ( 'NONE',  ( -18.59999999999999787, 44.14788529697245423, -236.0604079036328073 ) ) ;
#47467=EDGE_LOOP ( 'NONE', ( #251401, #40877, #33894 ) ) ;
#47492=DIRECTION ( 'NONE',  ( 1.000000000000000000, 0.000000000000000000, 0.000000000000000000 ) ) ;
#47505=CIRCLE ( 'NONE', #239068, 0.4000000000000097367 ) ;
#47507=DIRECTION ( 'NONE',  ( 0.000000000000000000, 0.9126074666063660468, 0.4088369013363524762 ) ) ;
#47527=ORIENTED_EDGE ( 'NONE', *, *, #122347, .F. ) ;
#47538=CARTESIAN_POINT ( 'NONE',  ( -23.25000000000000000, 26.06832281015329755, -254.4051978787608732 ) ) ;
#47546=AXIS2_PLACEMENT_3D ( 'NONE', #123800, #42981, #143348 ) ;
#47549=CARTESIAN_POINT ( 'NONE',  ( 18.59999999999999076, 51.96945017402672562, -231.5060697639786440 ) ) ;
#47551=AXIS2_PLACEMENT_3D ( 'NONE', #119001, #159413, #172907 ) ;
#47572=AXIS2_PLACEMENT_3D ( 'NONE', #200079, #94542, #134933 ) ;
#47598=DIRECTION ( 'NONE',  ( 0.000000000000000000, 0.9126074666063660468, 0.4088369013363524762 ) ) ;
#47599=CARTESIAN_POINT ( 'NONE',  ( 20.94999999999999929, 62.24653955602229161, -247.9500786234238490 ) ) ;
#47609=ORIENTED_EDGE ( 'NONE', *, *, #207621, .T. ) ;
#47615=DIRECTION ( 'NONE',  ( 1.000000000000000000, -0.000000000000000000, -0.000000000000000000 ) ) ;
#47618=EDGE_CURVE ( 'NONE', #105021, #76006, #9780, .T. ) ;
#47625=CARTESIAN_POINT ( 'NONE',  ( -21.93642651522410247, 33.66330848088261263, -242.8643360821705528 ) ) ;
#47646=CARTESIAN_POINT ( 'NONE',  ( -21.05000000000000071, 69.08367151115869831, -247.5088222940653679 ) ) ;
#47685=DIRECTION ( 'NONE',  ( -0.000000000000000000, 0.5283051335749948674, -0.8490545835447252943 ) ) ;
#47721=AXIS2_PLACEMENT_3D ( 'NONE', #62569, #85942, #41737 ) ;
#47735=DIRECTION ( 'NONE',  ( 1.000000000000000000, 0.000000000000000000, 0.000000000000000000 ) ) ;
#47755=CARTESIAN_POINT ( 'NONE',  ( -18.59999999999999787, 44.05662455031180968, -236.1012915937664616 ) ) ;
#47781=EDGE_LOOP ( 'NONE', ( #125482, #169566, #254018, #211583, #22556 ) ) ;
#47805=CIRCLE ( 'NONE', #72804, 0.09999999999999950595 ) ;
#47806=EDGE_CURVE ( 'NONE', #86798, #210461, #64086, .T. ) ;
#47809=DIRECTION ( 'NONE',  ( 1.000000000000000000, 0.000000000000000000, 0.000000000000000000 ) ) ;
#47816=AXIS2_PLACEMENT_3D ( 'NONE', #201512, #179408, #64570 ) ;
#47819=LINE ( 'NONE', #10001, #34529 ) ;
#47826=CARTESIAN_POINT ( 'NONE',  ( 21.05000000000000071, 61.88149656937974896, -248.1136133839584090 ) ) ;
#47827=EDGE_LOOP ( 'NONE', ( #148577, #243529, #139538, #391 ) ) ;
#47836=ORIENTED_EDGE ( 'NONE', *, *, #93988, .T. ) ;
#47852=EDGE_CURVE ( 'NONE', #40222, #782, #112915, .T. ) ;
#47869=CARTESIAN_POINT ( 'NONE',  ( 21.08479644141222664, 30.84445554993508765, -252.0918114234447671 ) ) ;
#47894=CARTESIAN_POINT ( 'NONE',  ( -23.15000000000000213, 46.23295349378772556, -240.7147059833253309 ) ) ;
#47900=ORIENTED_EDGE ( 'NONE', *, *, #218872, .F. ) ;
#47919=EDGE_LOOP ( 'NONE', ( #29343, #9848, #104594, #257752 ) ) ;
#47948=ORIENTED_EDGE ( 'NONE', *, *, #134216, .F. ) ;
#47949=DIRECTION ( 'NONE',  ( 1.000000000000000000, 0.000000000000000000, 0.000000000000000000 ) ) ;
#47998=VERTEX_POINT ( 'NONE', #237982 ) ;
#48036=DIRECTION ( 'NONE',  ( -2.952720810173289112E-16, -0.4088369013363282733, 0.9126074666063769270 ) ) ;
#48045=CARTESIAN_POINT ( 'NONE',  ( 18.59999999999999076, 46.45388641681647357, -243.1520440498138385 ) ) ;
#48056=CARTESIAN_POINT ( 'NONE',  ( 21.05000000000000071, 49.53130139001177668, -254.0846532093228802 ) ) ;
#48089=LINE ( 'NONE', #63812, #60928 ) ;
#48097=ORIENTED_EDGE ( 'NONE', *, *, #251535, .T. ) ;
#48102=CIRCLE ( 'NONE', #235353, 0.1000000000000028227 ) ;
#48118=DIRECTION ( 'NONE',  ( 0.000000000000000000, 0.3116596277708286733, 0.9501938099239273239 ) ) ;
#48125=CARTESIAN_POINT ( 'NONE',  ( -23.15000000000000213, 67.23127455305835554, -235.8551265064784559 ) ) ;
#48156=CARTESIAN_POINT ( 'NONE',  ( 21.13461538461538325, 43.58999342716158765, -234.8150793036844846 ) ) ;
#48163=ORIENTED_EDGE ( 'NONE', *, *, #217152, .T. ) ;
#48173=DIRECTION ( 'NONE',  ( 0.000000000000000000, -0.9126074666063767049, -0.4088369013363286619 ) ) ;
#48234=EDGE_LOOP ( 'NONE', ( #240136, #81587, #236487, #207226, #165582, #35480, #249533, #57741, #240774, #204642, #86484, #67531, #184029, #124267, #25776, #46850, #199703, #55487, #180423, #12315, #63463, #153691, #29731, #81508, #128071, #88696, #219386 ) ) ;
#48244=LINE ( 'NONE', #166950, #237536 ) ;
#48258=CARTESIAN_POINT ( 'NONE',  ( 23.14999999999999503, 51.38014393322265505, -230.1906178717505327 ) ) ;
#48273=EDGE_LOOP ( 'NONE', ( #249858, #34209 ) ) ;
#48299=TOROIDAL_SURFACE ( 'NONE', #110838, 0.2000000000000000111, 0.1000000000000000056 ) ;
#48313=AXIS2_PLACEMENT_3D ( 'NONE', #64411, #213523, #59555 ) ;
#48318=FACE_OUTER_BOUND ( 'NONE', #151530, .T. ) ;
#48340=DIRECTION ( 'NONE',  ( 0.000000000000000000, -0.9126074666063774821, -0.4088369013363273297 ) ) ;
#48342=VERTEX_POINT ( 'NONE', #95612 ) ;
#48381=LINE ( 'NONE', #27586, #228411 ) ;
#48423=CARTESIAN_POINT ( 'NONE',  ( -18.51697539158856998, 68.06642993404716435, -224.1774859612004036 ) ) ;
#48435=AXIS2_PLACEMENT_3D ( 'NONE', #249672, #150570, #91870 ) ;
#48464=AXIS2_PLACEMENT_3D ( 'NONE', #105216, #141816, #200517 ) ;
#48475=DIRECTION ( 'NONE',  ( -1.000000000000000000, -0.000000000000000000, 0.000000000000000000 ) ) ;
#48493=CIRCLE ( 'NONE', #36033, 0.2000000000000048683 ) ;
#48558=VERTEX_POINT ( 'NONE', #168487 ) ;
#48598=ORIENTED_EDGE ( 'NONE', *, *, #100024, .T. ) ;
#48604=DIRECTION ( 'NONE',  ( 1.000000000000000000, 0.000000000000000000, 0.000000000000000000 ) ) ;
#48609=EDGE_LOOP ( 'NONE', ( #114080, #17221, #94921, #28025 ) ) ;
#48614=CYLINDRICAL_SURFACE ( 'NONE', #154031, 0.09999999999999939493 ) ;
#48640=ORIENTED_EDGE ( 'NONE', *, *, #95572, .T. ) ;
#48655=CARTESIAN_POINT ( 'NONE',  ( 23.25000000000000000, 52.55093873171406216, -255.3069320826340061 ) ) ;
#48659=CARTESIAN_POINT ( 'NONE',  ( 21.09787244211748458, 44.24086307789509931, -236.5388354431762536 ) ) ;
#48703=ORIENTED_EDGE ( 'NONE', *, *, #252854, .T. ) ;
#48731=CARTESIAN_POINT ( 'NONE',  ( 18.49999999999999645, 74.73788286442776041, -233.7359682632885267 ) ) ;
#48754=CARTESIAN_POINT ( 'NONE',  ( -21.05000000000000071, 44.12194005689738674, -258.6913704466671788 ) ) ;
#48758=AXIS2_PLACEMENT_3D ( 'NONE', #133422, #132135, #192130 ) ;
#48760=VECTOR ( 'NONE', #119151, 1000.000000000000000 ) ;
#48772=CARTESIAN_POINT ( 'NONE',  ( 20.85000000000000142, 78.45218979564165807, -232.7313097695096076 ) ) ;
#48810=AXIS2_PLACEMENT_3D ( 'NONE', #128156, #169892, #188120 ) ;
#48826=LINE ( 'NONE', #85354, #60740 ) ;
#48879=CIRCLE ( 'NONE', #103033, 0.1000000000000065836 ) ;
#48893=CARTESIAN_POINT ( 'NONE',  ( 21.05000000000000071, 39.15968973805286168, -236.7234144681435453 ) ) ;
#48931=CARTESIAN_POINT ( 'NONE',  ( 18.59999999999999076, 43.12265650693429819, -239.4782534460092052 ) ) ;
#48939=ORIENTED_EDGE ( 'NONE', *, *, #88236, .F. ) ;
#48944=EDGE_CURVE ( 'NONE', #247446, #148383, #123551, .T. ) ;
#48951=EDGE_CURVE ( 'NONE', #215984, #71691, #52797, .T. ) ;
#48964=FACE_OUTER_BOUND ( 'NONE', #223750, .T. ) ;
#48965=AXIS2_PLACEMENT_3D ( 'NONE', #112322, #234824, #75761 ) ;
#49001=AXIS2_PLACEMENT_3D ( 'NONE', #119271, #56674, #157120 ) ;
#49030=DIRECTION ( 'NONE',  ( 0.000000000000000000, -0.9126074666063660468, -0.4088369013363524762 ) ) ;
#49044=ADVANCED_FACE ( 'NONE', ( #208561 ), #98929, .T. ) ;
#49046=FACE_OUTER_BOUND ( 'NONE', #18364, .T. ) ;
#49054=CARTESIAN_POINT ( 'NONE',  ( -20.94999999999999929, 43.39316802731212874, -245.2602608822587342 ) ) ;
#49071=ORIENTED_EDGE ( 'NONE', *, *, #19128, .T. ) ;
#49084=LINE ( 'NONE', #213290, #232773 ) ;
#49089=SPHERICAL_SURFACE ( 'NONE', #249872, 0.1000000000000000056 ) ;
#49133=DIRECTION ( 'NONE',  ( 0.000000000000000000, -0.9579639084728133192, -0.2868887416116073785 ) ) ;
#49155=FACE_OUTER_BOUND ( 'NONE', #188507, .T. ) ;
#49172=ORIENTED_EDGE ( 'NONE', *, *, #255430, .T. ) ;
#49178=VECTOR ( 'NONE', #173435, 1000.000000000000000 ) ;
#49292=CIRCLE ( 'NONE', #253289, 4.149999999999996803 ) ;
#49296=ORIENTED_EDGE ( 'NONE', *, *, #247327, .F. ) ;
#49297=ADVANCED_FACE ( 'NONE', ( #155538 ), #119651, .T. ) ;
#49309=DIRECTION ( 'NONE',  ( 0.000000000000000000, -0.9594490217226103734, -0.2818822000686205254 ) ) ;
#49339=ORIENTED_EDGE ( 'NONE', *, *, #23161, .T. ) ;
#49350=VERTEX_POINT ( 'NONE', #75968 ) ;
#49355=VERTEX_POINT ( 'NONE', #232494 ) ;
#49358=EDGE_CURVE ( 'NONE', #144142, #55598, #156819, .T. ) ;
#49391=CARTESIAN_POINT ( 'NONE',  ( 20.95265033839679347, 39.26570085966146451, -236.8644406904388404 ) ) ;
#49399=CIRCLE ( 'NONE', #41043, 0.8750000000000007772 ) ;
#49423=ORIENTED_EDGE ( 'NONE', *, *, #225077, .T. ) ;
#49424=CARTESIAN_POINT ( 'NONE',  ( 18.39999999999999858, 46.91436717984746707, -255.3877622108296634 ) ) ;
#49428=CARTESIAN_POINT ( 'NONE',  ( 18.59999999999999076, 39.24721131055453327, -235.5164460677962666 ) ) ;
#49442=ORIENTED_EDGE ( 'NONE', *, *, #515, .T. ) ;
#49469=CARTESIAN_POINT ( 'NONE',  ( -21.09107601085565875, 34.02126425780384267, -243.7595103637841305 ) ) ;
#49583=EDGE_CURVE ( 'NONE', #212825, #198468, #48381, .T. ) ;
#49592=EDGE_CURVE ( 'NONE', #26849, #47325, #146197, .T. ) ;
#49596=CYLINDRICAL_SURFACE ( 'NONE', #140691, 0.09999999999999939493 ) ;
#49603=VERTEX_POINT ( 'NONE', #5381 ) ;
#49605=DIRECTION ( 'NONE',  ( 0.000000000000000000, -0.4088369013363280513, 0.9126074666063769270 ) ) ;
#49624=DIRECTION ( 'NONE',  ( 1.000000000000000000, 0.000000000000000000, 0.000000000000000000 ) ) ;
#49700=AXIS2_PLACEMENT_3D ( 'NONE', #239563, #60907, #58323 ) ;
#49716=CARTESIAN_POINT ( 'NONE',  ( -18.54148534481894472, 68.09306500613196533, -224.1549646960459086 ) ) ;
#49721=ORIENTED_EDGE ( 'NONE', *, *, #125859, .T. ) ;
#49767=ORIENTED_EDGE ( 'NONE', *, *, #245208, .F. ) ;
#49779=AXIS2_PLACEMENT_3D ( 'NONE', #134069, #109366, #151088 ) ;
#49834=DIRECTION ( 'NONE',  ( 0.000000000000000000, 0.9126074666064696306, 0.4088369013361213278 ) ) ;
#49867=DIRECTION ( 'NONE',  ( 0.000000000000000000, 0.4088369013363281068, -0.9126074666063770380 ) ) ;
#49874=EDGE_CURVE ( 'NONE', #65743, #258063, #195288, .T. ) ;
#49882=ORIENTED_EDGE ( 'NONE', *, *, #193512, .T. ) ;
#49895=FACE_OUTER_BOUND ( 'NONE', #43095, .T. ) ;
#49903=DIRECTION ( 'NONE',  ( 0.000000000000000000, 0.9126074666063660468, 0.4088369013363524762 ) ) ;
#49911=CARTESIAN_POINT ( 'NONE',  ( -20.64999999999999858, 45.00644278977874535, -237.9768835835062077 ) ) ;
#49942=CARTESIAN_POINT ( 'NONE',  ( 18.49999999999998934, 30.62437029989165893, -230.5032680968432715 ) ) ;
#49947=CARTESIAN_POINT ( 'NONE',  ( 21.00000000000000000, 43.94346684630428967, -235.6041041703296344 ) ) ;
#49972=VECTOR ( 'NONE', #150445, 1000.000000000000000 ) ;
#50020=DIRECTION ( 'NONE',  ( -1.000000000000000000, 0.000000000000000000, 0.000000000000000000 ) ) ;
#50024=TOROIDAL_SURFACE ( 'NONE', #16727, 0.4000000000000003553, 0.1000000000000000056 ) ;
#50030=ORIENTED_EDGE ( 'NONE', *, *, #143859, .T. ) ;
#50061=VECTOR ( 'NONE', #134895, 1000.000000000000000 ) ;
#50083=FACE_OUTER_BOUND ( 'NONE', #156282, .T. ) ;
#50084=DIRECTION ( 'NONE',  ( 1.000000000000000000, 0.000000000000000000, 0.000000000000000000 ) ) ;
#50108=DIRECTION ( 'NONE',  ( 1.000000000000000000, 0.000000000000000000, 0.000000000000000000 ) ) ;
#50128=EDGE_LOOP ( 'NONE', ( #38941, #194109, #155629 ) ) ;
#50163=CARTESIAN_POINT ( 'NONE',  ( 20.94999999999999929, 61.88149656937974896, -248.1136133839584090 ) ) ;
#50169=EDGE_CURVE ( 'NONE', #85465, #52763, #166437, .T. ) ;
#50172=DIRECTION ( 'NONE',  ( 1.000000000000000000, 0.000000000000000000, 0.000000000000000000 ) ) ;
#50175=ORIENTED_EDGE ( 'NONE', *, *, #52992, .T. ) ;
#50178=ADVANCED_FACE ( 'NONE', ( #21806 ), #91402, .T. ) ;
#50179=CARTESIAN_POINT ( 'NONE',  ( -23.15000000000000213, 36.65892442174472876, -249.5511627012454596 ) ) ;
#50214=ADVANCED_FACE ( 'NONE', ( #156200 ), #57036, .T. ) ;
#50222=ORIENTED_EDGE ( 'NONE', *, *, #24791, .T. ) ;
#50232=CARTESIAN_POINT ( 'NONE',  ( 21.05000000000000071, 67.23127455305835554, -235.8551265064784559 ) ) ;
#50249=VERTEX_POINT ( 'NONE', #139139 ) ;
#50283=DIRECTION ( 'NONE',  ( 0.000000000000000000, 0.4088369013363281623, -0.9126074666063771490 ) ) ;
#50301=DIRECTION ( 'NONE',  ( -3.469446951953749873E-14, -0.4088369013363783999, 0.9126074666063545004 ) ) ;
#50310=DIRECTION ( 'NONE',  ( 1.000000000000000000, 0.000000000000000000, 0.000000000000000000 ) ) ;
#50318=ORIENTED_EDGE ( 'NONE', *, *, #2086, .T. ) ;
#50323=CARTESIAN_POINT ( 'NONE',  ( 20.94999999999999574, 44.49901850127302083, -247.5171717259850652 ) ) ;
#50343=DIRECTION ( 'NONE',  ( -1.000000000000000000, 0.000000000000000000, 0.000000000000000000 ) ) ;
#50344=CARTESIAN_POINT ( 'NONE',  ( 21.30000000000002558, 40.35498466150055918, -247.8953732508333587 ) ) ;
#50346=DIRECTION ( 'NONE',  ( 0.000000000000000000, -0.9126074666063545004, -0.4088369013363783999 ) ) ;
#50351=DIRECTION ( 'NONE',  ( 0.000000000000000000, -0.4088369013363281623, 0.9126074666063771490 ) ) ;
#50370=TOROIDAL_SURFACE ( 'NONE', #54487, 0.2000000000000000111, 0.1000000000000000056 ) ;
#50453=CARTESIAN_POINT ( 'NONE',  ( -18.59999999999999787, 48.04585786805223080, -246.4610531646956417 ) ) ;
#50483=ORIENTED_EDGE ( 'NONE', *, *, #62331, .F. ) ;
#50490=DIRECTION ( 'NONE',  ( 0.000000000000000000, 0.9126074666063844765, 0.4088369013363114535 ) ) ;
#50497=DIRECTION ( 'NONE',  ( 0.000000000000000000, -0.4088369013363280513, 0.9126074666063769270 ) ) ;
#50519=CARTESIAN_POINT ( 'NONE',  ( 20.94999999999999929, 67.23127455305835554, -235.8551265064784559 ) ) ;
#50525=DIRECTION ( 'NONE',  ( 1.000000000000000000, -2.986185139342070877E-16, 6.665775143889692774E-16 ) ) ;
#50533=DIRECTION ( 'NONE',  ( 1.000000000000000000, 0.000000000000000000, 0.000000000000000000 ) ) ;
#50547=LINE ( 'NONE', #109252, #83768 ) ;
#50582=ORIENTED_EDGE ( 'NONE', *, *, #54612, .T. ) ;
#50633=CYLINDRICAL_SURFACE ( 'NONE', #62184, 7.899999999999995914 ) ;
#50637=DIRECTION ( 'NONE',  ( 0.000000000000000000, 0.9126074666063774821, 0.4088369013363273297 ) ) ;
#50670=CARTESIAN_POINT ( 'NONE',  ( -23.15000000000000213, 47.48953316408024961, -242.5895867826444601 ) ) ;
#50687=CARTESIAN_POINT ( 'NONE',  ( 21.05000000000000071, 53.70241689174373079, -235.9987767062293074 ) ) ;
#50725=EDGE_CURVE ( 'NONE', #85846, #206700, #183167, .T. ) ;
#50726=CARTESIAN_POINT ( 'NONE',  ( -23.15000000000000213, 62.12148660976906456, -247.5636999539406133 ) ) ;
#50773=AXIS2_PLACEMENT_3D ( 'NONE', #42343, #24089, #223525 ) ;
#50930=DIRECTION ( 'NONE',  ( 0.000000000000000000, 0.9579639084728132081, 0.2868887416116073230 ) ) ;
#50945=CARTESIAN_POINT ( 'NONE',  ( -20.94999999999999929, 44.12194005689738674, -258.6913704466671788 ) ) ;
#50951=EDGE_CURVE ( 'NONE', #69009, #55978, #199382, .T. ) ;
#50986=CIRCLE ( 'NONE', #171858, 0.4000000000000097367 ) ;
#51007=FACE_OUTER_BOUND ( 'NONE', #225594, .T. ) ;
#51014=DIRECTION ( 'NONE',  ( -0.000000000000000000, 0.4088369013363276072, -0.9126074666063773710 ) ) ;
#51023=EDGE_CURVE ( 'NONE', #225362, #110197, #191750, .T. ) ;
#51025=CARTESIAN_POINT ( 'NONE',  ( -21.14999999999999858, 41.42187432231295219, -260.1830396872097140 ) ) ;
#51030=ORIENTED_EDGE ( 'NONE', *, *, #122612, .T. ) ;
#51036=VERTEX_POINT ( 'NONE', #148517 ) ;
#51117=ORIENTED_EDGE ( 'NONE', *, *, #213960, .F. ) ;
#51120=AXIS2_PLACEMENT_3D ( 'NONE', #51025, #85022, #164603 ) ;
#51156=DIRECTION ( 'NONE',  ( -0.000000000000000000, 0.9126074666063771490, 0.4088369013363281623 ) ) ;
#51170=EDGE_CURVE ( 'NONE', #198148, #96525, #87638, .T. ) ;
#51176=CARTESIAN_POINT ( 'NONE',  ( 20.85000000000000142, 74.95904887477786360, -233.7774272632847783 ) ) ;
#51191=EDGE_LOOP ( 'NONE', ( #211696, #8258, #14193, #229740 ) ) ;
#51230=EDGE_CURVE ( 'NONE', #214553, #105957, #123502, .T. ) ;
#51235=DIRECTION ( 'NONE',  ( -1.000000000000000000, 0.000000000000000000, 0.000000000000000000 ) ) ;
#51278=PLANE ( 'NONE',  #48758 ) ;
#51280=DIRECTION ( 'NONE',  ( 1.000000000000000000, 0.000000000000000000, 0.000000000000000000 ) ) ;
#51282=DIRECTION ( 'NONE',  ( 1.000000000000000000, 0.000000000000000000, 0.000000000000000000 ) ) ;
#51338=FACE_OUTER_BOUND ( 'NONE', #211447, .T. ) ;
#51367=DIRECTION ( 'NONE',  ( -6.938893903907222856E-15, -0.4088369013363283844, 0.9126074666063769270 ) ) ;
#51374=EDGE_CURVE ( 'NONE', #108499, #246752, #233598, .T. ) ;
#51437=DIRECTION ( 'NONE',  ( 0.000000000000000000, 0.4088369013363281623, -0.9126074666063771490 ) ) ;
#51473=ADVANCED_FACE ( 'NONE', ( #192461 ), #166995, .T. ) ;
#51483=ORIENTED_EDGE ( 'NONE', *, *, #8264, .F. ) ;
#51492=ORIENTED_EDGE ( 'NONE', *, *, #113019, .T. ) ;
#51505=CARTESIAN_POINT ( 'NONE',  ( -23.25000000000000000, 62.42744096235649920, -225.1319887738535499 ) ) ;
#51517=FACE_OUTER_BOUND ( 'NONE', #201211, .T. ) ;
#51543=DIRECTION ( 'NONE',  ( 1.000000000000000000, 0.000000000000000000, 0.000000000000000000 ) ) ;
#51567=CARTESIAN_POINT ( 'NONE',  ( -20.94684162483048695, 38.09882622057443058, -236.0309084375098223 ) ) ;
#51572=CARTESIAN_POINT ( 'NONE',  ( -22.50000000000000000, 31.85509083104287598, -238.8280249686205536 ) ) ;
#51575=CIRCLE ( 'NONE', #180808, 0.09999999999999939493 ) ;
#51580=VERTEX_POINT ( 'NONE', #59326 ) ;
#51603=ORIENTED_EDGE ( 'NONE', *, *, #130079, .T. ) ;
#51608=DIRECTION ( 'NONE',  ( -1.000000000000000000, -0.000000000000000000, -0.000000000000000000 ) ) ;
#51614=TOROIDAL_SURFACE ( 'NONE', #122603, 11.70000000000000639, 0.1000000000000000056 ) ;
#51632=DIRECTION ( 'NONE',  ( -0.000000000000000000, 0.9126074666063771490, 0.4088369013363281623 ) ) ;
#51645=CARTESIAN_POINT ( 'NONE',  ( -18.39999999999999858, 77.13860723519891849, -241.8264964602989266 ) ) ;
#51658=VECTOR ( 'NONE', #247084, 1000.000000000000000 ) ;
#51668=CIRCLE ( 'NONE', #147565, 11.70000000000000462 ) ;
#51673=CARTESIAN_POINT ( 'NONE',  ( 18.59999999999999076, 43.44873802792533013, -245.1397081572968659 ) ) ;
#51737=CARTESIAN_POINT ( 'NONE',  ( -20.94999999999999929, 67.23127455305835554, -235.8551265064784559 ) ) ;
#51755=ORIENTED_EDGE ( 'NONE', *, *, #49874, .T. ) ;
#51759=CARTESIAN_POINT ( 'NONE',  ( 20.97468175916166899, 43.49871072350438084, -234.8442676856975879 ) ) ;
#51775=VECTOR ( 'NONE', #180983, 1000.000000000000114 ) ;
#51812=VERTEX_POINT ( 'NONE', #9668 ) ;
#51817=ORIENTED_EDGE ( 'NONE', *, *, #5590, .F. ) ;
#51840=CIRCLE ( 'NONE', #14473, 1.899999999999993028 ) ;
#51847=CARTESIAN_POINT ( 'NONE',  ( 21.05000000000000071, 67.23127455305835554, -235.8551265064784559 ) ) ;
#51849=CARTESIAN_POINT ( 'NONE',  ( -18.59999999999999787, 78.48087866980282001, -232.8271061603568910 ) ) ;
#51876=ORIENTED_EDGE ( 'NONE', *, *, #252747, .T. ) ;
#51910=LINE ( 'NONE', #127629, #141094 ) ;
#51940=ORIENTED_EDGE ( 'NONE', *, *, #90764, .T. ) ;
#51948=EDGE_CURVE ( 'NONE', #229414, #219191, #204541, .T. ) ;
#51990=CYLINDRICAL_SURFACE ( 'NONE', #101815, 4.049999999999994493 ) ;
#52006=DIRECTION ( 'NONE',  ( 0.000000000000000000, 0.9126074666063769270, 0.4088369013363280513 ) ) ;
#52023=AXIS2_PLACEMENT_3D ( 'NONE', #102158, #181737, #86446 ) ;
#52036=FACE_OUTER_BOUND ( 'NONE', #46847, .T. ) ;
#52042=TOROIDAL_SURFACE ( 'NONE', #68834, 11.90000000000000213, 0.1000000000000000056 ) ;
#52045=VECTOR ( 'NONE', #207518, 1000.000000000000000 ) ;
#52142=DIRECTION ( 'NONE',  ( 0.000000000000000000, 0.9126074666063660468, 0.4088369013363524762 ) ) ;
#52155=DIRECTION ( 'NONE',  ( 1.000000000000000000, 0.000000000000000000, 0.000000000000000000 ) ) ;
#52160=VERTEX_POINT ( 'NONE', #22531 ) ;
#52167=LINE ( 'NONE', #189127, #160814 ) ;
#52179=FACE_OUTER_BOUND ( 'NONE', #201918, .T. ) ;
#52187=AXIS2_PLACEMENT_3D ( 'NONE', #243180, #206629, #223602 ) ;
#52189=AXIS2_PLACEMENT_3D ( 'NONE', #256581, #59691, #18020 ) ;
#52247=ORIENTED_EDGE ( 'NONE', *, *, #117044, .T. ) ;
#52271=DIRECTION ( 'NONE',  ( 0.000000000000000000, -0.9126074666063763718, -0.4088369013363294391 ) ) ;
#52274=ORIENTED_EDGE ( 'NONE', *, *, #9594, .F. ) ;
#52294=LINE ( 'NONE', #173606, #209276 ) ;
#52298=CARTESIAN_POINT ( 'NONE',  ( -20.64999999999999858, 67.23127455305835554, -235.8551265064784559 ) ) ;
#52321=EDGE_LOOP ( 'NONE', ( #86936, #196942 ) ) ;
#52323=CIRCLE ( 'NONE', #139812, 0.09999999999999939493 ) ;
#52337=CIRCLE ( 'NONE', #2457, 11.74999999999999822 ) ;
#52339=DIRECTION ( 'NONE',  ( 1.000000000000000000, -2.986185139342070877E-16, 6.665775143889692774E-16 ) ) ;
#52445=EDGE_LOOP ( 'NONE', ( #165280, #164404, #47295 ) ) ;
#52501=EDGE_CURVE ( 'NONE', #9091, #111624, #85654, .T. ) ;
#52536=AXIS2_PLACEMENT_3D ( 'NONE', #167902, #198329, #219168 ) ;
#52541=DIRECTION ( 'NONE',  ( 1.000000000000000000, 0.000000000000000000, -0.000000000000000000 ) ) ;
#52554=CARTESIAN_POINT ( 'NONE',  ( 20.12500000000000000, 51.97441255244040548, -232.0063394385699667 ) ) ;
#52605=EDGE_LOOP ( 'NONE', ( #100837, #255828, #214806, #117944, #56407, #132068, #106730, #186458, #37392, #206565, #28503 ) ) ;
#52608=ADVANCED_FACE ( 'NONE', ( #123112 ), #198773, .T. ) ;
#52623=EDGE_CURVE ( 'NONE', #114526, #200649, #46679, .T. ) ;
#52634=ORIENTED_EDGE ( 'NONE', *, *, #177955, .T. ) ;
#52647=LINE ( 'NONE', #74832, #7417 ) ;
#52656=ORIENTED_EDGE ( 'NONE', *, *, #146101, .T. ) ;
#52663=VERTEX_POINT ( 'NONE', #61849 ) ;
#52668=ORIENTED_EDGE ( 'NONE', *, *, #232407, .F. ) ;
#52676=CARTESIAN_POINT ( 'NONE',  ( -21.55000000000000426, 44.76114064897694789, -237.4293191035423831 ) ) ;
#52714=ORIENTED_EDGE ( 'NONE', *, *, #199562, .T. ) ;
#52744=CARTESIAN_POINT ( 'NONE',  ( -21.05000000000000071, 43.57281345108133053, -239.9888335660389487 ) ) ;
#52763=VERTEX_POINT ( 'NONE', #213432 ) ;
#52777=VECTOR ( 'NONE', #60208, 1000.000000000000000 ) ;
#52783=ORIENTED_EDGE ( 'NONE', *, *, #62845, .T. ) ;
#52795=CARTESIAN_POINT ( 'NONE',  ( -21.09096482362050295, 30.83537840773808725, -252.1168136673605602 ) ) ;
#52796=AXIS2_PLACEMENT_3D ( 'NONE', #71461, #126264, #85829 ) ;
#52797=CIRCLE ( 'NONE', #198558, 4.099999999999998757 ) ;
#52819=DIRECTION ( 'NONE',  ( 1.000000000000000000, 0.000000000000000000, 0.000000000000000000 ) ) ;
#52915=ADVANCED_FACE ( 'NONE', ( #63333 ), #128463, .T. ) ;
#52923=CARTESIAN_POINT ( 'NONE',  ( 21.05000000000000071, 56.45527679911575802, -225.2871936083021467 ) ) ;
#52927=EDGE_CURVE ( 'NONE', #74293, #65743, #134345, .T. ) ;
#52943=CARTESIAN_POINT ( 'NONE',  ( -22.59999999999999787, 25.89494711235935043, -254.2627752153468350 ) ) ;
#52953=AXIS2_PLACEMENT_3D ( 'NONE', #220949, #18903, #121882 ) ;
#52962=CARTESIAN_POINT ( 'NONE',  ( 21.05000000000000782, 30.86995437684140953, -252.0366859498353449 ) ) ;
#52992=EDGE_CURVE ( 'NONE', #195501, #55978, #196708, .T. ) ;
#53030=AXIS2_PLACEMENT_3D ( 'NONE', #165213, #126067, #166529 ) ;
#53049=CARTESIAN_POINT ( 'NONE',  ( -20.54999999999999716, 62.04503132991428060, -248.4786563706009588 ) ) ;
#53065=CARTESIAN_POINT ( 'NONE',  ( 21.05000012384814312, 43.42722438913664718, -234.8725066798682519 ) ) ;
#53069=ORIENTED_EDGE ( 'NONE', *, *, #206944, .F. ) ;
#53073=AXIS2_PLACEMENT_3D ( 'NONE', #108004, #5018, #187563 ) ;
#53075=ORIENTED_EDGE ( 'NONE', *, *, #108977, .F. ) ;
#53083=DIRECTION ( 'NONE',  ( -1.000000000000000000, 0.000000000000000000, 0.000000000000000000 ) ) ;
#53123=EDGE_LOOP ( 'NONE', ( #137244, #190832, #21329, #17213, #254409, #248994, #214348, #25547, #117336, #83616, #241733 ) ) ;
#53131=DIRECTION ( 'NONE',  ( 1.000000000000000000, 0.000000000000000000, 0.000000000000000000 ) ) ;
#53134=LINE ( 'NONE', #166703, #145838 ) ;
#53147=ORIENTED_EDGE ( 'NONE', *, *, #88236, .T. ) ;
#53156=ADVANCED_FACE ( 'NONE', ( #94459 ), #157032, .F. ) ;
#53163=CARTESIAN_POINT ( 'NONE',  ( 23.14999999999999503, 23.29878867550048938, -248.4686781323362084 ) ) ;
#53165=ADVANCED_FACE ( 'NONE', ( #38357 ), #196139, .T. ) ;
#53178=CARTESIAN_POINT ( 'NONE',  ( -21.05000000000000071, 44.18518595211054389, -258.7688298343402380 ) ) ;
#53206=TOROIDAL_SURFACE ( 'NONE', #103066, 12.77500000000000036, 0.1000000000000000056 ) ;
#53214=CARTESIAN_POINT ( 'NONE',  ( 20.04142135623730070, 51.38014393322265505, -230.1906178717505611 ) ) ;
#53218=FACE_OUTER_BOUND ( 'NONE', #111646, .T. ) ;
#53229=ORIENTED_EDGE ( 'NONE', *, *, #18098, .T. ) ;
#53246=ORIENTED_EDGE ( 'NONE', *, *, #225001, .F. ) ;
#53263=UNCERTAINTY_MEASURE_WITH_UNIT (LENGTH_MEASURE( 1.000000000000000082E-05 ), #55069, 'distance_accuracy_value', 'NONE');
#53269=DIRECTION ( 'NONE',  ( 0.000000000000000000, 0.4088369013362458948, -0.9126074666064137864 ) ) ;
#53285=LINE ( 'NONE', #233226, #185792 ) ;
#53330=CARTESIAN_POINT ( 'NONE',  ( 20.94999999999999929, 46.45388641681647357, -243.1520440498138385 ) ) ;
#53336=CARTESIAN_POINT ( 'NONE',  ( -18.59999999999999787, 21.13195309841794867, -243.6318585593224100 ) ) ;
#53337=DIRECTION ( 'NONE',  ( -1.000000000000000000, -2.986185139342072849E-16, 6.665775143889691788E-16 ) ) ;
#53363=CIRCLE ( 'NONE', #20062, 0.1000000000000023231 ) ;
#53384=EDGE_LOOP ( 'NONE', ( #70548, #167209, #31270, #75524 ) ) ;
#53385=CYLINDRICAL_SURFACE ( 'NONE', #227107, 0.09999999999999681366 ) ;
#53399=VECTOR ( 'NONE', #38161, 1000.000000000000000 ) ;
#53423=ORIENTED_EDGE ( 'NONE', *, *, #226020, .F. ) ;
#53427=DIRECTION ( 'NONE',  ( 0.000000000000000000, 0.9126074666063770380, 0.4088369013363281068 ) ) ;
#53440=ORIENTED_EDGE ( 'NONE', *, *, #92158, .F. ) ;
#53466=EDGE_CURVE ( 'NONE', #214984, #39096, #192259, .T. ) ;
#53541=EDGE_CURVE ( 'NONE', #235775, #19042, #229837, .T. ) ;
#53542=CARTESIAN_POINT ( 'NONE',  ( -20.54999999999999716, 67.23127455305835554, -235.8551265064784559 ) ) ;
#53570=CARTESIAN_POINT ( 'NONE',  ( -20.64999999999999858, 36.65892442174472876, -249.5511627012454596 ) ) ;
#53596=CARTESIAN_POINT ( 'NONE',  ( -23.25000000000000000, 65.31479887318495514, -236.7136839992847115 ) ) ;
#53621=PLANE ( 'NONE',  #232155 ) ;
#53623=VECTOR ( 'NONE', #9181, 1000.000000000000114 ) ;
#53680=FACE_OUTER_BOUND ( 'NONE', #214907, .T. ) ;
#53691=CARTESIAN_POINT ( 'NONE',  ( 21.05000000000000071, 40.81706895266054147, -238.0716534883986526 ) ) ;
#53704=EDGE_CURVE ( 'NONE', #65749, #140123, #142341, .T. ) ;
#53716=ORIENTED_EDGE ( 'NONE', *, *, #215560, .F. ) ;
#53720=DIRECTION ( 'NONE',  ( 1.000000000000000000, 0.000000000000000000, 0.000000000000000000 ) ) ;
#53725=DIRECTION ( 'NONE',  ( 1.000000000000000000, -1.207181226542539700E-16, 2.694675058168174199E-16 ) ) ;
#53729=DIRECTION ( 'NONE',  ( -1.000000000000000000, -0.000000000000000000, -0.000000000000000000 ) ) ;
#53731=CARTESIAN_POINT ( 'NONE',  ( 21.14999999999999858, 33.98486250090727623, -243.5821103306120108 ) ) ;
#53737=ORIENTED_EDGE ( 'NONE', *, *, #28010, .T. ) ;
#53764=CARTESIAN_POINT ( 'NONE',  ( -21.59142135623730852, 44.62899621218267043, -237.3789420470153857 ) ) ;
#53813=LINE ( 'NONE', #35562, #125257 ) ;
#53818=ORIENTED_EDGE ( 'NONE', *, *, #31748, .T. ) ;
#53834=DIRECTION ( 'NONE',  ( -0.7071067811865389130, -0.6453109281988527179, -0.2890913453342165984 ) ) ;
#53841=CARTESIAN_POINT ( 'NONE',  ( -23.15000000000000213, 42.94327155031035659, -233.8606566173841372 ) ) ;
#53851=EDGE_CURVE ( 'NONE', #123645, #40222, #154858, .T. ) ;
#53871=AXIS2_PLACEMENT_3D ( 'NONE', #155110, #76813, #256689 ) ;
#53886=ORIENTED_EDGE ( 'NONE', *, *, #99272, .F. ) ;
#53900=VERTEX_POINT ( 'NONE', #98628 ) ;
#53966=VERTEX_POINT ( 'NONE', #56944 ) ;
#53977=CIRCLE ( 'NONE', #191576, 0.09999999999999609201 ) ;
#53999=AXIS2_PLACEMENT_3D ( 'NONE', #183123, #107419, #245654 ) ;
#54009=ORIENTED_EDGE ( 'NONE', *, *, #31314, .F. ) ;
#54016=CIRCLE ( 'NONE', #8067, 0.4999999999999944489 ) ;
#54089=CARTESIAN_POINT ( 'NONE',  ( -21.05000000000000071, 30.73075574124491283, -252.3164853687435709 ) ) ;
#54115=ORIENTED_EDGE ( 'NONE', *, *, #98409, .T. ) ;
#54118=AXIS2_PLACEMENT_3D ( 'NONE', #67879, #52155, #73061 ) ;
#54143=CARTESIAN_POINT ( 'NONE',  ( 20.94999999999999929, 61.88149656937974896, -248.1136133839584090 ) ) ;
#54145=AXIS2_PLACEMENT_3D ( 'NONE', #131817, #56111, #135654 ) ;
#54154=AXIS2_PLACEMENT_3D ( 'NONE', #185710, #134368, #194392 ) ;
#54163=AXIS2_PLACEMENT_3D ( 'NONE', #160899, #123045, #240420 ) ;
#54168=DIRECTION ( 'NONE',  ( 1.000000000000000000, 0.000000000000000000, 0.000000000000000000 ) ) ;
#54198=ADVANCED_FACE ( 'NONE', ( #107653 ), #17616, .T. ) ;
#54257=VERTEX_POINT ( 'NONE', #111513 ) ;
#54262=AXIS2_PLACEMENT_3D ( 'NONE', #137740, #73973, #97312 ) ;
#54266=LINE ( 'NONE', #133807, #161794 ) ;
#54288=FACE_OUTER_BOUND ( 'NONE', #188956, .T. ) ;
#54293=CARTESIAN_POINT ( 'NONE',  ( 18.59999999999999076, 54.57427006634497957, -228.7596887170734306 ) ) ;
#54309=CIRCLE ( 'NONE', #87624, 11.70000000000000995 ) ;
#54311=CARTESIAN_POINT ( 'NONE',  ( -18.59999999999999787, 46.45388641681647357, -243.1520440498138385 ) ) ;
#54338=CARTESIAN_POINT ( 'NONE',  ( 20.95512820512820440, 51.70841171101545086, -231.1679749149966767 ) ) ;
#54364=CARTESIAN_POINT ( 'NONE',  ( -22.00356870142023880, 33.69312245273549422, -242.9308869566657165 ) ) ;
#54371=TOROIDAL_SURFACE ( 'NONE', #158462, 12.77499999999999858, 0.1000000000000000056 ) ;
#54377=VECTOR ( 'NONE', #182298, 1000.000000000000000 ) ;
#54395=EDGE_LOOP ( 'NONE', ( #15019, #257977, #43118, #148338 ) ) ;
#54416=EDGE_LOOP ( 'NONE', ( #210194, #102554, #244953, #243218 ) ) ;
#54427=FACE_OUTER_BOUND ( 'NONE', #248059, .T. ) ;
#54431=EDGE_LOOP ( 'NONE', ( #141106, #23038, #139334, #196670 ) ) ;
#54465=EDGE_CURVE ( 'NONE', #120046, #119120, #72001, .T. ) ;
#54473=DIRECTION ( 'NONE',  ( -1.000000000000000000, -0.000000000000000000, 0.000000000000000000 ) ) ;
#54487=AXIS2_PLACEMENT_3D ( 'NONE', #192048, #248141, #212879 ) ;
#54507=AXIS2_PLACEMENT_3D ( 'NONE', #173615, #15800, #32804 ) ;
#54527=AXIS2_PLACEMENT_3D ( 'NONE', #219937, #19169, #221204 ) ;
#54549=ORIENTED_EDGE ( 'NONE', *, *, #190067, .T. ) ;
#54563=AXIS2_PLACEMENT_3D ( 'NONE', #95677, #155696, #235206 ) ;
#54609=EDGE_CURVE ( 'NONE', #143336, #53900, #107344, .T. ) ;
#54612=EDGE_CURVE ( 'NONE', #139650, #97714, #5505, .T. ) ;
#54617=AXIS2_PLACEMENT_3D ( 'NONE', #115171, #193439, #14814 ) ;
#54628=CARTESIAN_POINT ( 'NONE',  ( 22.40000000000020819, 25.97741635855176057, -254.4468634167663197 ) ) ;
#54630=AXIS2_PLACEMENT_3D ( 'NONE', #15705, #97742, #136900 ) ;
#54633=ORIENTED_EDGE ( 'NONE', *, *, #47852, .F. ) ;
#54658=DIRECTION ( 'NONE',  ( 0.000000000000000000, 0.4088369013363296611, -0.9126074666063762608 ) ) ;
#54669=ORIENTED_EDGE ( 'NONE', *, *, #227368, .T. ) ;
#54671=VECTOR ( 'NONE', #35248, 1000.000000000000000 ) ;
#54715=CIRCLE ( 'NONE', #167182, 0.4999999999999944489 ) ;
#54744=AXIS2_PLACEMENT_3D ( 'NONE', #183253, #164968, #82822 ) ;
#54758=DIRECTION ( 'NONE',  ( -1.836970198721029934E-16, -0.4088369013363280513, 0.9126074666063769270 ) ) ;
#54761=DIRECTION ( 'NONE',  ( 0.000000000000000000, -0.9126074666063757057, -0.4088369013363309379 ) ) ;
#54765=AXIS2_PLACEMENT_3D ( 'NONE', #107665, #28168, #30734 ) ;
#54777=CARTESIAN_POINT ( 'NONE',  ( -22.49533356619865643, 31.83654316555210784, -238.9459102234746695 ) ) ;
#54802=CARTESIAN_POINT ( 'NONE',  ( 21.05000000000000071, 48.05226059848062192, -246.4732437245379231 ) ) ;
#54843=ORIENTED_EDGE ( 'NONE', *, *, #44511, .T. ) ;
#54884=DIRECTION ( 'NONE',  ( -0.000000000000000000, 0.4088369013363281068, -0.9126074666063770380 ) ) ;
#54927=ORIENTED_EDGE ( 'NONE', *, *, #3453, .F. ) ;
#54928=CARTESIAN_POINT ( 'NONE',  ( -18.50000000000000000, 26.73568686665825567, -252.5275129665054408 ) ) ;
#54951=ORIENTED_EDGE ( 'NONE', *, *, #35736, .F. ) ;
#54960=ORIENTED_EDGE ( 'NONE', *, *, #60215, .T. ) ;
#55050=ORIENTED_EDGE ( 'NONE', *, *, #185197, .T. ) ;
#55054=( BOUNDED_SURFACE ( )  B_SPLINE_SURFACE ( 3, 2, ( 
 ( #145109, #180407, #81271 ),
 ( #40923, #4314, #60438 ),
 ( #123008, #5585, #83822 ),
 ( #1744, #163415, #64307 ),
 ( #198676, #201237, #241657 ),
 ( #141274, #224652, #103405 ) ),
 .UNSPECIFIED., .F., .F., .T. ) 
 B_SPLINE_SURFACE_WITH_KNOTS ( ( 4, 2, 4 ),
 ( 3, 3 ),
 ( 0.0001792624049599606851, 0.0003686986002125007805, 0.0005581347954650409029 ),
 ( 0.000000000000000000, 1.000000000000000000 ),
 .UNSPECIFIED. ) 
 GEOMETRIC_REPRESENTATION_ITEM ( )  RATIONAL_B_SPLINE_SURFACE ( (
 ( 1.000000000000000000, 0.9238795325112759693, 1.000000000000000000),
 ( 1.000000000000000000, 0.9229318695234719483, 1.000000000000000000),
 ( 1.000000000000000000, 0.8926288119235574747, 1.000000000000000000),
 ( 1.000000000000000000, 0.8123777807266254758, 1.000000000000000000),
 ( 1.000000000000000000, 0.7629087100934772714, 1.000000000000000000),
 ( 1.000000000000000000, 0.7071067811865352493, 1.000000000000000000) ) ) 
 REPRESENTATION_ITEM ( '' )  SURFACE ( )  );
#55069=( LENGTH_UNIT ( ) NAMED_UNIT ( * ) SI_UNIT ( .MILLI., .METRE. ) );
#55072=B_SPLINE_CURVE_WITH_KNOTS ( 'NONE', 3,
 ( #77490, #55348, #217015, #214450, #20130, #35847, #115357, #38398 ),
 .UNSPECIFIED., .F., .F.,
 ( 4, 2, 2, 4 ),
 ( 0.000000000000000000, 0.0001094981963948359418, 0.0002189963927896718837, 0.0004379927855794091447 ),
 .UNSPECIFIED. ) ;
#55093=ORIENTED_EDGE ( 'NONE', *, *, #189115, .T. ) ;
#55101=CARTESIAN_POINT ( 'NONE',  ( -20.54999999999999716, 49.57218508014541669, -254.1759139559835035 ) ) ;
#55129=CARTESIAN_POINT ( 'NONE',  ( -18.59999999999999787, 38.25685495413521409, -235.9601135138701693 ) ) ;
#55175=CARTESIAN_POINT ( 'NONE',  ( -20.94999999999999929, 43.57568952063339651, -245.1784935019914826 ) ) ;
#55211=B_SPLINE_CURVE_WITH_KNOTS ( 'NONE', 3,
 ( #44070, #203134, #24525, #104009 ),
 .UNSPECIFIED., .F., .F.,
 ( 4, 4 ),
 ( 0.000000000000000000, 0.001767853679387123818 ),
 .UNSPECIFIED. ) ;
#55283=LINE ( 'NONE', #154460, #147744 ) ;
#55292=ORIENTED_EDGE ( 'NONE', *, *, #137823, .T. ) ;
#55316=TOROIDAL_SURFACE ( 'NONE', #242797, 0.6000000000000009770, 0.1000000000000000056 ) ;
#55317=CARTESIAN_POINT ( 'NONE',  ( 21.05000000000000071, 44.15903683684981473, -236.5744930507153185 ) ) ;
#55336=CARTESIAN_POINT ( 'NONE',  ( 18.55857864376267941, 55.00748275915436381, -229.9713042450930516 ) ) ;
#55348=CARTESIAN_POINT ( 'NONE',  ( -18.43707690579160996, 77.26488334054519669, -241.9697969554614758 ) ) ;
#55362=AXIS2_PLACEMENT_3D ( 'NONE', #148989, #10748, #88972 ) ;
#55371=LINE ( 'NONE', #237896, #248996 ) ;
#55374=VERTEX_POINT ( 'NONE', #25934 ) ;
#55384=AXIS2_PLACEMENT_3D ( 'NONE', #102719, #199293, #177188 ) ;
#55392=DIRECTION ( 'NONE',  ( 0.000000000000000000, 0.9126074666064005747, 0.4088369013362753712 ) ) ;
#55394=ADVANCED_FACE ( 'NONE', ( #191118 ), #39249, .T. ) ;
#55420=CARTESIAN_POINT ( 'NONE',  ( -21.00250684356851849, 38.25685495240594491, -235.9601135146448598 ) ) ;
#55487=ORIENTED_EDGE ( 'NONE', *, *, #162121, .T. ) ;
#55502=CARTESIAN_POINT ( 'NONE',  ( 21.13435531349758634, 30.73270609305163603, -252.2060354990268252 ) ) ;
#55505=CARTESIAN_POINT ( 'NONE',  ( 18.56579813702274961, 68.10670728244119232, -224.1434476749765565 ) ) ;
#55512=ADVANCED_FACE ( 'NONE', ( #176681 ), #151678, .T. ) ;
#55541=CARTESIAN_POINT ( 'NONE',  ( -20.94999999999999929, 47.95459712139159336, -246.5019368548292675 ) ) ;
#55570=EDGE_CURVE ( 'NONE', #45673, #132976, #130789, .T. ) ;
#55576=ORIENTED_EDGE ( 'NONE', *, *, #256119, .F. ) ;
#55578=FACE_OUTER_BOUND ( 'NONE', #233827, .T. ) ;
#55592=ORIENTED_EDGE ( 'NONE', *, *, #236387, .F. ) ;
#55598=VERTEX_POINT ( 'NONE', #4429 ) ;
#55599=DIRECTION ( 'NONE',  ( 0.000000000000000000, -0.9126074666063771490, -0.4088369013363281623 ) ) ;
#55614=CARTESIAN_POINT ( 'NONE',  ( 20.30466543256828160, 40.38736318471006115, -237.6856447363348650 ) ) ;
#55653=CARTESIAN_POINT ( 'NONE',  ( 18.49999999999999645, 44.52640028187936849, -247.3006740988509193 ) ) ;
#55670=AXIS2_PLACEMENT_3D ( 'NONE', #64911, #219690, #136281 ) ;
#55709=TOROIDAL_SURFACE ( 'NONE', #84937, 11.65000000000000036, 0.1000000000000000056 ) ;
#55751=CIRCLE ( 'NONE', #243037, 0.5000000000000001110 ) ;
#55759=AXIS2_PLACEMENT_3D ( 'NONE', #177212, #179758, #215015 ) ;
#55765=APPLICATION_CONTEXT ( 'automotive_design' ) ;
#55769=CARTESIAN_POINT ( 'NONE',  ( 20.94999999999999929, 36.65892442174472876, -249.5511627012454596 ) ) ;
#55796=EDGE_LOOP ( 'NONE', ( #247593, #136238, #174862, #42847 ) ) ;
#55850=FACE_OUTER_BOUND ( 'NONE', #6153, .T. ) ;
#55906=ORIENTED_EDGE ( 'NONE', *, *, #154252, .T. ) ;
#55912=VECTOR ( 'NONE', #183337, 1000.000000000000000 ) ;
#55925=CYLINDRICAL_SURFACE ( 'NONE', #89547, 0.09999999999999108213 ) ;
#55933=ORIENTED_EDGE ( 'NONE', *, *, #130596, .F. ) ;
#55946=ADVANCED_FACE ( 'NONE', ( #104494 ), #97629, .F. ) ;
#55949=AXIS2_PLACEMENT_3D ( 'NONE', #122021, #182003, #84115 ) ;
#55956=AXIS2_PLACEMENT_3D ( 'NONE', #235856, #80616, #157660 ) ;
#55978=VERTEX_POINT ( 'NONE', #6705 ) ;
#55994=DIRECTION ( 'NONE',  ( -1.000000000000000000, 0.000000000000000000, 0.000000000000000000 ) ) ;
#55996=DIRECTION ( 'NONE',  ( 0.000000000000000000, -0.9126074666063660468, -0.4088369013363524762 ) ) ;
#56020=EDGE_LOOP ( 'NONE', ( #102142, #163067, #152554, #180797 ) ) ;
#56036=AXIS2_PLACEMENT_3D ( 'NONE', #8974, #127645, #125085 ) ;
#56094=DIRECTION ( 'NONE',  ( 0.000000000000000000, -0.9126074666063622720, -0.4088369013363611360 ) ) ;
#56111=DIRECTION ( 'NONE',  ( 0.000000000000000000, 0.4088369013363281623, -0.9126074666063771490 ) ) ;
#56127=DIRECTION ( 'NONE',  ( 0.000000000000000000, 0.9126074666063545004, 0.4088369013363783999 ) ) ;
#56159=CARTESIAN_POINT ( 'NONE',  ( -23.15000000000000213, 54.80101577392981937, -239.2322065708440846 ) ) ;
#56256=CARTESIAN_POINT ( 'NONE',  ( -23.25000000000000000, 69.09936979046463534, -247.6075824278584605 ) ) ;
#56272=EDGE_CURVE ( 'NONE', #3898, #11614, #35527, .T. ) ;
#56273=DIRECTION ( 'NONE',  ( 1.000000000000000000, -1.207181226542539700E-16, 2.694675058168174199E-16 ) ) ;
#56294=AXIS2_PLACEMENT_3D ( 'NONE', #246521, #31375, #91316 ) ;
#56320=CARTESIAN_POINT ( 'NONE',  ( 20.94999999999999574, 43.44873802792533724, -245.1397081572968659 ) ) ;
#56338=VERTEX_POINT ( 'NONE', #147032 ) ;
#56350=ORIENTED_EDGE ( 'NONE', *, *, #26855, .F. ) ;
#56368=FACE_OUTER_BOUND ( 'NONE', #182295, .T. ) ;
#56386=CARTESIAN_POINT ( 'NONE',  ( 21.05000000000000071, 30.84068117814317134, -252.2514754752610031 ) ) ;
#56389=DIRECTION ( 'NONE',  ( 0.000000000000000000, -0.9947597004326452774, 0.1022405907414166287 ) ) ;
#56407=ORIENTED_EDGE ( 'NONE', *, *, #183202, .T. ) ;
#56413=VERTEX_POINT ( 'NONE', #193518 ) ;
#56452=LINE ( 'NONE', #197261, #39995 ) ;
#56485=DIRECTION ( 'NONE',  ( 0.000000000000000000, 0.4088369013363281623, -0.9126074666063771490 ) ) ;
#56488=CARTESIAN_POINT ( 'NONE',  ( -18.50000000000000000, 68.00366762990590530, -224.2307594727497815 ) ) ;
#56521=EDGE_LOOP ( 'NONE', ( #129747, #206877, #121433 ) ) ;
#56550=ORIENTED_EDGE ( 'NONE', *, *, #117449, .T. ) ;
#56568=DIRECTION ( 'NONE',  ( 0.000000000000000000, 0.8103668758649578141, -0.5859227990963213895 ) ) ;
#56569=CARTESIAN_POINT ( 'NONE',  ( 21.05281448260627641, 44.18064746791630881, -236.5651106086473021 ) ) ;
#56578=ADVANCED_FACE ( 'NONE', ( #39604 ), #16176, .T. ) ;
#56579=CARTESIAN_POINT ( 'NONE',  ( -20.64999999999999858, 67.23127455305835554, -235.8551265064784559 ) ) ;
#56589=DIRECTION ( 'NONE',  ( 0.000000000000000000, 0.9126074666063769270, 0.4088369013363282733 ) ) ;
#56674=DIRECTION ( 'NONE',  ( 0.000000000000000000, -0.9126074666063769270, -0.4088369013363280513 ) ) ;
#56689=DIRECTION ( 'NONE',  ( -0.000000000000000000, 0.9126074666063771490, 0.4088369013363281623 ) ) ;
#56699=CARTESIAN_POINT ( 'NONE',  ( -22.50000000000000000, 31.89597452117651244, -238.9192857152811769 ) ) ;
#56700=CYLINDRICAL_SURFACE ( 'NONE', #24634, 0.09999999999999939493 ) ;
#56703=DIRECTION ( 'NONE',  ( 0.000000000000000000, -0.9594490217226104845, -0.2818822000686205809 ) ) ;
#56710=DIRECTION ( 'NONE',  ( -1.000000000000000000, -0.000000000000000000, -0.000000000000000000 ) ) ;
#56716=LINE ( 'NONE', #77573, #6009 ) ;
#56720=CARTESIAN_POINT ( 'NONE',  ( -20.94999999999999929, 67.23127455305835554, -235.8551265064784559 ) ) ;
#56733=EDGE_CURVE ( 'NONE', #157687, #151159, #65218, .T. ) ;
#56785=DIRECTION ( 'NONE',  ( 0.000000000000000000, 0.9126074666063770380, 0.4088369013363282178 ) ) ;
#56790=CARTESIAN_POINT ( 'NONE',  ( 21.05000000000000071, 30.93396944080688016, -252.0807926308514766 ) ) ;
#56797=EDGE_LOOP ( 'NONE', ( #202475, #87911, #44709, #129207, #68887 ) ) ;
#56885=DIRECTION ( 'NONE',  ( 1.000000000000000000, 0.000000000000000000, 0.000000000000000000 ) ) ;
#56941=CIRCLE ( 'NONE', #140350, 0.09999999999999763245 ) ;
#56944=CARTESIAN_POINT ( 'NONE',  ( -23.15000000000000213, 32.96286418198891255, -251.2069521516576174 ) ) ;
#56982=ORIENTED_EDGE ( 'NONE', *, *, #244234, .F. ) ;
#57000=ORIENTED_EDGE ( 'NONE', *, *, #232314, .T. ) ;
#57013=LINE ( 'NONE', #158744, #160160 ) ;
#57036=CYLINDRICAL_SURFACE ( 'NONE', #49700, 0.09999999999999609201 ) ;
#57049=CARTESIAN_POINT ( 'NONE',  ( 20.94999999999999929, 56.24810294282597312, -228.0242159533278823 ) ) ;
#57064=DIRECTION ( 'NONE',  ( 0.000000000000000000, 0.4088369013363281623, -0.9126074666063771490 ) ) ;
#57074=ORIENTED_EDGE ( 'NONE', *, *, #26488, .T. ) ;
#57092=VECTOR ( 'NONE', #192001, 1000.000000000000114 ) ;
#57108=VECTOR ( 'NONE', #56785, 1000.000000000000114 ) ;
#57119=CARTESIAN_POINT ( 'NONE',  ( -21.05000000000000071, 46.53760404070597900, -243.0973507280067167 ) ) ;
#57155=VECTOR ( 'NONE', #113510, 1000.000000000000000 ) ;
#57156=ORIENTED_EDGE ( 'NONE', *, *, #122612, .F. ) ;
#57161=ORIENTED_EDGE ( 'NONE', *, *, #121374, .F. ) ;
#57173=ORIENTED_EDGE ( 'NONE', *, *, #73873, .T. ) ;
#57221=DIRECTION ( 'NONE',  ( 0.000000000000000000, 0.9126074666063771490, 0.4088369013363281623 ) ) ;
#57229=ORIENTED_EDGE ( 'NONE', *, *, #53851, .T. ) ;
#57234=CYLINDRICAL_SURFACE ( 'NONE', #12314, 0.1000000000000024342 ) ;
#57244=VERTEX_POINT ( 'NONE', #191316 ) ;
#57253=CARTESIAN_POINT ( 'NONE',  ( -20.88420186297724612, 68.10670728244119232, -224.1434476749765565 ) ) ;
#57263=VERTEX_POINT ( 'NONE', #133868 ) ;
#57267=DIRECTION ( 'NONE',  ( 1.000000000000000000, 0.000000000000000000, 0.000000000000000000 ) ) ;
#57327=VERTEX_POINT ( 'NONE', #3325 ) ;
#57335=FACE_OUTER_BOUND ( 'NONE', #109251, .T. ) ;
#57372=AXIS2_PLACEMENT_3D ( 'NONE', #177855, #120464, #57864 ) ;
#57391=VERTEX_POINT ( 'NONE', #81564 ) ;
#57400=EDGE_CURVE ( 'NONE', #116784, #79014, #181785, .T. ) ;
#57407=DIRECTION ( 'NONE',  ( 0.000000000000000000, 0.9126074666063770380, 0.4088369013363281068 ) ) ;
#57411=CIRCLE ( 'NONE', #236303, 0.09999999999999470424 ) ;
#57413=CARTESIAN_POINT ( 'NONE',  ( 20.94999999999997442, 74.95904887477786360, -233.7774272632847783 ) ) ;
#57421=EDGE_CURVE ( 'NONE', #106155, #96682, #44424, .T. ) ;
#57425=CARTESIAN_POINT ( 'NONE',  ( -18.50000000000000000, 78.48087866980282001, -232.8271061603568910 ) ) ;
#57431=CYLINDRICAL_SURFACE ( 'NONE', #39683, 0.09999999999999939493 ) ;
#57447=CARTESIAN_POINT ( 'NONE',  ( 20.84999999999999787, 56.11297552314564285, -227.9607914937811017 ) ) ;
#57471=DIRECTION ( 'NONE',  ( 1.000000000000000000, 0.000000000000000000, 0.000000000000000000 ) ) ;
#57476=CARTESIAN_POINT ( 'NONE',  ( 21.56666275994539816, 30.30957806568256885, -252.3955916421750203 ) ) ;
#57498=EDGE_CURVE ( 'NONE', #101051, #238500, #211009, .T. ) ;
#57523=EDGE_LOOP ( 'NONE', ( #196108, #130298, #104611, #207614 ) ) ;
#57532=CARTESIAN_POINT ( 'NONE',  ( 21.05000000000000071, 49.36776662947724503, -253.7196102226803021 ) ) ;
#57537=VERTEX_POINT ( 'NONE', #207990 ) ;
#57547=VECTOR ( 'NONE', #237627, 1000.000000000000114 ) ;
#57556=DIRECTION ( 'NONE',  ( 0.000000000000000000, 0.9126074666063660468, 0.4088369013363524762 ) ) ;
#57559=DIRECTION ( 'NONE',  ( 1.000000000000000000, 4.095934188116521533E-15, 3.985178720521109717E-14 ) ) ;
#57561=CARTESIAN_POINT ( 'NONE',  ( -21.05000000000000071, 56.02567683926420727, -227.9999002286038774 ) ) ;
#57578=VERTEX_POINT ( 'NONE', #213100 ) ;
#57580=CARTESIAN_POINT ( 'NONE',  ( 21.05000000000000071, 67.23127455305835554, -235.8551265064784559 ) ) ;
#57583=DIRECTION ( 'NONE',  ( 2.952720810173289112E-16, 0.4088369013363287729, -0.9126074666063767049 ) ) ;
#57591=DIRECTION ( 'NONE',  ( -1.000000000000000000, 0.000000000000000000, 0.000000000000000000 ) ) ;
#57597=VERTEX_POINT ( 'NONE', #191001 ) ;
#57616=DIRECTION ( 'NONE',  ( 1.000000000000000000, 0.000000000000000000, 0.000000000000000000 ) ) ;
#57679=CARTESIAN_POINT ( 'NONE',  ( 21.14999999999999858, 42.94327155031035659, -233.8606566173841372 ) ) ;
#57681=CARTESIAN_POINT ( 'NONE',  ( -18.50000000000000000, 44.10700160683882132, -235.9691471569721841 ) ) ;
#57720=ORIENTED_EDGE ( 'NONE', *, *, #132375, .T. ) ;
#57741=ORIENTED_EDGE ( 'NONE', *, *, #254736, .T. ) ;
#57757=VERTEX_POINT ( 'NONE', #237808 ) ;
#57764=ORIENTED_EDGE ( 'NONE', *, *, #78740, .F. ) ;
#57786=DIRECTION ( 'NONE',  ( 0.000000000000000000, 0.9126074666063770380, 0.4088369013363281068 ) ) ;
#57806=EDGE_LOOP ( 'NONE', ( #13489, #101538, #44009, #89502, #75432 ) ) ;
#57812=AXIS2_PLACEMENT_3D ( 'NONE', #119181, #237836, #17495 ) ;
#57821=CARTESIAN_POINT ( 'NONE',  ( -20.54999999999999716, 67.23127455305835554, -235.8551265064784559 ) ) ;
#57822=CARTESIAN_POINT ( 'NONE',  ( 23.14999999999999503, 21.17283678855157802, -243.7231193059830048 ) ) ;
#57864=DIRECTION ( 'NONE',  ( 0.000000000000000000, -0.9126074666063772600, -0.4088369013363274407 ) ) ;
#57869=ORIENTED_EDGE ( 'NONE', *, *, #177064, .F. ) ;
#57870=AXIS2_PLACEMENT_3D ( 'NONE', #160586, #240099, #57583 ) ;
#57880=DIRECTION ( 'NONE',  ( -1.000000000000000000, 0.000000000000000000, 0.000000000000000000 ) ) ;
#57892=LINE ( 'NONE', #136133, #103592 ) ;
#57976=CARTESIAN_POINT ( 'NONE',  ( 18.54286124688533377, 77.31795877665247474, -241.8819332742536972 ) ) ;
#57987=DIRECTION ( 'NONE',  ( -0.000000000000000000, -0.4088369013363281068, 0.9126074666063770380 ) ) ;
#58010=EDGE_LOOP ( 'NONE', ( #170531, #141891, #220498, #147487 ) ) ;
#58030=CIRCLE ( 'NONE', #120622, 0.09999999999999108213 ) ;
#58110=CARTESIAN_POINT ( 'NONE',  ( -20.94999999999999929, 56.27731819600170837, -227.9967441372480721 ) ) ;
#58126=VERTEX_POINT ( 'NONE', #96671 ) ;
#58133=EDGE_LOOP ( 'NONE', ( #206701, #227972, #44438, #251496 ) ) ;
#58170=EDGE_LOOP ( 'NONE', ( #192955, #17772, #1752, #9079, #153877 ) ) ;
#58173=DIRECTION ( 'NONE',  ( -0.000000000000000000, 0.8103668758649578141, -0.5859227990963212784 ) ) ;
#58220=ORIENTED_EDGE ( 'NONE', *, *, #19344, .T. ) ;
#58237=AXIS2_PLACEMENT_3D ( 'NONE', #141652, #101197, #242033 ) ;
#58249=DIRECTION ( 'NONE',  ( 1.000000000000000000, 0.000000000000000000, 0.000000000000000000 ) ) ;
#58264=DIRECTION ( 'NONE',  ( 0.000000000000000000, 0.9126074666063132002, 0.4088369013364708815 ) ) ;
#58274=LINE ( 'NONE', #62151, #15709 ) ;
#58289=FACE_OUTER_BOUND ( 'NONE', #120966, .T. ) ;
#58309=CARTESIAN_POINT ( 'NONE',  ( -18.39999999999999858, 46.96039402156217335, -255.3459641718773128 ) ) ;
#58315=CARTESIAN_POINT ( 'NONE',  ( 18.49999999999999645, 74.93036000061670165, -233.6816308724374949 ) ) ;
#58323=DIRECTION ( 'NONE',  ( 0.000000000000000000, 0.9126074666063545004, 0.4088369013363783999 ) ) ;
#58324=ADVANCED_FACE ( 'NONE', ( #62726 ), #6590, .T. ) ;
#58341=VERTEX_POINT ( 'NONE', #23632 ) ;
#58389=AXIS2_PLACEMENT_3D ( 'NONE', #256208, #195049, #236704 ) ;
#58414=DIRECTION ( 'NONE',  ( 1.000000000000000000, 0.000000000000000000, 0.000000000000000000 ) ) ;
#58418=AXIS2_PLACEMENT_3D ( 'NONE', #122547, #82089, #62564 ) ;
#58490=ORIENTED_EDGE ( 'NONE', *, *, #66800, .F. ) ;
#58507=ORIENTED_EDGE ( 'NONE', *, *, #15226, .T. ) ;
#58564=ORIENTED_EDGE ( 'NONE', *, *, #160054, .F. ) ;
#58581=CARTESIAN_POINT ( 'NONE',  ( -20.94999999999999929, 68.00366762990589109, -224.2307594727497815 ) ) ;
#58657=ORIENTED_EDGE ( 'NONE', *, *, #65821, .T. ) ;
#58669=ADVANCED_FACE ( 'NONE', ( #4653 ), #168934, .T. ) ;
#58718=CARTESIAN_POINT ( 'NONE',  ( 21.05000000000000071, 56.02567683926420727, -227.9999002286038774 ) ) ;
#58771=ORIENTED_EDGE ( 'NONE', *, *, #74002, .F. ) ;
#58835=CARTESIAN_POINT ( 'NONE',  ( 20.85000000000000142, 74.83412143252222393, -233.7087995678629966 ) ) ;
#58845=EDGE_LOOP ( 'NONE', ( #130493, #218182, #222, #105647 ) ) ;
#58856=DIRECTION ( 'NONE',  ( 0.000000000000000000, 0.3970902486047482305, -0.9177795674686920480 ) ) ;
#58861=EDGE_CURVE ( 'NONE', #258063, #21929, #257343, .T. ) ;
#58874=DIRECTION ( 'NONE',  ( 6.938893903907499746E-14, -0.9126074666063545004, -0.4088369013363783999 ) ) ;
#58891=EDGE_LOOP ( 'NONE', ( #77121, #194800, #181038, #22546, #241813 ) ) ;
#58896=AXIS2_PLACEMENT_3D ( 'NONE', #63459, #81710, #118325 ) ;
#58921=DIRECTION ( 'NONE',  ( -1.000000000000000000, 7.510212038922847255E-17, -1.676432719286211941E-16 ) ) ;
#58925=CARTESIAN_POINT ( 'NONE',  ( -21.05000000000000071, 44.47083028126616000, -247.4212268238128161 ) ) ;
#58934=CARTESIAN_POINT ( 'NONE',  ( -21.05000000000000071, 44.52640028187936849, -247.3006740988509193 ) ) ;
#58941=ORIENTED_EDGE ( 'NONE', *, *, #17861, .F. ) ;
#58959=CARTESIAN_POINT ( 'NONE',  ( -22.49436431346200038, 31.83493791481901880, -238.9466831125989756 ) ) ;
#58978=DIRECTION ( 'NONE',  ( 1.000000000000000000, 0.000000000000000000, 0.000000000000000000 ) ) ;
#59010=CYLINDRICAL_SURFACE ( 'NONE', #143737, 0.09999999999999681366 ) ;
#59014=AXIS2_PLACEMENT_3D ( 'NONE', #167309, #143851, #85137 ) ;
#59058=EDGE_CURVE ( 'NONE', #95600, #62294, #177705, .T. ) ;
#59074=DIRECTION ( 'NONE',  ( 0.000000000000000000, -0.9126074666063660468, -0.4088369013363524762 ) ) ;
#59078=VECTOR ( 'NONE', #256655, 1000.000000000000000 ) ;
#59084=FACE_OUTER_BOUND ( 'NONE', #221977, .T. ) ;
#59107=ORIENTED_EDGE ( 'NONE', *, *, #19615, .T. ) ;
#59135=CARTESIAN_POINT ( 'NONE',  ( 21.05095171578076574, 44.17356502458446244, -236.5680974831273033 ) ) ;
#59158=EDGE_CURVE ( 'NONE', #232621, #12655, #100566, .T. ) ;
#59201=DIRECTION ( 'NONE',  ( 0.000000000000000000, -0.9126074666063844765, -0.4088369013363114535 ) ) ;
#59215=CARTESIAN_POINT ( 'NONE',  ( 18.49999999999999645, 67.23127455305835554, -235.8551265064784559 ) ) ;
#59259=FACE_OUTER_BOUND ( 'NONE', #188078, .T. ) ;
#59303=DIRECTION ( 'NONE',  ( 0.000000000000000000, 0.9126074666063660468, 0.4088369013363524762 ) ) ;
#59311=ORIENTED_EDGE ( 'NONE', *, *, #36276, .T. ) ;
#59316=ADVANCED_FACE ( 'NONE', ( #41939 ), #158060, .T. ) ;
#59326=CARTESIAN_POINT ( 'NONE',  ( -21.05000000000000071, 56.16603649944111254, -228.1013850343386764 ) ) ;
#59341=EDGE_CURVE ( 'NONE', #227337, #216161, #41716, .T. ) ;
#59378=CIRCLE ( 'NONE', #192707, 0.09999999999999939493 ) ;
#59384=CARTESIAN_POINT ( 'NONE',  ( 22.48508240969612615, 26.00811813615022317, -254.2718847878610688 ) ) ;
#59388=AXIS2_PLACEMENT_3D ( 'NONE', #67185, #45049, #166323 ) ;
#59398=ORIENTED_EDGE ( 'NONE', *, *, #86287, .F. ) ;
#59405=ORIENTED_EDGE ( 'NONE', *, *, #221080, .F. ) ;
#59407=AXIS2_PLACEMENT_3D ( 'NONE', #91978, #132400, #97071 ) ;
#59453=ORIENTED_EDGE ( 'NONE', *, *, #205798, .T. ) ;
#59485=ORIENTED_EDGE ( 'NONE', *, *, #41985, .T. ) ;
#59527=FACE_OUTER_BOUND ( 'NONE', #227231, .T. ) ;
#59553=CARTESIAN_POINT ( 'NONE',  ( 20.94999999999999574, 47.95459712139159336, -246.5019368548292675 ) ) ;
#59555=DIRECTION ( 'NONE',  ( 0.000000000000000000, 0.9126074666064812879, 0.4088369013360954596 ) ) ;
#59565=VECTOR ( 'NONE', #209081, 1000.000000000000000 ) ;
#59613=CARTESIAN_POINT ( 'NONE',  ( 20.99749315643147440, 56.02567684099302880, -227.9999002278293858 ) ) ;
#59629=AXIS2_PLACEMENT_3D ( 'NONE', #111416, #132255, #193530 ) ;
#59672=LINE ( 'NONE', #45273, #189680 ) ;
#59673=EDGE_CURVE ( 'NONE', #191682, #233644, #221508, .T. ) ;
#59684=FACE_OUTER_BOUND ( 'NONE', #17411, .T. ) ;
#59691=DIRECTION ( 'NONE',  ( -1.000000000000000000, -0.000000000000000000, -0.000000000000000000 ) ) ;
#59699=VERTEX_POINT ( 'NONE', #244940 ) ;
#59701=DIRECTION ( 'NONE',  ( 4.239556034732056743E-17, 0.9579639084728132081, 0.2868887416116073785 ) ) ;
#59770=VECTOR ( 'NONE', #114365, 1000.000000000000000 ) ;
#59778=ORIENTED_EDGE ( 'NONE', *, *, #217551, .T. ) ;
#59804=ORIENTED_EDGE ( 'NONE', *, *, #205652, .F. ) ;
#59815=CARTESIAN_POINT ( 'NONE',  ( -20.85000000000000142, 68.11287320386161070, -224.1382462126928488 ) ) ;
#59816=ADVANCED_FACE ( 'NONE', ( #71468 ), #108513, .F. ) ;
#59826=ORIENTED_EDGE ( 'NONE', *, *, #73547, .F. ) ;
#59839=CARTESIAN_POINT ( 'NONE',  ( 22.37643362114956247, 33.45079766894996709, -242.6323179357828792 ) ) ;
#59902=ADVANCED_FACE ( 'NONE', ( #70189 ), #152290, .F. ) ;
#59931=ORIENTED_EDGE ( 'NONE', *, *, #41565, .T. ) ;
#59932=DIRECTION ( 'NONE',  ( 0.7070776581708965169, -0.6453375049857822399, -0.2891032514073239579 ) ) ;
#59937=CARTESIAN_POINT ( 'NONE',  ( -1.820710678118658388, 63.21415835242177650, -248.5348766565488461 ) ) ;
#59970=LINE ( 'NONE', #120002, #184926 ) ;
#59985=DIRECTION ( 'NONE',  ( -1.836970198721030427E-16, -0.4088369013363281623, 0.9126074666063771490 ) ) ;
#60025=CIRCLE ( 'NONE', #84944, 0.1999999999999987899 ) ;
#60033=DIRECTION ( 'NONE',  ( 1.000000000000000000, 0.000000000000000000, -0.000000000000000000 ) ) ;
#60038=EDGE_CURVE ( 'NONE', #182906, #187157, #106235, .T. ) ;
#60043=AXIS2_PLACEMENT_3D ( 'NONE', #209612, #90941, #190051 ) ;
#60056=AXIS2_PLACEMENT_3D ( 'NONE', #147147, #93264, #125037 ) ;
#60065=VERTEX_POINT ( 'NONE', #211020 ) ;
#60089=CARTESIAN_POINT ( 'NONE',  ( 18.59999999999999432, 43.57568952063339651, -245.1784935019914826 ) ) ;
#60101=ORIENTED_EDGE ( 'NONE', *, *, #206330, .F. ) ;
#60118=AXIS2_PLACEMENT_3D ( 'NONE', #249853, #7380, #25675 ) ;
#60122=ORIENTED_EDGE ( 'NONE', *, *, #190156, .T. ) ;
#60136=DIRECTION ( 'NONE',  ( -1.000000000000000000, 0.000000000000000000, 0.000000000000000000 ) ) ;
#60137=CARTESIAN_POINT ( 'NONE',  ( -18.59999999999999787, 51.38014393322265505, -230.1906178717505611 ) ) ;
#60153=CARTESIAN_POINT ( 'NONE',  ( 18.59999999999999432, 23.98305617022077030, -253.3362246115443099 ) ) ;
#60180=CARTESIAN_POINT ( 'NONE',  ( 18.44364597020195617, 46.98014916993328427, -255.3266904785022575 ) ) ;
#60194=VERTEX_POINT ( 'NONE', #166788 ) ;
#60203=LINE ( 'NONE', #17252, #196140 ) ;
#60208=DIRECTION ( 'NONE',  ( -1.000000000000000000, -0.000000000000000000, -0.000000000000000000 ) ) ;
#60214=DIRECTION ( 'NONE',  ( 1.000000000000000000, 0.000000000000000000, 0.000000000000000000 ) ) ;
#60215=EDGE_CURVE ( 'NONE', #197319, #4376, #237871, .T. ) ;
#60218=AXIS2_PLACEMENT_3D ( 'NONE', #239436, #142861, #80315 ) ;
#60288=ORIENTED_EDGE ( 'NONE', *, *, #148181, .T. ) ;
#60290=VERTEX_POINT ( 'NONE', #134032 ) ;
#60344=ADVANCED_FACE ( 'NONE', ( #219991 ), #105134, .T. ) ;
#60372=DIRECTION ( 'NONE',  ( 2.978066053179062821E-16, 0.4088369013363259419, -0.9126074666063780372 ) ) ;
#60384=DIRECTION ( 'NONE',  ( 1.000000000000000000, -2.836875882374966742E-15, 6.332486386695204832E-15 ) ) ;
#60385=ORIENTED_EDGE ( 'NONE', *, *, #59673, .T. ) ;
#60438=CARTESIAN_POINT ( 'NONE',  ( 21.05000000000000071, 34.07109384788311957, -243.8522760710328328 ) ) ;
#60452=EDGE_CURVE ( 'NONE', #22954, #208409, #79823, .T. ) ;
#60476=LINE ( 'NONE', #5627, #153616 ) ;
#60478=CARTESIAN_POINT ( 'NONE',  ( 22.39999999999999858, 33.38250548509083870, -242.4821227592188961 ) ) ;
#60492=EDGE_LOOP ( 'NONE', ( #16773, #39822, #153465, #147624 ) ) ;
#60538=AXIS2_PLACEMENT_3D ( 'NONE', #214600, #236725, #213314 ) ;
#60562=VERTEX_POINT ( 'NONE', #126019 ) ;
#60623=EDGE_LOOP ( 'NONE', ( #97802, #51940, #194671, #126054, #59453 ) ) ;
#60631=CARTESIAN_POINT ( 'NONE',  ( -23.25000000000000000, 32.96286418198890544, -251.2069521516576174 ) ) ;
#60633=DIRECTION ( 'NONE',  ( -1.000000000000000000, -0.000000000000000000, -0.000000000000000000 ) ) ;
#60655=( LENGTH_UNIT ( ) NAMED_UNIT ( * ) SI_UNIT ( .MILLI., .METRE. ) );
#60659=FACE_OUTER_BOUND ( 'NONE', #172580, .T. ) ;
#60660=CARTESIAN_POINT ( 'NONE',  ( 18.50000972452444969, 68.00519115550227411, -224.2294631537214400 ) ) ;
#60673=ORIENTED_EDGE ( 'NONE', *, *, #64320, .F. ) ;
#60713=AXIS2_PLACEMENT_3D ( 'NONE', #184464, #89217, #127071 ) ;
#60715=DIRECTION ( 'NONE',  ( 0.000000000000000000, 0.5859227990963362664, 0.8103668758649469339 ) ) ;
#60732=ADVANCED_FACE ( 'NONE', ( #61906 ), #82711, .T. ) ;
#60740=VECTOR ( 'NONE', #46252, 1000.000000000000114 ) ;
#60748=ADVANCED_FACE ( 'NONE', ( #222232 ), #43633, .T. ) ;
#60751=ORIENTED_EDGE ( 'NONE', *, *, #190956, .F. ) ;
#60757=AXIS2_PLACEMENT_3D ( 'NONE', #38757, #43564, #123110 ) ;
#60771=CARTESIAN_POINT ( 'NONE',  ( 20.87631937322886344, 39.29512351867782627, -236.8959183278824412 ) ) ;
#60786=CARTESIAN_POINT ( 'NONE',  ( 18.49999999999999289, 54.53338637621133955, -228.6684279704127789 ) ) ;
#60829=DIRECTION ( 'NONE',  ( -1.000000000000000000, -0.000000000000000000, -0.000000000000000000 ) ) ;
#60866=CARTESIAN_POINT ( 'NONE',  ( -21.64999999999999858, 53.04688186230822566, -234.1557136682916394 ) ) ;
#60868=EDGE_CURVE ( 'NONE', #206012, #19219, #67046, .T. ) ;
#60871=VERTEX_POINT ( 'NONE', #128313 ) ;
#60874=CARTESIAN_POINT ( 'NONE',  ( -18.40904629823850769, 77.13860739149254186, -241.8264963902813065 ) ) ;
#60889=CARTESIAN_POINT ( 'NONE',  ( -18.47653818581419571, 47.03188537331093499, -255.2758925175261311 ) ) ;
#60892=DIRECTION ( 'NONE',  ( 0.000000000000000000, 0.4088369013363281623, -0.9126074666063771490 ) ) ;
#60907=DIRECTION ( 'NONE',  ( 1.000000000000000000, 0.000000000000000000, 0.000000000000000000 ) ) ;
#60917=CARTESIAN_POINT ( 'NONE',  ( 21.02374657821576065, 56.16603649953788135, -228.1013850333971220 ) ) ;
#60923=ADVANCED_FACE ( 'NONE', ( #85289 ), #88372, .T. ) ;
#60928=VECTOR ( 'NONE', #122513, 1000.000000000000000 ) ;
#60931=DIRECTION ( 'NONE',  ( -0.000000000000000000, 0.5407049257165768008, -0.8412123295017919222 ) ) ;
#60950=AXIS2_PLACEMENT_3D ( 'NONE', #178953, #78513, #141077 ) ;
#61043=VERTEX_POINT ( 'NONE', #94297 ) ;
#61046=ADVANCED_FACE ( 'NONE', ( #153042 ), #96841, .T. ) ;
#61071=EDGE_LOOP ( 'NONE', ( #97911, #77407, #221681, #137726 ) ) ;
#61085=EDGE_LOOP ( 'NONE', ( #1071, #19129, #179621, #217251, #60101, #170799 ) ) ;
#61086=CARTESIAN_POINT ( 'NONE',  ( -20.94999999999999929, 44.05869416168422958, -258.6139110589941197 ) ) ;
#61130=VERTEX_POINT ( 'NONE', #6427 ) ;
#61182=EDGE_CURVE ( 'NONE', #226069, #151518, #184253, .T. ) ;
#61220=CARTESIAN_POINT ( 'NONE',  ( 23.15000000000000213, 48.89266972451527948, -253.5637804087949121 ) ) ;
#61232=FACE_OUTER_BOUND ( 'NONE', #68410, .T. ) ;
#61272=CARTESIAN_POINT ( 'NONE',  ( -18.46907102845852577, 77.19708304286818645, -241.7715114803566223 ) ) ;
#61283=ORIENTED_EDGE ( 'NONE', *, *, #13878, .F. ) ;
#61288=CARTESIAN_POINT ( 'NONE',  ( -21.53551880898957904, 30.42660484565359980, -252.2347178754784522 ) ) ;
#61298=FACE_OUTER_BOUND ( 'NONE', #99143, .T. ) ;
#61320=CARTESIAN_POINT ( 'NONE',  ( -20.94999999999999929, 36.65892442174472876, -249.5511627012454596 ) ) ;
#61348=DIRECTION ( 'NONE',  ( 0.000000000000000000, -0.9126074666063769270, -0.4088369013363280513 ) ) ;
#61419=AXIS2_PLACEMENT_3D ( 'NONE', #162658, #80506, #243461 ) ;
#61433=ORIENTED_EDGE ( 'NONE', *, *, #121587, .F. ) ;
#61439=DIRECTION ( 'NONE',  ( 0.000000000000000000, 0.9126074666063763718, 0.4088369013363297166 ) ) ;
#61468=AXIS2_PLACEMENT_3D ( 'NONE', #137810, #856, #217345 ) ;
#61499=DIRECTION ( 'NONE',  ( -0.000000000000000000, 0.1022405907414166287, 0.9947597004326451664 ) ) ;
#61539=FACE_OUTER_BOUND ( 'NONE', #195804, .T. ) ;
#61567=ORIENTED_EDGE ( 'NONE', *, *, #142390, .T. ) ;
#61580=CARTESIAN_POINT ( 'NONE',  ( -21.14999999999999858, 33.98486250090727623, -243.5821103306120108 ) ) ;
#61585=CIRCLE ( 'NONE', #161566, 0.4000000000000097367 ) ;
#61593=PLANE ( 'NONE',  #11471 ) ;
#61594=DIRECTION ( 'NONE',  ( 0.000000000000000000, 0.8103668758649578141, -0.5859227990963213895 ) ) ;
#61601=VERTEX_POINT ( 'NONE', #4808 ) ;
#61611=( BOUNDED_SURFACE ( )  B_SPLINE_SURFACE ( 3, 2, ( 
 ( #16440, #252441, #95935 ),
 ( #55502, #235446, #76372 ),
 ( #13857, #251154, #73855 ),
 ( #35995, #115504, #114233 ),
 ( #195078, #15141, #56790 ),
 ( #231627, #52962, #153404 ) ),
 .UNSPECIFIED., .F., .F., .F. ) 
 B_SPLINE_SURFACE_WITH_KNOTS ( ( 4, 2, 4 ),
 ( 3, 3 ),
 ( 0.0001300404313046471842, 0.0003183318589266437163, 0.0005066232865486402755 ),
 ( 0.000000000000000000, 1.000000000000000000 ),
 .UNSPECIFIED. ) 
 GEOMETRIC_REPRESENTATION_ITEM ( )  RATIONAL_B_SPLINE_SURFACE ( (
 ( 1.000000000000000000, 0.7071067811865402453, 1.000000000000000000),
 ( 1.000000000000000000, 0.7625113560538631097, 1.000000000000000000),
 ( 1.000000000000000000, 0.8126073484690463644, 1.000000000000000000),
 ( 1.000000000000000000, 0.8923049332730159655, 1.000000000000000000),
 ( 1.000000000000000000, 0.9231914937771280583, 1.000000000000000000),
 ( 1.000000000000000000, 0.9238795325112966195, 1.000000000000000000) ) ) 
 REPRESENTATION_ITEM ( '' )  SURFACE ( )  );
#61623=FACE_OUTER_BOUND ( 'NONE', #86959, .T. ) ;
#61629=VERTEX_POINT ( 'NONE', #145615 ) ;
#61641=DIRECTION ( 'NONE',  ( -0.000000000000000000, -0.9126074666063770380, -0.4088369013363281068 ) ) ;
#61681=CARTESIAN_POINT ( 'NONE',  ( -21.55000000000000426, 52.88334710177370113, -233.7906706816490896 ) ) ;
#61691=DIRECTION ( 'NONE',  ( 0.000000000000000000, -0.9947597004326491632, 0.1022405907413782566 ) ) ;
#61709=VECTOR ( 'NONE', #196933, 1000.000000000000000 ) ;
#61725=CIRCLE ( 'NONE', #174769, 0.1000000000000024342 ) ;
#61756=EDGE_CURVE ( 'NONE', #782, #95600, #184616, .T. ) ;
#61789=EDGE_CURVE ( 'NONE', #18598, #217929, #188910, .T. ) ;
#61801=AXIS2_PLACEMENT_3D ( 'NONE', #204922, #64150, #223205 ) ;
#61818=FACE_OUTER_BOUND ( 'NONE', #67772, .T. ) ;
#61849=CARTESIAN_POINT ( 'NONE',  ( -18.59999999999999787, 74.95904887477786360, -233.7774272632847783 ) ) ;
#61873=CARTESIAN_POINT ( 'NONE',  ( 23.24999999999999289, 21.17283678855157802, -243.7231193059830048 ) ) ;
#61906=FACE_OUTER_BOUND ( 'NONE', #69822, .T. ) ;
#61932=EDGE_CURVE ( 'NONE', #249163, #130019, #143096, .T. ) ;
#61955=VERTEX_POINT ( 'NONE', #44952 ) ;
#61958=CARTESIAN_POINT ( 'NONE',  ( 18.59999999999999787, 74.98773774893902555, -233.8732236541320333 ) ) ;
#62010=VERTEX_POINT ( 'NONE', #159764 ) ;
#62014=DIRECTION ( 'NONE',  ( 0.000000000000000000, -0.4088369013363280513, 0.9126074666063769270 ) ) ;
#62059=FACE_OUTER_BOUND ( 'NONE', #155097, .T. ) ;
#62074=CARTESIAN_POINT ( 'NONE',  ( -21.14999999999999858, 30.73075574124490572, -252.3164853687435709 ) ) ;
#62092=DIRECTION ( 'NONE',  ( 1.000000000000000000, 0.000000000000000000, 0.000000000000000000 ) ) ;
#62094=ADVANCED_FACE ( 'NONE', ( #26692 ), #188304, .T. ) ;
#62101=EDGE_LOOP ( 'NONE', ( #64753, #229174, #216647, #34550 ) ) ;
#62110=FACE_OUTER_BOUND ( 'NONE', #107121, .T. ) ;
#62112=CIRCLE ( 'NONE', #253624, 0.1000000000000024342 ) ;
#62147=VERTEX_POINT ( 'NONE', #210459 ) ;
#62151=CARTESIAN_POINT ( 'NONE',  ( -23.25000000000000000, 74.44087353924872730, -232.6253149859214773 ) ) ;
#62167=CARTESIAN_POINT ( 'NONE',  ( -21.05000000000000071, 34.10074028454091177, -243.7884649046354184 ) ) ;
#62174=AXIS2_PLACEMENT_3D ( 'NONE', #200434, #80440, #41384 ) ;
#62184=AXIS2_PLACEMENT_3D ( 'NONE', #130178, #209735, #110627 ) ;
#62186=ORIENTED_EDGE ( 'NONE', *, *, #168070, .T. ) ;
#62194=CARTESIAN_POINT ( 'NONE',  ( -18.45068461519104375, 46.98837717972348571, -255.3186424377302899 ) ) ;
#62199=VECTOR ( 'NONE', #124430, 1000.000000000000227 ) ;
#62219=CARTESIAN_POINT ( 'NONE',  ( 20.96077737575334865, 56.21923056145944742, -228.0513653586724274 ) ) ;
#62274=ORIENTED_EDGE ( 'NONE', *, *, #197223, .F. ) ;
#62278=DIRECTION ( 'NONE',  ( -1.000000000000000000, 0.000000000000000000, 0.000000000000000000 ) ) ;
#62294=VERTEX_POINT ( 'NONE', #18662 ) ;
#62300=ORIENTED_EDGE ( 'NONE', *, *, #140414, .T. ) ;
#62301=CARTESIAN_POINT ( 'NONE',  ( -23.15000000000000213, 67.23127455305835554, -235.8551265064784559 ) ) ;
#62313=DIRECTION ( 'NONE',  ( 1.000000000000000000, 0.000000000000000000, 0.000000000000000000 ) ) ;
#62321=EDGE_CURVE ( 'NONE', #235986, #246004, #163319, .T. ) ;
#62331=EDGE_CURVE ( 'NONE', #121939, #162201, #218105, .T. ) ;
#62335=FACE_OUTER_BOUND ( 'NONE', #245494, .T. ) ;
#62367=CIRCLE ( 'NONE', #216477, 0.09999999999999939493 ) ;
#62387=ORIENTED_EDGE ( 'NONE', *, *, #198553, .T. ) ;
#62411=DIRECTION ( 'NONE',  ( -1.000000000000000000, 7.510212038922847255E-17, -1.676432719286211941E-16 ) ) ;
#62420=CARTESIAN_POINT ( 'NONE',  ( -20.93302460841143287, 68.06642993404715014, -224.1774859612004036 ) ) ;
#62434=CARTESIAN_POINT ( 'NONE',  ( 20.94999999999999574, 44.18518595211054389, -258.7688298343402380 ) ) ;
#62440=CARTESIAN_POINT ( 'NONE',  ( 18.33683296300631227, 77.42198378243760715, -241.7117649660008567 ) ) ;
#62449=CARTESIAN_POINT ( 'NONE',  ( 18.59999999999999432, 46.50671693017397246, -243.2369495081682942 ) ) ;
#62458=CARTESIAN_POINT ( 'NONE',  ( 20.94999999999999929, 40.88152484246180052, -238.0427780438910474 ) ) ;
#62500=DIRECTION ( 'NONE',  ( -1.000000000000000000, -0.000000000000000000, -0.000000000000000000 ) ) ;
#62507=VERTEX_POINT ( 'NONE', #28981 ) ;
#62522=DIRECTION ( 'NONE',  ( 1.000000000000000000, 0.000000000000000000, -0.000000000000000000 ) ) ;
#62535=LINE ( 'NONE', #99059, #185250 ) ;
#62555=EDGE_CURVE ( 'NONE', #52663, #89722, #117783, .T. ) ;
#62564=DIRECTION ( 'NONE',  ( 0.000000000000000000, -0.4088369013363783999, 0.9126074666063545004 ) ) ;
#62569=CARTESIAN_POINT ( 'NONE',  ( 21.14999999999999858, 30.73075574124490217, -252.3164853687435709 ) ) ;
#62573=ORIENTED_EDGE ( 'NONE', *, *, #5178, .F. ) ;
#62575=CARTESIAN_POINT ( 'NONE',  ( -20.85000000000000142, 56.23643450586806836, -227.9054833905874204 ) ) ;
#62599=CARTESIAN_POINT ( 'NONE',  ( -21.07971444708686093, 30.84640344441752902, -252.0588669582742227 ) ) ;
#62621=ADVANCED_FACE ( 'NONE', ( #229706 ), #188016, .T. ) ;
#62625=LINE ( 'NONE', #142148, #44528 ) ;
#62660=FACE_OUTER_BOUND ( 'NONE', #43587, .T. ) ;
#62666=AXIS2_PLACEMENT_3D ( 'NONE', #230203, #111545, #172853 ) ;
#62673=DIRECTION ( 'NONE',  ( 0.000000000000000000, 0.9126074666063771490, 0.4088369013363281623 ) ) ;
#62676=ORIENTED_EDGE ( 'NONE', *, *, #232101, .F. ) ;
#62684=VERTEX_POINT ( 'NONE', #14533 ) ;
#62697=CARTESIAN_POINT ( 'NONE',  ( -1.739115166359751170E-14, 43.07541598710463404, -233.9110336739111631 ) ) ;
#62719=VERTEX_POINT ( 'NONE', #174922 ) ;
#62726=FACE_OUTER_BOUND ( 'NONE', #150542, .T. ) ;
#62727=DIRECTION ( 'NONE',  ( 0.000000000000000000, 0.9126074666063804797, 0.4088369013363203908 ) ) ;
#62733=AXIS2_PLACEMENT_3D ( 'NONE', #68914, #105410, #48036 ) ;
#62793=CARTESIAN_POINT ( 'NONE',  ( 23.15000000000000213, 69.09936979046463534, -247.6075824278584889 ) ) ;
#62821=CARTESIAN_POINT ( 'NONE',  ( -22.59080734064477625, 31.82702841783757108, -238.8405965839959322 ) ) ;
#62822=CYLINDRICAL_SURFACE ( 'NONE', #206606, 0.1000000000000142025 ) ;
#62845=EDGE_CURVE ( 'NONE', #116722, #224475, #5901, .T. ) ;
#62846=EDGE_CURVE ( 'NONE', #36945, #37194, #197450, .T. ) ;
#62848=ORIENTED_EDGE ( 'NONE', *, *, #111161, .F. ) ;
#62854=EDGE_CURVE ( 'NONE', #236709, #223475, #17818, .T. ) ;
#62873=FACE_BOUND ( 'NONE', #121883, .T. ) ;
#62898=AXIS2_PLACEMENT_3D ( 'NONE', #94331, #168798, #149204 ) ;
#62900=ADVANCED_FACE ( 'NONE', ( #243817 ), #10364, .T. ) ;
#62908=AXIS2_PLACEMENT_3D ( 'NONE', #72421, #68557, #52819 ) ;
#62953=CARTESIAN_POINT ( 'NONE',  ( 18.59999999999999076, 67.23127455305835554, -235.8551265064784559 ) ) ;
#62962=DIRECTION ( 'NONE',  ( -6.938893903907222856E-15, -0.4088369013363280513, 0.9126074666063769270 ) ) ;
#62999=EDGE_LOOP ( 'NONE', ( #252465, #40956, #35457, #245153 ) ) ;
#63007=AXIS2_PLACEMENT_3D ( 'NONE', #92325, #156185, #192726 ) ;
#63012=DIRECTION ( 'NONE',  ( 0.000000000000000000, 0.2818822000685679008, -0.9594490217226259166 ) ) ;
#63064=DIRECTION ( 'NONE',  ( 0.000000000000000000, 0.9126074666062508056, 0.4088369013366094928 ) ) ;
#63072=ORIENTED_EDGE ( 'NONE', *, *, #246878, .T. ) ;
#63075=AXIS2_PLACEMENT_3D ( 'NONE', #244981, #199464, #20827 ) ;
#63087=CYLINDRICAL_SURFACE ( 'NONE', #212902, 0.09999999999999609201 ) ;
#63124=DIRECTION ( 'NONE',  ( 1.000000000000000000, -0.000000000000000000, 0.000000000000000000 ) ) ;
#63140=DIRECTION ( 'NONE',  ( 1.000000000000000000, 0.000000000000000000, 0.000000000000000000 ) ) ;
#63146=EDGE_CURVE ( 'NONE', #233644, #161463, #172200, .T. ) ;
#63159=ORIENTED_EDGE ( 'NONE', *, *, #233134, .T. ) ;
#63165=ORIENTED_EDGE ( 'NONE', *, *, #90964, .F. ) ;
#63166=EDGE_CURVE ( 'NONE', #2789, #228417, #47213, .T. ) ;
#63177=FACE_OUTER_BOUND ( 'NONE', #202711, .T. ) ;
#63197=DIRECTION ( 'NONE',  ( -0.000000000000000000, -0.8490545835447238510, -0.5283051335749973099 ) ) ;
#63206=ORIENTED_EDGE ( 'NONE', *, *, #206129, .F. ) ;
#63209=DIRECTION ( 'NONE',  ( 0.000000000000000000, -0.9126074666063844765, -0.4088369013363114535 ) ) ;
#63215=DIRECTION ( 'NONE',  ( 0.000000000000000000, -0.2868887416115947775, 0.9579639084728169829 ) ) ;
#63216=CIRCLE ( 'NONE', #208979, 0.09999999999999939493 ) ;
#63218=ADVANCED_FACE ( 'NONE', ( #200211 ), #241889, .T. ) ;
#63219=DIRECTION ( 'NONE',  ( -1.836970198721029934E-16, -0.4088369013363280513, 0.9126074666063769270 ) ) ;
#63241=DIRECTION ( 'NONE',  ( 0.000000000000000000, -0.9634813093406718876, -0.2677755899091333047 ) ) ;
#63255=CARTESIAN_POINT ( 'NONE',  ( 21.14999999999999858, 43.07541598710462694, -233.9110336739111347 ) ) ;
#63263=ORIENTED_EDGE ( 'NONE', *, *, #109410, .F. ) ;
#63273=DIRECTION ( 'NONE',  ( -0.7071067811865475727, 0.2890913453342130457, -0.6453109281988448354 ) ) ;
#63277=ORIENTED_EDGE ( 'NONE', *, *, #24791, .F. ) ;
#63290=ORIENTED_EDGE ( 'NONE', *, *, #108623, .T. ) ;
#63303=EDGE_CURVE ( 'NONE', #52663, #238500, #29313, .T. ) ;
#63307=CARTESIAN_POINT ( 'NONE',  ( -18.50000000000000000, 44.10700160683882132, -235.9691471569721841 ) ) ;
#63311=CARTESIAN_POINT ( 'NONE',  ( 21.05000000000072191, 39.26334644455242540, -236.8761453142877542 ) ) ;
#63315=EDGE_CURVE ( 'NONE', #81651, #40310, #126535, .T. ) ;
#63333=FACE_OUTER_BOUND ( 'NONE', #216307, .T. ) ;
#63334=CARTESIAN_POINT ( 'NONE',  ( 23.24999999999999645, 67.23127455305835554, -235.8551265064784559 ) ) ;
#63360=ORIENTED_EDGE ( 'NONE', *, *, #17088, .T. ) ;
#63386=PLANE ( 'NONE',  #58237 ) ;
#63414=VERTEX_POINT ( 'NONE', #175249 ) ;
#63416=ADVANCED_FACE ( 'NONE', ( #16157 ), #13572, .T. ) ;
#63459=CARTESIAN_POINT ( 'NONE',  ( 18.59999999999999076, 53.24180694658302571, -234.8354225850497130 ) ) ;
#63463=ORIENTED_EDGE ( 'NONE', *, *, #67912, .F. ) ;
#63539=ORIENTED_EDGE ( 'NONE', *, *, #37597, .F. ) ;
#63554=EDGE_LOOP ( 'NONE', ( #135585, #87053, #13600, #166156 ) ) ;
#63559=ORIENTED_EDGE ( 'NONE', *, *, #222355, .T. ) ;
#63563=CARTESIAN_POINT ( 'NONE',  ( 18.51997666896889427, 47.01798221041575232, -255.2021870826413021 ) ) ;
#63570=ORIENTED_EDGE ( 'NONE', *, *, #13267, .F. ) ;
#63587=EDGE_CURVE ( 'NONE', #149671, #62010, #45961, .T. ) ;
#63590=EDGE_LOOP ( 'NONE', ( #99637, #108586, #53246, #186507 ) ) ;
#63596=DIRECTION ( 'NONE',  ( 1.000000000000000000, 0.000000000000000000, 0.000000000000000000 ) ) ;
#63599=ORIENTED_EDGE ( 'NONE', *, *, #21343, .F. ) ;
#63604=AXIS2_PLACEMENT_3D ( 'NONE', #258072, #139435, #118633 ) ;
#63632=DIRECTION ( 'NONE',  ( 0.000000000000000000, 0.9623856809447771665, 0.2716869542551821892 ) ) ;
#63680=DIRECTION ( 'NONE',  ( -1.000000000000000000, 0.000000000000000000, 0.000000000000000000 ) ) ;
#63702=CARTESIAN_POINT ( 'NONE',  ( 18.59999999999999787, 47.95459712139159336, -246.5019368548292675 ) ) ;
#63712=CARTESIAN_POINT ( 'NONE',  ( 22.32929514600007792, 33.47007643119025033, -242.6753381395425322 ) ) ;
#63731=DIRECTION ( 'NONE',  ( 0.000000000000000000, -0.9992764785629962843, -0.03803313543132441632 ) ) ;
#63769=CARTESIAN_POINT ( 'NONE',  ( 23.24999999999999645, 45.93587830916155212, -239.9163948487882863 ) ) ;
#63774=EDGE_CURVE ( 'NONE', #73568, #177428, #51668, .T. ) ;
#63793=CARTESIAN_POINT ( 'NONE',  ( 23.15000000000000213, 69.16514130714681130, -247.7543978865853660 ) ) ;
#63810=ORIENTED_EDGE ( 'NONE', *, *, #123947, .T. ) ;
#63812=CARTESIAN_POINT ( 'NONE',  ( 20.94999999999999929, 69.25640205380743453, -247.7135141964517402 ) ) ;
#63821=DIRECTION ( 'NONE',  ( 1.000000000000000000, 0.000000000000000000, 0.000000000000000000 ) ) ;
#63826=DIRECTION ( 'NONE',  ( -1.000000000000000000, -0.000000000000000000, 0.000000000000000000 ) ) ;
#63831=AXIS2_PLACEMENT_3D ( 'NONE', #62301, #157599, #182259 ) ;
#63897=AXIS2_PLACEMENT_3D ( 'NONE', #78473, #19819, #216711 ) ;
#63903=CARTESIAN_POINT ( 'NONE',  ( 21.14999999999999503, 44.06843597547144498, -258.9974126733343951 ) ) ;
#63912=ADVANCED_FACE ( 'NONE', ( #175923 ), #209937, .T. ) ;
#63924=LINE ( 'NONE', #204696, #245926 ) ;
#63967=CIRCLE ( 'NONE', #130598, 0.09999999999999857614 ) ;
#63972=ORIENTED_EDGE ( 'NONE', *, *, #120988, .F. ) ;
#63978=CARTESIAN_POINT ( 'NONE',  ( -21.05000000000000071, 43.57568952063339651, -245.1784935019914826 ) ) ;
#63991=DIRECTION ( 'NONE',  ( -1.000000000000000000, -0.000000000000000000, -0.000000000000000000 ) ) ;
#63995=EDGE_CURVE ( 'NONE', #175127, #63414, #135060, .T. ) ;
#64006=DIRECTION ( 'NONE',  ( -1.000000000000000000, -0.000000000000000000, 0.000000000000000000 ) ) ;
#64028=CARTESIAN_POINT ( 'NONE',  ( 21.14999999999999503, 31.98723526783714277, -238.8784020251475511 ) ) ;
#64029=DIRECTION ( 'NONE',  ( 0.000000000000000000, 0.1022405907414166426, 0.9947597004326453884 ) ) ;
#64040=DIRECTION ( 'NONE',  ( -1.000000000000000000, -0.000000000000000000, -0.000000000000000000 ) ) ;
#64086=CIRCLE ( 'NONE', #209846, 0.1999999999999987899 ) ;
#64088=DIRECTION ( 'NONE',  ( 0.000000000000000000, -0.9126074666063748175, -0.4088369013363328808 ) ) ;
#64091=CARTESIAN_POINT ( 'NONE',  ( 18.58143601961952029, 54.97944794300098437, -229.9087248094723464 ) ) ;
#64095=DIRECTION ( 'NONE',  ( -1.000000000000000000, -0.000000000000000000, -0.000000000000000000 ) ) ;
#64100=AXIS2_PLACEMENT_3D ( 'NONE', #171065, #250541, #71926 ) ;
#64103=TOROIDAL_SURFACE ( 'NONE', #126462, 0.2000000000000000111, 0.1000000000000000056 ) ;
#64119=DIRECTION ( 'NONE',  ( 1.000000000000000000, 0.000000000000000000, 0.000000000000000000 ) ) ;
#64123=VERTEX_POINT ( 'NONE', #113046 ) ;
#64144=CIRCLE ( 'NONE', #80682, 0.1999999999999865219 ) ;
#64150=DIRECTION ( 'NONE',  ( -0.000000000000000000, 0.9969158384938638928, -0.07847809223010317192 ) ) ;
#64157=ORIENTED_EDGE ( 'NONE', *, *, #129472, .F. ) ;
#64181=CIRCLE ( 'NONE', #205825, 0.2000000000000048683 ) ;
#64252=CARTESIAN_POINT ( 'NONE',  ( -21.05000000000000071, 56.18374508921704802, -227.9290876000916057 ) ) ;
#64261=DIRECTION ( 'NONE',  ( 4.336808689942128965E-15, 0.1022405907414274118, 0.9947597004326442782 ) ) ;
#64275=ORIENTED_EDGE ( 'NONE', *, *, #136753, .T. ) ;
#64286=AXIS2_PLACEMENT_3D ( 'NONE', #90842, #133826, #114267 ) ;
#64305=EDGE_CURVE ( 'NONE', #228417, #45673, #213412, .T. ) ;
#64307=CARTESIAN_POINT ( 'NONE',  ( 21.05000000000000071, 34.11495408474048929, -243.6626398385084826 ) ) ;
#64320=EDGE_CURVE ( 'NONE', #81651, #89898, #253821, .T. ) ;
#64322=DIRECTION ( 'NONE',  ( 0.000000000000000000, -0.9126074666063770380, -0.4088369013363281068 ) ) ;
#64335=FACE_OUTER_BOUND ( 'NONE', #111350, .T. ) ;
#64385=SPHERICAL_SURFACE ( 'NONE', #25149, 0.1000000000000000056 ) ;
#64396=ORIENTED_EDGE ( 'NONE', *, *, #14937, .T. ) ;
#64398=DIRECTION ( 'NONE',  ( 1.000000000000000000, 0.000000000000000000, 0.000000000000000000 ) ) ;
#64402=( GEOMETRIC_REPRESENTATION_CONTEXT ( 3 ) GLOBAL_UNCERTAINTY_ASSIGNED_CONTEXT ( ( #156309 ) ) GLOBAL_UNIT_ASSIGNED_CONTEXT ( ( #60655, #163637, #241876 ) ) REPRESENTATION_CONTEXT ( 'NONE', 'WORKASPACE' ) );
#64406=CARTESIAN_POINT ( 'NONE',  ( -23.15000000000000213, 51.33926024308902925, -230.0993571250899379 ) ) ;
#64411=CARTESIAN_POINT ( 'NONE',  ( -20.00857864376270001, 52.13794731297493712, -232.3713824252124880 ) ) ;
#64414=CARTESIAN_POINT ( 'NONE',  ( -23.15000000000000213, 36.65892442174472876, -249.5511627012454596 ) ) ;
#64436=ORIENTED_EDGE ( 'NONE', *, *, #193512, .F. ) ;
#64450=CARTESIAN_POINT ( 'NONE',  ( -21.14999999999999858, 33.98486250090727623, -243.5821103306120108 ) ) ;
#64456=AXIS2_PLACEMENT_3D ( 'NONE', #203972, #97464, #104836 ) ;
#64472=AXIS2_PLACEMENT_3D ( 'NONE', #16678, #157490, #115759 ) ;
#64520=CARTESIAN_POINT ( 'NONE',  ( 21.05000000000000071, 40.68212387350988735, -238.0221676322813096 ) ) ;
#64530=VECTOR ( 'NONE', #86239, 1000.000000000000114 ) ;
#64543=ADVANCED_FACE ( 'NONE', ( #226221 ), #52042, .T. ) ;
#64570=DIRECTION ( 'NONE',  ( 0.000000000000000000, 0.9126074666063769270, 0.4088369013363282733 ) ) ;
#64616=TOROIDAL_SURFACE ( 'NONE', #10481, 11.65000000000000036, 0.1000000000000000056 ) ;
#64646=CARTESIAN_POINT ( 'NONE',  ( -21.05000000000000071, 43.48442877397276618, -245.2193771921251084 ) ) ;
#64693=EDGE_CURVE ( 'NONE', #94408, #230665, #39630, .T. ) ;
#64696=CARTESIAN_POINT ( 'NONE',  ( -21.05000000000000071, 46.59314322379660922, -243.1831726892433210 ) ) ;
#64697=EDGE_CURVE ( 'NONE', #217763, #222344, #185344, .T. ) ;
#64727=LINE ( 'NONE', #182118, #225898 ) ;
#64729=EDGE_LOOP ( 'NONE', ( #222271, #253177, #221076, #122235 ) ) ;
#64753=ORIENTED_EDGE ( 'NONE', *, *, #230354, .T. ) ;
#64761=FACE_OUTER_BOUND ( 'NONE', #93650, .T. ) ;
#64764=FACE_OUTER_BOUND ( 'NONE', #47827, .T. ) ;
#64773=CARTESIAN_POINT ( 'NONE',  ( 21.05000000000000071, 63.58084468663284383, -237.4904741118237723 ) ) ;
#64777=SPHERICAL_SURFACE ( 'NONE', #116864, 0.1000000000000000056 ) ;
#64783=EDGE_LOOP ( 'NONE', ( #199579, #150837, #47948, #205653 ) ) ;
#64785=CARTESIAN_POINT ( 'NONE',  ( 22.48660254037844552, 31.85034414784619727, -238.9397275603479898 ) ) ;
#64797=CARTESIAN_POINT ( 'NONE',  ( 21.07928932188134397, 33.98134083355422774, -243.8161431329846778 ) ) ;
#64803=CYLINDRICAL_SURFACE ( 'NONE', #29421, 0.09999999999999609201 ) ;
#64809=CARTESIAN_POINT ( 'NONE',  ( -21.14999999999999858, 30.99601144558850763, -252.1976540812581504 ) ) ;
#64811=DIRECTION ( 'NONE',  ( 1.000000000000000000, -1.207181226542539700E-16, 2.694675058168174199E-16 ) ) ;
#64812=ORIENTED_EDGE ( 'NONE', *, *, #72680, .T. ) ;
#64822=DIRECTION ( 'NONE',  ( -1.000000000000000000, -0.000000000000000000, -0.000000000000000000 ) ) ;
#64826=VERTEX_POINT ( 'NONE', #28778 ) ;
#64831=LINE ( 'NONE', #186079, #171983 ) ;
#64839=AXIS2_PLACEMENT_3D ( 'NONE', #256900, #80861, #78297 ) ;
#64858=CARTESIAN_POINT ( 'NONE',  ( 20.94999999999999929, 67.23127455305835554, -235.8551265064784559 ) ) ;
#64890=AXIS2_PLACEMENT_3D ( 'NONE', #7571, #224036, #246186 ) ;
#64911=CARTESIAN_POINT ( 'NONE',  ( 21.05000000000000071, 69.09936979046463534, -247.6075824278584889 ) ) ;
#64915=AXIS2_PLACEMENT_3D ( 'NONE', #50323, #7363, #163887 ) ;
#64941=DIRECTION ( 'NONE',  ( -1.000000000000000000, -0.000000000000000000, -0.000000000000000000 ) ) ;
#64970=CARTESIAN_POINT ( 'NONE',  ( -20.54999999999999716, 54.34471204062663219, -239.4366250215122420 ) ) ;
#64975=B_SPLINE_CURVE_WITH_KNOTS ( 'NONE', 3,
 ( #243774, #142098, #185084, #27339, #121301, #220372, #143384, #61288, #5125, #83382 ),
 .UNSPECIFIED., .F., .F.,
 ( 4, 3, 3, 4 ),
 ( 4.906538933386797396E-18, 0.0002000000000002911992, 0.001000000000045103915, 0.001967863649472127805 ),
 .UNSPECIFIED. ) ;
#64990=CARTESIAN_POINT ( 'NONE',  ( 18.50000000000000355, 77.35494420175976416, -241.6200040285045532 ) ) ;
#65018=CARTESIAN_POINT ( 'NONE',  ( -20.54999999999999716, 62.08148826970418099, -247.6553521922769221 ) ) ;
#65037=AXIS2_PLACEMENT_3D ( 'NONE', #81831, #240953, #62313 ) ;
#65105=VECTOR ( 'NONE', #28820, 1000.000000000000000 ) ;
#65149=CARTESIAN_POINT ( 'NONE',  ( -21.11101077989000174, 30.79037258772926577, -252.1634526128120797 ) ) ;
#65185=DIRECTION ( 'NONE',  ( 0.000000000000000000, 0.9126074666063769270, 0.4088369013363280513 ) ) ;
#65193=ORIENTED_EDGE ( 'NONE', *, *, #196069, .T. ) ;
#65206=DIRECTION ( 'NONE',  ( 0.000000000000000000, -0.9656312546561486299, -0.2599159095384356855 ) ) ;
#65218=LINE ( 'NONE', #235839, #89820 ) ;
#65219=ORIENTED_EDGE ( 'NONE', *, *, #122194, .F. ) ;
#65226=CARTESIAN_POINT ( 'NONE',  ( 18.49999999999999289, 53.42432843990430058, -234.7536552047824330 ) ) ;
#65239=ADVANCED_FACE ( 'NONE', ( #186215 ), #101488, .T. ) ;
#65269=AXIS2_PLACEMENT_3D ( 'NONE', #245274, #146150, #48340 ) ;
#65298=VERTEX_POINT ( 'NONE', #12736 ) ;
#65300=CARTESIAN_POINT ( 'NONE',  ( -20.00857864376270001, 52.31097543990284038, -232.5130202284001371 ) ) ;
#65313=ORIENTED_EDGE ( 'NONE', *, *, #109769, .F. ) ;
#65328=FACE_OUTER_BOUND ( 'NONE', #154730, .T. ) ;
#65334=CARTESIAN_POINT ( 'NONE',  ( 22.00356870067775361, 30.03864867784147918, -252.5169646700140902 ) ) ;
#65337=MECHANICAL_DESIGN_GEOMETRIC_PRESENTATION_REPRESENTATION('',(#7067),#256818);
#65350=AXIS2_PLACEMENT_3D ( 'NONE', #38081, #195872, #115030 ) ;
#65388=ADVANCED_FACE ( 'NONE', ( #76519 ), #175645, .T. ) ;
#65389=LINE ( 'NONE', #8000, #119319 ) ;
#65414=EDGE_LOOP ( 'NONE', ( #178449, #76021, #163684, #235784 ) ) ;
#65416=CARTESIAN_POINT ( 'NONE',  ( -20.94999999999999929, 62.46832465249013921, -225.2232495205141731 ) ) ;
#65459=DIRECTION ( 'NONE',  ( 0.000000000000000000, 0.9126074666063772600, 0.4088369013363274962 ) ) ;
#65515=EDGE_CURVE ( 'NONE', #172262, #222515, #144000, .T. ) ;
#65577=CARTESIAN_POINT ( 'NONE',  ( 20.85000000000000142, 69.38854649060171198, -247.7638912529787376 ) ) ;
#65592=DIRECTION ( 'NONE',  ( -1.000000000000000000, 1.207181226542539700E-16, -2.694675058168174199E-16 ) ) ;
#65624=CARTESIAN_POINT ( 'NONE',  ( 20.95392731769792150, 40.80464997849164632, -237.9602131893646231 ) ) ;
#65653=DIRECTION ( 'NONE',  ( 0.000000000000000000, 0.4088369013363280513, -0.9126074666063769270 ) ) ;
#65657=CARTESIAN_POINT ( 'NONE',  ( 21.13461538461538680, 44.29694026544699881, -236.3931290369748126 ) ) ;
#65673=ORIENTED_EDGE ( 'NONE', *, *, #247804, .F. ) ;
#65691=CIRCLE ( 'NONE', #165863, 0.09999999999999063804 ) ;
#65707=DIRECTION ( 'NONE',  ( 0.000000000000000000, 0.2868887416115947775, -0.9579639084728169829 ) ) ;
#65729=CARTESIAN_POINT ( 'NONE',  ( -18.50000000000000000, 47.16152503674118890, -255.1462838189583806 ) ) ;
#65743=VERTEX_POINT ( 'NONE', #29431 ) ;
#65749=VERTEX_POINT ( 'NONE', #71105 ) ;
#65781=ADVANCED_FACE ( 'NONE', ( #93206 ), #149365, .F. ) ;
#65804=CARTESIAN_POINT ( 'NONE',  ( 18.39999999999999858, 77.42559394857967447, -241.6979299484999615 ) ) ;
#65809=EDGE_CURVE ( 'NONE', #18598, #147011, #254799, .T. ) ;
#65813=AXIS2_PLACEMENT_3D ( 'NONE', #185950, #227631, #247193 ) ;
#65821=EDGE_CURVE ( 'NONE', #131894, #10114, #97021, .T. ) ;
#65825=CIRCLE ( 'NONE', #257490, 12.87499999999999822 ) ;
#65833=ORIENTED_EDGE ( 'NONE', *, *, #21124, .F. ) ;
#65843=CARTESIAN_POINT ( 'NONE',  ( 18.59999999999996945, 68.11287320386161070, -224.1382462126928488 ) ) ;
#65849=CARTESIAN_POINT ( 'NONE',  ( 20.94788355080264353, 68.02921119886117651, -224.2090419302654141 ) ) ;
#65859=EDGE_LOOP ( 'NONE', ( #251179, #209050, #102223, #252899 ) ) ;
#65865=CIRCLE ( 'NONE', #111655, 0.09999999999999609201 ) ;
#65892=DIRECTION ( 'NONE',  ( 0.000000000000000000, 0.9126074666063770380, 0.4088369013363280513 ) ) ;
#65893=CARTESIAN_POINT ( 'NONE',  ( 21.05000000000000071, 39.29335463311362275, -236.8946393634875278 ) ) ;
#65899=AXIS2_PLACEMENT_3D ( 'NONE', #57532, #134499, #96641 ) ;
#65924=DIRECTION ( 'NONE',  ( -1.000000000000000000, -0.000000000000000000, -0.000000000000000000 ) ) ;
#65927=CARTESIAN_POINT ( 'NONE',  ( 23.14999999999999858, 67.23127455305835554, -235.8551265064784559 ) ) ;
#65938=CARTESIAN_POINT ( 'NONE',  ( -23.25000000000000000, 67.23127455305835554, -235.8551265064784559 ) ) ;
#65980=CARTESIAN_POINT ( 'NONE',  ( -1.739115166359751170E-14, 51.38014393322266216, -230.1906178717505611 ) ) ;
#65994=EDGE_CURVE ( 'NONE', #132474, #148485, #119445, .T. ) ;
#66006=DIRECTION ( 'NONE',  ( -0.000000000000000000, -0.9126074666063769270, -0.4088369013363282733 ) ) ;
#66011=CARTESIAN_POINT ( 'NONE',  ( 22.50000000000000000, 33.39917768972755141, -242.5193385251796769 ) ) ;
#66081=EDGE_LOOP ( 'NONE', ( #162132, #634, #176121, #200103, #219346, #74776, #255012, #229960, #138290, #36724, #54669, #48598 ) ) ;
#66114=AXIS2_PLACEMENT_3D ( 'NONE', #250396, #224714, #146457 ) ;
#66135=LINE ( 'NONE', #225185, #185672 ) ;
#66143=CARTESIAN_POINT ( 'NONE',  ( 18.41789779300711771, 46.96039426765801039, -255.3459640616293598 ) ) ;
#66148=CARTESIAN_POINT ( 'NONE',  ( -21.05000000000000071, 32.73471231533735448, -251.3091613769916535 ) ) ;
#66158=CARTESIAN_POINT ( 'NONE',  ( -23.15000000000000213, 54.34471204062663219, -239.4366250215122420 ) ) ;
#66197=ORIENTED_EDGE ( 'NONE', *, *, #233134, .F. ) ;
#66207=DIRECTION ( 'NONE',  ( -1.000000000000000000, -0.000000000000000000, 0.000000000000000000 ) ) ;
#66214=ORIENTED_EDGE ( 'NONE', *, *, #83648, .T. ) ;
#66308=DIRECTION ( 'NONE',  ( 1.000000000000000000, 0.000000000000000000, 0.000000000000000000 ) ) ;
#66311=FACE_OUTER_BOUND ( 'NONE', #126387, .T. ) ;
#66322=AXIS2_PLACEMENT_3D ( 'NONE', #34994, #255225, #237008 ) ;
#66326=EDGE_CURVE ( 'NONE', #177620, #212700, #23966, .T. ) ;
#66333=VECTOR ( 'NONE', #54473, 1000.000000000000000 ) ;
#66392=CIRCLE ( 'NONE', #162080, 0.4999999999999968359 ) ;
#66408=EDGE_CURVE ( 'NONE', #231005, #246455, #123911, .T. ) ;
#66442=DIRECTION ( 'NONE',  ( 0.000000000000000000, -0.4088369013363494231, 0.9126074666063672680 ) ) ;
#66469=VECTOR ( 'NONE', #98599, 1000.000000000000114 ) ;
#66513=AXIS2_PLACEMENT_3D ( 'NONE', #143480, #203471, #164347 ) ;
#66536=EDGE_CURVE ( 'NONE', #238500, #251464, #115506, .T. ) ;
#66544=ORIENTED_EDGE ( 'NONE', *, *, #109448, .T. ) ;
#66606=CIRCLE ( 'NONE', #174978, 0.09999999999999609201 ) ;
#66616=CARTESIAN_POINT ( 'NONE',  ( -23.25000000000000000, 47.91013932883114990, -242.3192343197862044 ) ) ;
#66630=CIRCLE ( 'NONE', #70933, 0.4999999999999944489 ) ;
#66653=ORIENTED_EDGE ( 'NONE', *, *, #102023, .F. ) ;
#66684=FACE_OUTER_BOUND ( 'NONE', #226359, .T. ) ;
#66686=TOROIDAL_SURFACE ( 'NONE', #170783, 3.899999999999999467, 0.1000000000000000056 ) ;
#66691=CARTESIAN_POINT ( 'NONE',  ( -22.50000000000000000, 36.56766367508408422, -249.5920463913791139 ) ) ;
#66728=DIRECTION ( 'NONE',  ( 0.000000000000000000, -0.4088369013363280513, 0.9126074666063769270 ) ) ;
#66735=CARTESIAN_POINT ( 'NONE',  ( -21.59142135623730852, 44.72025695884330787, -237.3380583568817315 ) ) ;
#66740=EDGE_LOOP ( 'NONE', ( #192195, #30714, #248773, #96802 ) ) ;
#66760=DIRECTION ( 'NONE',  ( -1.000000000000000000, -0.000000000000000000, -0.000000000000000000 ) ) ;
#66769=CARTESIAN_POINT ( 'NONE',  ( -18.59999999999999787, 48.14768554360777841, -246.4498133360871179 ) ) ;
#66785=DIRECTION ( 'NONE',  ( 1.000000000000000000, -1.335000415235278971E-16, 2.979993593738921214E-16 ) ) ;
#66800=EDGE_CURVE ( 'NONE', #84696, #27038, #136534, .T. ) ;
#66844=CARTESIAN_POINT ( 'NONE',  ( 19.75857864376269291, 54.48300931968434213, -228.8005724072070564 ) ) ;
#66889=CARTESIAN_POINT ( 'NONE',  ( 20.12481660106788439, 40.27144177145531501, -237.4941997744894024 ) ) ;
#66902=LINE ( 'NONE', #186876, #81938 ) ;
#66916=CIRCLE ( 'NONE', #120933, 0.8750000000000007772 ) ;
#66929=CIRCLE ( 'NONE', #220860, 0.1000000000000024342 ) ;
#66937=CYLINDRICAL_SURFACE ( 'NONE', #66114, 0.1000000000000024342 ) ;
#66941=EDGE_CURVE ( 'NONE', #114879, #24454, #55371, .T. ) ;
#66956=CIRCLE ( 'NONE', #4570, 0.2000000000000048683 ) ;
#66973=CARTESIAN_POINT ( 'NONE',  ( 18.59999999999999432, 43.57568952063339651, -245.1784935019914826 ) ) ;
#66989=CARTESIAN_POINT ( 'NONE',  ( 21.05000000000000071, 43.36285386911620776, -234.7972500504784534 ) ) ;
#66990=VERTEX_POINT ( 'NONE', #64406 ) ;
#67007=AXIS2_PLACEMENT_3D ( 'NONE', #96103, #174430, #234339 ) ;
#67046=LINE ( 'NONE', #48754, #213280 ) ;
#67077=CYLINDRICAL_SURFACE ( 'NONE', #10244, 4.049999999999994493 ) ;
#67090=DIRECTION ( 'NONE',  ( 1.000000000000000000, 0.000000000000000000, 0.000000000000000000 ) ) ;
#67113=DIRECTION ( 'NONE',  ( 0.000000000000000000, -0.9126074666063545004, -0.4088369013363783999 ) ) ;
#67124=FACE_OUTER_BOUND ( 'NONE', #219567, .T. ) ;
#67160=ORIENTED_EDGE ( 'NONE', *, *, #70675, .T. ) ;
#67185=CARTESIAN_POINT ( 'NONE',  ( 18.59999999999999076, 78.48087866980282001, -232.8271061603568910 ) ) ;
#67194=EDGE_LOOP ( 'NONE', ( #22214, #228303, #170885, #151438 ) ) ;
#67195=PLANE ( 'NONE',  #32697 ) ;
#67202=CARTESIAN_POINT ( 'NONE',  ( -23.15000000000000213, 56.06656052939784729, -228.0911609752645290 ) ) ;
#67208=DIRECTION ( 'NONE',  ( 0.000000000000000000, 0.9126074666063773710, 0.4088369013363274962 ) ) ;
#67223=ORIENTED_EDGE ( 'NONE', *, *, #220982, .T. ) ;
#67230=DIRECTION ( 'NONE',  ( 0.000000000000000000, -0.9126074666063769270, -0.4088369013363280513 ) ) ;
#67248=CARTESIAN_POINT ( 'NONE',  ( 20.85000000000000142, 78.48087866980282001, -232.8271061603568910 ) ) ;
#67302=CARTESIAN_POINT ( 'NONE',  ( -18.59999999999999787, 52.21971469324220294, -232.5539039185337913 ) ) ;
#67309=DIRECTION ( 'NONE',  ( 1.000000000000000000, 0.000000000000000000, 0.000000000000000000 ) ) ;
#67310=CARTESIAN_POINT ( 'NONE',  ( 23.14999999999999858, 56.06656052939784729, -228.0911609752645290 ) ) ;
#67323=EDGE_CURVE ( 'NONE', #218845, #243814, #81068, .T. ) ;
#67332=CYLINDRICAL_SURFACE ( 'NONE', #119614, 0.09999999999998002154 ) ;
#67343=DIRECTION ( 'NONE',  ( 1.000000000000000000, 0.000000000000000000, 0.000000000000000000 ) ) ;
#67363=FACE_OUTER_BOUND ( 'NONE', #40049, .T. ) ;
#67376=DIRECTION ( 'NONE',  ( 1.000000000000000000, 0.000000000000000000, 0.000000000000000000 ) ) ;
#67402=EDGE_CURVE ( 'NONE', #140123, #73589, #232046, .T. ) ;
#67403=ORIENTED_EDGE ( 'NONE', *, *, #30668, .T. ) ;
#67416=CARTESIAN_POINT ( 'NONE',  ( -22.39999999999999858, 33.47376623175146904, -242.4412390690852703 ) ) ;
#67423=CARTESIAN_POINT ( 'NONE',  ( 18.52165635395213883, 46.94608792946566211, -255.3317188026131248 ) ) ;
#67467=EDGE_CURVE ( 'NONE', #59699, #50249, #39794, .T. ) ;
#67505=ORIENTED_EDGE ( 'NONE', *, *, #156473, .T. ) ;
#67521=DIRECTION ( 'NONE',  ( 0.000000000000000000, 0.9126074666063767049, 0.4088369013363286619 ) ) ;
#67523=CIRCLE ( 'NONE', #246416, 0.1000000000000024342 ) ;
#67527=AXIS2_PLACEMENT_3D ( 'NONE', #111243, #72132, #151687 ) ;
#67531=ORIENTED_EDGE ( 'NONE', *, *, #43659, .T. ) ;
#67538=VERTEX_POINT ( 'NONE', #240532 ) ;
#67549=DIRECTION ( 'NONE',  ( 1.000000000000000000, 0.000000000000000000, 0.000000000000000000 ) ) ;
#67551=ORIENTED_EDGE ( 'NONE', *, *, #63774, .F. ) ;
#67565=DIRECTION ( 'NONE',  ( -1.000000000000000000, -0.000000000000000000, -0.000000000000000000 ) ) ;
#67567=EDGE_CURVE ( 'NONE', #57578, #108295, #11276, .T. ) ;
#67606=DIRECTION ( 'NONE',  ( 1.000000000000000000, 2.986185139342070877E-16, -6.665775143889691788E-16 ) ) ;
#67623=DIRECTION ( 'NONE',  ( 0.000000000000000000, -0.4088369013363296611, 0.9126074666063764829 ) ) ;
#67679=EDGE_CURVE ( 'NONE', #49603, #68445, #3050, .T. ) ;
#67742=DIRECTION ( 'NONE',  ( 1.000000000000000000, 0.000000000000000000, 0.000000000000000000 ) ) ;
#67752=CARTESIAN_POINT ( 'NONE',  ( -23.15000000000000213, 30.69873658968802488, -264.9868732779115703 ) ) ;
#67772=EDGE_LOOP ( 'NONE', ( #174789, #85750, #132978 ) ) ;
#67795=DIRECTION ( 'NONE',  ( 0.000000000000000000, -0.4088369013363783999, 0.9126074666063545004 ) ) ;
#67805=ADVANCED_FACE ( 'NONE', ( #116441 ), #215523, .T. ) ;
#67822=ORIENTED_EDGE ( 'NONE', *, *, #110532, .T. ) ;
#67879=CARTESIAN_POINT ( 'NONE',  ( 20.94999999999999574, 36.65892442174472876, -249.5511627012454596 ) ) ;
#67912=EDGE_CURVE ( 'NONE', #41742, #46950, #169720, .T. ) ;
#67914=CARTESIAN_POINT ( 'NONE',  ( -23.15000000000000213, 36.65892442174472876, -249.5511627012454596 ) ) ;
#67941=DIRECTION ( 'NONE',  ( 0.000000000000000000, -0.4088369013363280513, 0.9126074666063769270 ) ) ;
#67948=ADVANCED_FACE ( 'NONE', ( #219369, #221919, #62873 ), #61593, .F. ) ;
#67958=CARTESIAN_POINT ( 'NONE',  ( -18.41799967126709703, 46.96039440171526991, -255.3459640015733783 ) ) ;
#67981=DIRECTION ( 'NONE',  ( -1.000000000000000000, -0.000000000000000000, -0.000000000000000000 ) ) ;
#67986=CIRCLE ( 'NONE', #63897, 0.09999999999999950595 ) ;
#68027=VERTEX_POINT ( 'NONE', #186692 ) ;
#68030=CYLINDRICAL_SURFACE ( 'NONE', #71285, 0.09999999999999609201 ) ;
#68034=DIRECTION ( 'NONE',  ( 2.952720810173289112E-16, 0.4088369013363388205, -0.9126074666063722640 ) ) ;
#68085=CIRCLE ( 'NONE', #38881, 11.79999999999999716 ) ;
#68106=AXIS2_PLACEMENT_3D ( 'NONE', #88193, #7393, #89493 ) ;
#68108=CIRCLE ( 'NONE', #188912, 0.5000000000000057732 ) ;
#68126=CARTESIAN_POINT ( 'NONE',  ( 19.97071067811865319, 54.36283943849028333, -228.7769250045207912 ) ) ;
#68138=CARTESIAN_POINT ( 'NONE',  ( -20.94999999999999929, 43.47002849391839874, -245.0086825852825143 ) ) ;
#68139=EDGE_CURVE ( 'NONE', #111770, #7110, #57411, .T. ) ;
#68141=ORIENTED_EDGE ( 'NONE', *, *, #130079, .F. ) ;
#68145=CIRCLE ( 'NONE', #213896, 0.09999999999999609201 ) ;
#68150=LINE ( 'NONE', #171150, #170992 ) ;
#68175=CARTESIAN_POINT ( 'NONE',  ( 20.21567752745038504, 39.68329723881405613, -237.0215815498126233 ) ) ;
#68201=VERTEX_POINT ( 'NONE', #32776 ) ;
#68211=DIRECTION ( 'NONE',  ( 0.000000000000000000, -0.2868887416115947775, 0.9579639084728169829 ) ) ;
#68224=ADVANCED_FACE ( 'NONE', ( #251780 ), #74469, .F. ) ;
#68239=DIRECTION ( 'NONE',  ( -0.000000000000000000, 0.9126074666063771490, 0.4088369013363281623 ) ) ;
#68246=ORIENTED_EDGE ( 'NONE', *, *, #21124, .T. ) ;
#68303=EDGE_CURVE ( 'NONE', #115637, #168786, #239935, .T. ) ;
#68305=LINE ( 'NONE', #231243, #214211 ) ;
#68310=DIRECTION ( 'NONE',  ( 0.000000000000000000, 0.9126074666063771490, 0.4088369013363278293 ) ) ;
#68311=EDGE_CURVE ( 'NONE', #91860, #219191, #40479, .T. ) ;
#68328=EDGE_CURVE ( 'NONE', #118225, #69009, #99098, .T. ) ;
#68371=VECTOR ( 'NONE', #8373, 1000.000000000000114 ) ;
#68376=LINE ( 'NONE', #18340, #195594 ) ;
#68410=EDGE_LOOP ( 'NONE', ( #35442, #13271, #186068, #246965, #178831, #167803, #193213 ) ) ;
#68417=( BOUNDED_SURFACE ( )  B_SPLINE_SURFACE ( 3, 2, ( 
 ( #87455, #246536, #105717 ),
 ( #225665, #65334, #5333 ),
 ( #130444, #47037, #165748 ),
 ( #148743, #10514, #88729 ) ),
 .UNSPECIFIED., .F., .F., .F. ) 
 B_SPLINE_SURFACE_WITH_KNOTS ( ( 4, 4 ),
 ( 3, 3 ),
 ( -5.204170427930421283E-18, 0.001979672783031532438 ),
 ( 0.000000000000000000, 1.000000000000000000 ),
 .UNSPECIFIED. ) 
 GEOMETRIC_REPRESENTATION_ITEM ( )  RATIONAL_B_SPLINE_SURFACE ( (
 ( 1.000000000000000000, 0.7103081912007900289, 1.000000000000000000),
 ( 1.000000000000000000, 0.7104998333560322843, 1.000000000000000000),
 ( 1.000000000000000000, 0.7107238315753141578, 1.000000000000000000),
 ( 1.000000000000000000, 0.7110073749539798094, 1.000000000000000000) ) ) 
 REPRESENTATION_ITEM ( '' )  SURFACE ( )  );
#68427=AXIS2_PLACEMENT_3D ( 'NONE', #148153, #9931, #227684 ) ;
#68436=AXIS2_PLACEMENT_3D ( 'NONE', #170457, #154721, #213366 ) ;
#68445=VERTEX_POINT ( 'NONE', #49424 ) ;
#68447=EDGE_LOOP ( 'NONE', ( #3204, #166063, #33870, #164012 ) ) ;
#68541=VECTOR ( 'NONE', #40438, 1000.000000000000000 ) ;
#68557=DIRECTION ( 'NONE',  ( 0.000000000000000000, -0.4088369013363280513, 0.9126074666063769270 ) ) ;
#68581=CARTESIAN_POINT ( 'NONE',  ( 20.94999999999999929, 67.23127455305835554, -235.8551265064784559 ) ) ;
#68582=EDGE_CURVE ( 'NONE', #112216, #130629, #74220, .T. ) ;
#68592=CARTESIAN_POINT ( 'NONE',  ( 18.59999999999999076, 51.96945017402672562, -231.5060697639786440 ) ) ;
#68621=ORIENTED_EDGE ( 'NONE', *, *, #219395, .F. ) ;
#68630=SPHERICAL_SURFACE ( 'NONE', #68427, 0.1000000000000000056 ) ;
#68633=DIRECTION ( 'NONE',  ( 1.000000000000000000, 0.000000000000000000, 0.000000000000000000 ) ) ;
#68639=CIRCLE ( 'NONE', #85158, 0.1999999999999987899 ) ;
#68651=CARTESIAN_POINT ( 'NONE',  ( 20.97239005616515684, 44.21014168011738832, -236.4435994341349101 ) ) ;
#68660=VERTEX_POINT ( 'NONE', #194090 ) ;
#68676=DIRECTION ( 'NONE',  ( 1.000000000000000000, 0.000000000000000000, 0.000000000000000000 ) ) ;
#68685=DIRECTION ( 'NONE',  ( 0.000000000000000000, 0.9126074666063660468, 0.4088369013363524762 ) ) ;
#68706=ORIENTED_EDGE ( 'NONE', *, *, #93988, .F. ) ;
#68730=AXIS2_PLACEMENT_3D ( 'NONE', #26773, #145396, #164971 ) ;
#68740=CARTESIAN_POINT ( 'NONE',  ( 21.07928932188134397, 30.84304088367083097, -252.0482413927653340 ) ) ;
#68777=DIRECTION ( 'NONE',  ( -1.000000000000000000, 0.000000000000000000, 0.000000000000000000 ) ) ;
#68802=EDGE_LOOP ( 'NONE', ( #164621, #163357, #140945, #182619, #96247, #86918, #124388, #81927, #243555, #256273, #234209, #226251, #175603, #21046, #132265, #174405, #165963, #178075, #245679, #159914, #146447, #10229, #18931 ) ) ;
#68804=VERTEX_POINT ( 'NONE', #140492 ) ;
#68834=AXIS2_PLACEMENT_3D ( 'NONE', #250628, #171156, #214087 ) ;
#68866=EDGE_CURVE ( 'NONE', #172097, #199454, #62367, .T. ) ;
#68877=FACE_OUTER_BOUND ( 'NONE', #123138, .T. ) ;
#68879=B_SPLINE_CURVE_WITH_KNOTS ( 'NONE', 3,
 ( #88266, #225214, #7472, #226496, #86982, #47869, #206964, #68740 ),
 .UNSPECIFIED., .F., .F.,
 ( 4, 2, 2, 4 ),
 ( 0.000000000000000000, 0.0001306511400391170414, 0.0001959767100586792214, 0.0002613022800782414013 ),
 .UNSPECIFIED. ) ;
#68887=ORIENTED_EDGE ( 'NONE', *, *, #68958, .F. ) ;
#68914=CARTESIAN_POINT ( 'NONE',  ( 18.59999999999998366, 67.23127455305835554, -235.8551265064784559 ) ) ;
#68921=CARTESIAN_POINT ( 'NONE',  ( 20.94999999999999929, 55.59258605799641373, -234.6589115948038966 ) ) ;
#68936=ORIENTED_EDGE ( 'NONE', *, *, #176169, .T. ) ;
#68943=EDGE_CURVE ( 'NONE', #116074, #235820, #53977, .T. ) ;
#68944=CIRCLE ( 'NONE', #214653, 0.1000000000000024342 ) ;
#68951=CARTESIAN_POINT ( 'NONE',  ( -21.05000000000000071, 69.25640205380744874, -247.7135141964517402 ) ) ;
#68958=EDGE_CURVE ( 'NONE', #256823, #111166, #212410, .T. ) ;
#68972=CARTESIAN_POINT ( 'NONE',  ( 20.95545211741311320, 39.25398227402024531, -236.7884260933929284 ) ) ;
#69009=VERTEX_POINT ( 'NONE', #51645 ) ;
#69126=ADVANCED_FACE ( 'NONE', ( #175501 ), #55709, .T. ) ;
#69131=DIRECTION ( 'NONE',  ( 0.000000000000000000, -0.9126074666063769270, -0.4088369013363282733 ) ) ;
#69136=AXIS2_PLACEMENT_3D ( 'NONE', #108359, #250421, #150067 ) ;
#69141=EDGE_LOOP ( 'NONE', ( #57229, #14015, #123324 ) ) ;
#69167=AXIS2_PLACEMENT_3D ( 'NONE', #149862, #228111, #132863 ) ;
#69196=ORIENTED_EDGE ( 'NONE', *, *, #155085, .F. ) ;
#69239=ORIENTED_EDGE ( 'NONE', *, *, #206944, .T. ) ;
#69245=CARTESIAN_POINT ( 'NONE',  ( 21.14999999999999858, 45.21086124044690280, -238.4331873168094091 ) ) ;
#69258=CIRCLE ( 'NONE', #27589, 0.1000000000000185879 ) ;
#69261=DIRECTION ( 'NONE',  ( 0.000000000000000000, -0.8490545835447238510, -0.5283051335749973099 ) ) ;
#69262=CARTESIAN_POINT ( 'NONE',  ( -18.40000000000000568, 46.93054509580812095, -255.3593361228640219 ) ) ;
#69266=ORIENTED_EDGE ( 'NONE', *, *, #78286, .T. ) ;
#69269=DIRECTION ( 'NONE',  ( 1.000000000000000000, 0.000000000000000000, 0.000000000000000000 ) ) ;
#69297=CARTESIAN_POINT ( 'NONE',  ( -18.59999999999999787, 68.11287320386161070, -224.1382462126928488 ) ) ;
#69308=AXIS2_PLACEMENT_3D ( 'NONE', #115586, #238092, #16511 ) ;
#69311=CIRCLE ( 'NONE', #252429, 0.2000000000000048683 ) ;
#69330=DIRECTION ( 'NONE',  ( 1.000000000000000000, 0.000000000000000000, 0.000000000000000000 ) ) ;
#69343=ORIENTED_EDGE ( 'NONE', *, *, #84668, .T. ) ;
#69368=CARTESIAN_POINT ( 'NONE',  ( -21.05000000000000071, 46.59314322379660922, -243.1831726892433210 ) ) ;
#69371=VERTEX_POINT ( 'NONE', #75766 ) ;
#69384=CIRCLE ( 'NONE', #215122, 0.09999999999999108213 ) ;
#69406=TOROIDAL_SURFACE ( 'NONE', #198557, 12.97499999999999787, 0.1000000000000000056 ) ;
#69432=CARTESIAN_POINT ( 'NONE',  ( 23.15000000000000213, 69.20602499728043711, -247.8456586332460176 ) ) ;
#69472=EDGE_LOOP ( 'NONE', ( #36635, #173422, #81213, #145850, #46826 ) ) ;
#69505=FACE_OUTER_BOUND ( 'NONE', #191293, .T. ) ;
#69509=DIRECTION ( 'NONE',  ( 0.000000000000000000, 0.9126074666063769270, 0.4088369013363280513 ) ) ;
#69579=CARTESIAN_POINT ( 'NONE',  ( 21.05000000000000071, 69.38854649060171198, -247.7638912529787376 ) ) ;
#69614=DIRECTION ( 'NONE',  ( 1.000000000000000000, 0.000000000000000000, 0.000000000000000000 ) ) ;
#69618=CARTESIAN_POINT ( 'NONE',  ( -18.50000000000000000, 31.94635157770352052, -238.7871412784868994 ) ) ;
#69627=ORIENTED_EDGE ( 'NONE', *, *, #8930, .F. ) ;
#69640=ORIENTED_EDGE ( 'NONE', *, *, #110843, .T. ) ;
#69676=DIRECTION ( 'NONE',  ( 0.000000000000000000, 0.9126074666063772600, 0.4088369013363276627 ) ) ;
#69706=EDGE_CURVE ( 'NONE', #106227, #4597, #108162, .T. ) ;
#69707=CARTESIAN_POINT ( 'NONE',  ( 20.94999999999999929, 67.23127455305835554, -235.8551265064784559 ) ) ;
#69777=VERTEX_POINT ( 'NONE', #32513 ) ;
#69804=CARTESIAN_POINT ( 'NONE',  ( -20.94999999999999929, 69.16514130714681130, -247.7543978865853660 ) ) ;
#69813=DIRECTION ( 'NONE',  ( 0.000000000000000000, 0.8490545835447252943, 0.5283051335749947564 ) ) ;
#69822=EDGE_LOOP ( 'NONE', ( #216683, #242981, #16726, #175868 ) ) ;
#69831=ORIENTED_EDGE ( 'NONE', *, *, #45998, .T. ) ;
#69892=EDGE_CURVE ( 'NONE', #1615, #20493, #18696, .T. ) ;
#69899=DIRECTION ( 'NONE',  ( -1.000000000000000000, 0.000000000000000000, 0.000000000000000000 ) ) ;
#69930=DIRECTION ( 'NONE',  ( 1.000000000000000000, 0.000000000000000000, 0.000000000000000000 ) ) ;
#69933=FACE_OUTER_BOUND ( 'NONE', #92118, .T. ) ;
#69996=CIRCLE ( 'NONE', #198963, 3.900000000000004796 ) ;
#70061=CIRCLE ( 'NONE', #249132, 0.4999999999999944489 ) ;
#70091=DIRECTION ( 'NONE',  ( 1.000000000000000000, 0.000000000000000000, 0.000000000000000000 ) ) ;
#70096=ORIENTED_EDGE ( 'NONE', *, *, #71219, .F. ) ;
#70097=CARTESIAN_POINT ( 'NONE',  ( 22.47007471830800895, 33.50241300269675548, -242.5051845127899810 ) ) ;
#70105=ORIENTED_EDGE ( 'NONE', *, *, #248422, .F. ) ;
#70110=CARTESIAN_POINT ( 'NONE',  ( 21.11701782572533048, 43.45044756046340240, -234.7603190085133633 ) ) ;
#70189=FACE_OUTER_BOUND ( 'NONE', #249576, .T. ) ;
#70213=CARTESIAN_POINT ( 'NONE',  ( -20.94999999999999929, 78.48087866980282001, -232.8271061603568910 ) ) ;
#70291=CARTESIAN_POINT ( 'NONE',  ( 20.94999999999999929, 45.77234354862702048, -239.5513518621457365 ) ) ;
#70296=DIRECTION ( 'NONE',  ( -1.000000000000000000, -6.649824375826082804E-14, -1.991473509853015959E-14 ) ) ;
#70302=CARTESIAN_POINT ( 'NONE',  ( -18.59999999999999787, 51.38014393322265505, -230.1906178717505611 ) ) ;
#70303=EDGE_CURVE ( 'NONE', #139213, #212713, #48102, .T. ) ;
#70315=ORIENTED_EDGE ( 'NONE', *, *, #144830, .F. ) ;
#70316=EDGE_LOOP ( 'NONE', ( #108487, #120675, #18070, #96907 ) ) ;
#70336=DIRECTION ( 'NONE',  ( 0.000000000000000000, 0.9126074666063768159, 0.4088369013363282178 ) ) ;
#70377=PLANE ( 'NONE',  #110654 ) ;
#70386=CARTESIAN_POINT ( 'NONE',  ( 22.45463910399148588, 26.02743911761160689, -254.3139371331799623 ) ) ;
#70387=VERTEX_POINT ( 'NONE', #39879 ) ;
#70403=CARTESIAN_POINT ( 'NONE',  ( -22.50000000000094147, 25.98655542988606726, -254.2226763854396552 ) ) ;
#70406=EDGE_CURVE ( 'NONE', #932, #168498, #247836, .T. ) ;
#70432=DIRECTION ( 'NONE',  ( 0.000000000000000000, -0.9126074666063660468, -0.4088369013363524762 ) ) ;
#70441=VERTEX_POINT ( 'NONE', #145362 ) ;
#70449=VERTEX_POINT ( 'NONE', #63255 ) ;
#70513=AXIS2_PLACEMENT_3D ( 'NONE', #23088, #98707, #178314 ) ;
#70545=CIRCLE ( 'NONE', #107911, 0.1000000000000031558 ) ;
#70548=ORIENTED_EDGE ( 'NONE', *, *, #8991, .T. ) ;
#70574=DIRECTION ( 'NONE',  ( -2.915501640297154283E-16, -0.4088369013363279403, 0.9126074666063770380 ) ) ;
#70595=DIRECTION ( 'NONE',  ( 0.000000000000000000, 0.9126074666064841745, 0.4088369013360889648 ) ) ;
#70603=CARTESIAN_POINT ( 'NONE',  ( -18.59999999999999787, 78.48087866980282001, -232.8271061603568910 ) ) ;
#70661=CARTESIAN_POINT ( 'NONE',  ( 21.05000000000000071, 69.16514130714681130, -247.7543978865853660 ) ) ;
#70670=CARTESIAN_POINT ( 'NONE',  ( 23.24999999999999289, 21.13195309841794867, -243.6318585593223816 ) ) ;
#70675=EDGE_CURVE ( 'NONE', #129332, #68660, #185669, .T. ) ;
#70690=VERTEX_POINT ( 'NONE', #179098 ) ;
#70696=DIRECTION ( 'NONE',  ( -0.000000000000000000, -0.4088369013363281623, 0.9126074666063771490 ) ) ;
#70698=ORIENTED_EDGE ( 'NONE', *, *, #171325, .F. ) ;
#70748=ORIENTED_EDGE ( 'NONE', *, *, #25557, .F. ) ;
#70760=ADVANCED_FACE ( 'NONE', ( #224598 ), #244389, .T. ) ;
#70766=AXIS2_PLACEMENT_3D ( 'NONE', #76184, #93188, #252255 ) ;
#70783=VERTEX_POINT ( 'NONE', #203763 ) ;
#70785=DIRECTION ( 'NONE',  ( 0.000000000000000000, -0.9126074666063771490, -0.4088369013363278293 ) ) ;
#70837=ORIENTED_EDGE ( 'NONE', *, *, #19434, .F. ) ;
#70843=LINE ( 'NONE', #90366, #200090 ) ;
#70900=EDGE_CURVE ( 'NONE', #213658, #150739, #168536, .T. ) ;
#70920=CARTESIAN_POINT ( 'NONE',  ( 20.94999999999999929, 56.22462877935074488, -228.0203483467521721 ) ) ;
#70933=AXIS2_PLACEMENT_3D ( 'NONE', #38844, #214897, #118379 ) ;
#70951=CIRCLE ( 'NONE', #116704, 0.09999999999999609201 ) ;
#71000=CYLINDRICAL_SURFACE ( 'NONE', #194426, 11.79999999999999005 ) ;
#71002=EDGE_CURVE ( 'NONE', #246004, #102227, #102596, .T. ) ;
#71019=DIRECTION ( 'NONE',  ( 1.000000000000000000, 0.000000000000000000, 0.000000000000000000 ) ) ;
#71022=VERTEX_POINT ( 'NONE', #226721 ) ;
#71044=EDGE_CURVE ( 'NONE', #57597, #227768, #48089, .T. ) ;
#71072=ORIENTED_EDGE ( 'NONE', *, *, #227368, .F. ) ;
#71085=EDGE_CURVE ( 'NONE', #182894, #13509, #206687, .T. ) ;
#71105=CARTESIAN_POINT ( 'NONE',  ( -23.15000000000000213, 54.14029358995846053, -238.9803212882090691 ) ) ;
#71111=CARTESIAN_POINT ( 'NONE',  ( 21.97500000000000497, 51.97441255244040548, -232.0063394385699667 ) ) ;
#71207=ADVANCED_FACE ( 'NONE', ( #162709 ), #28357, .T. ) ;
#71211=CIRCLE ( 'NONE', #443, 0.1000000000000121764 ) ;
#71219=EDGE_CURVE ( 'NONE', #57263, #105021, #2665, .T. ) ;
#71232=CARTESIAN_POINT ( 'NONE',  ( 20.46382478191415188, 39.33264809402798079, -236.7398086741081613 ) ) ;
#71259=VERTEX_POINT ( 'NONE', #173011 ) ;
#71267=CIRCLE ( 'NONE', #133778, 0.09999999999999939493 ) ;
#71283=EDGE_LOOP ( 'NONE', ( #101448, #4661, #122487, #209742 ) ) ;
#71285=AXIS2_PLACEMENT_3D ( 'NONE', #10633, #69330, #45903 ) ;
#71352=CARTESIAN_POINT ( 'NONE',  ( 20.94999999999999574, 39.29335463311362275, -236.8946393634874994 ) ) ;
#71373=CARTESIAN_POINT ( 'NONE',  ( 21.04116576186320842, 43.56632586560215259, -234.8146366772427029 ) ) ;
#71426=ORIENTED_EDGE ( 'NONE', *, *, #64693, .F. ) ;
#71434=VECTOR ( 'NONE', #80930, 1000.000000000000114 ) ;
#71437=FACE_OUTER_BOUND ( 'NONE', #1444, .T. ) ;
#71461=CARTESIAN_POINT ( 'NONE',  ( -21.64999999999999858, 52.95562111564758823, -234.1965973584252652 ) ) ;
#71468=FACE_OUTER_BOUND ( 'NONE', #104222, .T. ) ;
#71471=DIRECTION ( 'NONE',  ( 0.000000000000000000, -0.9126074666063660468, -0.4088369013363524762 ) ) ;
#71502=LINE ( 'NONE', #166761, #25082 ) ;
#71505=DIRECTION ( 'NONE',  ( 0.000000000000000000, -0.9126074666063771490, -0.4088369013363281623 ) ) ;
#71649=ORIENTED_EDGE ( 'NONE', *, *, #44948, .T. ) ;
#71671=CARTESIAN_POINT ( 'NONE',  ( -22.45354308602216165, 25.93539154016570691, -254.3551730728916311 ) ) ;
#71691=VERTEX_POINT ( 'NONE', #211796 ) ;
#71785=CARTESIAN_POINT ( 'NONE',  ( 19.75857864376268935, 54.48300931968434213, -228.8005724072070564 ) ) ;
#71926=DIRECTION ( 'NONE',  ( 1.000000000000000000, 0.000000000000000000, 0.000000000000000000 ) ) ;
#71950=ORIENTED_EDGE ( 'NONE', *, *, #215419, .T. ) ;
#71953=EDGE_CURVE ( 'NONE', #69371, #68201, #36389, .T. ) ;
#71997=EDGE_CURVE ( 'NONE', #24454, #208529, #244455, .T. ) ;
#72001=CIRCLE ( 'NONE', #105257, 0.09999999999999538425 ) ;
#72017=ORIENTED_EDGE ( 'NONE', *, *, #99272, .T. ) ;
#72103=DIRECTION ( 'NONE',  ( 0.000000000000000000, -0.2599159095383244966, 0.9656312546561787169 ) ) ;
#72111=SURFACE_STYLE_FILL_AREA ( #175098 ) ;
#72132=DIRECTION ( 'NONE',  ( 1.000000000000000000, -1.335000415235278971E-16, 2.979993593738921214E-16 ) ) ;
#72136=FACE_OUTER_BOUND ( 'NONE', #42043, .T. ) ;
#72178=FACE_OUTER_BOUND ( 'NONE', #88075, .T. ) ;
#72202=CIRCLE ( 'NONE', #217900, 0.09999999999999939493 ) ;
#72203=ORIENTED_EDGE ( 'NONE', *, *, #174534, .T. ) ;
#72215=ADVANCED_FACE ( 'NONE', ( #7510 ), #247393, .F. ) ;
#72253=LINE ( 'NONE', #95643, #256645 ) ;
#72268=DIRECTION ( 'NONE',  ( 0.000000000000000000, 0.9126074666063772600, 0.4088369013363274962 ) ) ;
#72272=AXIS2_PLACEMENT_3D ( 'NONE', #61958, #200184, #180618 ) ;
#72348=AXIS2_PLACEMENT_3D ( 'NONE', #233905, #133521, #214346 ) ;
#72390=EDGE_CURVE ( 'NONE', #111166, #25855, #177666, .T. ) ;
#72392=EDGE_CURVE ( 'NONE', #185818, #97895, #248694, .T. ) ;
#72394=CARTESIAN_POINT ( 'NONE',  ( -21.07954763557547651, 30.85583369947000421, -252.0786915620676325 ) ) ;
#72405=DIRECTION ( 'NONE',  ( -1.000000000000000000, -0.000000000000000000, 0.000000000000000000 ) ) ;
#72421=CARTESIAN_POINT ( 'NONE',  ( 20.94999999999999929, 46.45388641681647357, -243.1520440498138385 ) ) ;
#72470=CARTESIAN_POINT ( 'NONE',  ( -20.97625342178432817, 38.23914636359209851, -236.1324109475626187 ) ) ;
#72473=CIRCLE ( 'NONE', #93296, 0.5999999999999968692 ) ;
#72508=EDGE_CURVE ( 'NONE', #51580, #47266, #196409, .T. ) ;
#72547=AXIS2_PLACEMENT_3D ( 'NONE', #40220, #63596, #118461 ) ;
#72548=DIRECTION ( 'NONE',  ( 0.000000000000000000, 0.4088369013363281623, -0.9126074666063771490 ) ) ;
#72558=VERTEX_POINT ( 'NONE', #99851 ) ;
#72572=EDGE_LOOP ( 'NONE', ( #30102, #159717, #186017, #51117 ) ) ;
#72625=CARTESIAN_POINT ( 'NONE',  ( -23.25000000000000000, 68.11287320386161070, -224.1382462126928488 ) ) ;
#72633=CARTESIAN_POINT ( 'NONE',  ( -21.14999999999999858, 30.68987205111127281, -252.2252246220829193 ) ) ;
#72654=DIRECTION ( 'NONE',  ( -0.000000000000000000, 0.9126074666063770380, 0.4088369013363281068 ) ) ;
#72659=CARTESIAN_POINT ( 'NONE',  ( 21.46681500591742520, 33.85532080845636216, -243.2929468148404908 ) ) ;
#72665=DIRECTION ( 'NONE',  ( 0.000000000000000000, -0.9126074666063660468, -0.4088369013363524762 ) ) ;
#72680=EDGE_CURVE ( 'NONE', #69777, #24915, #104976, .T. ) ;
#72725=DIRECTION ( 'NONE',  ( -7.304098846218134667E-16, 0.4088369013363281068, -0.9126074666063770380 ) ) ;
#72755=DIRECTION ( 'NONE',  ( 7.304098846218134667E-16, 0.4088369013363281068, -0.9126074666063770380 ) ) ;
#72804=AXIS2_PLACEMENT_3D ( 'NONE', #142450, #85018, #6796 ) ;
#72812=DIRECTION ( 'NONE',  ( 0.000000000000000000, -0.4088369013363280513, 0.9126074666063769270 ) ) ;
#72841=DIRECTION ( 'NONE',  ( 0.000000000000000000, 0.8490545835447254053, 0.5283051335749948674 ) ) ;
#72855=AXIS2_PLACEMENT_3D ( 'NONE', #175785, #140473, #197884 ) ;
#72867=AXIS2_PLACEMENT_3D ( 'NONE', #75916, #57616, #135864 ) ;
#72885=EDGE_LOOP ( 'NONE', ( #170916, #91452, #247658, #157186, #81616 ) ) ;
#72945=CARTESIAN_POINT ( 'NONE',  ( -23.25000000000000000, 67.23127455305835554, -235.8551265064784559 ) ) ;
#72954=ORIENTED_EDGE ( 'NONE', *, *, #250921, .F. ) ;
#72967=CARTESIAN_POINT ( 'NONE',  ( 18.59999999999999787, 64.14105355761505223, -250.1147034356626193 ) ) ;
#72980=EDGE_LOOP ( 'NONE', ( #218372, #227498, #43448 ) ) ;
#72993=DIRECTION ( 'NONE',  ( -0.000000000000000000, 0.9126074666063770380, 0.4088369013363281068 ) ) ;
#73031=DIRECTION ( 'NONE',  ( 0.000000000000000000, -0.4088369013363783999, 0.9126074666063545004 ) ) ;
#73061=DIRECTION ( 'NONE',  ( 0.000000000000000000, 0.9126074666063774821, 0.4088369013363270521 ) ) ;
#73066=ORIENTED_EDGE ( 'NONE', *, *, #73873, .F. ) ;
#73128=CARTESIAN_POINT ( 'NONE',  ( -20.54999999999999716, 53.08776555244186568, -234.2469744149522626 ) ) ;
#73153=CARTESIAN_POINT ( 'NONE',  ( -20.85000000000000142, 74.93036000061670165, -233.6816308724374949 ) ) ;
#73154=VECTOR ( 'NONE', #222096, 1000.000000000000114 ) ;
#73161=CARTESIAN_POINT ( 'NONE',  ( -21.05000000000000426, 38.23914636435921466, -236.1324109481172968 ) ) ;
#73227=EDGE_CURVE ( 'NONE', #150102, #57757, #140568, .T. ) ;
#73242=PLANE ( 'NONE',  #192925 ) ;
#73265=ORIENTED_EDGE ( 'NONE', *, *, #224912, .F. ) ;
#73284=ORIENTED_EDGE ( 'NONE', *, *, #174325, .F. ) ;
#73299=ORIENTED_EDGE ( 'NONE', *, *, #50169, .F. ) ;
#73318=EDGE_CURVE ( 'NONE', #130629, #142489, #198842, .T. ) ;
#73321=CARTESIAN_POINT ( 'NONE',  ( 21.05000000000000071, 36.65892442174472876, -249.5511627012454596 ) ) ;
#73340=AXIS2_PLACEMENT_3D ( 'NONE', #118022, #77585, #18918 ) ;
#73356=DIRECTION ( 'NONE',  ( 0.000000000000000000, 0.4088369013363311599, -0.9126074666063757057 ) ) ;
#73359=FACE_OUTER_BOUND ( 'NONE', #47781, .T. ) ;
#73369=CARTESIAN_POINT ( 'NONE',  ( -23.15000000000000213, 31.89597452117651244, -238.9192857152811769 ) ) ;
#73438=EDGE_LOOP ( 'NONE', ( #200582, #226461, #21252, #212897 ) ) ;
#73455=AXIS2_PLACEMENT_3D ( 'NONE', #129006, #130265, #52006 ) ;
#73466=EDGE_CURVE ( 'NONE', #132466, #186768, #23908, .T. ) ;
#73484=CARTESIAN_POINT ( 'NONE',  ( -20.00857864376270001, 52.31097543990284038, -232.5130202284001371 ) ) ;
#73490=ORIENTED_EDGE ( 'NONE', *, *, #251535, .F. ) ;
#73547=EDGE_CURVE ( 'NONE', #45859, #200649, #192950, .T. ) ;
#73556=SPHERICAL_SURFACE ( 'NONE', #164292, 0.1000000000000000056 ) ;
#73561=EDGE_LOOP ( 'NONE', ( #14712, #234322, #45990, #189799 ) ) ;
#73563=EDGE_LOOP ( 'NONE', ( #99448, #194916, #103238, #258070 ) ) ;
#73568=VERTEX_POINT ( 'NONE', #215068 ) ;
#73589=VERTEX_POINT ( 'NONE', #255426 ) ;
#73597=DIRECTION ( 'NONE',  ( -7.304098846218134667E-16, 0.4088369013363281068, -0.9126074666063770380 ) ) ;
#73612=EDGE_CURVE ( 'NONE', #133691, #179534, #244804, .T. ) ;
#73624=DIRECTION ( 'NONE',  ( -4.408576920032448588E-17, 0.8490545835447252943, 0.5283051335749948674 ) ) ;
#73642=CIRCLE ( 'NONE', #36231, 4.000000000000002665 ) ;
#73685=ADVANCED_FACE ( 'NONE', ( #201929 ), #164087, .F. ) ;
#73689=CARTESIAN_POINT ( 'NONE',  ( -21.14999999999999858, 30.68987205111127636, -252.2252246220829193 ) ) ;
#73696=AXIS2_PLACEMENT_3D ( 'NONE', #212045, #76346, #249869 ) ;
#73712=ORIENTED_EDGE ( 'NONE', *, *, #14035, .F. ) ;
#73726=VECTOR ( 'NONE', #149455, 1000.000000000000114 ) ;
#73742=ORIENTED_EDGE ( 'NONE', *, *, #196385, .F. ) ;
#73745=CARTESIAN_POINT ( 'NONE',  ( 23.14999999999998437, 31.85509083104287598, -238.8280249686205536 ) ) ;
#73762=AXIS2_PLACEMENT_3D ( 'NONE', #120356, #104572, #221949 ) ;
#73765=FACE_OUTER_BOUND ( 'NONE', #63590, .T. ) ;
#73804=CARTESIAN_POINT ( 'NONE',  ( -20.94999999999999929, 48.04585786805223080, -246.4610531646956417 ) ) ;
#73818=LINE ( 'NONE', #50344, #204455 ) ;
#73829=DIRECTION ( 'NONE',  ( 1.000000000000000000, 0.000000000000000000, 0.000000000000000000 ) ) ;
#73840=ORIENTED_EDGE ( 'NONE', *, *, #18487, .F. ) ;
#73844=EDGE_CURVE ( 'NONE', #37194, #241978, #186218, .T. ) ;
#73850=CARTESIAN_POINT ( 'NONE',  ( 20.94999999999999929, 54.26566224370346703, -236.3486064386993633 ) ) ;
#73852=EDGE_CURVE ( 'NONE', #200814, #99245, #226093, .T. ) ;
#73855=CARTESIAN_POINT ( 'NONE',  ( 21.05000000000000071, 30.84076144264166786, -252.2514173861790709 ) ) ;
#73871=DIRECTION ( 'NONE',  ( 3.265361837132813093E-16, 0.4088369013363281068, -0.9126074666063770380 ) ) ;
#73873=EDGE_CURVE ( 'NONE', #217763, #236784, #103157, .T. ) ;
#73876=DIRECTION ( 'NONE',  ( 0.000000000000000000, 0.2868887416115947775, -0.9579639084728169829 ) ) ;
#73896=DIRECTION ( 'NONE',  ( 0.000000000000000000, 0.9126074666063772600, 0.4088369013363274962 ) ) ;
#73899=AXIS2_PLACEMENT_3D ( 'NONE', #163430, #146402, #246801 ) ;
#73903=CARTESIAN_POINT ( 'NONE',  ( -21.22070241538126112, 33.92349738987645935, -243.6870831740097003 ) ) ;
#73930=DIRECTION ( 'NONE',  ( 0.000000000000000000, 0.9126074666063660468, 0.4088369013363524762 ) ) ;
#73946=VECTOR ( 'NONE', #15188, 1000.000000000000000 ) ;
#73973=DIRECTION ( 'NONE',  ( 1.000000000000000000, 0.000000000000000000, 0.000000000000000000 ) ) ;
#73989=B_SPLINE_CURVE_WITH_KNOTS ( 'NONE', 3,
 ( #69297, #148831, #147533, #247908, #110976, #87539, #27626, #49716, #129257, #130527, #48423, #207524, #108412, #28921, #189235, #30176, #210089, #228363, #131815 ),
 .UNSPECIFIED., .F., .F.,
 ( 4, 3, 3, 3, 3, 3, 4 ),
 ( 0.000000000000000000, 2.646747978908489188E-05, 5.271166642128679745E-05, 9.008788829884017187E-05, 0.0001426648776561119315, 0.0001897378458659873231, 0.0001917382627806427315 ),
 .UNSPECIFIED. ) ;
#73998=DIRECTION ( 'NONE',  ( 0.000000000000000000, 0.9126074666063775931, 0.4088369013363268301 ) ) ;
#74002=EDGE_CURVE ( 'NONE', #118767, #99245, #128477, .T. ) ;
#74020=EDGE_CURVE ( 'NONE', #168498, #131079, #130280, .T. ) ;
#74038=ORIENTED_EDGE ( 'NONE', *, *, #165133, .T. ) ;
#74047=DIRECTION ( 'NONE',  ( 0.000000000000000000, 0.2716869542551192951, -0.9623856809447951521 ) ) ;
#74053=ADVANCED_FACE ( 'NONE', ( #123047 ), #44790, .F. ) ;
#74059=DIRECTION ( 'NONE',  ( 2.952720810173288619E-16, 0.4088369013363286064, -0.9126074666063768159 ) ) ;
#74068=TOROIDAL_SURFACE ( 'NONE', #174027, 0.6000000000000017542, 0.1000000000000000056 ) ;
#74073=CIRCLE ( 'NONE', #165828, 0.1000000000000024342 ) ;
#74101=CARTESIAN_POINT ( 'NONE',  ( -20.54999999999999716, 62.08591502004791352, -248.5699171172615820 ) ) ;
#74119=DIRECTION ( 'NONE',  ( -1.000000000000000000, 1.207181226542539700E-16, -2.694675058168174199E-16 ) ) ;
#74169=ORIENTED_EDGE ( 'NONE', *, *, #226259, .T. ) ;
#74189=VECTOR ( 'NONE', #228922, 1000.000000000000000 ) ;
#74220=CIRCLE ( 'NONE', #219923, 0.1000000000000024342 ) ;
#74261=CARTESIAN_POINT ( 'NONE',  ( 21.05000000000000071, 45.02833974712562792, -238.5149546970766892 ) ) ;
#74292=ADVANCED_FACE ( 'NONE', ( #142156, #28684 ), #9069, .F. ) ;
#74293=VERTEX_POINT ( 'NONE', #5185 ) ;
#74315=CARTESIAN_POINT ( 'NONE',  ( -20.54999999999999716, 47.48953316408024961, -242.5895867826444601 ) ) ;
#74324=ORIENTED_EDGE ( 'NONE', *, *, #109274, .T. ) ;
#74346=CARTESIAN_POINT ( 'NONE',  ( 20.94999999999999929, 39.26973050389061370, -236.6309188891183055 ) ) ;
#74365=VECTOR ( 'NONE', #145899, 1000.000000000000114 ) ;
#74407=EDGE_LOOP ( 'NONE', ( #156490, #201017, #116115 ) ) ;
#74413=DIRECTION ( 'NONE',  ( 1.000000000000000000, -7.510212038922846022E-17, 1.676432719286211941E-16 ) ) ;
#74421=CARTESIAN_POINT ( 'NONE',  ( -20.94999999999999929, 67.84340367245323478, -228.0791829662263410 ) ) ;
#74469=CYLINDRICAL_SURFACE ( 'NONE', #149026, 0.09999999999999609201 ) ;
#74471=CARTESIAN_POINT ( 'NONE',  ( -21.05000000000000071, 30.90801580390628800, -252.0203440857197279 ) ) ;
#74488=ADVANCED_FACE ( 'NONE', ( #199265 ), #255322, .T. ) ;
#74526=EDGE_CURVE ( 'NONE', #217944, #68201, #182861, .T. ) ;
#74597=ADVANCED_FACE ( 'NONE', ( #202410 ), #32849, .T. ) ;
#74626=CIRCLE ( 'NONE', #253446, 0.1000000000000024342 ) ;
#74663=CARTESIAN_POINT ( 'NONE',  ( 18.41356215285960474, 46.96039402156211651, -255.3459641718773128 ) ) ;
#74665=DIRECTION ( 'NONE',  ( 0.000000000000000000, 0.9126074666063771490, 0.4088369013363281623 ) ) ;
#74681=AXIS2_PLACEMENT_3D ( 'NONE', #146430, #246827, #132026 ) ;
#74684=ORIENTED_EDGE ( 'NONE', *, *, #100841, .T. ) ;
#74715=CARTESIAN_POINT ( 'NONE',  ( 18.52928932304301668, 54.97610475762002835, -230.0816435235718131 ) ) ;
#74722=CARTESIAN_POINT ( 'NONE',  ( -21.05000000000000071, 56.06656052939784729, -228.0911609752645290 ) ) ;
#74738=CARTESIAN_POINT ( 'NONE',  ( -18.59999999999999787, 51.24799949642838470, -230.1402408152235637 ) ) ;
#74751=AXIS2_PLACEMENT_3D ( 'NONE', #108046, #71505, #151025 ) ;
#74776=ORIENTED_EDGE ( 'NONE', *, *, #32853, .T. ) ;
#74788=CARTESIAN_POINT ( 'NONE',  ( 18.59999999999999076, 53.41483507351092896, -234.9770603882373337 ) ) ;
#74802=CARTESIAN_POINT ( 'NONE',  ( -20.94999999999999929, 69.06797323185276127, -247.4100621602722470 ) ) ;
#74821=DIRECTION ( 'NONE',  ( 0.000000000000000000, -0.9126074666063844765, -0.4088369013363114535 ) ) ;
#74831=AXIS2_PLACEMENT_3D ( 'NONE', #192008, #13354, #129439 ) ;
#74832=CARTESIAN_POINT ( 'NONE',  ( -21.05000000000000071, 46.50671693017397246, -243.2369495081682942 ) ) ;
#74850=ORIENTED_EDGE ( 'NONE', *, *, #200035, .T. ) ;
#74869=VERTEX_POINT ( 'NONE', #85974 ) ;
#74874=ORIENTED_EDGE ( 'NONE', *, *, #194208, .F. ) ;
#74878=VERTEX_POINT ( 'NONE', #48156 ) ;
#74900=VERTEX_POINT ( 'NONE', #5153 ) ;
#74922=DIRECTION ( 'NONE',  ( 0.000000000000000000, -0.9126074666063770380, -0.4088369013363281068 ) ) ;
#74966=CARTESIAN_POINT ( 'NONE',  ( -20.94999999999999929, 67.65035251205981126, -227.9627438638999877 ) ) ;
#74987=ORIENTED_EDGE ( 'NONE', *, *, #155446, .F. ) ;
#75074=AXIS2_PLACEMENT_3D ( 'NONE', #203735, #27706, #245441 ) ;
#75154=TOROIDAL_SURFACE ( 'NONE', #208235, 7.800000000000000711, 0.1000000000000000056 ) ;
#75179=CARTESIAN_POINT ( 'NONE',  ( -21.78635804494510708, 33.69213361928919426, -243.1708424215785271 ) ) ;
#75190=ORIENTED_EDGE ( 'NONE', *, *, #236922, .F. ) ;
#75224=CARTESIAN_POINT ( 'NONE',  ( 21.07928932188134397, 33.98134083355422774, -243.8161431329846778 ) ) ;
#75230=ORIENTED_EDGE ( 'NONE', *, *, #213526, .T. ) ;
#75231=CARTESIAN_POINT ( 'NONE',  ( 22.47071067811866740, 33.41224047107335338, -242.5462774987836667 ) ) ;
#75233=EDGE_LOOP ( 'NONE', ( #168213, #38119, #213500, #203730 ) ) ;
#75240=CARTESIAN_POINT ( 'NONE',  ( 21.07189867249812210, 43.41933109301616156, -234.7705648221715933 ) ) ;
#75246=CARTESIAN_POINT ( 'NONE',  ( 20.97107704358301916, 40.84128431181879648, -237.9521109762849846 ) ) ;
#75249=VERTEX_POINT ( 'NONE', #225178 ) ;
#75279=TOROIDAL_SURFACE ( 'NONE', #196058, 4.099999999999999645, 0.1000000000000000056 ) ;
#75297=CARTESIAN_POINT ( 'NONE',  ( 23.15000000000000213, 62.08591502004790641, -248.5699171172615820 ) ) ;
#75298=ORIENTED_EDGE ( 'NONE', *, *, #82243, .F. ) ;
#75348=CARTESIAN_POINT ( 'NONE',  ( -23.25000000000000000, 74.83412143252222393, -233.7087995678629966 ) ) ;
#75357=DIRECTION ( 'NONE',  ( 1.000000000000000000, 0.000000000000000000, 0.000000000000000000 ) ) ;
#75359=ADVANCED_FACE ( 'NONE', ( #213019 ), #199783, .F. ) ;
#75392=FACE_OUTER_BOUND ( 'NONE', #200192, .T. ) ;
#75403=VECTOR ( 'NONE', #240887, 1000.000000000000114 ) ;
#75411=AXIS2_PLACEMENT_3D ( 'NONE', #217331, #197784, #199078 ) ;
#75432=ORIENTED_EDGE ( 'NONE', *, *, #78505, .F. ) ;
#75433=EDGE_LOOP ( 'NONE', ( #92386, #153761, #2985, #156093 ) ) ;
#75441=DIRECTION ( 'NONE',  ( -1.000000000000000000, 0.000000000000000000, 0.000000000000000000 ) ) ;
#75447=ORIENTED_EDGE ( 'NONE', *, *, #965, .F. ) ;
#75448=DIRECTION ( 'NONE',  ( 0.000000000000000000, 0.9126074666063660468, 0.4088369013363524762 ) ) ;
#75501=AXIS2_PLACEMENT_3D ( 'NONE', #55769, #96208, #214879 ) ;
#75524=ORIENTED_EDGE ( 'NONE', *, *, #250129, .T. ) ;
#75566=CYLINDRICAL_SURFACE ( 'NONE', #53871, 0.1000000000000024342 ) ;
#75577=EDGE_LOOP ( 'NONE', ( #204099, #223180, #257708, #218708 ) ) ;
#75578=VECTOR ( 'NONE', #217060, 1000.000000000000114 ) ;
#75608=DIRECTION ( 'NONE',  ( 1.000000000000000000, -1.335000415235278971E-16, 2.979993593738921214E-16 ) ) ;
#75646=ADVANCED_FACE ( 'NONE', ( #145029 ), #146315, .F. ) ;
#75652=AXIS2_PLACEMENT_3D ( 'NONE', #19561, #93945, #253016 ) ;
#75660=ADVANCED_FACE ( 'NONE', ( #87617 ), #158292, .F. ) ;
#75672=ORIENTED_EDGE ( 'NONE', *, *, #147739, .T. ) ;
#75681=DIRECTION ( 'NONE',  ( -1.000000000000000000, 0.000000000000000000, 0.000000000000000000 ) ) ;
#75685=CARTESIAN_POINT ( 'NONE',  ( -18.60000000000000142, 47.07326788871597500, -255.0992659944397758 ) ) ;
#75688=VERTEX_POINT ( 'NONE', #186756 ) ;
#75702=DIRECTION ( 'NONE',  ( 0.000000000000000000, 0.9090645160163607352, 0.4166553800443956734 ) ) ;
#75705=EDGE_LOOP ( 'NONE', ( #207923, #160529, #151467, #24540 ) ) ;
#75715=CYLINDRICAL_SURFACE ( 'NONE', #54154, 0.8750000000000007772 ) ;
#75761=DIRECTION ( 'NONE',  ( 0.000000000000000000, 0.9126074666063765939, 0.4088369013363289950 ) ) ;
#75766=CARTESIAN_POINT ( 'NONE',  ( 23.14999999999999503, 43.07541598710462694, -233.9110336739111347 ) ) ;
#75767=VECTOR ( 'NONE', #225643, 1000.000000000000000 ) ;
#75771=CARTESIAN_POINT ( 'NONE',  ( -23.15000000000000213, 48.40874555430183079, -244.2873875965402704 ) ) ;
#75785=CARTESIAN_POINT ( 'NONE',  ( 18.59999999999999787, 36.65892442174472876, -249.5511627012454596 ) ) ;
#75801=EDGE_LOOP ( 'NONE', ( #5319, #140102, #197650, #193972 ) ) ;
#75852=ADVANCED_FACE ( 'NONE', ( #253116 ), #155354, .T. ) ;
#75853=CARTESIAN_POINT ( 'NONE',  ( -21.05000000000000071, 67.23127455305835554, -235.8551265064784559 ) ) ;
#75908=CARTESIAN_POINT ( 'NONE',  ( 21.14999999999999858, 52.64219947837469959, -255.2660483925003803 ) ) ;
#75912=DIRECTION ( 'NONE',  ( 1.000000000000000000, 0.000000000000000000, 0.000000000000000000 ) ) ;
#75916=CARTESIAN_POINT ( 'NONE',  ( -20.94999999999999929, 36.65892442174472876, -249.5511627012454596 ) ) ;
#75921=ADVANCED_FACE ( 'NONE', ( #1359 ), #179306, .T. ) ;
#75952=( NAMED_UNIT ( * ) SI_UNIT ( $, .STERADIAN. ) SOLID_ANGLE_UNIT ( ) );
#75968=CARTESIAN_POINT ( 'NONE',  ( -23.25000000000000000, 48.79765034352288922, -253.5326144460178170 ) ) ;
#75974=CARTESIAN_POINT ( 'NONE',  ( 20.94999999999999929, 56.45527679911575802, -225.2871936083021467 ) ) ;
#75981=CARTESIAN_POINT ( 'NONE',  ( -18.59999999999999787, 67.65998959290219261, -227.8609496483021530 ) ) ;
#75982=ADVANCED_FACE ( 'NONE', ( #200864 ), #54371, .T. ) ;
#75985=DIRECTION ( 'NONE',  ( 0.000000000000000000, -0.4088369013363276072, 0.9126074666063773710 ) ) ;
#76006=VERTEX_POINT ( 'NONE', #176187 ) ;
#76018=DIRECTION ( 'NONE',  ( 0.000000000000000000, -0.9126074666063769270, -0.4088369013363280513 ) ) ;
#76021=ORIENTED_EDGE ( 'NONE', *, *, #246861, .F. ) ;
#76106=EDGE_CURVE ( 'NONE', #108295, #228170, #63924, .T. ) ;
#76119=FACE_OUTER_BOUND ( 'NONE', #188553, .T. ) ;
#76128=CARTESIAN_POINT ( 'NONE',  ( -22.50000000000000000, 30.95512775545487472, -252.1063933345974988 ) ) ;
#76157=CARTESIAN_POINT ( 'NONE',  ( 22.50000000000000000, 33.38250548509083870, -242.4821227592188961 ) ) ;
#76180=ORIENTED_EDGE ( 'NONE', *, *, #185438, .T. ) ;
#76184=CARTESIAN_POINT ( 'NONE',  ( -18.59999999999999787, 38.29773864426885410, -236.0513742605307925 ) ) ;
#76186=CARTESIAN_POINT ( 'NONE',  ( 20.95512820512820440, 40.84069494668059264, -237.9516373772122222 ) ) ;
#76192=DIRECTION ( 'NONE',  ( 0.000000000000000000, 0.5407049257165758016, -0.8412123295017925884 ) ) ;
#76193=ADVANCED_FACE ( 'NONE', ( #52036 ), #32534, .F. ) ;
#76256=ADVANCED_FACE ( 'NONE', ( #214975 ), #29650, .T. ) ;
#76291=DIRECTION ( 'NONE',  ( 0.000000000000000000, -0.2818822000686205809, 0.9594490217226104845 ) ) ;
#76296=DIRECTION ( 'NONE',  ( 0.000000000000000000, -0.4088369013363281623, 0.9126074666063771490 ) ) ;
#76322=ADVANCED_FACE ( 'NONE', ( #83127 ), #208714, .T. ) ;
#76346=DIRECTION ( 'NONE',  ( 1.000000000000000000, -2.986185139342066440E-16, 6.665775143889693760E-16 ) ) ;
#76372=CARTESIAN_POINT ( 'NONE',  ( 21.05000000000000071, 30.78786553159818951, -252.2909008153935133 ) ) ;
#76388=CARTESIAN_POINT ( 'NONE',  ( -21.05000000000000071, 44.58277672189309015, -247.4925639031954745 ) ) ;
#76397=AXIS2_PLACEMENT_3D ( 'NONE', #76128, #17441, #176540 ) ;
#76406=PLANE ( 'NONE',  #64286 ) ;
#76422=EDGE_CURVE ( 'NONE', #172262, #60290, #104596, .T. ) ;
#76463=CIRCLE ( 'NONE', #255493, 11.79999999999999893 ) ;
#76487=CARTESIAN_POINT ( 'NONE',  ( -21.07094088545304800, 33.98475570745946328, -243.8237622992367051 ) ) ;
#76519=FACE_OUTER_BOUND ( 'NONE', #237945, .T. ) ;
#76520=DIRECTION ( 'NONE',  ( 1.000000000000000000, 0.000000000000000000, 0.000000000000000000 ) ) ;
#76530=VECTOR ( 'NONE', #77972, 1000.000000000000000 ) ;
#76553=EDGE_CURVE ( 'NONE', #55598, #10735, #179660, .T. ) ;
#76577=DIRECTION ( 'NONE',  ( 0.000000000000000000, 0.9126074666063660468, 0.4088369013363524762 ) ) ;
#76596=CARTESIAN_POINT ( 'NONE',  ( -23.15000000000000213, 55.49311008795314137, -234.6486875357297492 ) ) ;
#76624=CARTESIAN_POINT ( 'NONE',  ( 20.94999999999999929, 56.27731819600170837, -227.9967441372480437 ) ) ;
#76676=CIRCLE ( 'NONE', #1655, 0.09999999999999939493 ) ;
#76692=CIRCLE ( 'NONE', #172426, 0.1000000000000024342 ) ;
#76711=FACE_OUTER_BOUND ( 'NONE', #173383, .T. ) ;
#76719=DIRECTION ( 'NONE',  ( 1.000000000000000000, 0.000000000000000000, 0.000000000000000000 ) ) ;
#76757=ADVANCED_FACE ( 'NONE', ( #181970 ), #243207, .T. ) ;
#76764=ORIENTED_EDGE ( 'NONE', *, *, #222134, .F. ) ;
#76799=DIRECTION ( 'NONE',  ( 0.000000000000000000, 0.9126074666063769270, 0.4088369013363283844 ) ) ;
#76813=DIRECTION ( 'NONE',  ( 1.000000000000000000, 0.000000000000000000, 0.000000000000000000 ) ) ;
#76822=DIRECTION ( 'NONE',  ( 1.000000000000000000, 0.000000000000000000, 0.000000000000000000 ) ) ;
#76836=CARTESIAN_POINT ( 'NONE',  ( -20.94788355080264353, 68.02921119886117651, -224.2090419302654141 ) ) ;
#76855=ORIENTED_EDGE ( 'NONE', *, *, #145025, .T. ) ;
#76961=DIRECTION ( 'NONE',  ( -1.000000000000000000, -0.000000000000000000, 0.000000000000000000 ) ) ;
#76972=CIRCLE ( 'NONE', #110292, 0.1000000000000024342 ) ;
#77006=AXIS2_PLACEMENT_3D ( 'NONE', #40629, #57559, #219209 ) ;
#77010=DIRECTION ( 'NONE',  ( 0.000000000000000000, 0.9126074666063770380, 0.4088369013363281068 ) ) ;
#77056=ORIENTED_EDGE ( 'NONE', *, *, #5513, .T. ) ;
#77057=DIRECTION ( 'NONE',  ( 1.000000000000000000, 0.000000000000000000, 0.000000000000000000 ) ) ;
#77081=ORIENTED_EDGE ( 'NONE', *, *, #230704, .T. ) ;
#77087=CIRCLE ( 'NONE', #193805, 0.09999999999999939493 ) ;
#77097=EDGE_CURVE ( 'NONE', #39261, #197319, #48244, .T. ) ;
#77117=AXIS2_PLACEMENT_3D ( 'NONE', #168531, #70696, #130635 ) ;
#77121=ORIENTED_EDGE ( 'NONE', *, *, #178101, .F. ) ;
#77135=VERTEX_POINT ( 'NONE', #108227 ) ;
#77150=ORIENTED_EDGE ( 'NONE', *, *, #206192, .T. ) ;
#77152=CIRCLE ( 'NONE', #18887, 7.899999999999995914 ) ;
#77178=CARTESIAN_POINT ( 'NONE',  ( -18.59999999999999787, 67.23127455305835554, -235.8551265064784559 ) ) ;
#77207=ORIENTED_EDGE ( 'NONE', *, *, #83085, .F. ) ;
#77249=CYLINDRICAL_SURFACE ( 'NONE', #211391, 0.1000000000000024342 ) ;
#77251=FACE_OUTER_BOUND ( 'NONE', #58133, .T. ) ;
#77252=DIRECTION ( 'NONE',  ( -1.000000000000000000, -0.000000000000000000, 0.000000000000000000 ) ) ;
#77253=CARTESIAN_POINT ( 'NONE',  ( 19.75857864376268935, 54.53338637621133955, -228.6684279704127789 ) ) ;
#77289=ORIENTED_EDGE ( 'NONE', *, *, #180201, .F. ) ;
#77334=VECTOR ( 'NONE', #149387, 1000.000000000000000 ) ;
#77338=DIRECTION ( 'NONE',  ( 0.000000000000000000, 0.9126074666063660468, 0.4088369013363524762 ) ) ;
#77407=ORIENTED_EDGE ( 'NONE', *, *, #125890, .F. ) ;
#77428=CARTESIAN_POINT ( 'NONE',  ( 21.05995757104869526, 44.20038294471087426, -236.5569497315613035 ) ) ;
#77457=DIRECTION ( 'NONE',  ( 0.000000000000000000, -0.1022405907414164900, -0.9947597004326451664 ) ) ;
#77490=CARTESIAN_POINT ( 'NONE',  ( -18.39999999999999858, 77.26488334054519669, -241.9697969554615611 ) ) ;
#77564=DIRECTION ( 'NONE',  ( 0.000000000000000000, 0.4088369013363281068, -0.9126074666063770380 ) ) ;
#77573=CARTESIAN_POINT ( 'NONE',  ( -20.54999999999999716, 44.91518204311810081, -238.0177672736398620 ) ) ;
#77577=EDGE_CURVE ( 'NONE', #43171, #258063, #143167, .T. ) ;
#77585=DIRECTION ( 'NONE',  ( 2.840903330521633255E-16, -0.09425075112713275638, -0.9955484899852801162 ) ) ;
#77618=CARTESIAN_POINT ( 'NONE',  ( -18.50000000000000000, 44.14788529697245423, -236.0604079036328073 ) ) ;
#77619=ADVANCED_FACE ( 'NONE', ( #92188 ), #126349, .F. ) ;
#77653=ADVANCED_FACE ( 'NONE', ( #12689 ), #191114, .F. ) ;
#77695=CARTESIAN_POINT ( 'NONE',  ( -21.05000000000000071, 69.28189128378591022, -247.5258150475912089 ) ) ;
#77699=LINE ( 'NONE', #121986, #88685 ) ;
#77711=ORIENTED_EDGE ( 'NONE', *, *, #237052, .F. ) ;
#77722=EDGE_CURVE ( 'NONE', #226018, #83103, #176036, .T. ) ;
#77730=FACE_OUTER_BOUND ( 'NONE', #136338, .T. ) ;
#77755=ORIENTED_EDGE ( 'NONE', *, *, #198498, .T. ) ;
#77771=LINE ( 'NONE', #119498, #106102 ) ;
#77795=CARTESIAN_POINT ( 'NONE',  ( -22.50000000000000000, 36.65892442174472876, -249.5511627012454596 ) ) ;
#77806=AXIS2_PLACEMENT_3D ( 'NONE', #49911, #190747, #231150 ) ;
#77814=CARTESIAN_POINT ( 'NONE',  ( -23.15000000000000213, 61.88149656937975607, -248.1136133839584090 ) ) ;
#77832=LINE ( 'NONE', #40038, #255119 ) ;
#77834=VERTEX_POINT ( 'NONE', #252107 ) ;
#77860=CARTESIAN_POINT ( 'NONE',  ( -20.54999999999999716, 61.88149656937975607, -248.1136133839584090 ) ) ;
#77864=LINE ( 'NONE', #75348, #930 ) ;
#77883=AXIS2_PLACEMENT_3D ( 'NONE', #4944, #122368, #158949 ) ;
#77920=DIRECTION ( 'NONE',  ( 1.000000000000000000, 0.000000000000000000, 0.000000000000000000 ) ) ;
#77935=CARTESIAN_POINT ( 'NONE',  ( -18.59999999999999787, 67.85125148167622910, -227.9794913823769491 ) ) ;
#77958=CIRCLE ( 'NONE', #219611, 0.1000000000000024342 ) ;
#77963=ORIENTED_EDGE ( 'NONE', *, *, #160054, .T. ) ;
#77972=DIRECTION ( 'NONE',  ( -1.000000000000000000, -0.000000000000000000, -0.000000000000000000 ) ) ;
#77980=LINE ( 'NONE', #57119, #185608 ) ;
#78000=AXIS2_PLACEMENT_3D ( 'NONE', #26150, #108248, #226898 ) ;
#78103=EDGE_CURVE ( 'NONE', #232311, #52763, #134471, .T. ) ;
#78110=CARTESIAN_POINT ( 'NONE',  ( 23.14999999999999858, 68.08983204586465376, -237.7716021863518563 ) ) ;
#78129=ORIENTED_EDGE ( 'NONE', *, *, #101447, .T. ) ;
#78185=DIRECTION ( 'NONE',  ( 0.000000000000000000, 0.9126074666063850316, 0.4088369013363101212 ) ) ;
#78203=CIRCLE ( 'NONE', #165723, 0.09999999999999939493 ) ;
#78213=DIRECTION ( 'NONE',  ( 2.952720810173289112E-16, 0.4088369013363281068, -0.9126074666063770380 ) ) ;
#78220=ADVANCED_FACE ( 'NONE', ( #197414 ), #98279, .T. ) ;
#78230=ADVANCED_FACE ( 'NONE', ( #223387 ), #224676, .T. ) ;
#78249=CARTESIAN_POINT ( 'NONE',  ( 20.94999999999999574, 56.21213088740040575, -228.0580413555848338 ) ) ;
#78286=EDGE_CURVE ( 'NONE', #245440, #65298, #205103, .T. ) ;
#78288=DIRECTION ( 'NONE',  ( 1.000000000000000000, 0.000000000000000000, 0.000000000000000000 ) ) ;
#78289=CARTESIAN_POINT ( 'NONE',  ( -23.15000000000000213, 54.92280082623103965, -239.2759596675668092 ) ) ;
#78297=DIRECTION ( 'NONE',  ( 0.000000000000000000, -0.4088369013363783999, 0.9126074666063545004 ) ) ;
#78310=ORIENTED_EDGE ( 'NONE', *, *, #106205, .T. ) ;
#78313=CARTESIAN_POINT ( 'NONE',  ( -23.25000000000000000, 74.86109765932731364, -233.8067614591677454 ) ) ;
#78324=CARTESIAN_POINT ( 'NONE',  ( -23.15000000000000213, 67.23127455305835554, -235.8551265064784559 ) ) ;
#78329=DIRECTION ( 'NONE',  ( 1.000000000000000000, 0.000000000000000000, 0.000000000000000000 ) ) ;
#78362=AXIS2_PLACEMENT_3D ( 'NONE', #188123, #167302, #48604 ) ;
#78381=AXIS2_PLACEMENT_3D ( 'NONE', #53330, #33814, #18047 ) ;
#78442=DIRECTION ( 'NONE',  ( 0.000000000000000000, -0.9126074666063773710, -0.4088369013363271631 ) ) ;
#78465=AXIS2_PLACEMENT_3D ( 'NONE', #252215, #73624, #116573 ) ;
#78473=CARTESIAN_POINT ( 'NONE',  ( 18.59999999999999076, 43.63140573099096287, -239.9077968784524444 ) ) ;
#78488=DIRECTION ( 'NONE',  ( -1.000000000000000000, 0.000000000000000000, 0.000000000000000000 ) ) ;
#78504=DIRECTION ( 'NONE',  ( 0.000000000000000000, 0.9126074666063770380, 0.4088369013363281068 ) ) ;
#78505=EDGE_CURVE ( 'NONE', #182894, #221888, #222123, .T. ) ;
#78513=DIRECTION ( 'NONE',  ( 0.000000000000000000, 0.9126074666063769270, 0.4088369013363280513 ) ) ;
#78566=CYLINDRICAL_SURFACE ( 'NONE', #47551, 12.87500000000000533 ) ;
#78569=VERTEX_POINT ( 'NONE', #21085 ) ;
#78572=AXIS2_PLACEMENT_3D ( 'NONE', #58925, #258, #156810 ) ;
#78581=FACE_OUTER_BOUND ( 'NONE', #215075, .T. ) ;
#78609=ORIENTED_EDGE ( 'NONE', *, *, #113244, .T. ) ;
#78662=ORIENTED_EDGE ( 'NONE', *, *, #52501, .T. ) ;
#78666=CARTESIAN_POINT ( 'NONE',  ( -20.94999999999999929, 46.45388641681647357, -243.1520440498138385 ) ) ;
#78684=ORIENTED_EDGE ( 'NONE', *, *, #155743, .F. ) ;
#78687=ORIENTED_EDGE ( 'NONE', *, *, #206140, .T. ) ;
#78716=DIRECTION ( 'NONE',  ( 0.000000000000000000, -0.9594490217226103734, -0.2818822000686205254 ) ) ;
#78740=EDGE_CURVE ( 'NONE', #148485, #181336, #152593, .T. ) ;
#78755=CARTESIAN_POINT ( 'NONE',  ( -21.05000000000000426, 34.11487388478676053, -243.6629159006578504 ) ) ;
#78810=CIRCLE ( 'NONE', #70513, 11.90000000000001101 ) ;
#78827=DIRECTION ( 'NONE',  ( 0.000000000000000000, 0.9126074666063772600, 0.4088369013363274407 ) ) ;
#78833=CARTESIAN_POINT ( 'NONE',  ( 20.12500000000000000, 52.06567329910104291, -231.9654557484363409 ) ) ;
#78851=EDGE_CURVE ( 'NONE', #32455, #212713, #252322, .T. ) ;
#78867=CARTESIAN_POINT ( 'NONE',  ( -20.54999999999999716, 62.24653955602229871, -247.9500786234238490 ) ) ;
#78891=AXIS2_PLACEMENT_3D ( 'NONE', #217410, #19228, #233170 ) ;
#78913=CIRCLE ( 'NONE', #199774, 0.09999999999999939493 ) ;
#78937=ORIENTED_EDGE ( 'NONE', *, *, #51230, .F. ) ;
#78948=VERTEX_POINT ( 'NONE', #123380 ) ;
#79014=VERTEX_POINT ( 'NONE', #124666 ) ;
#79021=EDGE_CURVE ( 'NONE', #250431, #25855, #180791, .T. ) ;
#79035=CARTESIAN_POINT ( 'NONE',  ( 20.75572585718203911, 40.78216703416070033, -237.9711013405598692 ) ) ;
#79059=ORIENTED_EDGE ( 'NONE', *, *, #45494, .T. ) ;
#79062=ADVANCED_FACE ( 'NONE', ( #48964 ), #2530, .F. ) ;
#79064=CIRCLE ( 'NONE', #87457, 0.09999999999999063804 ) ;
#79102=DIRECTION ( 'NONE',  ( -1.000000000000000000, -0.000000000000000000, -0.000000000000000000 ) ) ;
#79110=CARTESIAN_POINT ( 'NONE',  ( 20.94999999999999929, 67.23127455305835554, -235.8551265064784559 ) ) ;
#79127=EDGE_CURVE ( 'NONE', #56338, #164531, #89364, .T. ) ;
#79135=EDGE_CURVE ( 'NONE', #168895, #57327, #111515, .T. ) ;
#79161=CARTESIAN_POINT ( 'NONE',  ( -18.50000000000000000, 47.16152503674118890, -255.1462838189583806 ) ) ;
#79169=VERTEX_POINT ( 'NONE', #112802 ) ;
#79170=CARTESIAN_POINT ( 'NONE',  ( 20.99999999999997868, 36.65892442174472876, -249.5511627012454596 ) ) ;
#79171=ORIENTED_EDGE ( 'NONE', *, *, #114968, .T. ) ;
#79188=CARTESIAN_POINT ( 'NONE',  ( -23.15000000000000213, 48.89266972451527948, -253.5637804087949121 ) ) ;
#79189=AXIS2_PLACEMENT_3D ( 'NONE', #85495, #150650, #86800 ) ;
#79214=CARTESIAN_POINT ( 'NONE',  ( 21.14250536705908345, 33.99405510657214791, -243.6026301039981945 ) ) ;
#79248=SPHERICAL_SURFACE ( 'NONE', #18063, 0.1000000000000000056 ) ;
#79318=CIRCLE ( 'NONE', #237742, 4.300000000000029132 ) ;
#79350=ORIENTED_EDGE ( 'NONE', *, *, #186164, .F. ) ;
#79372=VECTOR ( 'NONE', #129499, 1000.000000000000114 ) ;
#79382=VERTEX_POINT ( 'NONE', #198744 ) ;
#79418=CARTESIAN_POINT ( 'NONE',  ( -20.85000000000000142, 56.23643450586806836, -227.9054833905874204 ) ) ;
#79426=CARTESIAN_POINT ( 'NONE',  ( -20.85000000000000142, 67.23127455305835554, -235.8551265064784559 ) ) ;
#79463=DIRECTION ( 'NONE',  ( 1.000000000000000000, 0.000000000000000000, 0.000000000000000000 ) ) ;
#79467=CARTESIAN_POINT ( 'NONE',  ( 21.05000000000000071, 36.65892442174472876, -249.5511627012454596 ) ) ;
#79478=DIRECTION ( 'NONE',  ( 0.000000000000000000, 0.9126074666063660468, 0.4088369013363524762 ) ) ;
#79505=AXIS2_PLACEMENT_3D ( 'NONE', #50232, #124662, #129782 ) ;
#79525=CARTESIAN_POINT ( 'NONE',  ( -18.42637059832563295, 77.14546960815955856, -241.8200751569217459 ) ) ;
#79575=ORIENTED_EDGE ( 'NONE', *, *, #8106, .T. ) ;
#79611=CARTESIAN_POINT ( 'NONE',  ( -22.59999999999999787, 36.65892442174472876, -249.5511627012454596 ) ) ;
#79615=CARTESIAN_POINT ( 'NONE',  ( -21.29999999999995808, 36.65892442174472876, -249.5511627012454596 ) ) ;
#79621=DIRECTION ( 'NONE',  ( 0.000000000000000000, -0.4088369013363783999, 0.9126074666063545004 ) ) ;
#79633=AXIS2_PLACEMENT_3D ( 'NONE', #178422, #58414, #137962 ) ;
#79641=CARTESIAN_POINT ( 'NONE',  ( -20.94999999999999929, 69.25047167775285573, -247.4556800696333596 ) ) ;
#79643=ORIENTED_EDGE ( 'NONE', *, *, #42962, .T. ) ;
#79678=EDGE_CURVE ( 'NONE', #132976, #106155, #81042, .T. ) ;
#79689=EDGE_CURVE ( 'NONE', #136568, #119565, #86083, .T. ) ;
#79692=CARTESIAN_POINT ( 'NONE',  ( 23.14999999999998437, 36.65892442174472876, -249.5511627012454596 ) ) ;
#79708=CARTESIAN_POINT ( 'NONE',  ( 20.94999999999999929, 67.84340367245323478, -228.0791829662263410 ) ) ;
#79709=LINE ( 'NONE', #159288, #53623 ) ;
#79718=DIRECTION ( 'NONE',  ( -1.000000000000000000, -0.000000000000000000, 0.000000000000000000 ) ) ;
#79727=CARTESIAN_POINT ( 'NONE',  ( 18.45068634130096896, 46.98837814534854829, -255.3186415057529075 ) ) ;
#79761=CARTESIAN_POINT ( 'NONE',  ( -23.15000000000000213, 62.12679871018154643, -248.6611778639222337 ) ) ;
#79823=CIRCLE ( 'NONE', #242142, 0.1000000000000024342 ) ;
#79838=ORIENTED_EDGE ( 'NONE', *, *, #52501, .F. ) ;
#79881=CARTESIAN_POINT ( 'NONE',  ( 20.94999999999999574, 39.29335463311362275, -236.8946393634874994 ) ) ;
#79891=EDGE_CURVE ( 'NONE', #251464, #89722, #105734, .T. ) ;
#79932=CARTESIAN_POINT ( 'NONE',  ( -20.54999999999999716, 61.88149656937975607, -248.1136133839584090 ) ) ;
#79934=CARTESIAN_POINT ( 'NONE',  ( 20.94999999999999929, 44.34387878855809362, -247.3824414791181994 ) ) ;
#79966=ORIENTED_EDGE ( 'NONE', *, *, #24063, .T. ) ;
#79977=FACE_OUTER_BOUND ( 'NONE', #188329, .T. ) ;
#79983=CARTESIAN_POINT ( 'NONE',  ( -21.05000000000000071, 44.55458850188623643, -247.3966190010231969 ) ) ;
#80041=EDGE_CURVE ( 'NONE', #116074, #175127, #20812, .T. ) ;
#80063=EDGE_CURVE ( 'NONE', #217616, #192641, #211200, .T. ) ;
#80089=EDGE_CURVE ( 'NONE', #87416, #245692, #152975, .T. ) ;
#80103=DIRECTION ( 'NONE',  ( 0.000000000000000000, -0.6936040289657786628, -0.7203564749500342979 ) ) ;
#80124=ORIENTED_EDGE ( 'NONE', *, *, #83085, .T. ) ;
#80143=VECTOR ( 'NONE', #95925, 1000.000000000000000 ) ;
#80199=ORIENTED_EDGE ( 'NONE', *, *, #34357, .F. ) ;
#80210=DIRECTION ( 'NONE',  ( 0.000000000000000000, -0.2677755899090746849, 0.9634813093406884299 ) ) ;
#80315=DIRECTION ( 'NONE',  ( 0.7071067811865475727, -0.2890913453342130457, 0.6453109281988448354 ) ) ;
#80324=CARTESIAN_POINT ( 'NONE',  ( 23.14999999999999858, 68.04894835573102796, -237.6803414396912046 ) ) ;
#80374=LINE ( 'NONE', #159970, #104622 ) ;
#80413=VERTEX_POINT ( 'NONE', #76596 ) ;
#80421=CARTESIAN_POINT ( 'NONE',  ( -18.41353343127311248, 46.96039402156218756, -255.3459641718773696 ) ) ;
#80440=DIRECTION ( 'NONE',  ( -1.000000000000000000, 1.207181226542539700E-16, -2.694675058168174199E-16 ) ) ;
#80451=ORIENTED_EDGE ( 'NONE', *, *, #28390, .T. ) ;
#80466=ORIENTED_EDGE ( 'NONE', *, *, #145484, .T. ) ;
#80486=AXIS2_PLACEMENT_3D ( 'NONE', #72967, #12987, #152501 ) ;
#80492=AXIS2_PLACEMENT_3D ( 'NONE', #134828, #196124, #17473 ) ;
#80506=DIRECTION ( 'NONE',  ( 0.000000000000000000, 0.9126074666063769270, 0.4088369013363283844 ) ) ;
#80516=VECTOR ( 'NONE', #123600, 1000.000000000000114 ) ;
#80555=LINE ( 'NONE', #256600, #51775 ) ;
#80595=FACE_OUTER_BOUND ( 'NONE', #104617, .T. ) ;
#80598=AXIS2_PLACEMENT_3D ( 'NONE', #228720, #129605, #212985 ) ;
#80601=ADVANCED_FACE ( 'NONE', ( #17304 ), #77249, .F. ) ;
#80614=CARTESIAN_POINT ( 'NONE',  ( 20.95000000000000284, 56.16603649944111254, -228.1013850343386480 ) ) ;
#80616=DIRECTION ( 'NONE',  ( -1.000000000000000000, 1.207181226542539700E-16, -2.694675058168174199E-16 ) ) ;
#80659=EDGE_CURVE ( 'NONE', #103333, #183612, #120020, .T. ) ;
#80682=AXIS2_PLACEMENT_3D ( 'NONE', #255419, #235896, #241061 ) ;
#80695=FACE_OUTER_BOUND ( 'NONE', #87675, .T. ) ;
#80722=VECTOR ( 'NONE', #9698, 1000.000000000000114 ) ;
#80751=ORIENTED_EDGE ( 'NONE', *, *, #150307, .T. ) ;
#80774=AXIS2_PLACEMENT_3D ( 'NONE', #198289, #36687, #253113 ) ;
#80846=CARTESIAN_POINT ( 'NONE',  ( -20.64999999999999858, 44.96555909964510533, -237.8856228368455845 ) ) ;
#80861=DIRECTION ( 'NONE',  ( 0.000000000000000000, 0.9126074666063735963, 0.4088369013363361004 ) ) ;
#80926=LINE ( 'NONE', #79641, #145417 ) ;
#80927=CIRCLE ( 'NONE', #114261, 0.09999999999999854838 ) ;
#80930=DIRECTION ( 'NONE',  ( 0.000000000000000000, 0.9126074666063770380, 0.4088369013363281068 ) ) ;
#80944=EDGE_LOOP ( 'NONE', ( #106443, #57764, #100142, #199737 ) ) ;
#80973=DIRECTION ( 'NONE',  ( 0.000000000000000000, 0.9126074666063769270, 0.4088369013363283844 ) ) ;
#80994=DIRECTION ( 'NONE',  ( -1.000000000000000000, -0.000000000000000000, -0.000000000000000000 ) ) ;
#81008=AXIS2_PLACEMENT_3D ( 'NONE', #2314, #84378, #205651 ) ;
#81013=CIRCLE ( 'NONE', #10321, 0.1000000000000091788 ) ;
#81021=LINE ( 'NONE', #199731, #82971 ) ;
#81027=ORIENTED_EDGE ( 'NONE', *, *, #13846, .T. ) ;
#81042=LINE ( 'NONE', #2794, #52777 ) ;
#81050=CARTESIAN_POINT ( 'NONE',  ( 20.94999999999999929, 43.08177281680065818, -239.3869926993485535 ) ) ;
#81068=LINE ( 'NONE', #41983, #36822 ) ;
#81077=CIRCLE ( 'NONE', #80492, 11.79999999999999005 ) ;
#81092=CARTESIAN_POINT ( 'NONE',  ( 21.05000000000000071, 69.09936979046463534, -247.6075824278584889 ) ) ;
#81093=CARTESIAN_POINT ( 'NONE',  ( -22.39999999999999858, 33.38250548509083160, -242.4821227592188961 ) ) ;
#81094=DIRECTION ( 'NONE',  ( 0.000000000000000000, -0.4088369013363276072, 0.9126074666063772600 ) ) ;
#81137=DIRECTION ( 'NONE',  ( -1.000000000000000000, 1.207181226542539946E-16, -2.694675058168174692E-16 ) ) ;
#81171=CARTESIAN_POINT ( 'NONE',  ( -20.94999999999999929, 43.86852340793510763, -246.3213511806884810 ) ) ;
#81207=ORIENTED_EDGE ( 'NONE', *, *, #143859, .F. ) ;
#81213=ORIENTED_EDGE ( 'NONE', *, *, #118738, .T. ) ;
#81231=ORIENTED_EDGE ( 'NONE', *, *, #185438, .F. ) ;
#81244=ORIENTED_EDGE ( 'NONE', *, *, #151493, .F. ) ;
#81271=CARTESIAN_POINT ( 'NONE',  ( 21.05000000000000071, 34.01125473725045367, -243.8802146427659352 ) ) ;
#81301=CARTESIAN_POINT ( 'NONE',  ( -23.25000000000000000, 55.39363411790988323, -234.6384634766556303 ) ) ;
#81306=CARTESIAN_POINT ( 'NONE',  ( 20.95159278453404283, 40.76026667850895535, -237.9528832822917082 ) ) ;
#81356=FACE_OUTER_BOUND ( 'NONE', #248771, .T. ) ;
#81362=CIRCLE ( 'NONE', #168925, 0.1000000000000024342 ) ;
#81381=CARTESIAN_POINT ( 'NONE',  ( -23.25000000000000000, 67.23127455305835554, -235.8551265064784559 ) ) ;
#81397=PLANE ( 'NONE',  #30887 ) ;
#81461=LINE ( 'NONE', #218414, #20385 ) ;
#81483=ORIENTED_EDGE ( 'NONE', *, *, #245811, .T. ) ;
#81508=ORIENTED_EDGE ( 'NONE', *, *, #201677, .F. ) ;
#81518=DIRECTION ( 'NONE',  ( -1.000000000000000000, 1.207181226542539700E-16, -2.694675058168174199E-16 ) ) ;
#81522=VECTOR ( 'NONE', #237381, 1000.000000000000000 ) ;
#81529=CARTESIAN_POINT ( 'NONE',  ( -20.94999999999999929, 47.95459712139160047, -246.5019368548292675 ) ) ;
#81533=VERTEX_POINT ( 'NONE', #118351 ) ;
#81541=ORIENTED_EDGE ( 'NONE', *, *, #217612, .T. ) ;
#81545=VECTOR ( 'NONE', #107051, 1000.000000000000114 ) ;
#81546=ADVANCED_FACE ( 'NONE', ( #21814 ), #109592, .T. ) ;
#81550=ORIENTED_EDGE ( 'NONE', *, *, #255333, .F. ) ;
#81564=CARTESIAN_POINT ( 'NONE',  ( -20.64999999999999858, 47.45383559552795560, -242.5236527704543334 ) ) ;
#81584=DIRECTION ( 'NONE',  ( -1.000000000000000000, -0.000000000000000000, -0.000000000000000000 ) ) ;
#81587=ORIENTED_EDGE ( 'NONE', *, *, #38928, .T. ) ;
#81616=ORIENTED_EDGE ( 'NONE', *, *, #252478, .F. ) ;
#81621=CARTESIAN_POINT ( 'NONE',  ( 23.14999999999999503, 53.28269063671665151, -234.9266833317103647 ) ) ;
#81651=VERTEX_POINT ( 'NONE', #64773 ) ;
#81657=CARTESIAN_POINT ( 'NONE',  ( 18.59999999999997655, 62.42744096235649920, -225.1319887738535499 ) ) ;
#81666=CARTESIAN_POINT ( 'NONE',  ( -18.59999999999999787, 38.20647789760820956, -236.0922579506644468 ) ) ;
#81692=AXIS2_PLACEMENT_3D ( 'NONE', #189228, #152693, #90099 ) ;
#81697=ORIENTED_EDGE ( 'NONE', *, *, #92158, .T. ) ;
#81699=DIRECTION ( 'NONE',  ( 0.000000000000000000, 0.4088369013363281623, -0.9126074666063771490 ) ) ;
#81710=DIRECTION ( 'NONE',  ( 1.000000000000000000, -1.335000415235278971E-16, 2.979993593738921214E-16 ) ) ;
#81712=EDGE_CURVE ( 'NONE', #148222, #157687, #224569, .T. ) ;
#81713=CIRCLE ( 'NONE', #48435, 11.74999999999999822 ) ;
#81734=CARTESIAN_POINT ( 'NONE',  ( -20.85000000000000142, 78.48087866980282001, -232.8271061603568910 ) ) ;
#81741=FACE_OUTER_BOUND ( 'NONE', #101754, .T. ) ;
#81745=ADVANCED_FACE ( 'NONE', ( #46466 ), #183437, .T. ) ;
#81751=CARTESIAN_POINT ( 'NONE',  ( -23.15000000000000213, 47.40541193113006813, -242.6436572752161283 ) ) ;
#81782=DIRECTION ( 'NONE',  ( -1.000000000000000000, 1.207181226542539700E-16, -2.694675058168174199E-16 ) ) ;
#81793=AXIS2_PLACEMENT_3D ( 'NONE', #172800, #67230, #146738 ) ;
#81817=CARTESIAN_POINT ( 'NONE',  ( 18.49351773456738357, 47.07696351123693290, -255.2313122348375316 ) ) ;
#81831=CARTESIAN_POINT ( 'NONE',  ( 21.14999999999999858, 21.17283678855157802, -243.7231193059830048 ) ) ;
#81851=CARTESIAN_POINT ( 'NONE',  ( -18.59999999999999787, 42.98415524044398950, -233.9519173640448173 ) ) ;
#81861=CARTESIAN_POINT ( 'NONE',  ( -21.05000000000000071, 46.53760404070597900, -243.0973507280067167 ) ) ;
#81868=ORIENTED_EDGE ( 'NONE', *, *, #61182, .F. ) ;
#81878=FACE_OUTER_BOUND ( 'NONE', #213215, .T. ) ;
#81896=ORIENTED_EDGE ( 'NONE', *, *, #165133, .F. ) ;
#81901=AXIS2_PLACEMENT_3D ( 'NONE', #235377, #56710, #136258 ) ;
#81927=ORIENTED_EDGE ( 'NONE', *, *, #69706, .T. ) ;
#81932=CARTESIAN_POINT ( 'NONE',  ( -20.87600722750343252, 68.10911674539558192, -224.1414149070238864 ) ) ;
#81938=VECTOR ( 'NONE', #164729, 1000.000000000000000 ) ;
#81971=ORIENTED_EDGE ( 'NONE', *, *, #186669, .F. ) ;
#82013=LINE ( 'NONE', #84565, #13725 ) ;
#82040=AXIS2_PLACEMENT_3D ( 'NONE', #112581, #210401, #113852 ) ;
#82042=LINE ( 'NONE', #181202, #7063 ) ;
#82061=CIRCLE ( 'NONE', #252766, 4.000000000000002665 ) ;
#82089=DIRECTION ( 'NONE',  ( 0.000000000000000000, 0.9126074666063770380, 0.4088369013363283289 ) ) ;
#82151=DIRECTION ( 'NONE',  ( 0.000000000000000000, 0.9126074666063660468, 0.4088369013363524762 ) ) ;
#82158=DIRECTION ( 'NONE',  ( 1.000000000000000000, 0.000000000000000000, 0.000000000000000000 ) ) ;
#82166=DIRECTION ( 'NONE',  ( 0.000000000000000000, 0.9126074666063771490, 0.4088369013363276627 ) ) ;
#82243=EDGE_CURVE ( 'NONE', #115670, #221119, #228696, .T. ) ;
#82268=EDGE_CURVE ( 'NONE', #18296, #79169, #231268, .T. ) ;
#82272=CARTESIAN_POINT ( 'NONE',  ( -18.59999999999999787, 46.53760404070597900, -243.0973507280067167 ) ) ;
#82294=CIRCLE ( 'NONE', #228079, 0.09999999999999609201 ) ;
#82299=TOROIDAL_SURFACE ( 'NONE', #49001, 0.9750000000000019762, 0.1000000000000000056 ) ;
#82382=AXIS2_PLACEMENT_3D ( 'NONE', #257967, #38989, #238456 ) ;
#82384=ADVANCED_FACE ( 'NONE', ( #78581 ), #40783, .F. ) ;
#82385=DIRECTION ( 'NONE',  ( 0.000000000000000000, 0.9126074666064696306, 0.4088369013361213278 ) ) ;
#82450=AXIS2_PLACEMENT_3D ( 'NONE', #231659, #253755, #256262 ) ;
#82451=CARTESIAN_POINT ( 'NONE',  ( 18.54116936837186458, 46.96053119008168153, -255.3059777784767448 ) ) ;
#82468=AXIS2_PLACEMENT_3D ( 'NONE', #64970, #42852, #23317 ) ;
#82507=CARTESIAN_POINT ( 'NONE',  ( 18.59999999999999432, 43.48442877397276618, -245.2193771921251084 ) ) ;
#82515=ADVANCED_FACE ( 'NONE', ( #224515 ), #84974, .T. ) ;
#82610=ORIENTED_EDGE ( 'NONE', *, *, #2091, .F. ) ;
#82611=AXIS2_PLACEMENT_3D ( 'NONE', #108585, #9477, #149016 ) ;
#82613=DIRECTION ( 'NONE',  ( 0.000000000000000000, -0.9126074666063769270, -0.4088369013363280513 ) ) ;
#82630=ORIENTED_EDGE ( 'NONE', *, *, #100841, .F. ) ;
#82646=EDGE_CURVE ( 'NONE', #215970, #217929, #204266, .T. ) ;
#82665=VERTEX_POINT ( 'NONE', #228383 ) ;
#82711=CYLINDRICAL_SURFACE ( 'NONE', #50773, 0.1000000000000024342 ) ;
#82715=EDGE_CURVE ( 'NONE', #241306, #148485, #156575, .T. ) ;
#82730=VECTOR ( 'NONE', #237763, 1000.000000000000114 ) ;
#82779=ORIENTED_EDGE ( 'NONE', *, *, #186174, .T. ) ;
#82789=CIRCLE ( 'NONE', #116186, 0.09999999999999414912 ) ;
#82798=DIRECTION ( 'NONE',  ( 0.000000000000000000, 0.9126074666063770380, 0.4088369013363281068 ) ) ;
#82810=CARTESIAN_POINT ( 'NONE',  ( 20.89192007715127630, 68.10318897902124036, -224.1464165264002872 ) ) ;
#82815=ORIENTED_EDGE ( 'NONE', *, *, #216443, .T. ) ;
#82822=DIRECTION ( 'NONE',  ( 1.000000000000000000, 0.000000000000000000, 0.000000000000000000 ) ) ;
#82826=DIRECTION ( 'NONE',  ( 0.000000000000000000, -0.2818822000685679008, 0.9594490217226259166 ) ) ;
#82876=CARTESIAN_POINT ( 'NONE',  ( 20.97565083910961548, 39.29220182519587468, -236.8938058441740964 ) ) ;
#82884=EDGE_LOOP ( 'NONE', ( #35157, #241307, #57, #115145 ) ) ;
#82921=AXIS2_PLACEMENT_3D ( 'NONE', #14667, #39370, #195866 ) ;
#82971=VECTOR ( 'NONE', #45765, 1000.000000000000114 ) ;
#82991=CIRCLE ( 'NONE', #174667, 0.09999999999999939493 ) ;
#83019=FACE_OUTER_BOUND ( 'NONE', #98690, .T. ) ;
#83050=CARTESIAN_POINT ( 'NONE',  ( 18.49999999999999289, 55.04793976901536467, -229.8170162380219494 ) ) ;
#83078=DIRECTION ( 'NONE',  ( 0.000000000000000000, 0.9126074666063844765, 0.4088369013363113980 ) ) ;
#83085=EDGE_CURVE ( 'NONE', #2697, #34062, #73818, .T. ) ;
#83103=VERTEX_POINT ( 'NONE', #114195 ) ;
#83127=FACE_OUTER_BOUND ( 'NONE', #35542, .T. ) ;
#83132=SPHERICAL_SURFACE ( 'NONE', #160142, 0.1000000000000000056 ) ;
#83140=CARTESIAN_POINT ( 'NONE',  ( -21.64999999999999858, 53.08776555244186568, -234.2469744149522626 ) ) ;
#83155=CARTESIAN_POINT ( 'NONE',  ( -22.45305610364634674, 25.97741635855165399, -254.4468634167652681 ) ) ;
#83161=TOROIDAL_SURFACE ( 'NONE', #124907, 7.791421356237335338, 0.1000000000000000056 ) ;
#83184=EDGE_LOOP ( 'NONE', ( #84443, #187244 ) ) ;
#83191=DIRECTION ( 'NONE',  ( 1.000000000000000000, -0.000000000000000000, -0.000000000000000000 ) ) ;
#83205=EDGE_CURVE ( 'NONE', #136568, #214442, #71211, .T. ) ;
#83207=ORIENTED_EDGE ( 'NONE', *, *, #114094, .T. ) ;
#83224=DIRECTION ( 'NONE',  ( 0.000000000000000000, 0.9126074666063545004, 0.4088369013363783999 ) ) ;
#83251=CARTESIAN_POINT ( 'NONE',  ( 21.53551880898956838, 33.79472821003547267, -243.3997680843710611 ) ) ;
#83254=DIRECTION ( 'NONE',  ( -1.000000000000000000, 0.000000000000000000, 0.000000000000000000 ) ) ;
#83259=VECTOR ( 'NONE', #110043, 1000.000000000000114 ) ;
#83274=CARTESIAN_POINT ( 'NONE',  ( -21.05000000000000071, 69.09936979046463534, -247.6075824278584889 ) ) ;
#83331=DIRECTION ( 'NONE',  ( 0.000000000000000000, 0.9126074666063920260, 0.4088369013362946891 ) ) ;
#83343=FACE_OUTER_BOUND ( 'NONE', #220466, .T. ) ;
#83353=EDGE_CURVE ( 'NONE', #236784, #215460, #130889, .T. ) ;
#83356=VECTOR ( 'NONE', #215730, 1000.000000000000000 ) ;
#83362=DIRECTION ( 'NONE',  ( 0.000000000000000000, -0.9126074666063660468, -0.4088369013363524762 ) ) ;
#83368=CARTESIAN_POINT ( 'NONE',  ( -18.47690164073607377, 77.21658254787745079, -241.7530424840200851 ) ) ;
#83382=CARTESIAN_POINT ( 'NONE',  ( -21.07928932188134041, 30.84304088367084162, -252.0482413927653340 ) ) ;
#83426=DIRECTION ( 'NONE',  ( 0.000000000000000000, 0.4088369013363281068, -0.9126074666063770380 ) ) ;
#83429=ADVANCED_FACE ( 'NONE', ( #235137 ), #196022, .F. ) ;
#83452=DIRECTION ( 'NONE',  ( -1.000000000000000000, -0.000000000000000000, -0.000000000000000000 ) ) ;
#83458=ORIENTED_EDGE ( 'NONE', *, *, #187038, .F. ) ;
#83501=DIRECTION ( 'NONE',  ( 1.000000000000000000, -2.986185139342070877E-16, 6.665775143889692774E-16 ) ) ;
#83521=DIRECTION ( 'NONE',  ( -0.000000000000000000, 0.4088369013363281623, -0.9126074666063771490 ) ) ;
#83616=ORIENTED_EDGE ( 'NONE', *, *, #26787, .T. ) ;
#83624=AXIS2_PLACEMENT_3D ( 'NONE', #5731, #244357, #68310 ) ;
#83631=CARTESIAN_POINT ( 'NONE',  ( -18.47079683080319867, 47.01888943380454577, -255.2887095692685193 ) ) ;
#83648=EDGE_CURVE ( 'NONE', #50249, #69777, #37509, .T. ) ;
#83674=EDGE_LOOP ( 'NONE', ( #124348, #187281, #76764 ) ) ;
#83676=ORIENTED_EDGE ( 'NONE', *, *, #74020, .T. ) ;
#83700=DIRECTION ( 'NONE',  ( 0.000000000000000000, 0.09425075112713275638, 0.9955484899852801162 ) ) ;
#83740=EDGE_CURVE ( 'NONE', #145909, #32455, #152761, .T. ) ;
#83756=ORIENTED_EDGE ( 'NONE', *, *, #102171, .F. ) ;
#83766=FACE_OUTER_BOUND ( 'NONE', #58845, .T. ) ;
#83767=CARTESIAN_POINT ( 'NONE',  ( -21.05315837636350196, 56.18370557670049692, -227.9291052944747094 ) ) ;
#83768=VECTOR ( 'NONE', #246215, 1000.000000000000114 ) ;
#83773=CARTESIAN_POINT ( 'NONE',  ( -22.59999999999999787, 36.65892442174472876, -249.5511627012454596 ) ) ;
#83774=LINE ( 'NONE', #159521, #22286 ) ;
#83801=DIRECTION ( 'NONE',  ( 0.000000000000000000, 0.4088369013362687654, -0.9126074666064034613 ) ) ;
#83822=CARTESIAN_POINT ( 'NONE',  ( 21.05000000000000071, 34.10066453776878603, -243.7889862147425788 ) ) ;
#83840=CARTESIAN_POINT ( 'NONE',  ( -20.05000000000000426, 52.17883100310857003, -232.4626431718731396 ) ) ;
#83865=CARTESIAN_POINT ( 'NONE',  ( 20.95443524775735256, 40.81698247481438102, -237.9596272153440850 ) ) ;
#83871=DIRECTION ( 'NONE',  ( 1.000000000000000000, 0.000000000000000000, 0.000000000000000000 ) ) ;
#83894=DIRECTION ( 'NONE',  ( 0.000000000000000000, 0.9126074666063844765, 0.4088369013363114535 ) ) ;
#83920=DIRECTION ( 'NONE',  ( 0.000000000000000000, -0.4088369013363280513, 0.9126074666063769270 ) ) ;
#83929=CARTESIAN_POINT ( 'NONE',  ( -20.64999999999999858, 47.48953316408024961, -242.5895867826444601 ) ) ;
#83986=DIRECTION ( 'NONE',  ( -1.000000000000000000, -0.000000000000000000, 0.000000000000000000 ) ) ;
#84004=CARTESIAN_POINT ( 'NONE',  ( -18.59999999999999787, 67.84340367245323478, -228.0791829662263410 ) ) ;
#84027=EDGE_CURVE ( 'NONE', #242320, #5729, #186428, .T. ) ;
#84080=ORIENTED_EDGE ( 'NONE', *, *, #138459, .T. ) ;
#84105=CARTESIAN_POINT ( 'NONE',  ( 23.14999999999999858, 45.93587830916155212, -239.9163948487882863 ) ) ;
#84106=ORIENTED_EDGE ( 'NONE', *, *, #239227, .F. ) ;
#84115=DIRECTION ( 'NONE',  ( 0.000000000000000000, -0.9126074666059857954, -0.4088369013372012972 ) ) ;
#84156=CYLINDRICAL_SURFACE ( 'NONE', #120645, 4.000000000000002665 ) ;
#84175=EDGE_LOOP ( 'NONE', ( #199700, #122354, #58490, #2668 ) ) ;
#84207=DIRECTION ( 'NONE',  ( 0.000000000000000000, -0.4088369013363280513, 0.9126074666063769270 ) ) ;
#84208=ORIENTED_EDGE ( 'NONE', *, *, #40833, .T. ) ;
#84219=AXIS2_PLACEMENT_3D ( 'NONE', #162354, #204022, #63215 ) ;
#84222=CARTESIAN_POINT ( 'NONE',  ( 18.52928932188133970, 51.94054103949330425, -231.4415386711587530 ) ) ;
#84249=CYLINDRICAL_SURFACE ( 'NONE', #84388, 0.1000000000000024342 ) ;
#84273=FACE_OUTER_BOUND ( 'NONE', #242923, .T. ) ;
#84278=CARTESIAN_POINT ( 'NONE',  ( 21.05000000000000071, 32.73471231533727632, -251.3091613769917103 ) ) ;
#84279=DIRECTION ( 'NONE',  ( -1.000000000000000000, 8.623019343401623015E-17, 8.389849937938898203E-16 ) ) ;
#84291=CARTESIAN_POINT ( 'NONE',  ( 22.50014994443965222, 31.77938584363926466, -238.8622469772242596 ) ) ;
#84296=ORIENTED_EDGE ( 'NONE', *, *, #54612, .F. ) ;
#84304=ADVANCED_FACE ( 'NONE', ( #55850 ), #156303, .T. ) ;
#84325=VERTEX_POINT ( 'NONE', #200525 ) ;
#84330=EDGE_CURVE ( 'NONE', #252130, #53966, #254317, .T. ) ;
#84343=ORIENTED_EDGE ( 'NONE', *, *, #202580, .T. ) ;
#84363=CARTESIAN_POINT ( 'NONE',  ( 18.46082813848040161, 47.00025378330893489, -255.3070137009749772 ) ) ;
#84378=DIRECTION ( 'NONE',  ( 1.000000000000000000, 0.000000000000000000, 0.000000000000000000 ) ) ;
#84388=AXIS2_PLACEMENT_3D ( 'NONE', #225076, #45179, #148135 ) ;
#84389=VERTEX_POINT ( 'NONE', #66148 ) ;
#84403=AXIS2_PLACEMENT_3D ( 'NONE', #125817, #187111, #91840 ) ;
#84405=DIRECTION ( 'NONE',  ( -1.000000000000000000, -0.000000000000000000, 0.000000000000000000 ) ) ;
#84443=ORIENTED_EDGE ( 'NONE', *, *, #8178, .T. ) ;
#84495=CARTESIAN_POINT ( 'NONE',  ( 20.85000000000000142, 56.27731819600170837, -227.9967441372480437 ) ) ;
#84516=CARTESIAN_POINT ( 'NONE',  ( -23.15000000000000213, 24.87281074564535288, -251.9822168787707710 ) ) ;
#84545=CARTESIAN_POINT ( 'NONE',  ( -20.15000000000000568, 52.16189642417536021, -232.4248417328940093 ) ) ;
#84559=DIRECTION ( 'NONE',  ( 0.000000000000000000, 0.2868887416115947775, -0.9579639084728169829 ) ) ;
#84560=AXIS2_PLACEMENT_3D ( 'NONE', #198704, #20083, #25226 ) ;
#84565=CARTESIAN_POINT ( 'NONE',  ( -23.15000000000000213, 54.14029358995846763, -238.9803212882090691 ) ) ;
#84570=EDGE_LOOP ( 'NONE', ( #228977, #13571, #246524, #172775 ) ) ;
#84599=LINE ( 'NONE', #125070, #73726 ) ;
#84606=CIRCLE ( 'NONE', #9639, 0.1000000000000024342 ) ;
#84623=AXIS2_PLACEMENT_3D ( 'NONE', #254936, #60633, #43668 ) ;
#84649=VERTEX_POINT ( 'NONE', #21289 ) ;
#84668=EDGE_CURVE ( 'NONE', #127037, #215121, #187901, .T. ) ;
#84671=AXIS2_PLACEMENT_3D ( 'NONE', #182821, #160702, #121579 ) ;
#84693=CARTESIAN_POINT ( 'NONE',  ( 20.94999999999999929, 53.86595165227826243, -236.3638196928718855 ) ) ;
#84696=VERTEX_POINT ( 'NONE', #102050 ) ;
#84712=ORIENTED_EDGE ( 'NONE', *, *, #159369, .F. ) ;
#84741=CARTESIAN_POINT ( 'NONE',  ( 21.05000000000000071, 56.06656052939784729, -228.0911609752645290 ) ) ;
#84752=CARTESIAN_POINT ( 'NONE',  ( -18.50000000000000000, 42.98415524044399660, -233.9519173640447889 ) ) ;
#84777=EDGE_LOOP ( 'NONE', ( #29020, #230970, #74038, #107147 ) ) ;
#84799=AXIS2_PLACEMENT_3D ( 'NONE', #245963, #67309, #222512 ) ;
#84802=ORIENTED_EDGE ( 'NONE', *, *, #29457, .T. ) ;
#84804=ORIENTED_EDGE ( 'NONE', *, *, #190067, .F. ) ;
#84806=CARTESIAN_POINT ( 'NONE',  ( 21.05000000000000426, 34.06939550845276443, -243.8530697005520267 ) ) ;
#84821=AXIS2_PLACEMENT_3D ( 'NONE', #120699, #238041, #3270 ) ;
#84824=ORIENTED_EDGE ( 'NONE', *, *, #40651, .T. ) ;
#84831=CARTESIAN_POINT ( 'NONE',  ( -20.64999999999999858, 54.18213181965657554, -236.9344197582443883 ) ) ;
#84836=CARTESIAN_POINT ( 'NONE',  ( -21.05000000000000071, 56.55475276915903038, -225.2974176673762940 ) ) ;
#84840=CARTESIAN_POINT ( 'NONE',  ( -18.59999999999999787, 78.48087866980282001, -232.8271061603568910 ) ) ;
#84892=DIRECTION ( 'NONE',  ( 0.000000000000000000, 0.4088369013363281068, -0.9126074666063770380 ) ) ;
#84919=CARTESIAN_POINT ( 'NONE',  ( -18.59999996769639097, 47.04086122480761389, -255.1600965361087106 ) ) ;
#84925=DIRECTION ( 'NONE',  ( 0.000000000000000000, 0.9126074666063545004, 0.4088369013363783999 ) ) ;
#84937=AXIS2_PLACEMENT_3D ( 'NONE', #99762, #159774, #39844 ) ;
#84944=AXIS2_PLACEMENT_3D ( 'NONE', #155315, #101689, #45609 ) ;
#84974=CYLINDRICAL_SURFACE ( 'NONE', #175114, 0.09999999999999939493 ) ;
#84983=EDGE_CURVE ( 'NONE', #57597, #785, #242217, .T. ) ;
#85005=AXIS2_PLACEMENT_3D ( 'NONE', #251136, #235429, #114216 ) ;
#85018=DIRECTION ( 'NONE',  ( 0.000000000000000000, -0.8103668758649471560, 0.5859227990963360444 ) ) ;
#85022=DIRECTION ( 'NONE',  ( 0.000000000000000000, -0.9126074666063769270, -0.4088369013363280513 ) ) ;
#85036=CIRCLE ( 'NONE', #230653, 0.09999999999999609201 ) ;
#85043=VERTEX_POINT ( 'NONE', #68951 ) ;
#85048=FACE_OUTER_BOUND ( 'NONE', #233319, .T. ) ;
#85069=ORIENTED_EDGE ( 'NONE', *, *, #240068, .F. ) ;
#85100=ORIENTED_EDGE ( 'NONE', *, *, #106205, .F. ) ;
#85121=VECTOR ( 'NONE', #248756, 1000.000000000000114 ) ;
#85132=AXIS2_PLACEMENT_3D ( 'NONE', #46472, #129864, #69930 ) ;
#85137=DIRECTION ( 'NONE',  ( 1.000000000000000000, 0.000000000000000000, 0.000000000000000000 ) ) ;
#85158=AXIS2_PLACEMENT_3D ( 'NONE', #248726, #25830, #149642 ) ;
#85166=CARTESIAN_POINT ( 'NONE',  ( -18.59999999999999787, 43.57568952063339651, -245.1784935019914826 ) ) ;
#85200=CARTESIAN_POINT ( 'NONE',  ( 21.14999999999999858, 36.75018516840536620, -249.5102790111118338 ) ) ;
#85203=AXIS2_PLACEMENT_3D ( 'NONE', #89196, #12262, #74821 ) ;
#85237=DIRECTION ( 'NONE',  ( -1.000000000000000000, -0.000000000000000000, -0.000000000000000000 ) ) ;
#85251=FACE_OUTER_BOUND ( 'NONE', #46750, .T. ) ;
#85285=DIRECTION ( 'NONE',  ( 0.000000000000000000, -0.9126074666063771490, -0.4088369013363281623 ) ) ;
#85289=FACE_OUTER_BOUND ( 'NONE', #99831, .T. ) ;
#85298=CARTESIAN_POINT ( 'NONE',  ( 21.05000000000000071, 39.17763777304804762, -236.9343730377117083 ) ) ;
#85339=LINE ( 'NONE', #65804, #122309 ) ;
#85354=CARTESIAN_POINT ( 'NONE',  ( 18.52928932188133970, 55.04340642595498423, -230.0514932066152198 ) ) ;
#85366=DIRECTION ( 'NONE',  ( 0.000000000000000000, 0.4088369013363149507, -0.9126074666063829222 ) ) ;
#85378=CARTESIAN_POINT ( 'NONE',  ( 20.94999999999999929, 68.00366762990589109, -224.2307594727497815 ) ) ;
#85404=EDGE_CURVE ( 'NONE', #171512, #129596, #117516, .T. ) ;
#85433=CARTESIAN_POINT ( 'NONE',  ( -23.15000000000000213, 67.23127455305835554, -235.8551265064784559 ) ) ;
#85465=VERTEX_POINT ( 'NONE', #169189 ) ;
#85495=CARTESIAN_POINT ( 'NONE',  ( -18.39999999999999858, 77.17949092533254429, -241.9177572069595783 ) ) ;
#85496=CARTESIAN_POINT ( 'NONE',  ( -20.94999999999999929, 55.59258605799641373, -234.6589115948038966 ) ) ;
#85558=EDGE_CURVE ( 'NONE', #126259, #21323, #229944, .T. ) ;
#85566=CARTESIAN_POINT ( 'NONE',  ( -18.59999999999999787, 44.18876898710608003, -236.1516686502934590 ) ) ;
#85579=CIRCLE ( 'NONE', #247933, 0.09999999999999609201 ) ;
#85593=DIRECTION ( 'NONE',  ( 0.000000000000000000, 0.9126074666063772600, 0.4088369013363274407 ) ) ;
#85611=CARTESIAN_POINT ( 'NONE',  ( 21.08134388332232234, 33.99988033202343729, -243.8010834761945773 ) ) ;
#85616=FACE_OUTER_BOUND ( 'NONE', #233492, .T. ) ;
#85622=DIRECTION ( 'NONE',  ( 0.000000000000000000, -0.9126074666063769270, -0.4088369013363280513 ) ) ;
#85635=CARTESIAN_POINT ( 'NONE',  ( 21.00000000000000000, 52.06567329910104291, -231.9654557484363409 ) ) ;
#85640=ORIENTED_EDGE ( 'NONE', *, *, #42533, .F. ) ;
#85654=LINE ( 'NONE', #106517, #113331 ) ;
#85700=CARTESIAN_POINT ( 'NONE',  ( 18.49999999999999645, 47.95459712139159336, -246.5019368548292675 ) ) ;
#85708=DIRECTION ( 'NONE',  ( 1.000000000000000000, 0.000000000000000000, 0.000000000000000000 ) ) ;
#85738=ORIENTED_EDGE ( 'NONE', *, *, #24193, .T. ) ;
#85750=ORIENTED_EDGE ( 'NONE', *, *, #169861, .T. ) ;
#85753=CARTESIAN_POINT ( 'NONE',  ( 20.94999999999999574, 46.50671693017397246, -243.2369495081682942 ) ) ;
#85756=FACE_OUTER_BOUND ( 'NONE', #214945, .T. ) ;
#85757=FACE_OUTER_BOUND ( 'NONE', #174870, .T. ) ;
#85766=TOROIDAL_SURFACE ( 'NONE', #248119, 3.899999999999999467, 0.1000000000000000056 ) ;
#85778=DIRECTION ( 'NONE',  ( 0.000000000000000000, 0.9126074666063772600, 0.4088369013363277182 ) ) ;
#85786=CARTESIAN_POINT ( 'NONE',  ( 18.49999999999999289, 55.08797342919077522, -230.1090097671678905 ) ) ;
#85815=EDGE_CURVE ( 'NONE', #4597, #124911, #100899, .T. ) ;
#85829=DIRECTION ( 'NONE',  ( 0.000000000000000000, -0.9126074666063660468, -0.4088369013363524762 ) ) ;
#85846=VERTEX_POINT ( 'NONE', #47599 ) ;
#85873=CARTESIAN_POINT ( 'NONE',  ( -20.94999999999999929, 44.52640028187936849, -247.3006740988509193 ) ) ;
#85888=DIRECTION ( 'NONE',  ( 1.000000000000000000, 0.000000000000000000, 0.000000000000000000 ) ) ;
#85911=CARTESIAN_POINT ( 'NONE',  ( 20.95520789717937404, 39.25246210041684947, -236.7994979020228357 ) ) ;
#85928=ORIENTED_EDGE ( 'NONE', *, *, #167821, .F. ) ;
#85931=CARTESIAN_POINT ( 'NONE',  ( 18.49999999999999645, 43.63140573099096287, -239.9077968784524444 ) ) ;
#85942=DIRECTION ( 'NONE',  ( -0.000000000000000000, -0.9126074666063771490, -0.4088369013363281623 ) ) ;
#85972=EDGE_CURVE ( 'NONE', #142241, #61955, #228837, .T. ) ;
#85974=CARTESIAN_POINT ( 'NONE',  ( -23.15000000000000213, 46.19206980365409265, -240.6234452366647076 ) ) ;
#85978=DIRECTION ( 'NONE',  ( 0.000000000000000000, 0.7745938767306564943, 0.6324589521315772123 ) ) ;
#85991=CARTESIAN_POINT ( 'NONE',  ( -21.05000000000000071, 33.98486250090727623, -243.5821103306120108 ) ) ;
#85994=DIRECTION ( 'NONE',  ( -1.000000000000000000, 0.000000000000000000, 0.000000000000000000 ) ) ;
#86010=AXIS2_PLACEMENT_3D ( 'NONE', #192416, #76296, #18901 ) ;
#86022=EDGE_LOOP ( 'NONE', ( #107522, #203411, #139025, #181216 ) ) ;
#86036=ORIENTED_EDGE ( 'NONE', *, *, #97223, .F. ) ;
#86075=FACE_OUTER_BOUND ( 'NONE', #51191, .T. ) ;
#86078=ORIENTED_EDGE ( 'NONE', *, *, #96319, .T. ) ;
#86082=ORIENTED_EDGE ( 'NONE', *, *, #235597, .T. ) ;
#86083=CIRCLE ( 'NONE', #123729, 0.09999999999999609201 ) ;
#86111=ORIENTED_EDGE ( 'NONE', *, *, #174891, .T. ) ;
#86118=DIRECTION ( 'NONE',  ( 2.952720810173289112E-16, 0.4088369013363281623, -0.9126074666063770380 ) ) ;
#86126=ORIENTED_EDGE ( 'NONE', *, *, #46805, .F. ) ;
#86127=ADVANCED_FACE ( 'NONE', ( #119157 ), #180413, .T. ) ;
#86128=EDGE_CURVE ( 'NONE', #125226, #973, #216946, .T. ) ;
#86129=EDGE_CURVE ( 'NONE', #230182, #12655, #6278, .T. ) ;
#86155=CYLINDRICAL_SURFACE ( 'NONE', #65269, 11.79999999999999538 ) ;
#86157=AXIS2_PLACEMENT_3D ( 'NONE', #238465, #256695, #140642 ) ;
#86172=DIRECTION ( 'NONE',  ( 0.000000000000000000, -0.9579639084728132081, -0.2868887416116073785 ) ) ;
#86194=AXIS2_PLACEMENT_3D ( 'NONE', #122126, #216071, #136525 ) ;
#86206=CARTESIAN_POINT ( 'NONE',  ( -22.57320508075687115, 31.85509083104287598, -238.8280249686205536 ) ) ;
#86216=LINE ( 'NONE', #66691, #105124 ) ;
#86239=DIRECTION ( 'NONE',  ( -0.000000000000000000, -0.9126074666063770380, -0.4088369013363281068 ) ) ;
#86250=ADVANCED_FACE ( 'NONE', ( #163420 ), #143830, .F. ) ;
#86253=ADVANCED_FACE ( 'NONE', ( #134218 ), #115969, .T. ) ;
#86275=AXIS2_PLACEMENT_3D ( 'NONE', #101574, #216417, #181164 ) ;
#86287=EDGE_CURVE ( 'NONE', #182258, #69777, #155120, .T. ) ;
#86379=CARTESIAN_POINT ( 'NONE',  ( 20.95512820512820440, 43.40368376489742275, -234.8883907171572787 ) ) ;
#86380=ORIENTED_EDGE ( 'NONE', *, *, #30136, .T. ) ;
#86381=CIRCLE ( 'NONE', #124033, 0.09999999999999108213 ) ;
#86382=AXIS2_PLACEMENT_3D ( 'NONE', #60137, #140992, #164401 ) ;
#86384=ADVANCED_FACE ( 'NONE', ( #179795 ), #239760, .T. ) ;
#86422=CARTESIAN_POINT ( 'NONE',  ( 23.14999999999998437, 36.65892442174472876, -249.5511627012454596 ) ) ;
#86427=DIRECTION ( 'NONE',  ( 1.000000000000000000, 0.000000000000000000, 0.000000000000000000 ) ) ;
#86446=DIRECTION ( 'NONE',  ( 0.000000000000000000, 0.9126074666063772600, 0.4088369013363276627 ) ) ;
#86477=DIRECTION ( 'NONE',  ( -1.000000000000000000, -8.623019343401632876E-17, -8.389849937938899189E-16 ) ) ;
#86484=ORIENTED_EDGE ( 'NONE', *, *, #135583, .F. ) ;
#86530=LINE ( 'NONE', #87819, #26480 ) ;
#86544=FACE_OUTER_BOUND ( 'NONE', #73561, .T. ) ;
#86551=CARTESIAN_POINT ( 'NONE',  ( 20.94999999999999929, 47.95459712139159336, -246.5019368548292675 ) ) ;
#86611=CARTESIAN_POINT ( 'NONE',  ( -20.64999999999999858, 46.15118611352045974, -240.5321844900040844 ) ) ;
#86618=VERTEX_POINT ( 'NONE', #31012 ) ;
#86643=EDGE_CURVE ( 'NONE', #108899, #175784, #32287, .T. ) ;
#86705=CARTESIAN_POINT ( 'NONE',  ( -21.05000000000000071, 46.45388641681647357, -243.1520440498138385 ) ) ;
#86713=CARTESIAN_POINT ( 'NONE',  ( 23.14999999999999858, 53.66153320161009788, -235.9075159595686841 ) ) ;
#86759=CARTESIAN_POINT ( 'NONE',  ( 20.94999999999999929, 67.23127455305835554, -235.8551265064784559 ) ) ;
#86798=VERTEX_POINT ( 'NONE', #119512 ) ;
#86800=DIRECTION ( 'NONE',  ( 0.000000000000000000, -0.9126074666063545004, -0.4088369013363783999 ) ) ;
#86809=VERTEX_POINT ( 'NONE', #199038 ) ;
#86844=AXIS2_PLACEMENT_3D ( 'NONE', #251644, #91294, #52142 ) ;
#86862=VECTOR ( 'NONE', #167745, 1000.000000000000227 ) ;
#86877=FACE_OUTER_BOUND ( 'NONE', #221607, .T. ) ;
#86914=CARTESIAN_POINT ( 'NONE',  ( -21.05000000000000071, 36.65892442174472876, -249.5511627012454596 ) ) ;
#86918=ORIENTED_EDGE ( 'NONE', *, *, #173568, .T. ) ;
#86936=ORIENTED_EDGE ( 'NONE', *, *, #163176, .T. ) ;
#86959=EDGE_LOOP ( 'NONE', ( #229431, #44309, #136845, #101431 ) ) ;
#86982=CARTESIAN_POINT ( 'NONE',  ( 21.09610168723073542, 30.82370917696424328, -252.1284611548308874 ) ) ;
#86990=DIRECTION ( 'NONE',  ( 0.000000000000000000, -0.4088369013363783999, 0.9126074666063545004 ) ) ;
#87015=DIRECTION ( 'NONE',  ( 0.000000000000000000, 0.9126074666063769270, 0.4088369013363280513 ) ) ;
#87053=ORIENTED_EDGE ( 'NONE', *, *, #153324, .F. ) ;
#87057=DIRECTION ( 'NONE',  ( 0.000000000000000000, 0.9126074666063770380, 0.4088369013363281068 ) ) ;
#87062=EDGE_CURVE ( 'NONE', #34161, #1847, #185881, .T. ) ;
#87065=DIRECTION ( 'NONE',  ( 2.952720810173289112E-16, 0.4088369013363266635, -0.9126074666063777041 ) ) ;
#87091=ORIENTED_EDGE ( 'NONE', *, *, #124523, .T. ) ;
#87122=CARTESIAN_POINT ( 'NONE',  ( -18.50000000000000000, 36.65892442174472876, -249.5511627012454596 ) ) ;
#87131=EDGE_CURVE ( 'NONE', #187124, #39261, #72473, .T. ) ;
#87136=PLANE ( 'NONE',  #53073 ) ;
#87147=CARTESIAN_POINT ( 'NONE',  ( 18.49505816908823164, 77.27516569126373724, -241.6972430987673022 ) ) ;
#87164=AXIS2_PLACEMENT_3D ( 'NONE', #42096, #184138, #19957 ) ;
#87196=CARTESIAN_POINT ( 'NONE',  ( -20.54999999999999716, 54.34471204062663219, -239.4366250215122420 ) ) ;
#87200=EDGE_LOOP ( 'NONE', ( #181046, #229423, #188750, #35383 ) ) ;
#87231=DIRECTION ( 'NONE',  ( 0.000000000000000000, -0.9501938099239353175, 0.3116596277708039708 ) ) ;
#87268=FACE_OUTER_BOUND ( 'NONE', #200102, .T. ) ;
#87277=CARTESIAN_POINT ( 'NONE',  ( -18.50000000000000000, 67.23127455305835554, -235.8551265064784559 ) ) ;
#87332=AXIS2_PLACEMENT_3D ( 'NONE', #35916, #137542, #197522 ) ;
#87334=ORIENTED_EDGE ( 'NONE', *, *, #121587, .T. ) ;
#87362=EDGE_LOOP ( 'NONE', ( #68246, #48939, #149531, #146014 ) ) ;
#87368=DIRECTION ( 'NONE',  ( -2.940209281316619043E-16, -0.4088369013363290505, 0.9126074666063767049 ) ) ;
#87384=EDGE_CURVE ( 'NONE', #97414, #246455, #9508, .T. ) ;
#87391=ADVANCED_FACE ( 'NONE', ( #89042 ), #25249, .T. ) ;
#87403=DIRECTION ( 'NONE',  ( 0.000000000000000000, -0.9126074666063545004, -0.4088369013363783999 ) ) ;
#87416=VERTEX_POINT ( 'NONE', #104722 ) ;
#87431=ORIENTED_EDGE ( 'NONE', *, *, #222375, .F. ) ;
#87455=CARTESIAN_POINT ( 'NONE',  ( 22.39999999999999503, 29.54900078958455367, -252.7363208912387620 ) ) ;
#87457=AXIS2_PLACEMENT_3D ( 'NONE', #109923, #91658, #188195 ) ;
#87508=ORIENTED_EDGE ( 'NONE', *, *, #86287, .T. ) ;
#87514=ORIENTED_EDGE ( 'NONE', *, *, #99196, .T. ) ;
#87527=DIRECTION ( 'NONE',  ( 0.000000000000000000, 0.9126074666063773710, 0.4088369013363274962 ) ) ;
#87533=DIRECTION ( 'NONE',  ( 1.000000000000000000, 0.000000000000000000, 0.000000000000000000 ) ) ;
#87539=CARTESIAN_POINT ( 'NONE',  ( -18.55807992284872299, 68.10318897902124036, -224.1464165264002588 ) ) ;
#87555=CARTESIAN_POINT ( 'NONE',  ( -18.59999999999999787, 43.63140573099096287, -239.9077968784524444 ) ) ;
#87573=CARTESIAN_POINT ( 'NONE',  ( 21.14999999999999858, 41.42187432231294508, -260.1830396872097140 ) ) ;
#87617=FACE_OUTER_BOUND ( 'NONE', #2959, .T. ) ;
#87624=AXIS2_PLACEMENT_3D ( 'NONE', #86914, #227724, #107784 ) ;
#87636=EDGE_CURVE ( 'NONE', #65743, #66990, #137168, .T. ) ;
#87638=CIRCLE ( 'NONE', #8552, 0.09999999999999735489 ) ;
#87667=B_SPLINE_CURVE_WITH_KNOTS ( 'NONE', 3,
 ( #38840, #79214, #942, #218722, #20568, #100051, #179639, #160081, #120958, #200472, #21837, #101307, #180910, #85611, #148190, #105165, #23136, #246016, #64797 ),
 .UNSPECIFIED., .F., .F.,
 ( 4, 3, 3, 3, 3, 3, 4 ),
 ( 0.000000000000000000, 7.110282409890261485E-05, 0.0001508797727291307672, 0.0002027344179858337034, 0.0002343294522348885335, 0.0002454816334821149936, 0.0002619873080085548971 ),
 .UNSPECIFIED. ) ;
#87675=EDGE_LOOP ( 'NONE', ( #154070, #95145, #3394, #246875 ) ) ;
#87772=CARTESIAN_POINT ( 'NONE',  ( 21.09546886439575886, 44.19670749624917505, -236.4455533064239319 ) ) ;
#87779=DIRECTION ( 'NONE',  ( 0.000000000000000000, -0.9126074666063660468, -0.4088369013363524762 ) ) ;
#87799=CARTESIAN_POINT ( 'NONE',  ( -18.50000000000000000, 42.94327155031035659, -233.8606566173841372 ) ) ;
#87819=CARTESIAN_POINT ( 'NONE',  ( 18.49999999999996803, 67.75954444190071513, -227.8703747234148693 ) ) ;
#87861=CARTESIAN_POINT ( 'NONE',  ( -23.15000000000000213, 36.65892442174472876, -249.5511627012454596 ) ) ;
#87911=ORIENTED_EDGE ( 'NONE', *, *, #29868, .F. ) ;
#87916=AXIS2_PLACEMENT_3D ( 'NONE', #16703, #111957, #135330 ) ;
#87945=DIRECTION ( 'NONE',  ( 1.000000000000000000, 0.000000000000000000, 0.000000000000000000 ) ) ;
#87989=DIRECTION ( 'NONE',  ( 1.000000000000000000, 0.000000000000000000, 0.000000000000000000 ) ) ;
#87997=CARTESIAN_POINT ( 'NONE',  ( 20.95512820512820085, 39.31056039967181448, -236.7220595557971023 ) ) ;
#88075=EDGE_LOOP ( 'NONE', ( #100097, #23537, #222785, #236821 ) ) ;
#88165=ORIENTED_EDGE ( 'NONE', *, *, #198043, .F. ) ;
#88186=CARTESIAN_POINT ( 'NONE',  ( -20.64999999999999858, 54.18213181965657554, -236.9344197582443883 ) ) ;
#88193=CARTESIAN_POINT ( 'NONE',  ( -23.25000000000000000, 36.65892442174472876, -249.5511627012454596 ) ) ;
#88194=CARTESIAN_POINT ( 'NONE',  ( -18.59999999999999787, 51.38014393322265505, -230.1906178717505611 ) ) ;
#88225=CIRCLE ( 'NONE', #188218, 0.09999999999999939493 ) ;
#88236=EDGE_CURVE ( 'NONE', #38559, #120435, #27731, .T. ) ;
#88251=ORIENTED_EDGE ( 'NONE', *, *, #165556, .T. ) ;
#88266=CARTESIAN_POINT ( 'NONE',  ( 21.14999999999999858, 30.68987205111126926, -252.2252246220829193 ) ) ;
#88288=TOROIDAL_SURFACE ( 'NONE', #254686, 0.4000000000000015210, 0.1000000000000000056 ) ;
#88290=ORIENTED_EDGE ( 'NONE', *, *, #79891, .T. ) ;
#88304=ORIENTED_EDGE ( 'NONE', *, *, #102023, .T. ) ;
#88317=AXIS2_PLACEMENT_3D ( 'NONE', #239876, #116077, #199474 ) ;
#88322=CIRCLE ( 'NONE', #92447, 0.5000000000000044409 ) ;
#88327=DIRECTION ( 'NONE',  ( -1.000000000000000000, -0.000000000000000000, -0.000000000000000000 ) ) ;
#88335=SPHERICAL_SURFACE ( 'NONE', #171929, 0.1000000000000000056 ) ;
#88346=ORIENTED_EDGE ( 'NONE', *, *, #178761, .T. ) ;
#88372=TOROIDAL_SURFACE ( 'NONE', #100822, 12.77499999999999858, 0.1000000000000000056 ) ;
#88448=VECTOR ( 'NONE', #50172, 1000.000000000000000 ) ;
#88457=ADVANCED_FACE ( 'NONE', ( #228622 ), #205168, .T. ) ;
#88470=CIRCLE ( 'NONE', #229973, 0.1000000000000024342 ) ;
#88483=CARTESIAN_POINT ( 'NONE',  ( 20.95132126680579887, 39.27898052006931806, -236.8829280990189829 ) ) ;
#88484=DIRECTION ( 'NONE',  ( 2.952720810173289112E-16, 0.4088369013363287729, -0.9126074666063767049 ) ) ;
#88540=DIRECTION ( 'NONE',  ( 0.000000000000000000, 0.9126074666063783702, 0.4088369013363252757 ) ) ;
#88545=ORIENTED_EDGE ( 'NONE', *, *, #52927, .T. ) ;
#88565=ORIENTED_EDGE ( 'NONE', *, *, #147777, .T. ) ;
#88566=CARTESIAN_POINT ( 'NONE',  ( -18.59999999999999787, 46.45388641681647357, -243.1520440498138385 ) ) ;
#88578=DIRECTION ( 'NONE',  ( -0.000000000000000000, 0.9126074666063770380, 0.4088369013363281068 ) ) ;
#88590=AXIS2_PLACEMENT_3D ( 'NONE', #133086, #169683, #212628 ) ;
#88591=EDGE_CURVE ( 'NONE', #143659, #86809, #35569, .T. ) ;
#88650=CARTESIAN_POINT ( 'NONE',  ( -18.59999999999999787, 74.73788286442776041, -233.7359682632885267 ) ) ;
#88659=ORIENTED_EDGE ( 'NONE', *, *, #149868, .F. ) ;
#88662=ORIENTED_EDGE ( 'NONE', *, *, #102171, .T. ) ;
#88683=ORIENTED_EDGE ( 'NONE', *, *, #191308, .F. ) ;
#88685=VECTOR ( 'NONE', #99815, 999.9999999999998863 ) ;
#88696=ORIENTED_EDGE ( 'NONE', *, *, #183595, .T. ) ;
#88709=EDGE_LOOP ( 'NONE', ( #239066, #223549, #41668, #161002 ) ) ;
#88729=CARTESIAN_POINT ( 'NONE',  ( 21.07094088545368393, 30.85066122990914650, -252.0448291528320510 ) ) ;
#88738=EDGE_CURVE ( 'NONE', #70690, #9758, #36270, .T. ) ;
#88762=CARTESIAN_POINT ( 'NONE',  ( -20.85000000000000142, 74.86109765932731364, -233.8067614591677454 ) ) ;
#88784=CIRCLE ( 'NONE', #26462, 0.2000000000000048683 ) ;
#88785=LINE ( 'NONE', #228332, #57155 ) ;
#88863=EDGE_CURVE ( 'NONE', #89516, #146851, #47191, .T. ) ;
#88874=ADVANCED_FACE ( 'NONE', ( #234568 ), #191635, .T. ) ;
#88890=TOROIDAL_SURFACE ( 'NONE', #9786, 0.4000000000000017431, 0.1000000000000000056 ) ;
#88929=FACE_OUTER_BOUND ( 'NONE', #3431, .T. ) ;
#88972=DIRECTION ( 'NONE',  ( 0.000000000000000000, -0.9126074666063660468, -0.4088369013363524762 ) ) ;
#89012=EDGE_CURVE ( 'NONE', #241241, #103333, #182319, .T. ) ;
#89024=VERTEX_POINT ( 'NONE', #242422 ) ;
#89042=FACE_OUTER_BOUND ( 'NONE', #146191, .T. ) ;
#89058=ADVANCED_FACE ( 'NONE', ( #20847 ), #88890, .F. ) ;
#89066=CARTESIAN_POINT ( 'NONE',  ( 21.04105312098505465, 44.28144824342318486, -236.4111193842065006 ) ) ;
#89107=B_SPLINE_CURVE_WITH_KNOTS ( 'NONE', 3,
 ( #256709, #20738, #122392, #161531, #200646, #76836, #181096, #19443, #62420, #140658, #2417, #218902, #37743, #157711, #57253, #81932, #141942, #241066, #59815 ),
 .UNSPECIFIED., .F., .F.,
 ( 4, 3, 3, 3, 3, 3, 4 ),
 ( -2.000416914665993304E-06, 0.000000000000000000, 4.714008503744424863E-05, 9.979203887778155101E-05, 0.0001372215519229429831, 0.0001635031576221004132, 0.0001900083748504148421 ),
 .UNSPECIFIED. ) ;
#89138=DIRECTION ( 'NONE',  ( -0.000000000000000000, 0.9126074666063771490, 0.4088369013363281623 ) ) ;
#89196=CARTESIAN_POINT ( 'NONE',  ( -20.54999999999999716, 49.36776662947724503, -253.7196102226803021 ) ) ;
#89204=DIRECTION ( 'NONE',  ( 0.000000000000000000, -0.9126074666064696306, -0.4088369013361213278 ) ) ;
#89217=DIRECTION ( 'NONE',  ( -1.000000000000000000, 1.207181226542539700E-16, -2.694675058168174199E-16 ) ) ;
#89230=ORIENTED_EDGE ( 'NONE', *, *, #102012, .T. ) ;
#89334=VECTOR ( 'NONE', #112044, 1000.000000000000114 ) ;
#89364=LINE ( 'NONE', #51505, #15031 ) ;
#89374=ORIENTED_EDGE ( 'NONE', *, *, #72392, .T. ) ;
#89379=TOROIDAL_SURFACE ( 'NONE', #189358, 0.2000000000000000111, 0.1000000000000000056 ) ;
#89404=DIRECTION ( 'NONE',  ( 1.000000000000000000, 0.000000000000000000, 0.000000000000000000 ) ) ;
#89430=ORIENTED_EDGE ( 'NONE', *, *, #114229, .T. ) ;
#89458=EDGE_CURVE ( 'NONE', #241192, #117897, #239564, .T. ) ;
#89459=CARTESIAN_POINT ( 'NONE',  ( -18.59999999999999787, 47.95459712139159336, -246.5019368548292675 ) ) ;
#89491=DIRECTION ( 'NONE',  ( -1.000000000000000000, -0.000000000000000000, -0.000000000000000000 ) ) ;
#89493=DIRECTION ( 'NONE',  ( 0.000000000000000000, 0.9126074666063781482, 0.4088369013363255533 ) ) ;
#89502=ORIENTED_EDGE ( 'NONE', *, *, #9222, .F. ) ;
#89516=VERTEX_POINT ( 'NONE', #178330 ) ;
#89538=ORIENTED_EDGE ( 'NONE', *, *, #141766, .T. ) ;
#89547=AXIS2_PLACEMENT_3D ( 'NONE', #156371, #54658, #118516 ) ;
#89549=VERTEX_POINT ( 'NONE', #245982 ) ;
#89594=ADVANCED_FACE ( 'NONE', ( #64764 ), #68630, .F. ) ;
#89602=CARTESIAN_POINT ( 'NONE',  ( -20.64999999999999858, 47.74660456829661825, -241.9541913331436263 ) ) ;
#89603=DIRECTION ( 'NONE',  ( 1.000000000000000000, -1.207181226542539700E-16, 2.694675058168174199E-16 ) ) ;
#89624=FACE_OUTER_BOUND ( 'NONE', #146133, .T. ) ;
#89625=ORIENTED_EDGE ( 'NONE', *, *, #141863, .T. ) ;
#89627=CARTESIAN_POINT ( 'NONE',  ( 21.09696443733127325, 43.44010277435545930, -234.7623226765231266 ) ) ;
#89631=ADVANCED_FACE ( 'NONE', ( #84273 ), #169045, .T. ) ;
#89691=VECTOR ( 'NONE', #207137, 1000.000000000000000 ) ;
#89693=ADVANCED_FACE ( 'NONE', ( #112886 ), #92029, .T. ) ;
#89713=CARTESIAN_POINT ( 'NONE',  ( 18.46905048506371116, 77.19704573657351432, -241.7715467033954440 ) ) ;
#89716=ADVANCED_FACE ( 'NONE', ( #210698 ), #78566, .T. ) ;
#89718=AXIS2_PLACEMENT_3D ( 'NONE', #178800, #198314, #237448 ) ;
#89722=VERTEX_POINT ( 'NONE', #32088 ) ;
#89723=FACE_OUTER_BOUND ( 'NONE', #69472, .T. ) ;
#89753=AXIS2_PLACEMENT_3D ( 'NONE', #57821, #237765, #173990 ) ;
#89755=AXIS2_PLACEMENT_3D ( 'NONE', #102075, #236472, #237760 ) ;
#89771=DIRECTION ( 'NONE',  ( -1.000000000000000000, -0.000000000000000000, -0.000000000000000000 ) ) ;
#89786=CIRCLE ( 'NONE', #64839, 0.09999999999999609201 ) ;
#89820=VECTOR ( 'NONE', #113335, 1000.000000000000114 ) ;
#89849=DIRECTION ( 'NONE',  ( 0.7071067811865475727, -0.2890913453342130457, 0.6453109281988448354 ) ) ;
#89865=AXIS2_PLACEMENT_3D ( 'NONE', #89459, #148158, #206854 ) ;
#89872=CARTESIAN_POINT ( 'NONE',  ( -18.60000000000001563, 47.04011997029079595, -255.1614879447985800 ) ) ;
#89892=CIRCLE ( 'NONE', #6702, 0.1000000000000024342 ) ;
#89897=DIRECTION ( 'NONE',  ( 2.259780016855445309E-14, -0.2599159095383298257, 0.9656312546561772736 ) ) ;
#89898=VERTEX_POINT ( 'NONE', #26315 ) ;
#89899=CARTESIAN_POINT ( 'NONE',  ( 22.50046968638039857, 25.91727838046696064, -254.3137924129949567 ) ) ;
#89923=CYLINDRICAL_SURFACE ( 'NONE', #210705, 0.09999999999999939493 ) ;
#90029=AXIS2_PLACEMENT_3D ( 'NONE', #254336, #135676, #95284 ) ;
#90061=DIRECTION ( 'NONE',  ( 1.000000000000000000, 0.000000000000000000, 0.000000000000000000 ) ) ;
#90068=DIRECTION ( 'NONE',  ( 1.000000000000000000, 0.000000000000000000, 0.000000000000000000 ) ) ;
#90098=AXIS2_PLACEMENT_3D ( 'NONE', #120690, #138897, #218455 ) ;
#90099=DIRECTION ( 'NONE',  ( 1.000000000000000000, 0.000000000000000000, 0.000000000000000000 ) ) ;
#90142=SHAPE_REPRESENTATION ( 'Injection Molded Chain Links 9', ( #2425 ), #231953 ) ;
#90222=DIRECTION ( 'NONE',  ( 0.000000000000000000, -0.9126074666063844765, -0.4088369013363114535 ) ) ;
#90229=CARTESIAN_POINT ( 'NONE',  ( 19.87657994472052536, 54.45653398996847017, -228.7028568925953778 ) ) ;
#90234=ORIENTED_EDGE ( 'NONE', *, *, #207417, .F. ) ;
#90273=B_SPLINE_CURVE_WITH_KNOTS ( 'NONE', 3,
 ( #26456, #6874, #164676, #47265, #125540, #86379 ),
 .UNSPECIFIED., .F., .F.,
 ( 4, 2, 4 ),
 ( 0.000000000000000000, 0.0001497467027049168508, 0.0002994934054098337016 ),
 .UNSPECIFIED. ) ;
#90294=ORIENTED_EDGE ( 'NONE', *, *, #233150, .F. ) ;
#90328=ORIENTED_EDGE ( 'NONE', *, *, #65809, .T. ) ;
#90330=CARTESIAN_POINT ( 'NONE',  ( -23.15000000000000213, 43.07541598710462694, -233.9110336739111347 ) ) ;
#90348=DIRECTION ( 'NONE',  ( -2.827886303505248766E-16, -0.8103668758649577031, 0.5859227990963212784 ) ) ;
#90349=CARTESIAN_POINT ( 'NONE',  ( 22.39999999999999503, 29.58621655554530250, -252.7196486866020280 ) ) ;
#90366=CARTESIAN_POINT ( 'NONE',  ( -20.54999999999999716, 60.76440593117145994, -251.6273999706070583 ) ) ;
#90374=ORIENTED_EDGE ( 'NONE', *, *, #44668, .T. ) ;
#90404=CARTESIAN_POINT ( 'NONE',  ( -21.05000000000000071, 70.97296516614450468, -234.1788952109995137 ) ) ;
#90416=CARTESIAN_POINT ( 'NONE',  ( -20.64999999999999858, 49.57218508014541669, -254.1759139559835035 ) ) ;
#90454=VECTOR ( 'NONE', #72993, 1000.000000000000114 ) ;
#90470=EDGE_CURVE ( 'NONE', #121939, #241985, #255251, .T. ) ;
#90490=TOROIDAL_SURFACE ( 'NONE', #86194, 11.70000000000000639, 0.1000000000000000056 ) ;
#90517=ORIENTED_EDGE ( 'NONE', *, *, #9111, .T. ) ;
#90531=ORIENTED_EDGE ( 'NONE', *, *, #63166, .T. ) ;
#90581=EDGE_CURVE ( 'NONE', #51812, #21148, #184930, .T. ) ;
#90582=AXIS2_PLACEMENT_3D ( 'NONE', #25354, #36256, #255222 ) ;
#90603=CARTESIAN_POINT ( 'NONE',  ( 23.14999999999998437, 40.35498466150056629, -247.8953732508333587 ) ) ;
#90607=CARTESIAN_POINT ( 'NONE',  ( -18.50000000000000000, 67.23127455305835554, -235.8551265064784559 ) ) ;
#90645=CARTESIAN_POINT ( 'NONE',  ( 23.25000000000000000, 45.25174493058054281, -238.5244480634700324 ) ) ;
#90660=CARTESIAN_POINT ( 'NONE',  ( 21.05000000000000071, 54.36558989155976462, -236.3448031251562327 ) ) ;
#90698=ADVANCED_FACE ( 'NONE', ( #225141 ), #247282, .T. ) ;
#90719=CARTESIAN_POINT ( 'NONE',  ( -20.94999999999999929, 38.25685495413521409, -235.9601135138701693 ) ) ;
#90723=CARTESIAN_POINT ( 'NONE',  ( 22.39999999999999858, 29.50811709945092076, -252.6450601445781103 ) ) ;
#90724=VECTOR ( 'NONE', #122558, 1000.000000000000114 ) ;
#90764=EDGE_CURVE ( 'NONE', #120409, #2697, #18523, .T. ) ;
#90768=VERTEX_POINT ( 'NONE', #248580 ) ;
#90781=CARTESIAN_POINT ( 'NONE',  ( -20.85000000000000142, 68.11287320386161070, -224.1382462126928488 ) ) ;
#90785=AXIS2_PLACEMENT_3D ( 'NONE', #210927, #226622, #247482 ) ;
#90839=EDGE_CURVE ( 'NONE', #230182, #214984, #212041, .T. ) ;
#90842=CARTESIAN_POINT ( 'NONE',  ( -18.50000000000000000, 29.81973725181492085, -263.0247672247078867 ) ) ;
#90896=CARTESIAN_POINT ( 'NONE',  ( 23.14999999999999858, 53.86595165227826243, -236.3638196928718855 ) ) ;
#90921=CARTESIAN_POINT ( 'NONE',  ( -23.15000000000000213, 49.36776662947724503, -253.7196102226803021 ) ) ;
#90941=DIRECTION ( 'NONE',  ( 2.952720810173289112E-16, 0.4088369013363280513, -0.9126074666063769270 ) ) ;
#90958=ORIENTED_EDGE ( 'NONE', *, *, #13878, .T. ) ;
#90964=EDGE_CURVE ( 'NONE', #53966, #173788, #239294, .T. ) ;
#91015=TOROIDAL_SURFACE ( 'NONE', #45215, 4.149999999999999467, 0.1000000000000000056 ) ;
#91073=CARTESIAN_POINT ( 'NONE',  ( 18.59999999999999787, 77.35494420175977837, -241.6200040285045532 ) ) ;
#91120=DIRECTION ( 'NONE',  ( -3.265361837132813093E-16, -0.4088369013363280513, 0.9126074666063769270 ) ) ;
#91221=CARTESIAN_POINT ( 'NONE',  ( -22.50000000000093436, 25.89494711235937530, -254.2627752153468919 ) ) ;
#91223=ORIENTED_EDGE ( 'NONE', *, *, #227348, .T. ) ;
#91244=ORIENTED_EDGE ( 'NONE', *, *, #192882, .F. ) ;
#91294=DIRECTION ( 'NONE',  ( -1.000000000000000000, -0.000000000000000000, -0.000000000000000000 ) ) ;
#91303=CARTESIAN_POINT ( 'NONE',  ( 21.05000000000000071, 34.01125473725045367, -243.8802146427659352 ) ) ;
#91311=ORIENTED_EDGE ( 'NONE', *, *, #168054, .F. ) ;
#91316=DIRECTION ( 'NONE',  ( 0.000000000000000000, 0.9126074666063660468, 0.4088369013363524762 ) ) ;
#91363=DIRECTION ( 'NONE',  ( 1.000000000000000000, 0.000000000000000000, -0.000000000000000000 ) ) ;
#91373=EDGE_LOOP ( 'NONE', ( #121426, #131092, #251314, #67822 ) ) ;
#91398=CYLINDRICAL_SURFACE ( 'NONE', #97936, 0.09999999999999609201 ) ;
#91402=TOROIDAL_SURFACE ( 'NONE', #20669, 11.90000000000000391, 0.1000000000000000056 ) ;
#91403=VERTEX_POINT ( 'NONE', #237713 ) ;
#91430=EDGE_LOOP ( 'NONE', ( #74850, #5417, #98567, #62300 ) ) ;
#91451=TOROIDAL_SURFACE ( 'NONE', #237193, 12.97499999999999609, 0.1000000000000000056 ) ;
#91452=ORIENTED_EDGE ( 'NONE', *, *, #159550, .F. ) ;
#91485=ORIENTED_EDGE ( 'NONE', *, *, #49592, .F. ) ;
#91487=ADVANCED_FACE ( 'NONE', ( #223266 ), #156294, .T. ) ;
#91498=AXIS2_PLACEMENT_3D ( 'NONE', #183948, #146097, #206085 ) ;
#91579=DIRECTION ( 'NONE',  ( -0.7071067811865412445, -0.2890913453339235550, 0.6453109281989813928 ) ) ;
#91587=EDGE_LOOP ( 'NONE', ( #35200, #5784, #124641, #237084 ) ) ;
#91609=CARTESIAN_POINT ( 'NONE',  ( -23.15000000000000213, 48.79765034352288922, -253.5326144460178170 ) ) ;
#91621=EDGE_CURVE ( 'NONE', #192597, #220241, #239470, .T. ) ;
#91645=DIRECTION ( 'NONE',  ( -4.408576920032448588E-17, 0.8490545835447252943, 0.5283051335749948674 ) ) ;
#91652=DIRECTION ( 'NONE',  ( 1.000000000000000000, -1.207181226542539700E-16, 2.694675058168174199E-16 ) ) ;
#91658=DIRECTION ( 'NONE',  ( 0.000000000000000000, 0.8490545835447238510, 0.5283051335749973099 ) ) ;
#91687=ORIENTED_EDGE ( 'NONE', *, *, #55570, .F. ) ;
#91698=DIRECTION ( 'NONE',  ( 0.000000000000000000, -0.9126074666063545004, -0.4088369013363783999 ) ) ;
#91701=EDGE_LOOP ( 'NONE', ( #88545, #207375, #153710, #206318 ) ) ;
#91714=ADVANCED_FACE ( 'NONE', ( #16763 ), #168272, .F. ) ;
#91808=EDGE_CURVE ( 'NONE', #111477, #101051, #66135, .T. ) ;
#91814=CARTESIAN_POINT ( 'NONE',  ( -20.85000000000000142, 78.48087866980282001, -232.8271061603568910 ) ) ;
#91821=ADVANCED_FACE ( 'NONE', ( #126091 ), #107828, .F. ) ;
#91824=ORIENTED_EDGE ( 'NONE', *, *, #49874, .F. ) ;
#91829=DIRECTION ( 'NONE',  ( 0.000000000000000000, 0.9126074666063769270, 0.4088369013363280513 ) ) ;
#91840=DIRECTION ( 'NONE',  ( 0.000000000000000000, -0.07847809223012357227, -0.9969158384938622275 ) ) ;
#91860=VERTEX_POINT ( 'NONE', #131239 ) ;
#91870=DIRECTION ( 'NONE',  ( 2.952720810173289112E-16, 0.4088369013363282733, -0.9126074666063769270 ) ) ;
#91889=VECTOR ( 'NONE', #224847, 1000.000000000000000 ) ;
#91918=VERTEX_POINT ( 'NONE', #67416 ) ;
#91926=AXIS2_PLACEMENT_3D ( 'NONE', #223861, #50351, #148193 ) ;
#91934=CIRCLE ( 'NONE', #216832, 0.09999999999999950595 ) ;
#91944=CARTESIAN_POINT ( 'NONE',  ( 18.49999999999999289, 23.29878867550048938, -248.4686781323362084 ) ) ;
#91952=ADVANCED_FACE ( 'NONE', ( #33471 ), #192504, .T. ) ;
#91972=DIRECTION ( 'NONE',  ( 0.000000000000000000, -0.9165223833629894123, 0.3999834006488590110 ) ) ;
#91978=CARTESIAN_POINT ( 'NONE',  ( 20.94999999999999929, 67.23127455305835554, -235.8551265064784559 ) ) ;
#91983=CARTESIAN_POINT ( 'NONE',  ( 22.49806830649814060, 31.82532512087596288, -238.9510566881495777 ) ) ;
#92000=ADVANCED_FACE ( 'NONE', ( #95953 ), #93894, .T. ) ;
#92001=CIRCLE ( 'NONE', #150287, 0.09999999999999609201 ) ;
#92010=CARTESIAN_POINT ( 'NONE',  ( -21.03922262424680056, 38.16640938004818651, -236.1388068296846541 ) ) ;
#92020=CYLINDRICAL_SURFACE ( 'NONE', #239996, 0.1000000000000024342 ) ;
#92022=ORIENTED_EDGE ( 'NONE', *, *, #35358, .F. ) ;
#92029=CYLINDRICAL_SURFACE ( 'NONE', #218420, 0.09999999999999108213 ) ;
#92031=DIRECTION ( 'NONE',  ( -0.000000000000000000, 0.4088369013363283844, -0.9126074666063769270 ) ) ;
#92046=ORIENTED_EDGE ( 'NONE', *, *, #163245, .T. ) ;
#92049=CIRCLE ( 'NONE', #167115, 0.2000000000000048683 ) ;
#92053=ADVANCED_FACE ( 'NONE', ( #223592 ), #162378, .F. ) ;
#92070=CARTESIAN_POINT ( 'NONE',  ( 18.59999999999996945, 67.85909929089923764, -227.8797997985275856 ) ) ;
#92115=ORIENTED_EDGE ( 'NONE', *, *, #210037, .T. ) ;
#92118=EDGE_LOOP ( 'NONE', ( #24073, #84343, #197844, #122600 ) ) ;
#92119=CIRCLE ( 'NONE', #254414, 0.09999999999999939493 ) ;
#92145=CARTESIAN_POINT ( 'NONE',  ( 23.15000000000000213, 49.36776662947724503, -253.7196102226803021 ) ) ;
#92146=ORIENTED_EDGE ( 'NONE', *, *, #102982, .T. ) ;
#92154=AXIS2_PLACEMENT_3D ( 'NONE', #106561, #7478, #86990 ) ;
#92158=EDGE_CURVE ( 'NONE', #118767, #174500, #48826, .T. ) ;
#92188=FACE_OUTER_BOUND ( 'NONE', #60492, .T. ) ;
#92218=PLANE ( 'NONE',  #240478 ) ;
#92291=DIRECTION ( 'NONE',  ( 0.000000000000000000, 0.9126074666063844765, 0.4088369013363114535 ) ) ;
#92319=ORIENTED_EDGE ( 'NONE', *, *, #23772, .F. ) ;
#92325=CARTESIAN_POINT ( 'NONE',  ( 20.94999999999999574, 43.39316802731212874, -245.2602608822587342 ) ) ;
#92364=CARTESIAN_POINT ( 'NONE',  ( 21.14999999999999858, 42.98415524044398950, -233.9519173640447889 ) ) ;
#92367=AXIS2_PLACEMENT_3D ( 'NONE', #111303, #228694, #172606 ) ;
#92386=ORIENTED_EDGE ( 'NONE', *, *, #9708, .T. ) ;
#92398=DIRECTION ( 'NONE',  ( 0.000000000000000000, 0.9126074666063660468, 0.4088369013363524762 ) ) ;
#92432=FACE_OUTER_BOUND ( 'NONE', #143662, .T. ) ;
#92434=DIRECTION ( 'NONE',  ( 0.000000000000000000, 0.9126074666063844765, 0.4088369013363114535 ) ) ;
#92447=AXIS2_PLACEMENT_3D ( 'NONE', #241148, #62500, #136888 ) ;
#92460=VERTEX_POINT ( 'NONE', #35721 ) ;
#92490=ORIENTED_EDGE ( 'NONE', *, *, #217240, .T. ) ;
#92495=EDGE_LOOP ( 'NONE', ( #107912, #33440, #44825, #166369 ) ) ;
#92497=DIRECTION ( 'NONE',  ( 0.000000000000000000, 0.9126074666063769270, 0.4088369013363280513 ) ) ;
#92522=DIRECTION ( 'NONE',  ( 0.000000000000000000, -0.3999834006488773852, -0.9165223833629813077 ) ) ;
#92536=EDGE_LOOP ( 'NONE', ( #218826, #104879, #106956, #178064 ) ) ;
#92544=CARTESIAN_POINT ( 'NONE',  ( -18.59999999999999787, 42.98415524044398950, -233.9519173640448173 ) ) ;
#92559=ORIENTED_EDGE ( 'NONE', *, *, #43659, .F. ) ;
#92583=CARTESIAN_POINT ( 'NONE',  ( -18.59999999999999787, 47.07326788871598211, -255.0992659944397190 ) ) ;
#92601=CIRCLE ( 'NONE', #213402, 0.1999999999999998446 ) ;
#92611=CARTESIAN_POINT ( 'NONE',  ( -20.85000000000000142, 72.03510814376021187, -246.5782642391033903 ) ) ;
#92627=DIRECTION ( 'NONE',  ( 0.000000000000000000, 0.9126074666063545004, 0.4088369013363783999 ) ) ;
#92628=CIRCLE ( 'NONE', #217699, 11.80000000000001315 ) ;
#92649=EDGE_CURVE ( 'NONE', #243903, #168786, #106907, .T. ) ;
#92658=TOROIDAL_SURFACE ( 'NONE', #5717, 11.65000000000000036, 0.1000000000000000056 ) ;
#92660=DIRECTION ( 'NONE',  ( 0.000000000000000000, 0.9126074666063660468, 0.4088369013363524762 ) ) ;
#92672=CARTESIAN_POINT ( 'NONE',  ( 21.05000000000000071, 45.65843669757526158, -240.2045374387683410 ) ) ;
#92676=AXIS2_PLACEMENT_3D ( 'NONE', #74788, #154334, #254637 ) ;
#92700=CARTESIAN_POINT ( 'NONE',  ( 18.59999999999997655, 67.23127455305835554, -235.8551265064784559 ) ) ;
#92722=CIRCLE ( 'NONE', #163653, 0.09999999999999609201 ) ;
#92758=DIRECTION ( 'NONE',  ( 1.000000000000000000, -1.335000415235278971E-16, 2.979993593738921214E-16 ) ) ;
#92776=ORIENTED_EDGE ( 'NONE', *, *, #237721, .T. ) ;
#92804=VECTOR ( 'NONE', #169512, 1000.000000000000114 ) ;
#92815=ORIENTED_EDGE ( 'NONE', *, *, #215549, .F. ) ;
#92822=TOROIDAL_SURFACE ( 'NONE', #63604, 7.800000000000000711, 0.1000000000000000056 ) ;
#92829=VECTOR ( 'NONE', #123127, 1000.000000000000114 ) ;
#92913=VECTOR ( 'NONE', #114601, 1000.000000000000114 ) ;
#92926=ADVANCED_FACE ( 'NONE', ( #207079 ), #144496, .T. ) ;
#92954=CARTESIAN_POINT ( 'NONE',  ( -20.85000000000000142, 67.23127455305835554, -235.8551265064784559 ) ) ;
#92986=CARTESIAN_POINT ( 'NONE',  ( -18.59999999999999787, 78.57213941646344324, -232.7862224702232652 ) ) ;
#92996=CARTESIAN_POINT ( 'NONE',  ( -21.14999999999999858, 38.08698097766499302, -236.1457910985472779 ) ) ;
#93020=TOROIDAL_SURFACE ( 'NONE', #38866, 0.2000000000000000111, 0.1000000000000000056 ) ;
#93027=CARTESIAN_POINT ( 'NONE',  ( 20.95512820512820795, 44.16399506693049659, -236.4628398677790813 ) ) ;
#93066=DIRECTION ( 'NONE',  ( 0.000000000000000000, 0.9126074666063844765, 0.4088369013363113980 ) ) ;
#93074=AXIS2_PLACEMENT_3D ( 'NONE', #116922, #196446, #17803 ) ;
#93087=VERTEX_POINT ( 'NONE', #171836 ) ;
#93143=ORIENTED_EDGE ( 'NONE', *, *, #217507, .T. ) ;
#93168=AXIS2_PLACEMENT_3D ( 'NONE', #253456, #236470, #190955 ) ;
#93177=DIRECTION ( 'NONE',  ( 1.000000000000000000, 0.000000000000000000, 0.000000000000000000 ) ) ;
#93187=ORIENTED_EDGE ( 'NONE', *, *, #79021, .T. ) ;
#93188=DIRECTION ( 'NONE',  ( 0.000000000000000000, -0.4088369013363280513, 0.9126074666063769270 ) ) ;
#93200=AXIS2_PLACEMENT_3D ( 'NONE', #168830, #245757, #67113 ) ;
#93206=FACE_OUTER_BOUND ( 'NONE', #54395, .T. ) ;
#93242=VERTEX_POINT ( 'NONE', #240764 ) ;
#93264=DIRECTION ( 'NONE',  ( -1.000000000000000000, 1.207181226542539700E-16, -2.694675058168174199E-16 ) ) ;
#93266=DIRECTION ( 'NONE',  ( 0.000000000000000000, 0.9126074666063774821, 0.4088369013363270521 ) ) ;
#93296=AXIS2_PLACEMENT_3D ( 'NONE', #31975, #232737, #134869 ) ;
#93328=ORIENTED_EDGE ( 'NONE', *, *, #124898, .T. ) ;
#93343=DIRECTION ( 'NONE',  ( 1.836970198721030427E-16, 0.4088369013363281623, -0.9126074666063771490 ) ) ;
#93360=AXIS2_PLACEMENT_3D ( 'NONE', #98601, #256370, #37410 ) ;
#93361=DIRECTION ( 'NONE',  ( 0.000000000000000000, 0.8490545835447252943, 0.5283051335749947564 ) ) ;
#93405=ORIENTED_EDGE ( 'NONE', *, *, #53704, .T. ) ;
#93409=DIRECTION ( 'NONE',  ( 0.000000000000000000, -0.9126074666063545004, -0.4088369013363783999 ) ) ;
#93477=ORIENTED_EDGE ( 'NONE', *, *, #217152, .F. ) ;
#93572=FACE_OUTER_BOUND ( 'NONE', #165942, .T. ) ;
#93608=AXIS2_PLACEMENT_3D ( 'NONE', #181507, #180220, #43268 ) ;
#93650=EDGE_LOOP ( 'NONE', ( #129561, #94447, #256867, #32971 ) ) ;
#93666=CIRCLE ( 'NONE', #22782, 0.1000000000000024342 ) ;
#93674=DIRECTION ( 'NONE',  ( -0.000000000000000000, -0.9126074666063770380, -0.4088369013363281068 ) ) ;
#93676=AXIS2_PLACEMENT_3D ( 'NONE', #226980, #49624, #127887 ) ;
#93707=CARTESIAN_POINT ( 'NONE',  ( -20.94999999999999929, 35.94660524813657076, -234.4748257877825495 ) ) ;
#93751=DIRECTION ( 'NONE',  ( -0.000000000000000000, 0.4088369013363282733, -0.9126074666063769270 ) ) ;
#93757=ORIENTED_EDGE ( 'NONE', *, *, #160543, .T. ) ;
#93770=FACE_OUTER_BOUND ( 'NONE', #82884, .T. ) ;
#93773=ORIENTED_EDGE ( 'NONE', *, *, #184687, .F. ) ;
#93779=ORIENTED_EDGE ( 'NONE', *, *, #86643, .T. ) ;
#93781=ADVANCED_FACE ( 'NONE', ( #106041 ), #184311, .T. ) ;
#93804=CARTESIAN_POINT ( 'NONE',  ( 21.07928932188134397, 30.84304088367083097, -252.0482413927653340 ) ) ;
#93828=EDGE_CURVE ( 'NONE', #253877, #68201, #133345, .T. ) ;
#93846=DIRECTION ( 'NONE',  ( 0.000000000000000000, 0.4088369013363229998, -0.9126074666063793694 ) ) ;
#93866=EDGE_LOOP ( 'NONE', ( #165686, #185521, #235543, #13205 ) ) ;
#93893=DIRECTION ( 'NONE',  ( -1.000000000000000000, -0.000000000000000000, 0.000000000000000000 ) ) ;
#93894=TOROIDAL_SURFACE ( 'NONE', #106523, 11.65000000000000036, 0.1000000000000000056 ) ;
#93920=VERTEX_POINT ( 'NONE', #111210 ) ;
#93945=DIRECTION ( 'NONE',  ( 1.000000000000000000, -1.207181226542539700E-16, 2.694675058168174199E-16 ) ) ;
#93949=DIRECTION ( 'NONE',  ( 0.000000000000000000, 0.9126074666063804797, 0.4088369013363203908 ) ) ;
#93988=EDGE_CURVE ( 'NONE', #44800, #75249, #49399, .T. ) ;
#93993=DIRECTION ( 'NONE',  ( 0.000000000000000000, -0.9126074666063769270, -0.4088369013363280513 ) ) ;
#94013=DIRECTION ( 'NONE',  ( -1.000000000000000000, 7.510212038922846022E-17, -1.676432719286211941E-16 ) ) ;
#94049=VECTOR ( 'NONE', #46236, 1000.000000000000114 ) ;
#94065=ORIENTED_EDGE ( 'NONE', *, *, #21700, .F. ) ;
#94091=EDGE_LOOP ( 'NONE', ( #51030, #174605, #116153, #157750 ) ) ;
#94097=VERTEX_POINT ( 'NONE', #121505 ) ;
#94117=AXIS2_PLACEMENT_3D ( 'NONE', #77795, #158666, #118226 ) ;
#94135=CARTESIAN_POINT ( 'NONE',  ( 21.33487959338958362, 33.90926806716007746, -243.4133681147159223 ) ) ;
#94159=EDGE_LOOP ( 'NONE', ( #134548, #178181, #88683, #33626 ) ) ;
#94165=CARTESIAN_POINT ( 'NONE',  ( -20.94999999999999929, 69.09936979046463534, -247.6075824278584889 ) ) ;
#94170=EDGE_CURVE ( 'NONE', #79169, #161112, #13102, .T. ) ;
#94197=EDGE_CURVE ( 'NONE', #11614, #61629, #28851, .T. ) ;
#94237=CARTESIAN_POINT ( 'NONE',  ( 22.39999999999999858, 36.65892442174472876, -249.5511627012454596 ) ) ;
#94258=ORIENTED_EDGE ( 'NONE', *, *, #201994, .T. ) ;
#94269=CIRCLE ( 'NONE', #240026, 0.09999999999999939493 ) ;
#94297=CARTESIAN_POINT ( 'NONE',  ( -20.85000000000000142, 74.83412143252222393, -233.7087995678629966 ) ) ;
#94301=CARTESIAN_POINT ( 'NONE',  ( 21.08489247129320887, 44.30010541822777981, -236.4001943044475809 ) ) ;
#94305=CIRCLE ( 'NONE', #90029, 4.149999999999993250 ) ;
#94308=CARTESIAN_POINT ( 'NONE',  ( -22.39999999999999503, 33.38250548509083160, -242.4821227592188961 ) ) ;
#94331=CARTESIAN_POINT ( 'NONE',  ( 20.84999999999999432, 74.93036000061670165, -233.6816308724374949 ) ) ;
#94347=DIRECTION ( 'NONE',  ( 1.000000000000000000, 0.000000000000000000, 0.000000000000000000 ) ) ;
#94408=VERTEX_POINT ( 'NONE', #181163 ) ;
#94432=B_SPLINE_CURVE_WITH_KNOTS ( 'NONE', 3,
 ( #134633, #113810, #56386, #253313, #175122, #150389, #152980, #194670 ),
 .UNSPECIFIED., .F., .F.,
 ( 4, 2, 2, 4 ),
 ( 0.000000000000000000, 0.0001881495939909944156, 0.0002822243909864270727, 0.0003762991879818597570 ),
 .UNSPECIFIED. ) ;
#94438=AXIS2_PLACEMENT_3D ( 'NONE', #63702, #6287, #143235 ) ;
#94447=ORIENTED_EDGE ( 'NONE', *, *, #109274, .F. ) ;
#94448=ADVANCED_FACE ( 'NONE', ( #128553 ), #161611, .F. ) ;
#94459=FACE_OUTER_BOUND ( 'NONE', #42028, .T. ) ;
#94505=LINE ( 'NONE', #257377, #83356 ) ;
#94523=DIRECTION ( 'NONE',  ( 0.000000000000000000, 0.4088369013363783999, -0.9126074666063545004 ) ) ;
#94542=DIRECTION ( 'NONE',  ( -1.000000000000000000, -0.000000000000000000, -0.000000000000000000 ) ) ;
#94560=EDGE_CURVE ( 'NONE', #109819, #93920, #28870, .T. ) ;
#94578=FACE_OUTER_BOUND ( 'NONE', #191624, .T. ) ;
#94648=AXIS2_PLACEMENT_3D ( 'NONE', #238886, #64095, #139755 ) ;
#94654=DIRECTION ( 'NONE',  ( 0.000000000000000000, 0.5859227990963362664, 0.8103668758649469339 ) ) ;
#94697=ORIENTED_EDGE ( 'NONE', *, *, #18930, .T. ) ;
#94705=CARTESIAN_POINT ( 'NONE',  ( -22.24259225415828212, 33.50553549281345056, -242.7544660500353757 ) ) ;
#94708=ADVANCED_FACE ( 'NONE', ( #218330 ), #82299, .F. ) ;
#94712=EDGE_LOOP ( 'NONE', ( #190591, #141544, #109589, #75230 ) ) ;
#94736=CARTESIAN_POINT ( 'NONE',  ( -23.25000000000000000, 40.44624540816119662, -247.8544895606997329 ) ) ;
#94741=CARTESIAN_POINT ( 'NONE',  ( -20.85000000000000142, 74.95904887477786360, -233.7774272632847783 ) ) ;
#94766=CONICAL_SURFACE ( 'NONE', #40664, 4.299999999999953637, 0.7853981633974466137 ) ;
#94774=CARTESIAN_POINT ( 'NONE',  ( 20.53930447208009014, 40.69342982378280738, -237.9069413209054744 ) ) ;
#94816=CARTESIAN_POINT ( 'NONE',  ( 21.05000000000000071, 70.97296516614450468, -234.1788952109995137 ) ) ;
#94839=CARTESIAN_POINT ( 'NONE',  ( -18.50000000000000000, 52.32046880629621199, -232.2896150449452364 ) ) ;
#94854=VERTEX_POINT ( 'NONE', #185654 ) ;
#94858=DIRECTION ( 'NONE',  ( -1.000000000000000000, -0.000000000000000000, -0.000000000000000000 ) ) ;
#94886=ORIENTED_EDGE ( 'NONE', *, *, #181788, .F. ) ;
#94921=ORIENTED_EDGE ( 'NONE', *, *, #136026, .F. ) ;
#94987=DIRECTION ( 'NONE',  ( -0.000000000000000000, 0.8103668758649578141, -0.5859227990963212784 ) ) ;
#95006=DIRECTION ( 'NONE',  ( 0.000000000000000000, 0.4088369013363283844, -0.9126074666063769270 ) ) ;
#95035=DIRECTION ( 'NONE',  ( 1.000000000000000000, 0.000000000000000000, 0.000000000000000000 ) ) ;
#95060=VERTEX_POINT ( 'NONE', #57679 ) ;
#95071=EDGE_CURVE ( 'NONE', #91918, #96525, #107455, .T. ) ;
#95084=ORIENTED_EDGE ( 'NONE', *, *, #23486, .F. ) ;
#95097=CARTESIAN_POINT ( 'NONE',  ( 21.59780538579342490, 30.36975234701187176, -252.2601773037668806 ) ) ;
#95145=ORIENTED_EDGE ( 'NONE', *, *, #5219, .F. ) ;
#95146=EDGE_LOOP ( 'NONE', ( #257548, #254061, #224955, #86126 ) ) ;
#95155=EDGE_LOOP ( 'NONE', ( #124192, #198363, #70096, #44464 ) ) ;
#95166=CARTESIAN_POINT ( 'NONE',  ( 18.49999999999999289, 54.57427006634497957, -228.7596887170734306 ) ) ;
#95176=EDGE_CURVE ( 'NONE', #60871, #57597, #158130, .T. ) ;
#95178=ORIENTED_EDGE ( 'NONE', *, *, #244581, .F. ) ;
#95198=ORIENTED_EDGE ( 'NONE', *, *, #188829, .T. ) ;
#95207=CARTESIAN_POINT ( 'NONE',  ( 23.15000000000000213, 49.57218508014540959, -254.1759139559835035 ) ) ;
#95263=CARTESIAN_POINT ( 'NONE',  ( 23.14999999999999503, 45.29262862071417572, -238.6157088101306556 ) ) ;
#95266=ORIENTED_EDGE ( 'NONE', *, *, #74020, .F. ) ;
#95276=CARTESIAN_POINT ( 'NONE',  ( -21.05000000000000426, 30.91403104479204345, -252.1478540170565736 ) ) ;
#95284=DIRECTION ( 'NONE',  ( 0.000000000000000000, 0.4088369013363279403, -0.9126074666063771490 ) ) ;
#95357=ADVANCED_FACE ( 'NONE', ( #232199 ), #131789, .F. ) ;
#95373=EDGE_CURVE ( 'NONE', #182399, #191682, #70061, .T. ) ;
#95386=ORIENTED_EDGE ( 'NONE', *, *, #144169, .F. ) ;
#95414=FACE_OUTER_BOUND ( 'NONE', #205300, .T. ) ;
#95453=CYLINDRICAL_SURFACE ( 'NONE', #82921, 0.09999999999999950595 ) ;
#95504=FILL_AREA_STYLE_COLOUR ( '', #119518 ) ;
#95511=LINE ( 'NONE', #96765, #26235 ) ;
#95535=DIRECTION ( 'NONE',  ( 0.000000000000000000, -0.9126074666063660468, -0.4088369013363524762 ) ) ;
#95537=DIRECTION ( 'NONE',  ( 0.000000000000000000, 0.9126074666063660468, 0.4088369013363524762 ) ) ;
#95555=ORIENTED_EDGE ( 'NONE', *, *, #256196, .F. ) ;
#95556=EDGE_CURVE ( 'NONE', #15852, #51812, #24456, .T. ) ;
#95572=EDGE_CURVE ( 'NONE', #21323, #13609, #126345, .T. ) ;
#95600=VERTEX_POINT ( 'NONE', #100339 ) ;
#95612=CARTESIAN_POINT ( 'NONE',  ( -21.05000000000000071, 44.00266445878927613, -258.8505972146074896 ) ) ;
#95638=FACE_OUTER_BOUND ( 'NONE', #69141, .T. ) ;
#95643=CARTESIAN_POINT ( 'NONE',  ( 18.49999999999999289, 21.17283678855157802, -243.7231193059830332 ) ) ;
#95658=CARTESIAN_POINT ( 'NONE',  ( 23.25000000000000355, 52.04006110304540300, -267.2673759609633635 ) ) ;
#95677=CARTESIAN_POINT ( 'NONE',  ( -20.64999999999999858, 44.91518204311810081, -238.0177672736398620 ) ) ;
#95685=ORIENTED_EDGE ( 'NONE', *, *, #8475, .T. ) ;
#95728=CIRCLE ( 'NONE', #20770, 0.09999999999999939493 ) ;
#95748=FACE_OUTER_BOUND ( 'NONE', #132616, .T. ) ;
#95835=AXIS2_PLACEMENT_3D ( 'NONE', #95263, #166177, #35333 ) ;
#95856=ADVANCED_FACE ( 'NONE', ( #75392 ), #173230, .F. ) ;
#95899=AXIS2_PLACEMENT_3D ( 'NONE', #86422, #203829, #160877 ) ;
#95906=ORIENTED_EDGE ( 'NONE', *, *, #9721, .F. ) ;
#95914=DIRECTION ( 'NONE',  ( 0.000000000000000000, 0.9126074666063844765, 0.4088369013363113980 ) ) ;
#95925=DIRECTION ( 'NONE',  ( 1.000000000000000000, 0.000000000000000000, 0.000000000000000000 ) ) ;
#95935=CARTESIAN_POINT ( 'NONE',  ( 21.05000000000000071, 30.73075574124490572, -252.3164853687435709 ) ) ;
#95940=CARTESIAN_POINT ( 'NONE',  ( 18.58222699835054570, 68.11153784908182729, -224.1393723182492579 ) ) ;
#95953=FACE_OUTER_BOUND ( 'NONE', #170843, .T. ) ;
#95992=ADVANCED_FACE ( 'NONE', ( #141740 ), #120502, .T. ) ;
#96001=ADVANCED_FACE ( 'NONE', ( #165165 ), #2218, .T. ) ;
#96022=AXIS2_PLACEMENT_3D ( 'NONE', #192081, #241547, #25098 ) ;
#96047=CARTESIAN_POINT ( 'NONE',  ( -22.39999999999999858, 33.47376623175147614, -242.4412390690852703 ) ) ;
#96070=ORIENTED_EDGE ( 'NONE', *, *, #124211, .T. ) ;
#96093=CARTESIAN_POINT ( 'NONE',  ( 18.59999999999998366, 67.23127455305835554, -235.8551265064784559 ) ) ;
#96103=CARTESIAN_POINT ( 'NONE',  ( -22.39999999999999858, 33.38250548509083160, -242.4821227592188961 ) ) ;
#96138=VECTOR ( 'NONE', #254261, 1000.000000000000000 ) ;
#96154=AXIS2_PLACEMENT_3D ( 'NONE', #235352, #56689, #136232 ) ;
#96208=DIRECTION ( 'NONE',  ( -1.000000000000000000, -0.000000000000000000, -0.000000000000000000 ) ) ;
#96209=CARTESIAN_POINT ( 'NONE',  ( 20.85000000000000142, 78.48087866980282001, -232.8271061603568910 ) ) ;
#96247=ORIENTED_EDGE ( 'NONE', *, *, #185197, .F. ) ;
#96275=ORIENTED_EDGE ( 'NONE', *, *, #110851, .T. ) ;
#96306=ADVANCED_FACE ( 'NONE', ( #29107 ), #48614, .F. ) ;
#96309=DIRECTION ( 'NONE',  ( -1.000000000000000000, 1.207181226542539700E-16, -2.694675058168174199E-16 ) ) ;
#96319=EDGE_CURVE ( 'NONE', #198468, #183601, #133134, .T. ) ;
#96332=CIRCLE ( 'NONE', #17263, 0.3999999999999983569 ) ;
#96339=LINE ( 'NONE', #113361, #18817 ) ;
#96346=SPHERICAL_SURFACE ( 'NONE', #157522, 0.1000000000000000056 ) ;
#96422=DIRECTION ( 'NONE',  ( 1.000000000000000000, 0.000000000000000000, 0.000000000000000000 ) ) ;
#96450=AXIS2_PLACEMENT_3D ( 'NONE', #245012, #23435, #164210 ) ;
#96456=DIRECTION ( 'NONE',  ( -0.000000000000000000, 0.9126074666063770380, 0.4088369013363281068 ) ) ;
#96474=ORIENTED_EDGE ( 'NONE', *, *, #188289, .F. ) ;
#96484=CYLINDRICAL_SURFACE ( 'NONE', #12133, 0.09999999999999939493 ) ;
#96489=ORIENTED_EDGE ( 'NONE', *, *, #51230, .T. ) ;
#96507=CARTESIAN_POINT ( 'NONE',  ( -21.14999999999999858, 31.98723526783714988, -238.8784020251475511 ) ) ;
#96509=ADVANCED_FACE ( 'NONE', ( #62660 ), #120090, .T. ) ;
#96525=VERTEX_POINT ( 'NONE', #160494 ) ;
#96538=DIRECTION ( 'NONE',  ( 0.000000000000000000, -0.8371762388950346745, -0.5469332180710581026 ) ) ;
#96569=CARTESIAN_POINT ( 'NONE',  ( -23.25000000000000000, 30.73962027982165779, -265.0781340245722504 ) ) ;
#96573=ORIENTED_EDGE ( 'NONE', *, *, #216596, .F. ) ;
#96609=EDGE_CURVE ( 'NONE', #210045, #198468, #28, .T. ) ;
#96635=ORIENTED_EDGE ( 'NONE', *, *, #249062, .F. ) ;
#96641=DIRECTION ( 'NONE',  ( 0.000000000000000000, 0.9126074666063844765, 0.4088369013363113980 ) ) ;
#96671=CARTESIAN_POINT ( 'NONE',  ( 20.94999999999999929, 69.06797323185276127, -247.4100621602722470 ) ) ;
#96678=ORIENTED_EDGE ( 'NONE', *, *, #80063, .F. ) ;
#96682=VERTEX_POINT ( 'NONE', #45655 ) ;
#96687=DIRECTION ( 'NONE',  ( -4.408576920032448588E-17, -0.9594490217226104845, -0.2818822000686205254 ) ) ;
#96689=EDGE_LOOP ( 'NONE', ( #6905, #68141, #122862, #229592 ) ) ;
#96693=EDGE_CURVE ( 'NONE', #7829, #182906, #33392, .T. ) ;
#96707=CARTESIAN_POINT ( 'NONE',  ( 18.41815437325358573, 77.14150793766424385, -241.8237832882541625 ) ) ;
#96716=DIRECTION ( 'NONE',  ( 0.000000000000000000, -0.3945274997758418944, 0.9188841341108372474 ) ) ;
#96765=CARTESIAN_POINT ( 'NONE',  ( 21.05000000000000071, 36.69980811187836878, -249.6424234479061113 ) ) ;
#96782=ORIENTED_EDGE ( 'NONE', *, *, #29438, .F. ) ;
#96802=ORIENTED_EDGE ( 'NONE', *, *, #114094, .F. ) ;
#96841=CYLINDRICAL_SURFACE ( 'NONE', #92676, 0.09999999999999939493 ) ;
#96850=ORIENTED_EDGE ( 'NONE', *, *, #186174, .F. ) ;
#96857=AXIS2_PLACEMENT_3D ( 'NONE', #126536, #27480, #186516 ) ;
#96867=CARTESIAN_POINT ( 'NONE',  ( -18.59999999999999787, 68.11287320386161070, -224.1382462126928488 ) ) ;
#96887=CIRCLE ( 'NONE', #34594, 11.70000000000000284 ) ;
#96907=ORIENTED_EDGE ( 'NONE', *, *, #89012, .F. ) ;
#96928=EDGE_CURVE ( 'NONE', #97342, #119120, #201843, .T. ) ;
#96933=CYLINDRICAL_SURFACE ( 'NONE', #54563, 0.09999999999999939493 ) ;
#96943=ORIENTED_EDGE ( 'NONE', *, *, #190156, .F. ) ;
#97001=EDGE_LOOP ( 'NONE', ( #199006, #172703, #241545, #204751, #79059, #155143, #55, #236151 ) ) ;
#97012=CARTESIAN_POINT ( 'NONE',  ( -21.05000000000000071, 34.04033409713371583, -243.8666379817185543 ) ) ;
#97021=LINE ( 'NONE', #74966, #44440 ) ;
#97031=LINE ( 'NONE', #236572, #17358 ) ;
#97063=ORIENTED_EDGE ( 'NONE', *, *, #181939, .F. ) ;
#97071=DIRECTION ( 'NONE',  ( 0.000000000000000000, 0.9126074666063751506, 0.4088369013363322146 ) ) ;
#97078=AXIS2_PLACEMENT_3D ( 'NONE', #137206, #197172, #58921 ) ;
#97096=AXIS2_PLACEMENT_3D ( 'NONE', #213033, #235176, #39575 ) ;
#97110=PLANE ( 'NONE',  #150945 ) ;
#97130=ORIENTED_EDGE ( 'NONE', *, *, #216596, .T. ) ;
#97135=CIRCLE ( 'NONE', #205502, 7.899999999999995914 ) ;
#97175=AXIS2_PLACEMENT_3D ( 'NONE', #123362, #191056, #250980 ) ;
#97188=ORIENTED_EDGE ( 'NONE', *, *, #184085, .T. ) ;
#97190=CARTESIAN_POINT ( 'NONE',  ( 18.59999999999996945, 68.11287320386161070, -224.1382462126928488 ) ) ;
#97213=EDGE_CURVE ( 'NONE', #181336, #4366, #254882, .T. ) ;
#97223=EDGE_CURVE ( 'NONE', #242821, #41483, #27874, .T. ) ;
#97225=CIRCLE ( 'NONE', #72348, 0.1000000000000024342 ) ;
#97237=EDGE_LOOP ( 'NONE', ( #194961, #179820, #210403, #52714 ) ) ;
#97261=AXIS2_PLACEMENT_3D ( 'NONE', #210994, #67941, #34955 ) ;
#97268=DIRECTION ( 'NONE',  ( 0.000000000000000000, -0.9126074666064696306, -0.4088369013361213278 ) ) ;
#97272=AXIS2_PLACEMENT_3D ( 'NONE', #31569, #229732, #225843 ) ;
#97312=DIRECTION ( 'NONE',  ( 0.000000000000000000, 0.9126074666063791474, 0.4088369013363231108 ) ) ;
#97334=DIRECTION ( 'NONE',  ( 0.000000000000000000, -0.9594490217226103734, -0.2818822000686205254 ) ) ;
#97342=VERTEX_POINT ( 'NONE', #165979 ) ;
#97354=FACE_OUTER_BOUND ( 'NONE', #210264, .T. ) ;
#97366=CARTESIAN_POINT ( 'NONE',  ( -21.05000000000000071, 69.20602499728043711, -247.8456586332460176 ) ) ;
#97383=VERTEX_POINT ( 'NONE', #207661 ) ;
#97390=CARTESIAN_POINT ( 'NONE',  ( -22.46246831459151494, 26.01821253579841198, -254.2940600222800072 ) ) ;
#97414=VERTEX_POINT ( 'NONE', #27757 ) ;
#97419=CARTESIAN_POINT ( 'NONE',  ( 20.04142135623730070, 54.35086488289006468, -228.7501953506800305 ) ) ;
#97452=DIRECTION ( 'NONE',  ( 0.000000000000000000, -0.9126074666063771490, -0.4088369013363281623 ) ) ;
#97464=DIRECTION ( 'NONE',  ( -1.000000000000000000, 1.207181226542539700E-16, -2.694675058168174199E-16 ) ) ;
#97473=AXIS2_PLACEMENT_3D ( 'NONE', #182585, #117467, #140879 ) ;
#97482=CARTESIAN_POINT ( 'NONE',  ( 22.50000000000000000, 29.50811709945092076, -252.6450601445781103 ) ) ;
#97528=CIRCLE ( 'NONE', #14205, 0.1000000000000051820 ) ;
#97563=ADVANCED_FACE ( 'NONE', ( #215338 ), #18427, .F. ) ;
#97569=AXIS2_PLACEMENT_3D ( 'NONE', #32520, #134127, #255318 ) ;
#97579=CARTESIAN_POINT ( 'NONE',  ( -18.59999999999999787, 43.57568952063339651, -245.1784935019914826 ) ) ;
#97580=ORIENTED_EDGE ( 'NONE', *, *, #173568, .F. ) ;
#97624=EDGE_CURVE ( 'NONE', #70449, #69371, #22305, .T. ) ;
#97629=TOROIDAL_SURFACE ( 'NONE', #218437, 0.2000000000000000111, 0.1000000000000000056 ) ;
#97634=CARTESIAN_POINT ( 'NONE',  ( 20.85000000000000142, 56.23643450586807546, -227.9054833905874204 ) ) ;
#97637=ORIENTED_EDGE ( 'NONE', *, *, #169861, .F. ) ;
#97680=CARTESIAN_POINT ( 'NONE',  ( -20.15000000000000568, 52.25315717083599765, -232.3839580427603835 ) ) ;
#97689=LINE ( 'NONE', #179843, #158989 ) ;
#97714=VERTEX_POINT ( 'NONE', #125236 ) ;
#97729=DIRECTION ( 'NONE',  ( 0.000000000000000000, 0.9126074666063660468, 0.4088369013363524762 ) ) ;
#97742=DIRECTION ( 'NONE',  ( 0.000000000000000000, -0.4088369013363280513, 0.9126074666063769270 ) ) ;
#97745=AXIS2_PLACEMENT_3D ( 'NONE', #109117, #129960, #188668 ) ;
#97786=AXIS2_PLACEMENT_3D ( 'NONE', #122752, #64040, #118896 ) ;
#97789=EDGE_CURVE ( 'NONE', #100153, #102227, #92628, .T. ) ;
#97802=ORIENTED_EDGE ( 'NONE', *, *, #125456, .F. ) ;
#97833=EDGE_CURVE ( 'NONE', #70783, #62010, #234266, .T. ) ;
#97877=EDGE_LOOP ( 'NONE', ( #152506, #171212, #182654, #127547 ) ) ;
#97880=DIRECTION ( 'NONE',  ( 1.000000000000000000, 0.000000000000000000, 0.000000000000000000 ) ) ;
#97881=AXIS2_PLACEMENT_3D ( 'NONE', #114855, #134393, #234806 ) ;
#97890=CARTESIAN_POINT ( 'NONE',  ( 20.94999999999999929, 49.53130139001177668, -254.0846532093228802 ) ) ;
#97895=VERTEX_POINT ( 'NONE', #230768 ) ;
#97911=ORIENTED_EDGE ( 'NONE', *, *, #162620, .T. ) ;
#97929=EDGE_CURVE ( 'NONE', #206700, #243903, #155220, .T. ) ;
#97933=DIRECTION ( 'NONE',  ( 0.000000000000000000, 0.9126074666063769270, 0.4088369013363280513 ) ) ;
#97936=AXIS2_PLACEMENT_3D ( 'NONE', #45844, #107094, #150105 ) ;
#97960=DIRECTION ( 'NONE',  ( -1.836970198721030427E-16, -0.4088369013363281623, 0.9126074666063771490 ) ) ;
#97975=ORIENTED_EDGE ( 'NONE', *, *, #256196, .T. ) ;
#98046=CARTESIAN_POINT ( 'NONE',  ( 18.50000000000000355, 54.96412023489454413, -230.1191065505895779 ) ) ;
#98090=AXIS2_PLACEMENT_3D ( 'NONE', #229098, #129968, #189970 ) ;
#98113=DIRECTION ( 'NONE',  ( 0.000000000000000000, 0.9126074666063602736, 0.4088369013363654103 ) ) ;
#98144=AXIS2_PLACEMENT_3D ( 'NONE', #189012, #109451, #212438 ) ;
#98241=EDGE_CURVE ( 'NONE', #47998, #249181, #159470, .T. ) ;
#98254=CARTESIAN_POINT ( 'NONE',  ( 18.59999999999999432, 47.89822068137787170, -246.3100470504847692 ) ) ;
#98262=PLANE ( 'NONE',  #136396 ) ;
#98279=CYLINDRICAL_SURFACE ( 'NONE', #84560, 0.1000000000000024342 ) ;
#98299=DIRECTION ( 'NONE',  ( -0.000000000000000000, 0.9594490217226103734, 0.2818822000686205254 ) ) ;
#98357=DIRECTION ( 'NONE',  ( 1.000000000000000000, 0.000000000000000000, 0.000000000000000000 ) ) ;
#98387=ORIENTED_EDGE ( 'NONE', *, *, #77577, .F. ) ;
#98398=CARTESIAN_POINT ( 'NONE',  ( 23.24999999999999645, 23.64630004163636912, -249.2443944789516195 ) ) ;
#98401=DIRECTION ( 'NONE',  ( 1.000000000000000000, 0.000000000000000000, -0.000000000000000000 ) ) ;
#98409=EDGE_CURVE ( 'NONE', #38307, #250431, #192168, .T. ) ;
#98432=AXIS2_PLACEMENT_3D ( 'NONE', #183210, #80210, #63241 ) ;
#98527=ORIENTED_EDGE ( 'NONE', *, *, #163176, .F. ) ;
#98567=ORIENTED_EDGE ( 'NONE', *, *, #2783, .T. ) ;
#98597=EDGE_CURVE ( 'NONE', #245440, #241978, #9817, .T. ) ;
#98599=DIRECTION ( 'NONE',  ( -3.265361837132813093E-16, -0.4088369013363281068, 0.9126074666063770380 ) ) ;
#98601=CARTESIAN_POINT ( 'NONE',  ( -20.64999999999999858, 62.04148992963929743, -247.7470044306132024 ) ) ;
#98617=CARTESIAN_POINT ( 'NONE',  ( -23.24999999999999645, 77.17949092533254429, -241.9177572069595783 ) ) ;
#98622=ORIENTED_EDGE ( 'NONE', *, *, #53466, .T. ) ;
#98628=CARTESIAN_POINT ( 'NONE',  ( 18.49999999999999645, 46.55954744353147134, -243.3218549665227783 ) ) ;
#98630=CIRCLE ( 'NONE', #202906, 0.1000000000000028227 ) ;
#98637=DIRECTION ( 'NONE',  ( 0.000000000000000000, -0.9126074666063769270, -0.4088369013363280513 ) ) ;
#98641=AXIS2_PLACEMENT_3D ( 'NONE', #56579, #137419, #216953 ) ;
#98656=CARTESIAN_POINT ( 'NONE',  ( -18.59999999999999787, 52.13794731297493712, -232.3713824252124880 ) ) ;
#98662=DIRECTION ( 'NONE',  ( 1.000000000000000000, 0.000000000000000000, 0.000000000000000000 ) ) ;
#98690=EDGE_LOOP ( 'NONE', ( #180595, #95685, #110655, #16190 ) ) ;
#98707=DIRECTION ( 'NONE',  ( -1.000000000000000000, -0.000000000000000000, 0.000000000000000000 ) ) ;
#98717=DIRECTION ( 'NONE',  ( -1.000000000000000000, -0.000000000000000000, -0.000000000000000000 ) ) ;
#98784=ORIENTED_EDGE ( 'NONE', *, *, #66408, .T. ) ;
#98798=DIRECTION ( 'NONE',  ( -0.000000000000000000, -0.9126074666063770380, -0.4088369013363281068 ) ) ;
#98815=ORIENTED_EDGE ( 'NONE', *, *, #244905, .T. ) ;
#98820=AXIS2_PLACEMENT_3D ( 'NONE', #10646, #227105, #167184 ) ;
#98874=PLANE ( 'NONE',  #136686 ) ;
#98929=( BOUNDED_SURFACE ( )  B_SPLINE_SURFACE ( 3, 2, ( 
 ( #6478, #85991, #7783 ),
 ( #148573, #246387, #110722 ),
 ( #165579, #145990, #228118 ),
 ( #49469, #225506, #62167 ),
 ( #125977, #221215, #23061 ),
 ( #244637, #145535, #3457 ) ),
 .UNSPECIFIED., .F., .F., .F. ) 
 B_SPLINE_SURFACE_WITH_KNOTS ( ( 4, 2, 4 ),
 ( 3, 3 ),
 ( 0.0001300404313046746687, 0.0003183318589266851870, 0.0005066232865486956782 ),
 ( 0.000000000000000000, 1.000000000000000000 ),
 .UNSPECIFIED. ) 
 GEOMETRIC_REPRESENTATION_ITEM ( )  RATIONAL_B_SPLINE_SURFACE ( (
 ( 1.000000000000000000, 0.7071067811865352493, 1.000000000000000000),
 ( 1.000000000000000000, 0.7625113560541721958, 1.000000000000000000),
 ( 1.000000000000000000, 0.8126073484686229254, 1.000000000000000000),
 ( 1.000000000000000000, 0.8923049332734449557, 1.000000000000000000),
 ( 1.000000000000000000, 0.9231914937768058715, 1.000000000000000000),
 ( 1.000000000000000000, 0.9238795325112977297, 1.000000000000000000) ) ) 
 REPRESENTATION_ITEM ( '' )  SURFACE ( )  );
#98959=CARTESIAN_POINT ( 'NONE',  ( 22.42357213249528769, 33.43151901755100397, -242.5892977220127307 ) ) ;
#98968=CARTESIAN_POINT ( 'NONE',  ( -21.05000000000000071, 56.02567683926420727, -227.9999002286038774 ) ) ;
#98971=CARTESIAN_POINT ( 'NONE',  ( 22.39999999999999503, 33.38250548509083870, -242.4821227592189246 ) ) ;
#98975=AXIS2_PLACEMENT_3D ( 'NONE', #227347, #128263, #244338 ) ;
#98984=CARTESIAN_POINT ( 'NONE',  ( -20.94999999999999929, 46.45388641681647357, -243.1520440498138385 ) ) ;
#98995=ADVANCED_FACE ( 'NONE', ( #64335 ), #242956, .F. ) ;
#99031=CIRCLE ( 'NONE', #61468, 0.09999999999999609201 ) ;
#99059=CARTESIAN_POINT ( 'NONE',  ( -21.14999999999999858, 31.85509083104287598, -238.8280249686205536 ) ) ;
#99060=CARTESIAN_POINT ( 'NONE',  ( 21.87500000000000355, 43.94346684630428967, -235.6041041703296344 ) ) ;
#99070=ORIENTED_EDGE ( 'NONE', *, *, #18098, .F. ) ;
#99078=ORIENTED_EDGE ( 'NONE', *, *, #146783, .T. ) ;
#99098=LINE ( 'NONE', #37893, #149213 ) ;
#99133=AXIS2_PLACEMENT_3D ( 'NONE', #147858, #128293, #51280 ) ;
#99141=DIRECTION ( 'NONE',  ( 0.000000000000000000, -0.5859227990963362664, -0.8103668758649469339 ) ) ;
#99143=EDGE_LOOP ( 'NONE', ( #137994, #178942, #20962 ) ) ;
#99196=EDGE_CURVE ( 'NONE', #192936, #120046, #37857, .T. ) ;
#99241=ORIENTED_EDGE ( 'NONE', *, *, #139496, .T. ) ;
#99245=VERTEX_POINT ( 'NONE', #121149 ) ;
#99272=EDGE_CURVE ( 'NONE', #79014, #199454, #107973, .T. ) ;
#99282=DIRECTION ( 'NONE',  ( 0.000000000000000000, 0.9126074666063769270, 0.4088369013363280513 ) ) ;
#99291=EDGE_LOOP ( 'NONE', ( #6524, #33147, #209188, #124022, #135012, #86078, #5743, #8947, #46522, #191236, #208499, #214719, #177865, #221087, #58657, #83756 ) ) ;
#99292=CARTESIAN_POINT ( 'NONE',  ( 23.14999999999999503, 56.02567683926420727, -227.9999002286038774 ) ) ;
#99300=DIRECTION ( 'NONE',  ( -0.000000000000000000, -0.9126074666063770380, -0.4088369013363281068 ) ) ;
#99339=TOROIDAL_SURFACE ( 'NONE', #174238, 4.149999999999999467, 0.1000000000000000056 ) ;
#99356=CIRCLE ( 'NONE', #166048, 0.09999999999999609201 ) ;
#99393=ORIENTED_EDGE ( 'NONE', *, *, #84027, .F. ) ;
#99400=FACE_OUTER_BOUND ( 'NONE', #4269, .T. ) ;
#99403=FACE_OUTER_BOUND ( 'NONE', #226247, .T. ) ;
#99404=AXIS2_PLACEMENT_3D ( 'NONE', #5860, #164952, #146648 ) ;
#99448=ORIENTED_EDGE ( 'NONE', *, *, #227497, .T. ) ;
#99485=ORIENTED_EDGE ( 'NONE', *, *, #60868, .T. ) ;
#99489=ORIENTED_EDGE ( 'NONE', *, *, #104764, .T. ) ;
#99512=CARTESIAN_POINT ( 'NONE',  ( 20.95512820512820440, 44.11820694106860685, -236.4833523840364933 ) ) ;
#99525=VERTEX_POINT ( 'NONE', #55653 ) ;
#99536=CYLINDRICAL_SURFACE ( 'NONE', #11693, 0.09999999999999609201 ) ;
#99551=CARTESIAN_POINT ( 'NONE',  ( 20.94999999999999574, 44.47083028126616000, -247.4212268238128161 ) ) ;
#99584=LINE ( 'NONE', #1782, #7467 ) ;
#99623=DIRECTION ( 'NONE',  ( 1.000000000000000000, 0.000000000000000000, 0.000000000000000000 ) ) ;
#99637=ORIENTED_EDGE ( 'NONE', *, *, #248422, .T. ) ;
#99692=PLANE ( 'NONE',  #16499 ) ;
#99709=LINE ( 'NONE', #39801, #119799 ) ;
#99730=DIRECTION ( 'NONE',  ( 0.000000000000000000, -0.9126074666063602736, -0.4088369013363654103 ) ) ;
#99740=EDGE_CURVE ( 'NONE', #191031, #81651, #4666, .T. ) ;
#99762=CARTESIAN_POINT ( 'NONE',  ( 22.60000000000000142, 36.65892442174472876, -249.5511627012454596 ) ) ;
#99768=DIRECTION ( 'NONE',  ( -1.000000000000000000, -0.000000000000000000, -0.000000000000000000 ) ) ;
#99770=DIRECTION ( 'NONE',  ( 1.000000000000000000, 0.000000000000000000, 0.000000000000000000 ) ) ;
#99777=CARTESIAN_POINT ( 'NONE',  ( 18.50596464788227280, 68.04082873524789932, -224.1991862745061894 ) ) ;
#99815=DIRECTION ( 'NONE',  ( 2.840903330521632269E-16, -0.09425075112713275638, -0.9955484899852801162 ) ) ;
#99817=VERTEX_POINT ( 'NONE', #245894 ) ;
#99831=EDGE_LOOP ( 'NONE', ( #113930, #166327, #20207, #70698 ) ) ;
#99838=LINE ( 'NONE', #197678, #168092 ) ;
#99851=CARTESIAN_POINT ( 'NONE',  ( 23.15000000000000213, 62.08148826970417389, -247.6553521922769221 ) ) ;
#99860=ORIENTED_EDGE ( 'NONE', *, *, #238420, .F. ) ;
#99877=CARTESIAN_POINT ( 'NONE',  ( -21.00023020733438983, 34.04610124266385185, -243.7188077099090719 ) ) ;
#99900=ORIENTED_EDGE ( 'NONE', *, *, #63146, .T. ) ;
#99909=CARTESIAN_POINT ( 'NONE',  ( 20.94999999999999574, 44.52640028187936849, -247.3006740988509193 ) ) ;
#99927=DIRECTION ( 'NONE',  ( 0.000000000000000000, -0.9126074666063770380, -0.4088369013363281068 ) ) ;
#99943=SPHERICAL_SURFACE ( 'NONE', #67007, 0.1000000000000000056 ) ;
#99945=ORIENTED_EDGE ( 'NONE', *, *, #176818, .T. ) ;
#99974=ORIENTED_EDGE ( 'NONE', *, *, #156774, .F. ) ;
#99991=ORIENTED_EDGE ( 'NONE', *, *, #119643, .F. ) ;
#99996=CIRCLE ( 'NONE', #254135, 0.09999999999999939493 ) ;
#100019=CIRCLE ( 'NONE', #133380, 0.1000000000000024342 ) ;
#100022=DIRECTION ( 'NONE',  ( 1.000000000000000000, 0.000000000000000000, 0.000000000000000000 ) ) ;
#100023=CARTESIAN_POINT ( 'NONE',  ( 21.04386569057787426, 56.16954312985733111, -227.9354499029107046 ) ) ;
#100024=EDGE_CURVE ( 'NONE', #101237, #139650, #97031, .T. ) ;
#100036=CIRCLE ( 'NONE', #54262, 2.099999999999998312 ) ;
#100051=CARTESIAN_POINT ( 'NONE',  ( 21.11101077988997332, 34.01873560909758254, -243.6951092311880984 ) ) ;
#100097=ORIENTED_EDGE ( 'NONE', *, *, #214294, .T. ) ;
#100103=CARTESIAN_POINT ( 'NONE',  ( 21.05000000000000071, 39.23476235320398331, -236.9756760510740037 ) ) ;
#100121=CARTESIAN_POINT ( 'NONE',  ( -22.47071067811865319, 29.57301391503006016, -252.6169816238249552 ) ) ;
#100142=ORIENTED_EDGE ( 'NONE', *, *, #199187, .F. ) ;
#100153=VERTEX_POINT ( 'NONE', #125628 ) ;
#100181=AXIS2_PLACEMENT_3D ( 'NONE', #199256, #243498, #42733 ) ;
#100257=VECTOR ( 'NONE', #94987, 1000.000000000000114 ) ;
#100266=ORIENTED_EDGE ( 'NONE', *, *, #130596, .T. ) ;
#100276=CARTESIAN_POINT ( 'NONE',  ( -23.15000000000000213, 47.91013932883114990, -242.3192343197862044 ) ) ;
#100277=DIRECTION ( 'NONE',  ( -0.000000000000000000, 0.8490545835447373957, 0.5283051335749753274 ) ) ;
#100330=FACE_OUTER_BOUND ( 'NONE', #225816, .T. ) ;
#100339=CARTESIAN_POINT ( 'NONE',  ( -23.25000000000000000, 31.89597452117651244, -238.9192857152811769 ) ) ;
#100340=CARTESIAN_POINT ( 'NONE',  ( -20.54999999999999716, 36.65892442174472876, -249.5511627012454596 ) ) ;
#100354=AXIS2_PLACEMENT_3D ( 'NONE', #12760, #216054, #34899 ) ;
#100367=EDGE_CURVE ( 'NONE', #214553, #185809, #88225, .T. ) ;
#100416=ORIENTED_EDGE ( 'NONE', *, *, #63587, .F. ) ;
#100428=AXIS2_PLACEMENT_3D ( 'NONE', #229308, #89771, #50637 ) ;
#100451=AXIS2_PLACEMENT_3D ( 'NONE', #126417, #106843, #122590 ) ;
#100473=CIRCLE ( 'NONE', #246262, 0.1000000000000024342 ) ;
#100474=DIRECTION ( 'NONE',  ( 1.000000000000000000, 0.000000000000000000, 0.000000000000000000 ) ) ;
#100483=DIRECTION ( 'NONE',  ( 0.000000000000000000, -0.9126074666063660468, -0.4088369013363524762 ) ) ;
#100485=ORIENTED_EDGE ( 'NONE', *, *, #222355, .F. ) ;
#100492=ORIENTED_EDGE ( 'NONE', *, *, #8991, .F. ) ;
#100494=EDGE_CURVE ( 'NONE', #119565, #134457, #159029, .T. ) ;
#100498=ORIENTED_EDGE ( 'NONE', *, *, #56272, .T. ) ;
#100508=DIRECTION ( 'NONE',  ( -1.000000000000000000, -0.000000000000000000, -0.000000000000000000 ) ) ;
#100566=LINE ( 'NONE', #75908, #170935 ) ;
#100574=CARTESIAN_POINT ( 'NONE',  ( -23.15000000000000213, 69.05648948627110428, -235.0374527038057977 ) ) ;
#100582=DIRECTION ( 'NONE',  ( 0.000000000000000000, 0.9126074666063777041, 0.4088369013363266080 ) ) ;
#100592=DIRECTION ( 'NONE',  ( 0.000000000000000000, 0.9126074666064812879, 0.4088369013360954596 ) ) ;
#100610=CARTESIAN_POINT ( 'NONE',  ( 22.39999999999999503, 29.50811709945092076, -252.6450601445781103 ) ) ;
#100614=CARTESIAN_POINT ( 'NONE',  ( -20.54999999999999716, 52.73346022503534414, -255.2251647023667260 ) ) ;
#100638=CARTESIAN_POINT ( 'NONE',  ( 23.14999999999998437, 36.65892442174472876, -249.5511627012454596 ) ) ;
#100660=DIRECTION ( 'NONE',  ( 0.000000000000000000, 0.9126074666063771490, 0.4088369013363281623 ) ) ;
#100663=LINE ( 'NONE', #19896, #193334 ) ;
#100671=DIRECTION ( 'NONE',  ( 0.000000000000000000, 0.4088369013363345461, -0.9126074666063741514 ) ) ;
#100684=DIRECTION ( 'NONE',  ( 0.7071067811865475727, -0.2890913453342130457, 0.6453109281988448354 ) ) ;
#100738=ORIENTED_EDGE ( 'NONE', *, *, #65994, .T. ) ;
#100778=AXIS2_PLACEMENT_3D ( 'NONE', #6485, #239985, #103011 ) ;
#100800=ORIENTED_EDGE ( 'NONE', *, *, #156774, .T. ) ;
#100811=CARTESIAN_POINT ( 'NONE',  ( -23.15000000000000213, 67.23127455305835554, -235.8551265064784559 ) ) ;
#100822=AXIS2_PLACEMENT_3D ( 'NONE', #87861, #147877, #5755 ) ;
#100837=ORIENTED_EDGE ( 'NONE', *, *, #137316, .T. ) ;
#100841=EDGE_CURVE ( 'NONE', #223565, #175784, #138483, .T. ) ;
#100843=CARTESIAN_POINT ( 'NONE',  ( 21.05000000000000071, 40.73959002362250459, -238.0637172570269513 ) ) ;
#100873=ORIENTED_EDGE ( 'NONE', *, *, #218829, .F. ) ;
#100899=CIRCLE ( 'NONE', #59388, 0.1000000000000032113 ) ;
#100943=CARTESIAN_POINT ( 'NONE',  ( -21.07946286933444213, 34.00139816787577018, -243.8065871723481735 ) ) ;
#101051=VERTEX_POINT ( 'NONE', #92986 ) ;
#101077=CARTESIAN_POINT ( 'NONE',  ( 21.05000000000000071, 47.95459712139159336, -246.5019368548292675 ) ) ;
#101080=AXIS2_PLACEMENT_3D ( 'NONE', #184916, #148363, #85778 ) ;
#101092=CYLINDRICAL_SURFACE ( 'NONE', #35400, 0.09999999999999950595 ) ;
#101099=VERTEX_POINT ( 'NONE', #194696 ) ;
#101115=ORIENTED_EDGE ( 'NONE', *, *, #116570, .F. ) ;
#101133=ORIENTED_EDGE ( 'NONE', *, *, #88738, .T. ) ;
#101142=CARTESIAN_POINT ( 'NONE',  ( 20.30531438145591139, 39.64564273954285767, -237.1493556402196248 ) ) ;
#101149=ORIENTED_EDGE ( 'NONE', *, *, #27430, .F. ) ;
#101155=AXIS2_PLACEMENT_3D ( 'NONE', #81529, #62014, #710 ) ;
#101186=AXIS2_PLACEMENT_3D ( 'NONE', #160138, #59701, #24480 ) ;
#101197=DIRECTION ( 'NONE',  ( 1.000000000000000000, -1.335000415235279464E-16, 2.979993593738922200E-16 ) ) ;
#101206=ORIENTED_EDGE ( 'NONE', *, *, #36726, .F. ) ;
#101237=VERTEX_POINT ( 'NONE', #204911 ) ;
#101251=CARTESIAN_POINT ( 'NONE',  ( 21.97500000000000497, 43.94346684630428967, -235.6041041703296344 ) ) ;
#101273=CARTESIAN_POINT ( 'NONE',  ( -18.59999999999999787, 36.65892442174472876, -249.5511627012454596 ) ) ;
#101274=DIRECTION ( 'NONE',  ( 1.000000000000000000, 0.000000000000000000, 0.000000000000000000 ) ) ;
#101296=EDGE_CURVE ( 'NONE', #171102, #53900, #238655, .T. ) ;
#101307=CARTESIAN_POINT ( 'NONE',  ( 21.08376601933332495, 34.00789988715292367, -243.7895282553435550 ) ) ;
#101337=ORIENTED_EDGE ( 'NONE', *, *, #130543, .T. ) ;
#101342=LINE ( 'NONE', #256569, #76530 ) ;
#101395=EDGE_CURVE ( 'NONE', #134457, #214442, #88784, .T. ) ;
#101396=DIRECTION ( 'NONE',  ( -1.000000000000000000, -0.000000000000000000, 0.000000000000000000 ) ) ;
#101402=DIRECTION ( 'NONE',  ( 0.000000000000000000, 0.9126074666063545004, 0.4088369013363783999 ) ) ;
#101423=DIRECTION ( 'NONE',  ( -1.000000000000000000, -0.000000000000000000, 0.000000000000000000 ) ) ;
#101425=FACE_OUTER_BOUND ( 'NONE', #175572, .T. ) ;
#101431=ORIENTED_EDGE ( 'NONE', *, *, #17849, .F. ) ;
#101447=EDGE_CURVE ( 'NONE', #247446, #229414, #97135, .T. ) ;
#101448=ORIENTED_EDGE ( 'NONE', *, *, #181788, .T. ) ;
#101470=DIRECTION ( 'NONE',  ( 0.000000000000000000, -0.9126074666063660468, -0.4088369013363524762 ) ) ;
#101484=ORIENTED_EDGE ( 'NONE', *, *, #197931, .F. ) ;
#101488=CYLINDRICAL_SURFACE ( 'NONE', #64890, 0.09999999999999939493 ) ;
#101507=ADVANCED_FACE ( 'NONE', ( #255551 ), #5573, .T. ) ;
#101527=AXIS2_PLACEMENT_3D ( 'NONE', #148341, #209601, #190039 ) ;
#101528=CARTESIAN_POINT ( 'NONE',  ( -20.85000000000000142, 78.57744179526842743, -232.8011145694030972 ) ) ;
#101537=DIRECTION ( 'NONE',  ( -1.000000000000000000, 0.000000000000000000, 0.000000000000000000 ) ) ;
#101538=ORIENTED_EDGE ( 'NONE', *, *, #88863, .F. ) ;
#101574=CARTESIAN_POINT ( 'NONE',  ( 18.59999999999999076, 46.45388641681647357, -243.1520440498138385 ) ) ;
#101586=ORIENTED_EDGE ( 'NONE', *, *, #140415, .T. ) ;
#101598=DIRECTION ( 'NONE',  ( 0.000000000000000000, 0.9126074666063844765, 0.4088369013363113980 ) ) ;
#101607=CIRCLE ( 'NONE', #60118, 0.2000000000000048683 ) ;
#101625=EDGE_CURVE ( 'NONE', #208529, #130019, #122135, .T. ) ;
#101656=DIRECTION ( 'NONE',  ( -1.000000000000000000, 7.667232114526941871E-17, -1.711482807214921537E-16 ) ) ;
#101674=ORIENTED_EDGE ( 'NONE', *, *, #191308, .T. ) ;
#101689=DIRECTION ( 'NONE',  ( 0.000000000000000000, -0.9126074666063770380, -0.4088369013363281068 ) ) ;
#101711=DIRECTION ( 'NONE',  ( 1.000000000000000000, 0.000000000000000000, 0.000000000000000000 ) ) ;
#101754=EDGE_LOOP ( 'NONE', ( #28601, #59778, #151549 ) ) ;
#101764=CARTESIAN_POINT ( 'NONE',  ( -23.25000000000000000, 55.39363411790988323, -234.6384634766556303 ) ) ;
#101806=CARTESIAN_POINT ( 'NONE',  ( 21.05000000000000071, 34.07612324756792077, -243.5412266404783566 ) ) ;
#101815=AXIS2_PLACEMENT_3D ( 'NONE', #170733, #205948, #145967 ) ;
#101872=VERTEX_POINT ( 'NONE', #11572 ) ;
#101901=VECTOR ( 'NONE', #98299, 1000.000000000000227 ) ;
#101904=DIRECTION ( 'NONE',  ( -0.000000000000000000, 0.9126074666063771490, 0.4088369013363281623 ) ) ;
#101912=CIRCLE ( 'NONE', #26962, 0.1000000000000056677 ) ;
#101921=TOROIDAL_SURFACE ( 'NONE', #143456, 7.800000000000000711, 0.1000000000000000056 ) ;
#101948=CIRCLE ( 'NONE', #160274, 0.09999999999999063804 ) ;
#101969=CARTESIAN_POINT ( 'NONE',  ( 21.05000000000000071, 44.52640028187936849, -247.3006740988509193 ) ) ;
#101977=EDGE_LOOP ( 'NONE', ( #88659, #86111, #117968 ) ) ;
#101994=DIRECTION ( 'NONE',  ( 1.301042606982683734E-14, -0.1022405907414274118, -0.9947597004326442782 ) ) ;
#102002=EDGE_CURVE ( 'NONE', #162201, #176943, #122311, .T. ) ;
#102004=ADVANCED_FACE ( 'NONE', ( #214881 ), #255238, .F. ) ;
#102011=CARTESIAN_POINT ( 'NONE',  ( 18.39999999999999858, 46.91436717984746707, -255.3877622108296634 ) ) ;
#102012=EDGE_CURVE ( 'NONE', #228214, #197595, #9875, .T. ) ;
#102023=EDGE_CURVE ( 'NONE', #242320, #70449, #201591, .T. ) ;
#102050=CARTESIAN_POINT ( 'NONE',  ( 21.05000000000000071, 46.45388641681647357, -243.1520440498138385 ) ) ;
#102075=CARTESIAN_POINT ( 'NONE',  ( 22.39999999999999858, 33.38250548509083870, -242.4821227592188961 ) ) ;
#102130=ADVANCED_FACE ( 'NONE', ( #199172 ), #106506, .T. ) ;
#102142=ORIENTED_EDGE ( 'NONE', *, *, #71002, .T. ) ;
#102152=FACE_OUTER_BOUND ( 'NONE', #116543, .T. ) ;
#102153=CARTESIAN_POINT ( 'NONE',  ( -21.05000000000000071, 34.07612324756792077, -243.5412266404783566 ) ) ;
#102154=CARTESIAN_POINT ( 'NONE',  ( -20.54999999999999716, 67.23127455305835554, -235.8551265064784559 ) ) ;
#102158=CARTESIAN_POINT ( 'NONE',  ( 21.05000000000000071, 67.23127455305835554, -235.8551265064784559 ) ) ;
#102171=EDGE_CURVE ( 'NONE', #13509, #10114, #101607, .T. ) ;
#102175=ORIENTED_EDGE ( 'NONE', *, *, #109785, .T. ) ;
#102178=CIRCLE ( 'NONE', #247960, 0.09999999999999939493 ) ;
#102223=ORIENTED_EDGE ( 'NONE', *, *, #45505, .F. ) ;
#102227=VERTEX_POINT ( 'NONE', #184726 ) ;
#102254=CARTESIAN_POINT ( 'NONE',  ( 21.05000000000000071, 56.02567683926420727, -227.9999002286038774 ) ) ;
#102292=CIRCLE ( 'NONE', #144015, 0.09999999999999854838 ) ;
#102308=CARTESIAN_POINT ( 'NONE',  ( 22.59999999999999432, 31.79543193779693055, -238.8548925032096122 ) ) ;
#102348=DIRECTION ( 'NONE',  ( 0.7071067811865475727, -0.2890913453342130457, 0.6453109281988449464 ) ) ;
#102357=CIRCLE ( 'NONE', #214631, 0.09999999999999609201 ) ;
#102376=CARTESIAN_POINT ( 'NONE',  ( 20.94983749550516450, 68.01715840423028681, -224.2192812407665201 ) ) ;
#102389=CIRCLE ( 'NONE', #218948, 0.1000000000000024342 ) ;
#102411=CARTESIAN_POINT ( 'NONE',  ( -22.39999999999999858, 26.06832281015329755, -254.4051978787608732 ) ) ;
#102432=VERTEX_POINT ( 'NONE', #104550 ) ;
#102437=DIRECTION ( 'NONE',  ( 1.000000000000000000, 0.000000000000000000, 0.000000000000000000 ) ) ;
#102470=LINE ( 'NONE', #24276, #55912 ) ;
#102526=CARTESIAN_POINT ( 'NONE',  ( 20.94999999999999574, 44.12194005689738674, -258.6913704466671788 ) ) ;
#102528=CARTESIAN_POINT ( 'NONE',  ( -20.64999999999999858, 46.15118611352045974, -240.5321844900040844 ) ) ;
#102540=CARTESIAN_POINT ( 'NONE',  ( -18.59999994787167310, 77.40586390956570995, -241.7326700300080802 ) ) ;
#102554=ORIENTED_EDGE ( 'NONE', *, *, #10457, .F. ) ;
#102564=CIRCLE ( 'NONE', #177656, 0.09999999999999939493 ) ;
#102596=CIRCLE ( 'NONE', #219140, 0.1000000000000003386 ) ;
#102654=CARTESIAN_POINT ( 'NONE',  ( 20.94999999999999929, 55.59258605799641373, -234.6589115948038966 ) ) ;
#102676=VERTEX_POINT ( 'NONE', #173602 ) ;
#102679=CARTESIAN_POINT ( 'NONE',  ( -21.14999999999999858, 26.06832281015329755, -254.4051978787608732 ) ) ;
#102692=DIRECTION ( 'NONE',  ( -1.000000000000000000, 0.000000000000000000, 0.000000000000000000 ) ) ;
#102696=ORIENTED_EDGE ( 'NONE', *, *, #250129, .F. ) ;
#102719=CARTESIAN_POINT ( 'NONE',  ( 23.14999999999999858, 67.23127455305835554, -235.8551265064784559 ) ) ;
#102730=ADVANCED_FACE ( 'NONE', ( #156588 ), #57431, .T. ) ;
#102773=ADVANCED_FACE ( 'NONE', ( #155299 ), #253068, .T. ) ;
#102790=DIRECTION ( 'NONE',  ( 1.000000000000000000, 0.000000000000000000, 0.000000000000000000 ) ) ;
#102815=CARTESIAN_POINT ( 'NONE',  ( 18.60000000000000142, 77.44184265367995579, -241.6694879557322508 ) ) ;
#102832=CARTESIAN_POINT ( 'NONE',  ( 20.94999999999999574, 43.52285900727589762, -245.0935880436369985 ) ) ;
#102836=DIRECTION ( 'NONE',  ( 7.589415207398578370E-15, 0.4088369013363281623, -0.9126074666063771490 ) ) ;
#102881=CYLINDRICAL_SURFACE ( 'NONE', #63075, 0.09999999999999609201 ) ;
#102923=ORIENTED_EDGE ( 'NONE', *, *, #125789, .F. ) ;
#102972=ORIENTED_EDGE ( 'NONE', *, *, #208054, .T. ) ;
#102980=SPHERICAL_SURFACE ( 'NONE', #202188, 0.1000000000000000056 ) ;
#102981=DIRECTION ( 'NONE',  ( 0.000000000000000000, 0.1569827930593259702, -0.9876013379310970564 ) ) ;
#102982=EDGE_CURVE ( 'NONE', #191945, #173788, #231212, .T. ) ;
#102983=CARTESIAN_POINT ( 'NONE',  ( -21.08198257630413508, 30.84639965801013517, -252.0755024353131830 ) ) ;
#102992=EDGE_CURVE ( 'NONE', #188456, #227500, #226908, .T. ) ;
#103003=CARTESIAN_POINT ( 'NONE',  ( 20.85000000000000142, 74.34961279258810407, -232.6661986760551315 ) ) ;
#103011=DIRECTION ( 'NONE',  ( 0.000000000000000000, -0.4088369013363494231, 0.9126074666063672680 ) ) ;
#103033=AXIS2_PLACEMENT_3D ( 'NONE', #84545, #204531, #247521 ) ;
#103066=AXIS2_PLACEMENT_3D ( 'NONE', #118878, #26192, #86118 ) ;
#103157=CIRCLE ( 'NONE', #153277, 0.1000000000000024342 ) ;
#103189=ADVANCED_FACE ( 'NONE', ( #118405 ), #177114, .F. ) ;
#103208=CARTESIAN_POINT ( 'NONE',  ( -22.59999999999999787, 31.79543193779693055, -238.8548925032096122 ) ) ;
#103215=FACE_OUTER_BOUND ( 'NONE', #128058, .T. ) ;
#103216=CARTESIAN_POINT ( 'NONE',  ( -21.05000000000000071, 36.65892442174472876, -249.5511627012454596 ) ) ;
#103238=ORIENTED_EDGE ( 'NONE', *, *, #178307, .F. ) ;
#103239=AXIS2_PLACEMENT_3D ( 'NONE', #187796, #20051, #219502 ) ;
#103259=ORIENTED_EDGE ( 'NONE', *, *, #221440, .T. ) ;
#103261=DIRECTION ( 'NONE',  ( 0.000000000000000000, 0.5859227990963362664, 0.8103668758649469339 ) ) ;
#103266=DIRECTION ( 'NONE',  ( 0.000000000000000000, 0.3116596277708317264, 0.9501938099239264357 ) ) ;
#103289=TOROIDAL_SURFACE ( 'NONE', #236567, 4.099999999999999645, 0.1000000000000000056 ) ;
#103290=DIRECTION ( 'NONE',  ( 0.000000000000000000, 0.9126074666063791474, 0.4088369013363231663 ) ) ;
#103322=ORIENTED_EDGE ( 'NONE', *, *, #198157, .F. ) ;
#103325=EDGE_CURVE ( 'NONE', #62684, #60562, #59672, .T. ) ;
#103333=VERTEX_POINT ( 'NONE', #163944 ) ;
#103356=CARTESIAN_POINT ( 'NONE',  ( -20.94560253601877164, 56.04839098492278993, -227.9897245711966036 ) ) ;
#103361=CARTESIAN_POINT ( 'NONE',  ( -21.05000000000000071, 55.59258605799641373, -234.6589115948038966 ) ) ;
#103384=EDGE_LOOP ( 'NONE', ( #121341, #133300, #14125, #17686 ) ) ;
#103405=CARTESIAN_POINT ( 'NONE',  ( 21.05000000000000071, 34.07612324756792077, -243.5412266404783566 ) ) ;
#103435=FACE_OUTER_BOUND ( 'NONE', #167167, .T. ) ;
#103449=CYLINDRICAL_SURFACE ( 'NONE', #54163, 0.1000000000000024342 ) ;
#103455=TOROIDAL_SURFACE ( 'NONE', #232498, 0.2000000000000000111, 0.1000000000000000056 ) ;
#103459=CARTESIAN_POINT ( 'NONE',  ( 20.94999999999999929, 45.93587830916155212, -239.9163948487882863 ) ) ;
#103468=CIRCLE ( 'NONE', #61801, 0.1000000000000121764 ) ;
#103475=FACE_OUTER_BOUND ( 'NONE', #225514, .T. ) ;
#103480=FACE_OUTER_BOUND ( 'NONE', #241287, .T. ) ;
#103520=DIRECTION ( 'NONE',  ( 0.000000000000000000, 0.9126074666063773710, 0.4088369013363274962 ) ) ;
#103551=CIRCLE ( 'NONE', #141011, 0.1000000000000117045 ) ;
#103574=CARTESIAN_POINT ( 'NONE',  ( -20.85000000000000142, 67.85909929089923764, -227.8797997985275856 ) ) ;
#103585=ADVANCED_FACE ( 'NONE', ( #34724 ), #61611, .T. ) ;
#103591=AXIS2_PLACEMENT_3D ( 'NONE', #191525, #70296, #11591 ) ;
#103592=VECTOR ( 'NONE', #138691, 1000.000000000000000 ) ;
#103599=CARTESIAN_POINT ( 'NONE',  ( 20.94999999999999929, 48.89266972451527948, -253.5637804087949121 ) ) ;
#103631=EDGE_LOOP ( 'NONE', ( #226892, #89430, #169217, #225285 ) ) ;
#103659=CARTESIAN_POINT ( 'NONE',  ( 22.46250603428203974, 26.01852785471617935, -254.2947602979349142 ) ) ;
#103675=FACE_OUTER_BOUND ( 'NONE', #212532, .T. ) ;
#103691=MANIFOLD_SOLID_BREP ( 'Stock-MAS-200-1', #120133 ) ;
#103702=DIRECTION ( 'NONE',  ( 1.000000000000000000, 0.000000000000000000, -0.000000000000000000 ) ) ;
#103704=AXIS2_PLACEMENT_3D ( 'NONE', #125514, #8144, #205021 ) ;
#103741=DIRECTION ( 'NONE',  ( 0.000000000000000000, -0.4088369013363783999, 0.9126074666063545004 ) ) ;
#103795=FACE_OUTER_BOUND ( 'NONE', #209879, .T. ) ;
#103800=ADVANCED_FACE ( 'NONE', ( #187067 ), #189862, .F. ) ;
#103826=CARTESIAN_POINT ( 'NONE',  ( 21.05000000000000071, 62.08591502004790641, -248.5699171172615820 ) ) ;
#103830=LINE ( 'NONE', #66011, #229515 ) ;
#103867=CARTESIAN_POINT ( 'NONE',  ( -18.59999999999999787, 26.73568686665825567, -252.5275129665054408 ) ) ;
#103895=CARTESIAN_POINT ( 'NONE',  ( 22.49999999999999645, 31.80488924422933295, -238.9605610896540213 ) ) ;
#104009=CARTESIAN_POINT ( 'NONE',  ( -22.39999999999999858, 29.54900078958453236, -252.7363208912387051 ) ) ;
#104038=VERTEX_POINT ( 'NONE', #206973 ) ;
#104061=AXIS2_PLACEMENT_3D ( 'NONE', #2658, #198299, #79621 ) ;
#104195=DIRECTION ( 'NONE',  ( 0.000000000000000000, -0.1022405907414166426, -0.9947597004326453884 ) ) ;
#104212=CARTESIAN_POINT ( 'NONE',  ( -20.64999999999999858, 54.14029358995846053, -238.9803212882090691 ) ) ;
#104216=AXIS2_PLACEMENT_3D ( 'NONE', #44817, #222136, #83894 ) ;
#104222=EDGE_LOOP ( 'NONE', ( #80751, #146022, #151036, #38310 ) ) ;
#104250=DIRECTION ( 'NONE',  ( 0.000000000000000000, -0.9126074666063733742, -0.4088369013363362114 ) ) ;
#104263=CARTESIAN_POINT ( 'NONE',  ( -21.14999999999999858, 30.68987205111127281, -252.2252246220829193 ) ) ;
#104264=ADVANCED_FACE ( 'NONE', ( #200248 ), #101092, .F. ) ;
#104266=ORIENTED_EDGE ( 'NONE', *, *, #222705, .T. ) ;
#104272=ORIENTED_EDGE ( 'NONE', *, *, #229081, .T. ) ;
#104297=CARTESIAN_POINT ( 'NONE',  ( -20.54999999999999716, 55.48145342050126061, -241.1189016111836736 ) ) ;
#104324=ORIENTED_EDGE ( 'NONE', *, *, #217612, .F. ) ;
#104336=VERTEX_POINT ( 'NONE', #136382 ) ;
#104359=ORIENTED_EDGE ( 'NONE', *, *, #248291, .F. ) ;
#104370=AXIS2_PLACEMENT_3D ( 'NONE', #192760, #74119, #88484 ) ;
#104404=DIRECTION ( 'NONE',  ( 0.000000000000000000, 0.9126074666063769270, 0.4088369013363283844 ) ) ;
#104413=ORIENTED_EDGE ( 'NONE', *, *, #145040, .T. ) ;
#104417=EDGE_CURVE ( 'NONE', #138284, #68660, #123028, .T. ) ;
#104485=CIRCLE ( 'NONE', #4542, 0.1000000000000032113 ) ;
#104489=CARTESIAN_POINT ( 'NONE',  ( -18.58693740092193636, 47.00678169108851989, -255.2226550330250348 ) ) ;
#104494=FACE_OUTER_BOUND ( 'NONE', #194543, .T. ) ;
#104550=CARTESIAN_POINT ( 'NONE',  ( 23.25000000000000000, 62.12148660976905745, -247.5636999539406133 ) ) ;
#104572=DIRECTION ( 'NONE',  ( -0.000000000000000000, 0.4088369013363281623, -0.9126074666063771490 ) ) ;
#104580=SPHERICAL_SURFACE ( 'NONE', #87164, 0.1000000000000000056 ) ;
#104583=CARTESIAN_POINT ( 'NONE',  ( 18.60000000000000142, 47.07326788871598922, -255.0992659944397190 ) ) ;
#104594=ORIENTED_EDGE ( 'NONE', *, *, #158632, .F. ) ;
#104596=CIRCLE ( 'NONE', #92154, 0.09999999999999609201 ) ;
#104611=ORIENTED_EDGE ( 'NONE', *, *, #181101, .F. ) ;
#104617=EDGE_LOOP ( 'NONE', ( #193495, #156094, #35851 ) ) ;
#104622=VECTOR ( 'NONE', #60829, 1000.000000000000000 ) ;
#104623=ORIENTED_EDGE ( 'NONE', *, *, #164017, .F. ) ;
#104645=ORIENTED_EDGE ( 'NONE', *, *, #244651, .T. ) ;
#104649=ORIENTED_EDGE ( 'NONE', *, *, #190017, .T. ) ;
#104658=CIRCLE ( 'NONE', #75501, 12.97499999999999787 ) ;
#104683=ORIENTED_EDGE ( 'NONE', *, *, #143894, .F. ) ;
#104702=CARTESIAN_POINT ( 'NONE',  ( 21.05000000000085336, 40.76780962062015590, -237.9639380751402200 ) ) ;
#104703=DIRECTION ( 'NONE',  ( -0.000000000000000000, -0.8103668758649578141, 0.5859227990963212784 ) ) ;
#104717=EDGE_CURVE ( 'NONE', #74878, #145938, #90273, .T. ) ;
#104722=CARTESIAN_POINT ( 'NONE',  ( -23.15000000000000213, 65.40605961984560679, -236.6728003091511425 ) ) ;
#104755=DIRECTION ( 'NONE',  ( -0.000000000000000000, 0.9126074666063771490, 0.4088369013363281623 ) ) ;
#104764=EDGE_CURVE ( 'NONE', #214553, #94097, #19153, .T. ) ;
#104776=ORIENTED_EDGE ( 'NONE', *, *, #27113, .F. ) ;
#104813=CARTESIAN_POINT ( 'NONE',  ( -2.995603634470829482E-16, 52.64219947837469959, -255.2660483925003803 ) ) ;
#104836=DIRECTION ( 'NONE',  ( 2.952720810173288619E-16, 0.4088369013363282178, -0.9126074666063768159 ) ) ;
#104846=CIRCLE ( 'NONE', #200745, 0.09999999999999854838 ) ;
#104860=EDGE_CURVE ( 'NONE', #241306, #34161, #106606, .T. ) ;
#104874=CARTESIAN_POINT ( 'NONE',  ( 22.57320508075687115, 31.85509083104287598, -238.8280249686205536 ) ) ;
#104879=ORIENTED_EDGE ( 'NONE', *, *, #167891, .F. ) ;
#104895=EDGE_CURVE ( 'NONE', #75249, #242431, #31612, .T. ) ;
#104898=CARTESIAN_POINT ( 'NONE',  ( -20.94999999999999929, 44.52640028187936849, -247.3006740988509193 ) ) ;
#104942=CARTESIAN_POINT ( 'NONE',  ( 20.88420186297724612, 68.10670728244119232, -224.1434476749765565 ) ) ;
#104960=EDGE_LOOP ( 'NONE', ( #142191, #133995, #219719, #96678, #204706 ) ) ;
#104968=CARTESIAN_POINT ( 'NONE',  ( -18.50000000000000000, 43.57568952063339651, -245.1784935019914826 ) ) ;
#104975=CARTESIAN_POINT ( 'NONE',  ( 21.05000000000000071, 39.20537871576060240, -236.6597480159109921 ) ) ;
#104976=LINE ( 'NONE', #86713, #40303 ) ;
#104980=ORIENTED_EDGE ( 'NONE', *, *, #117250, .T. ) ;
#104983=VERTEX_POINT ( 'NONE', #234923 ) ;
#104994=CARTESIAN_POINT ( 'NONE',  ( 19.92426406871192412, 54.53338637621133245, -228.6684279704127505 ) ) ;
#105021=VERTEX_POINT ( 'NONE', #118839 ) ;
#105028=ORIENTED_EDGE ( 'NONE', *, *, #58861, .T. ) ;
#105089=CIRCLE ( 'NONE', #134156, 0.1000000000000062367 ) ;
#105124=VECTOR ( 'NONE', #81094, 1000.000000000000114 ) ;
#105134=CYLINDRICAL_SURFACE ( 'NONE', #4795, 0.09999999999999771572 ) ;
#105165=CARTESIAN_POINT ( 'NONE',  ( 21.08035267497491105, 33.99482676082369892, -243.8066059240260586 ) ) ;
#105211=CARTESIAN_POINT ( 'NONE',  ( -21.53699400388026319, 30.46440795807614776, -252.3262297579089193 ) ) ;
#105216=CARTESIAN_POINT ( 'NONE',  ( 21.00000000000000000, 43.85220609964365224, -235.6449878604632886 ) ) ;
#105226=DIRECTION ( 'NONE',  ( 0.000000000000000000, 0.9126074666063753726, 0.4088369013363320481 ) ) ;
#105242=LINE ( 'NONE', #226491, #232549 ) ;
#105257=AXIS2_PLACEMENT_3D ( 'NONE', #3093, #219581, #125631 ) ;
#105272=AXIS2_PLACEMENT_3D ( 'NONE', #81381, #85237, #205204 ) ;
#105279=EDGE_CURVE ( 'NONE', #19019, #242320, #11731, .T. ) ;
#105312=ORIENTED_EDGE ( 'NONE', *, *, #140202, .T. ) ;
#105347=CARTESIAN_POINT ( 'NONE',  ( 19.99999999999998934, 54.53338637621133955, -228.6684279704127789 ) ) ;
#105352=AXIS2_PLACEMENT_3D ( 'NONE', #225155, #81782, #45260 ) ;
#105386=DIRECTION ( 'NONE',  ( -0.000000000000000000, -0.9126074666063771490, -0.4088369013363281623 ) ) ;
#105407=CARTESIAN_POINT ( 'NONE',  ( 23.24999999999999645, 66.37271706025207152, -233.9386508266050839 ) ) ;
#105410=DIRECTION ( 'NONE',  ( 1.000000000000000000, -1.335000415235278971E-16, 2.979993593738921214E-16 ) ) ;
#105422=VERTEX_POINT ( 'NONE', #158947 ) ;
#105428=AXIS2_PLACEMENT_3D ( 'NONE', #142537, #222052, #123002 ) ;
#105460=VERTEX_POINT ( 'NONE', #173403 ) ;
#105462=CARTESIAN_POINT ( 'NONE',  ( 18.60000000000000142, 47.16152503674116758, -255.1462838189583238 ) ) ;
#105483=CIRCLE ( 'NONE', #172212, 7.899999999999995914 ) ;
#105498=CARTESIAN_POINT ( 'NONE',  ( -20.94999999999999929, 36.65892442174472876, -249.5511627012454596 ) ) ;
#105559=CARTESIAN_POINT ( 'NONE',  ( -18.39999999999999858, 46.91436717984746707, -255.3877622108296634 ) ) ;
#105577=EDGE_CURVE ( 'NONE', #70387, #222885, #19539, .T. ) ;
#105595=ORIENTED_EDGE ( 'NONE', *, *, #230732, .T. ) ;
#105647=ORIENTED_EDGE ( 'NONE', *, *, #25293, .T. ) ;
#105672=DIRECTION ( 'NONE',  ( 0.000000000000000000, -0.9126074666064696306, -0.4088369013361213278 ) ) ;
#105675=CIRCLE ( 'NONE', #84821, 11.79999999999999005 ) ;
#105688=DIRECTION ( 'NONE',  ( -0.000000000000000000, 0.9126074666063770380, 0.4088369013363281068 ) ) ;
#105712=EDGE_CURVE ( 'NONE', #53966, #252130, #2756, .T. ) ;
#105717=CARTESIAN_POINT ( 'NONE',  ( 22.47071067811864964, 29.57301391503007792, -252.6169816238249552 ) ) ;
#105734=LINE ( 'NONE', #226994, #223467 ) ;
#105762=CIRCLE ( 'NONE', #26709, 0.4999999999999944489 ) ;
#105789=ORIENTED_EDGE ( 'NONE', *, *, #112784, .F. ) ;
#105792=EDGE_CURVE ( 'NONE', #109264, #18074, #136121, .T. ) ;
#105838=CIRCLE ( 'NONE', #176610, 0.1000000000000024342 ) ;
#105875=ADVANCED_FACE ( 'NONE', ( #244224 ), #26495, .T. ) ;
#105957=VERTEX_POINT ( 'NONE', #183001 ) ;
#105976=DIRECTION ( 'NONE',  ( 1.000000000000000000, 0.000000000000000000, 0.000000000000000000 ) ) ;
#106039=CYLINDRICAL_SURFACE ( 'NONE', #236789, 0.09999999999999939493 ) ;
#106041=FACE_OUTER_BOUND ( 'NONE', #24635, .T. ) ;
#106044=DIRECTION ( 'NONE',  ( 1.000000000000000000, 0.000000000000000000, 0.000000000000000000 ) ) ;
#106056=EDGE_LOOP ( 'NONE', ( #75672, #182301, #7972, #106207 ) ) ;
#106100=EDGE_CURVE ( 'NONE', #216161, #96682, #154182, .T. ) ;
#106102=VECTOR ( 'NONE', #235570, 1000.000000000000114 ) ;
#106155=VERTEX_POINT ( 'NONE', #35507 ) ;
#106171=DIRECTION ( 'NONE',  ( -0.000000000000000000, 0.9969158384938637818, -0.07847809223010315804 ) ) ;
#106176=CARTESIAN_POINT ( 'NONE',  ( 20.84999999999998721, 68.11287320386161070, -224.1382462126928488 ) ) ;
#106182=DIRECTION ( 'NONE',  ( 0.000000000000000000, 0.9126074666063660468, 0.4088369013363524762 ) ) ;
#106201=DIRECTION ( 'NONE',  ( 1.000000000000000000, 0.000000000000000000, 0.000000000000000000 ) ) ;
#106205=EDGE_CURVE ( 'NONE', #212700, #32720, #61585, .T. ) ;
#106207=ORIENTED_EDGE ( 'NONE', *, *, #17088, .F. ) ;
#106210=EDGE_CURVE ( 'NONE', #230417, #212700, #3113, .T. ) ;
#106214=DIRECTION ( 'NONE',  ( -1.000000000000000000, 0.000000000000000000, 0.000000000000000000 ) ) ;
#106227=VERTEX_POINT ( 'NONE', #255758 ) ;
#106234=ADVANCED_FACE ( 'NONE', ( #217937 ), #53206, .T. ) ;
#106235=LINE ( 'NONE', #3283, #171303 ) ;
#106251=ORIENTED_EDGE ( 'NONE', *, *, #107694, .F. ) ;
#106278=CARTESIAN_POINT ( 'NONE',  ( 21.05000000000000071, 39.17748843728426067, -236.9342652831892622 ) ) ;
#106387=CARTESIAN_POINT ( 'NONE',  ( 20.85000000000000142, 78.57744179526842743, -232.8011145694030972 ) ) ;
#106415=ADVANCED_FACE ( 'NONE', ( #112160 ), #49596, .T. ) ;
#106443=ORIENTED_EDGE ( 'NONE', *, *, #122007, .T. ) ;
#106448=ORIENTED_EDGE ( 'NONE', *, *, #178076, .T. ) ;
#106450=PLANE ( 'NONE',  #231564 ) ;
#106472=CARTESIAN_POINT ( 'NONE',  ( 21.30000000000002558, 36.65892442174472876, -249.5511627012454596 ) ) ;
#106506=( BOUNDED_SURFACE ( )  B_SPLINE_SURFACE ( 3, 2, ( 
 ( #929, #19251, #103895 ),
 ( #139168, #84291, #220015 ),
 ( #41403, #163901, #243424 ),
 ( #218712, #178349, #64785 ) ),
 .UNSPECIFIED., .F., .F., .F. ) 
 B_SPLINE_SURFACE_WITH_KNOTS ( ( 4, 4 ),
 ( 3, 3 ),
 ( 0.0006461284895273969623, 0.0007503702773985950749 ),
 ( 0.000000000000000000, 1.000000000000000000 ),
 .UNSPECIFIED. ) 
 GEOMETRIC_REPRESENTATION_ITEM ( )  RATIONAL_B_SPLINE_SURFACE ( (
 ( 1.000000000000000000, 0.7071067811865475727, 1.000000000000000000),
 ( 1.000000000000000000, 0.7076476444648585051, 1.000000000000000000),
 ( 1.000000000000000000, 0.7075727925192710766, 1.000000000000000000),
 ( 1.000000000000000000, 0.7071067811865923147, 1.000000000000000000) ) ) 
 REPRESENTATION_ITEM ( '' )  SURFACE ( )  );
#106516=TOROIDAL_SURFACE ( 'NONE', #27494, 4.099999999999999645, 0.1000000000000000056 ) ;
#106517=CARTESIAN_POINT ( 'NONE',  ( 18.59999999999999076, 55.05538098155519577, -230.0782228604559805 ) ) ;
#106523=AXIS2_PLACEMENT_3D ( 'NONE', #176808, #136341, #137638 ) ;
#106527=CARTESIAN_POINT ( 'NONE',  ( 18.39999999999999147, 46.96039402156218046, -255.3459641718772843 ) ) ;
#106533=EDGE_LOOP ( 'NONE', ( #69239, #73490, #25187, #32484 ) ) ;
#106536=ORIENTED_EDGE ( 'NONE', *, *, #76422, .F. ) ;
#106559=ORIENTED_EDGE ( 'NONE', *, *, #213771, .F. ) ;
#106561=CARTESIAN_POINT ( 'NONE',  ( -21.44999999999999929, 44.92467540951147953, -237.7943620901849613 ) ) ;
#106576=DIRECTION ( 'NONE',  ( 0.000000000000000000, 0.4088369013363281623, -0.9126074666063771490 ) ) ;
#106601=ORIENTED_EDGE ( 'NONE', *, *, #139267, .F. ) ;
#106602=DIRECTION ( 'NONE',  ( 0.000000000000000000, 0.9126074666063770380, 0.4088369013363281068 ) ) ;
#106606=CIRCLE ( 'NONE', #27575, 0.09999999999999063804 ) ;
#106645=CARTESIAN_POINT ( 'NONE',  ( -18.59999999999999787, 78.48087866980282001, -232.8271061603568910 ) ) ;
#106675=EDGE_LOOP ( 'NONE', ( #193757, #6643, #237646, #27766 ) ) ;
#106702=ADVANCED_FACE ( 'NONE', ( #71437 ), #230495, .F. ) ;
#106727=EDGE_CURVE ( 'NONE', #129596, #171512, #49292, .T. ) ;
#106730=ORIENTED_EDGE ( 'NONE', *, *, #76553, .T. ) ;
#106734=DIRECTION ( 'NONE',  ( 0.9880948137434723000, -0.06289798482097132271, 0.1404011487086684051 ) ) ;
#106767=CARTESIAN_POINT ( 'NONE',  ( -20.54999999999999716, 61.88149656937975607, -248.1136133839584090 ) ) ;
#106771=ORIENTED_EDGE ( 'NONE', *, *, #143894, .T. ) ;
#106779=CARTESIAN_POINT ( 'NONE',  ( 20.95378194480896639, 39.25578854815272933, -236.8440500613521351 ) ) ;
#106782=EDGE_CURVE ( 'NONE', #147011, #168551, #249039, .T. ) ;
#106832=ORIENTED_EDGE ( 'NONE', *, *, #154252, .F. ) ;
#106843=DIRECTION ( 'NONE',  ( 0.000000000000000000, -0.9126074666063769270, -0.4088369013363280513 ) ) ;
#106880=AXIS2_PLACEMENT_3D ( 'NONE', #8350, #51282, #27934 ) ;
#106906=AXIS2_PLACEMENT_3D ( 'NONE', #44777, #202564, #143860 ) ;
#106907=CIRCLE ( 'NONE', #252653, 0.09999999999999939493 ) ;
#106928=CARTESIAN_POINT ( 'NONE',  ( 20.85000000000000142, 66.90607807833499976, -235.8243394455619182 ) ) ;
#106956=ORIENTED_EDGE ( 'NONE', *, *, #7992, .F. ) ;
#106970=PLANE ( 'NONE',  #220068 ) ;
#106989=CARTESIAN_POINT ( 'NONE',  ( 21.30000000000002558, 36.65892442174472876, -249.5511627012454596 ) ) ;
#107003=FACE_OUTER_BOUND ( 'NONE', #87200, .T. ) ;
#107033=CIRCLE ( 'NONE', #65350, 0.1000000000000056677 ) ;
#107046=AXIS2_PLACEMENT_3D ( 'NONE', #57580, #220536, #194572 ) ;
#107051=DIRECTION ( 'NONE',  ( -0.000000000000000000, -0.9579639084728132081, -0.2868887416116073230 ) ) ;
#107081=DIRECTION ( 'NONE',  ( 1.000000000000000000, 0.000000000000000000, 0.000000000000000000 ) ) ;
#107094=DIRECTION ( 'NONE',  ( -1.000000000000000000, 2.986185139342070877E-16, -6.665775143889692774E-16 ) ) ;
#107110=CARTESIAN_POINT ( 'NONE',  ( 20.94999999999999574, 44.00266445878927613, -258.8505972146074896 ) ) ;
#107121=EDGE_LOOP ( 'NONE', ( #212894, #162408, #130770, #12808 ) ) ;
#107147=ORIENTED_EDGE ( 'NONE', *, *, #103325, .F. ) ;
#107293=CARTESIAN_POINT ( 'NONE',  ( 21.05000000000000071, 32.27467314984873070, -239.7646184017148698 ) ) ;
#107313=DIRECTION ( 'NONE',  ( -1.000000000000000000, -0.000000000000000000, 0.000000000000000000 ) ) ;
#107319=CARTESIAN_POINT ( 'NONE',  ( 20.95483826173900255, 40.82941501609197843, -237.9566743329193343 ) ) ;
#107344=LINE ( 'NONE', #228598, #30501 ) ;
#107345=CARTESIAN_POINT ( 'NONE',  ( -23.15000000000000213, 51.33926024308902214, -230.0993571250899379 ) ) ;
#107349=CARTESIAN_POINT ( 'NONE',  ( 21.06086055315973482, 44.20743049992722717, -236.5545395267883180 ) ) ;
#107350=ORIENTED_EDGE ( 'NONE', *, *, #88863, .T. ) ;
#107360=DIRECTION ( 'NONE',  ( 0.000000000000000000, 0.9126074666063773710, 0.4088369013363272741 ) ) ;
#107394=VECTOR ( 'NONE', #227303, 1000.000000000000114 ) ;
#107395=FACE_OUTER_BOUND ( 'NONE', #48273, .T. ) ;
#107419=DIRECTION ( 'NONE',  ( 0.000000000000000000, 0.9126074666063770380, 0.4088369013363281068 ) ) ;
#107431=CIRCLE ( 'NONE', #253170, 0.09999999999999470424 ) ;
#107440=DIRECTION ( 'NONE',  ( 0.000000000000000000, 0.4088369013363322146, -0.9126074666063751506 ) ) ;
#107455=CIRCLE ( 'NONE', #124214, 0.1000000000000024342 ) ;
#107471=AXIS2_PLACEMENT_3D ( 'NONE', #38952, #256639, #139295 ) ;
#107495=DIRECTION ( 'NONE',  ( 0.000000000000000000, 0.9126074666063770380, 0.4088369013363281068 ) ) ;
#107499=EDGE_CURVE ( 'NONE', #131894, #14564, #89107, .T. ) ;
#107522=ORIENTED_EDGE ( 'NONE', *, *, #155725, .T. ) ;
#107527=DIRECTION ( 'NONE',  ( 1.000000000000000000, 0.000000000000000000, 0.000000000000000000 ) ) ;
#107542=ORIENTED_EDGE ( 'NONE', *, *, #73227, .T. ) ;
#107609=EDGE_CURVE ( 'NONE', #217030, #101051, #92001, .T. ) ;
#107642=VECTOR ( 'NONE', #251695, 1000.000000000000114 ) ;
#107649=ORIENTED_EDGE ( 'NONE', *, *, #224912, .T. ) ;
#107653=FACE_OUTER_BOUND ( 'NONE', #256006, .T. ) ;
#107665=CARTESIAN_POINT ( 'NONE',  ( -23.15000000000000213, 46.15118611352045974, -240.5321844900040844 ) ) ;
#107683=ORIENTED_EDGE ( 'NONE', *, *, #185598, .T. ) ;
#107694=EDGE_CURVE ( 'NONE', #51580, #34297, #15147, .T. ) ;
#107699=LINE ( 'NONE', #222488, #18465 ) ;
#107779=DIRECTION ( 'NONE',  ( -2.602085213965227050E-14, 0.9126074666063771490, 0.4088369013363281623 ) ) ;
#107784=DIRECTION ( 'NONE',  ( 0.000000000000000000, 0.9126074666063768159, 0.4088369013363288285 ) ) ;
#107796=AXIS2_PLACEMENT_3D ( 'NONE', #55541, #155991, #235492 ) ;
#107804=CIRCLE ( 'NONE', #178776, 0.4999999999999944489 ) ;
#107812=EDGE_LOOP ( 'NONE', ( #63072, #5683, #199893, #159847 ) ) ;
#107828=CYLINDRICAL_SURFACE ( 'NONE', #10702, 0.09999999999999609201 ) ;
#107847=ADVANCED_FACE ( 'NONE', ( #159941 ), #29505, .F. ) ;
#107864=ORIENTED_EDGE ( 'NONE', *, *, #18930, .F. ) ;
#107899=LINE ( 'NONE', #244835, #175075 ) ;
#107907=ADVANCED_FACE ( 'NONE', ( #62110 ), #199050, .T. ) ;
#107911=AXIS2_PLACEMENT_3D ( 'NONE', #114819, #150122, #31469 ) ;
#107912=ORIENTED_EDGE ( 'NONE', *, *, #43954, .T. ) ;
#107934=ORIENTED_EDGE ( 'NONE', *, *, #174805, .T. ) ;
#107946=ORIENTED_EDGE ( 'NONE', *, *, #43954, .F. ) ;
#107971=ORIENTED_EDGE ( 'NONE', *, *, #119685, .T. ) ;
#107973=LINE ( 'NONE', #148384, #196048 ) ;
#108004=CARTESIAN_POINT ( 'NONE',  ( -21.05000000000000071, 35.94660524813657076, -234.4748257877825495 ) ) ;
#108014=EDGE_CURVE ( 'NONE', #228214, #115670, #102564, .T. ) ;
#108029=CIRCLE ( 'NONE', #141333, 0.09999999999999609201 ) ;
#108035=EDGE_CURVE ( 'NONE', #255259, #89722, #69311, .T. ) ;
#108046=CARTESIAN_POINT ( 'NONE',  ( -20.64999999999999858, 62.04503132991428060, -248.4786563706009588 ) ) ;
#108055=CIRCLE ( 'NONE', #149766, 0.1000000000000024342 ) ;
#108086=CARTESIAN_POINT ( 'NONE',  ( 20.95512820512820440, 39.31056039967181448, -236.7220595557971023 ) ) ;
#108100=CARTESIAN_POINT ( 'NONE',  ( 18.59999999999999076, 43.16354019706792400, -239.5695141926698284 ) ) ;
#108128=FACE_OUTER_BOUND ( 'NONE', #186350, .T. ) ;
#108162=LINE ( 'NONE', #166884, #239281 ) ;
#108171=CARTESIAN_POINT ( 'NONE',  ( 18.49999999999999289, 67.65998959290219261, -227.8609496483021530 ) ) ;
#108174=LINE ( 'NONE', #126437, #132187 ) ;
#108205=ORIENTED_EDGE ( 'NONE', *, *, #206330, .T. ) ;
#108227=CARTESIAN_POINT ( 'NONE',  ( -20.94999999999999929, 74.74783850729544099, -233.7633982527047465 ) ) ;
#108232=AXIS2_PLACEMENT_3D ( 'NONE', #81171, #236412, #40815 ) ;
#108237=ORIENTED_EDGE ( 'NONE', *, *, #138635, .T. ) ;
#108248=DIRECTION ( 'NONE',  ( -1.000000000000000000, -0.000000000000000000, 0.000000000000000000 ) ) ;
#108285=ORIENTED_EDGE ( 'NONE', *, *, #153401, .F. ) ;
#108295=VERTEX_POINT ( 'NONE', #185594 ) ;
#108309=AXIS2_PLACEMENT_3D ( 'NONE', #200677, #222780, #242356 ) ;
#108359=CARTESIAN_POINT ( 'NONE',  ( -18.59999999999999787, 22.19492904189240079, -246.0046379724989549 ) ) ;
#108374=DIRECTION ( 'NONE',  ( 0.000000000000000000, 0.9126074666063770380, 0.4088369013363282178 ) ) ;
#108399=AXIS2_PLACEMENT_3D ( 'NONE', #253816, #70091, #203801 ) ;
#108402=CARTESIAN_POINT ( 'NONE',  ( -18.50000000000000000, 67.85909929089923764, -227.8797997985275856 ) ) ;
#108412=CARTESIAN_POINT ( 'NONE',  ( -18.50596464788227635, 68.04082873524789932, -224.1991862745062178 ) ) ;
#108444=ORIENTED_EDGE ( 'NONE', *, *, #31748, .F. ) ;
#108485=DIRECTION ( 'NONE',  ( 0.000000000000000000, 0.9126074666063774821, 0.4088369013363270521 ) ) ;
#108487=ORIENTED_EDGE ( 'NONE', *, *, #239867, .T. ) ;
#108499=VERTEX_POINT ( 'NONE', #90330 ) ;
#108513=TOROIDAL_SURFACE ( 'NONE', #112797, 0.2000000000000000111, 0.1000000000000000056 ) ;
#108585=CARTESIAN_POINT ( 'NONE',  ( 23.14999999999999858, 67.23127455305835554, -235.8551265064784559 ) ) ;
#108586=ORIENTED_EDGE ( 'NONE', *, *, #8106, .F. ) ;
#108619=EDGE_LOOP ( 'NONE', ( #74684, #139586, #28856, #78684 ) ) ;
#108623=EDGE_CURVE ( 'NONE', #109264, #62684, #252805, .T. ) ;
#108641=DIRECTION ( 'NONE',  ( 1.000000000000000000, 0.000000000000000000, 0.000000000000000000 ) ) ;
#108664=ORIENTED_EDGE ( 'NONE', *, *, #188289, .T. ) ;
#108666=ADVANCED_FACE ( 'NONE', ( #66311 ), #87136, .F. ) ;
#108668=DIRECTION ( 'NONE',  ( 1.000000000000000000, 0.000000000000000000, -0.000000000000000000 ) ) ;
#108678=ORIENTED_EDGE ( 'NONE', *, *, #154865, .F. ) ;
#108686=DIRECTION ( 'NONE',  ( 1.000000000000000000, 0.000000000000000000, 0.000000000000000000 ) ) ;
#108767=FACE_OUTER_BOUND ( 'NONE', #112735, .T. ) ;
#108782=DIRECTION ( 'NONE',  ( -0.000000000000000000, 0.9126074666063770380, 0.4088369013363281068 ) ) ;
#108809=AXIS2_PLACEMENT_3D ( 'NONE', #106767, #143332, #204586 ) ;
#108813=LINE ( 'NONE', #188363, #13127 ) ;
#108852=EDGE_CURVE ( 'NONE', #245185, #115670, #202926, .T. ) ;
#108899=VERTEX_POINT ( 'NONE', #40047 ) ;
#108904=ADVANCED_FACE ( 'NONE', ( #116986 ), #90490, .F. ) ;
#108928=ORIENTED_EDGE ( 'NONE', *, *, #247005, .T. ) ;
#108954=LINE ( 'NONE', #226319, #74189 ) ;
#108974=FACE_OUTER_BOUND ( 'NONE', #238464, .T. ) ;
#108977=EDGE_CURVE ( 'NONE', #89516, #238120, #58274, .T. ) ;
#108979=EDGE_CURVE ( 'NONE', #180643, #19042, #99031, .T. ) ;
#108993=DIRECTION ( 'NONE',  ( -1.000000000000000000, 1.335000415235278971E-16, -2.979993593738921214E-16 ) ) ;
#109005=VERTEX_POINT ( 'NONE', #81666 ) ;
#109037=CARTESIAN_POINT ( 'NONE',  ( 21.03675099975492202, 44.27880510233411826, -236.4124706813595083 ) ) ;
#109062=FACE_OUTER_BOUND ( 'NONE', #164727, .T. ) ;
#109091=CARTESIAN_POINT ( 'NONE',  ( -20.64999999999999858, 61.88149656937975607, -248.1136133839584090 ) ) ;
#109098=CARTESIAN_POINT ( 'NONE',  ( -23.25000000000000000, 67.85909929089923764, -227.8797997985275856 ) ) ;
#109100=CARTESIAN_POINT ( 'NONE',  ( -21.14999999999999858, 26.02743912001966464, -254.3139371321002216 ) ) ;
#109117=CARTESIAN_POINT ( 'NONE',  ( -23.15000000000000213, 69.16514130714681130, -247.7543978865853660 ) ) ;
#109175=CARTESIAN_POINT ( 'NONE',  ( 21.14999999999999858, 43.45833571831321507, -234.7657887233444001 ) ) ;
#109181=DIRECTION ( 'NONE',  ( -1.000000000000000000, -0.000000000000000000, 0.000000000000000000 ) ) ;
#109184=ORIENTED_EDGE ( 'NONE', *, *, #222553, .F. ) ;
#109185=AXIS2_PLACEMENT_3D ( 'NONE', #63769, #28552, #7663 ) ;
#109187=EDGE_LOOP ( 'NONE', ( #137024, #75298, #171450, #243197 ) ) ;
#109196=CARTESIAN_POINT ( 'NONE',  ( 21.30000000000002558, 40.35498466150055918, -247.8953732508333587 ) ) ;
#109227=CARTESIAN_POINT ( 'NONE',  ( -21.05000000000000071, 56.16603649944111254, -228.1013850343386764 ) ) ;
#109233=AXIS2_PLACEMENT_3D ( 'NONE', #237675, #166830, #246331 ) ;
#109236=ORIENTED_EDGE ( 'NONE', *, *, #115294, .T. ) ;
#109244=CARTESIAN_POINT ( 'NONE',  ( -23.25000000000000000, 36.65892442174472876, -249.5511627012454596 ) ) ;
#109251=EDGE_LOOP ( 'NONE', ( #117403, #61433, #189357, #10933 ) ) ;
#109252=CARTESIAN_POINT ( 'NONE',  ( -21.05000000000000071, 43.51422117117169108, -240.0698702536254530 ) ) ;
#109264=VERTEX_POINT ( 'NONE', #230198 ) ;
#109274=EDGE_CURVE ( 'NONE', #68660, #178487, #151978, .T. ) ;
#109296=ORIENTED_EDGE ( 'NONE', *, *, #228972, .T. ) ;
#109366=DIRECTION ( 'NONE',  ( 1.000000000000000000, 0.000000000000000000, 0.000000000000000000 ) ) ;
#109391=AXIS2_PLACEMENT_3D ( 'NONE', #25458, #71019, #9724 ) ;
#109410=EDGE_CURVE ( 'NONE', #125186, #89024, #244986, .T. ) ;
#109428=DIRECTION ( 'NONE',  ( 1.000000000000000000, 0.000000000000000000, 0.000000000000000000 ) ) ;
#109440=CARTESIAN_POINT ( 'NONE',  ( 21.05000000000000071, 44.10931966560507789, -259.0886734199950183 ) ) ;
#109441=AXIS2_PLACEMENT_3D ( 'NONE', #39458, #198488, #117669 ) ;
#109448=EDGE_CURVE ( 'NONE', #69009, #9522, #6989, .T. ) ;
#109451=DIRECTION ( 'NONE',  ( 0.000000000000000000, 0.4088369013363281623, -0.9126074666063771490 ) ) ;
#109460=CARTESIAN_POINT ( 'NONE',  ( 22.49999999999999645, 26.00793465928167691, -254.2726825744909718 ) ) ;
#109495=DIRECTION ( 'NONE',  ( 0.000000000000000000, 0.9126074666063773710, 0.4088369013363274962 ) ) ;
#109503=DIRECTION ( 'NONE',  ( -0.000000000000000000, 0.4088369013363281623, -0.9126074666063771490 ) ) ;
#109517=VECTOR ( 'NONE', #128791, 1000.000000000000000 ) ;
#109520=CARTESIAN_POINT ( 'NONE',  ( 21.05000000000000071, 62.04148992963929032, -247.7470044306132024 ) ) ;
#109541=ORIENTED_EDGE ( 'NONE', *, *, #227138, .T. ) ;
#109550=DIRECTION ( 'NONE',  ( 0.000000000000000000, -0.9126074666063769270, -0.4088369013363280513 ) ) ;
#109581=CARTESIAN_POINT ( 'NONE',  ( 20.94999999999999929, 53.33306769324366314, -234.7945388949160872 ) ) ;
#109589=ORIENTED_EDGE ( 'NONE', *, *, #203920, .T. ) ;
#109592=( BOUNDED_SURFACE ( )  B_SPLINE_SURFACE ( 3, 2, ( 
 ( #238270, #239576, #161334 ),
 ( #60917, #240860, #59613 ),
 ( #122198, #100023, #3510 ),
 ( #62219, #141741, #235706 ),
 ( #57049, #17943, #40119 ),
 ( #136599, #139152, #216142 ) ),
 .UNSPECIFIED., .F., .F., .F. ) 
 B_SPLINE_SURFACE_WITH_KNOTS ( ( 4, 2, 4 ),
 ( 3, 3 ),
 ( -1.776356839400250465E-15, 0.7853981633974468357, 1.570796326794895448 ),
 ( 0.000000000000000000, 1.000000000000000000 ),
 .UNSPECIFIED. ) 
 GEOMETRIC_REPRESENTATION_ITEM ( )  RATIONAL_B_SPLINE_SURFACE ( (
 ( 1.000000000000000000, 0.4999999999999926170, 1.000000000000000000),
 ( 1.000000000000000000, 0.4993418825367712532, 1.000000000000000000),
 ( 1.000000000000000000, 0.5278258667012460936, 1.000000000000000000),
 ( 1.000000000000000000, 0.6092287576740391675, 1.000000000000000000),
 ( 1.000000000000000000, 0.6611148371745850794, 1.000000000000000000),
 ( 1.000000000000000000, 0.7071067811865597852, 1.000000000000000000) ) ) 
 REPRESENTATION_ITEM ( '' )  SURFACE ( )  );
#109619=CARTESIAN_POINT ( 'NONE',  ( -20.54999999999999716, 54.27339256631721298, -236.8935360681107625 ) ) ;
#109625=ORIENTED_EDGE ( 'NONE', *, *, #9550, .T. ) ;
#109642=CARTESIAN_POINT ( 'NONE',  ( -18.52186455168912360, 46.94619712998765948, -255.3315249897759145 ) ) ;
#109653=DIRECTION ( 'NONE',  ( 1.000000000000000000, 0.000000000000000000, 0.000000000000000000 ) ) ;
#109655=EDGE_LOOP ( 'NONE', ( #238638, #18322, #135167, #19717 ) ) ;
#109686=ORIENTED_EDGE ( 'NONE', *, *, #26163, .F. ) ;
#109703=ORIENTED_EDGE ( 'NONE', *, *, #173598, .F. ) ;
#109728=CARTESIAN_POINT ( 'NONE',  ( -21.05000000000000071, 48.04585786805223080, -246.4610531646956417 ) ) ;
#109744=ADVANCED_FACE ( 'NONE', ( #233759 ), #17282, .F. ) ;
#109769=EDGE_CURVE ( 'NONE', #124376, #4366, #197175, .T. ) ;
#109785=EDGE_CURVE ( 'NONE', #136054, #79014, #16010, .T. ) ;
#109819=VERTEX_POINT ( 'NONE', #47078 ) ;
#109851=CARTESIAN_POINT ( 'NONE',  ( 20.72390388899080804, 39.18426925412079953, -236.8157669261957494 ) ) ;
#109855=VECTOR ( 'NONE', #69813, 1000.000000000000227 ) ;
#109869=DIRECTION ( 'NONE',  ( 1.000000000000000000, 0.000000000000000000, 0.000000000000000000 ) ) ;
#109909=AXIS2_PLACEMENT_3D ( 'NONE', #50519, #212206, #73998 ) ;
#109923=CARTESIAN_POINT ( 'NONE',  ( 20.94999999999999929, 43.47002849391839874, -245.0086825852825143 ) ) ;
#109930=DIRECTION ( 'NONE',  ( 0.000000000000000000, -0.4088369013363276072, 0.9126074666063773710 ) ) ;
#109946=CARTESIAN_POINT ( 'NONE',  ( -20.64999999999999858, 45.00644278977874535, -237.9768835835062077 ) ) ;
#109961=DIRECTION ( 'NONE',  ( 0.000000000000000000, 0.9126074666063773710, 0.4088369013363274962 ) ) ;
#110005=DIRECTION ( 'NONE',  ( 0.000000000000000000, -0.9126074666063770380, -0.4088369013363281068 ) ) ;
#110018=ADVANCED_FACE ( 'NONE', ( #113489 ), #30127, .T. ) ;
#110019=AXIS2_PLACEMENT_3D ( 'NONE', #156223, #153693, #234435 ) ;
#110043=DIRECTION ( 'NONE',  ( 0.000000000000000000, -0.4088369013363276072, 0.9126074666063772600 ) ) ;
#110051=VECTOR ( 'NONE', #167336, 1000.000000000000114 ) ;
#110053=AXIS2_PLACEMENT_3D ( 'NONE', #240555, #220973, #59303 ) ;
#110141=DIRECTION ( 'NONE',  ( 1.000000000000000000, 0.000000000000000000, 0.000000000000000000 ) ) ;
#110147=DIRECTION ( 'NONE',  ( 0.000000000000000000, 0.9126074666063632712, 0.4088369013363589710 ) ) ;
#110169=MECHANICAL_DESIGN_GEOMETRIC_PRESENTATION_REPRESENTATION('',(#118587),#64402);
#110176=EDGE_LOOP ( 'NONE', ( #159237, #235396, #187255, #134700 ) ) ;
#110197=VERTEX_POINT ( 'NONE', #61220 ) ;
#110218=DIRECTION ( 'NONE',  ( 0.000000000000000000, 0.9126074666063844765, 0.4088369013363113980 ) ) ;
#110253=ADVANCED_FACE ( 'NONE', ( #165468 ), #45506, .T. ) ;
#110266=CYLINDRICAL_SURFACE ( 'NONE', #230027, 0.4999999999999944489 ) ;
#110277=ORIENTED_EDGE ( 'NONE', *, *, #29868, .T. ) ;
#110292=AXIS2_PLACEMENT_3D ( 'NONE', #212848, #189430, #49903 ) ;
#110315=ADVANCED_FACE ( 'NONE', ( #73765 ), #246651, .T. ) ;
#110322=AXIS2_PLACEMENT_3D ( 'NONE', #96507, #213910, #253034 ) ;
#110327=ORIENTED_EDGE ( 'NONE', *, *, #30565, .T. ) ;
#110329=DIRECTION ( 'NONE',  ( -0.000000000000000000, 0.9876013379310886187, 0.1569827930593787890 ) ) ;
#110353=EDGE_LOOP ( 'NONE', ( #208324, #118310, #249697, #196588 ) ) ;
#110367=DIRECTION ( 'NONE',  ( 0.000000000000000000, 0.4088369013363281623, -0.9126074666063771490 ) ) ;
#110430=ORIENTED_EDGE ( 'NONE', *, *, #209876, .T. ) ;
#110432=ADVANCED_FACE ( 'NONE', ( #59259 ), #56700, .F. ) ;
#110448=ORIENTED_EDGE ( 'NONE', *, *, #238420, .T. ) ;
#110464=CARTESIAN_POINT ( 'NONE',  ( -20.64999999999999858, 46.10080905699345521, -240.6643289267983334 ) ) ;
#110472=CARTESIAN_POINT ( 'NONE',  ( 21.07094088545304800, 33.98475570745946328, -243.8237622992367051 ) ) ;
#110478=EDGE_LOOP ( 'NONE', ( #164936, #191556, #215508, #133547 ) ) ;
#110485=DIRECTION ( 'NONE',  ( -1.000000000000000000, -0.000000000000000000, -0.000000000000000000 ) ) ;
#110486=ORIENTED_EDGE ( 'NONE', *, *, #223417, .F. ) ;
#110511=ORIENTED_EDGE ( 'NONE', *, *, #238472, .T. ) ;
#110532=EDGE_CURVE ( 'NONE', #92460, #166897, #138800, .T. ) ;
#110539=ADVANCED_FACE ( 'NONE', ( #86544 ), #126986, .T. ) ;
#110542=VERTEX_POINT ( 'NONE', #65729 ) ;
#110552=EDGE_CURVE ( 'NONE', #86798, #61130, #228801, .T. ) ;
#110562=DIRECTION ( 'NONE',  ( 0.000000000000000000, 0.9126074666063771490, 0.4088369013363278293 ) ) ;
#110598=ADVANCED_FACE ( 'NONE', ( #44887 ), #203951, .F. ) ;
#110623=LINE ( 'NONE', #74101, #40536 ) ;
#110627=DIRECTION ( 'NONE',  ( 0.000000000000000000, 0.9126074666063773710, 0.4088369013363274962 ) ) ;
#110630=LINE ( 'NONE', #229307, #251998 ) ;
#110654=AXIS2_PLACEMENT_3D ( 'NONE', #251540, #93751, #209867 ) ;
#110655=ORIENTED_EDGE ( 'NONE', *, *, #132375, .F. ) ;
#110672=ORIENTED_EDGE ( 'NONE', *, *, #26855, .T. ) ;
#110698=TOROIDAL_SURFACE ( 'NONE', #144569, 0.2000000000000000111, 0.1000000000000000056 ) ;
#110714=VECTOR ( 'NONE', #5616, 1000.000000000000114 ) ;
#110722=CARTESIAN_POINT ( 'NONE',  ( -21.05000000000000071, 34.10170768283902021, -243.5983364837296392 ) ) ;
#110735=VERTEX_POINT ( 'NONE', #203518 ) ;
#110761=ORIENTED_EDGE ( 'NONE', *, *, #194341, .T. ) ;
#110771=VERTEX_POINT ( 'NONE', #125269 ) ;
#110787=DIRECTION ( 'NONE',  ( 1.000000000000000000, 0.000000000000000000, 0.000000000000000000 ) ) ;
#110792=FACE_OUTER_BOUND ( 'NONE', #29352, .T. ) ;
#110803=CARTESIAN_POINT ( 'NONE',  ( 21.14999999999999858, 45.02833974712562792, -238.5149546970766892 ) ) ;
#110838=AXIS2_PLACEMENT_3D ( 'NONE', #141857, #84405, #186129 ) ;
#110843=EDGE_CURVE ( 'NONE', #139949, #99525, #78913, .T. ) ;
#110850=EDGE_LOOP ( 'NONE', ( #131384, #215246, #50222, #7679 ) ) ;
#110851=EDGE_CURVE ( 'NONE', #2789, #48342, #173432, .T. ) ;
#110951=CARTESIAN_POINT ( 'NONE',  ( -18.50000000000000000, 64.02438395623025258, -266.2629958759080182 ) ) ;
#110976=CARTESIAN_POINT ( 'NONE',  ( -18.56579813702275672, 68.10670728244119232, -224.1434476749765565 ) ) ;
#111037=DIRECTION ( 'NONE',  ( -1.000000000000000000, 0.000000000000000000, 0.000000000000000000 ) ) ;
#111038=CIRCLE ( 'NONE', #194455, 0.09999999999999481526 ) ;
#111045=ORIENTED_EDGE ( 'NONE', *, *, #185462, .F. ) ;
#111078=AXIS2_PLACEMENT_3D ( 'NONE', #225356, #46724, #227945 ) ;
#111079=AXIS2_PLACEMENT_3D ( 'NONE', #103003, #26067, #44345 ) ;
#111140=CARTESIAN_POINT ( 'NONE',  ( -21.59142135623730852, 52.75120266497943078, -233.7402936251220638 ) ) ;
#111161=EDGE_CURVE ( 'NONE', #183191, #36016, #140994, .T. ) ;
#111166=VERTEX_POINT ( 'NONE', #220527 ) ;
#111210=CARTESIAN_POINT ( 'NONE',  ( 22.48660254037844197, 31.85034414784619017, -238.9397275603479898 ) ) ;
#111218=CARTESIAN_POINT ( 'NONE',  ( 20.94999999999999929, 71.99422445362657186, -246.4870034924427671 ) ) ;
#111224=SURFACE_SIDE_STYLE ('',( #72111 ) ) ;
#111243=CARTESIAN_POINT ( 'NONE',  ( 18.59999999999999076, 67.23127455305835554, -235.8551265064784559 ) ) ;
#111244=DIRECTION ( 'NONE',  ( 0.000000000000000000, 0.9126074666063772600, 0.4088369013363277737 ) ) ;
#111261=DIRECTION ( 'NONE',  ( 0.000000000000000000, 0.9126074666063660468, 0.4088369013363524762 ) ) ;
#111272=AXIS2_PLACEMENT_3D ( 'NONE', #253082, #171048, #250518 ) ;
#111276=EDGE_LOOP ( 'NONE', ( #172445, #145795, #106536, #44359 ) ) ;
#111280=EDGE_LOOP ( 'NONE', ( #256670, #233786, #67223, #246211 ) ) ;
#111291=ADVANCED_FACE ( 'NONE', ( #209956 ), #149495, .T. ) ;
#111297=ORIENTED_EDGE ( 'NONE', *, *, #197979, .F. ) ;
#111303=CARTESIAN_POINT ( 'NONE',  ( 22.59999999999999787, 31.80488924422933295, -238.9605610896540213 ) ) ;
#111350=EDGE_LOOP ( 'NONE', ( #220474, #139600, #206309 ) ) ;
#111407=EDGE_CURVE ( 'NONE', #130629, #158029, #117262, .T. ) ;
#111416=CARTESIAN_POINT ( 'NONE',  ( -23.15000000000000213, 21.17283678855157802, -243.7231193059830332 ) ) ;
#111432=DIRECTION ( 'NONE',  ( 0.000000000000000000, 0.9126074666063753726, 0.4088369013363320481 ) ) ;
#111477=VERTEX_POINT ( 'NONE', #198070 ) ;
#111490=CIRCLE ( 'NONE', #32422, 0.09999999999999939493 ) ;
#111513=CARTESIAN_POINT ( 'NONE',  ( 22.60000000000000142, 31.76322370622491320, -238.8696546380523671 ) ) ;
#111515=LINE ( 'NONE', #91944, #214923 ) ;
#111530=VECTOR ( 'NONE', #195534, 1000.000000000000114 ) ;
#111545=DIRECTION ( 'NONE',  ( 2.557131231893037478E-16, -0.1022405907414165593, -0.9947597004326453884 ) ) ;
#111547=CARTESIAN_POINT ( 'NONE',  ( 21.00000000000000000, 52.06567329910104291, -231.9654557484363409 ) ) ;
#111585=CARTESIAN_POINT ( 'NONE',  ( -20.94999999999999929, 38.09878670418233781, -236.0309261423825262 ) ) ;
#111592=EDGE_CURVE ( 'NONE', #228170, #168895, #166079, .T. ) ;
#111609=CARTESIAN_POINT ( 'NONE',  ( 20.94999999999999929, 62.08591502004790641, -248.5699171172615820 ) ) ;
#111613=CIRCLE ( 'NONE', #65813, 12.77500000000002522 ) ;
#111620=EDGE_LOOP ( 'NONE', ( #146051, #179201, #89538, #159525 ) ) ;
#111624=VERTEX_POINT ( 'NONE', #28465 ) ;
#111646=EDGE_LOOP ( 'NONE', ( #98784, #46151, #237102, #223301 ) ) ;
#111655=AXIS2_PLACEMENT_3D ( 'NONE', #90404, #14761, #91698 ) ;
#111667=ORIENTED_EDGE ( 'NONE', *, *, #40894, .T. ) ;
#111694=AXIS2_PLACEMENT_3D ( 'NONE', #84693, #67742, #147274 ) ;
#111711=ORIENTED_EDGE ( 'NONE', *, *, #139496, .F. ) ;
#111726=AXIS2_PLACEMENT_3D ( 'NONE', #183855, #221675, #65185 ) ;
#111766=CARTESIAN_POINT ( 'NONE',  ( 21.09551895715256009, 43.48418023705998792, -234.8549715607070709 ) ) ;
#111770=VERTEX_POINT ( 'NONE', #119198 ) ;
#111783=CARTESIAN_POINT ( 'NONE',  ( 21.10642757222115407, 43.44585438861653159, -234.7606813603525779 ) ) ;
#111840=ORIENTED_EDGE ( 'NONE', *, *, #9375, .F. ) ;
#111860=DIRECTION ( 'NONE',  ( 1.000000000000000000, 0.000000000000000000, 0.000000000000000000 ) ) ;
#111880=ORIENTED_EDGE ( 'NONE', *, *, #247256, .F. ) ;
#111889=CYLINDRICAL_SURFACE ( 'NONE', #192507, 0.09999999999999609201 ) ;
#111906=LINE ( 'NONE', #191463, #213840 ) ;
#111940=ORIENTED_EDGE ( 'NONE', *, *, #83353, .T. ) ;
#111957=DIRECTION ( 'NONE',  ( -0.9880948137434723000, -0.06289798482097130883, 0.1404011487086683774 ) ) ;
#111974=LINE ( 'NONE', #169407, #157835 ) ;
#111996=ORIENTED_EDGE ( 'NONE', *, *, #56733, .F. ) ;
#112011=ADVANCED_FACE ( 'NONE', ( #186888 ), #83161, .F. ) ;
#112019=ORIENTED_EDGE ( 'NONE', *, *, #20362, .F. ) ;
#112022=EDGE_LOOP ( 'NONE', ( #15534, #135239, #254019, #30129 ) ) ;
#112044=DIRECTION ( 'NONE',  ( 2.827886303505249259E-16, 0.8103668758649578141, -0.5859227990963212784 ) ) ;
#112048=DIRECTION ( 'NONE',  ( -1.000000000000000000, -0.000000000000000000, 0.000000000000000000 ) ) ;
#112104=CARTESIAN_POINT ( 'NONE',  ( 23.14999999999998437, 41.46275801244657799, -260.2743004338703940 ) ) ;
#112141=DIRECTION ( 'NONE',  ( 0.000000000000000000, -0.4088369013363297166, 0.9126074666063763718 ) ) ;
#112144=VECTOR ( 'NONE', #197833, 1000.000000000000000 ) ;
#112160=FACE_OUTER_BOUND ( 'NONE', #213340, .T. ) ;
#112161=EDGE_CURVE ( 'NONE', #240937, #218845, #183172, .T. ) ;
#112182=DIRECTION ( 'NONE',  ( 1.000000000000000000, 0.000000000000000000, 0.000000000000000000 ) ) ;
#112216=VERTEX_POINT ( 'NONE', #243966 ) ;
#112228=DIRECTION ( 'NONE',  ( 0.000000000000000000, -0.4088369013363280513, 0.9126074666063769270 ) ) ;
#112256=CARTESIAN_POINT ( 'NONE',  ( -18.59999999999999787, 43.92448011351754644, -236.0509145372394357 ) ) ;
#112279=DIRECTION ( 'NONE',  ( 0.000000000000000000, 0.9126074666064696306, 0.4088369013361213278 ) ) ;
#112295=VERTEX_POINT ( 'NONE', #122765 ) ;
#112296=AXIS2_PLACEMENT_3D ( 'NONE', #47826, #208225, #93066 ) ;
#112322=CARTESIAN_POINT ( 'NONE',  ( 20.94999999999999929, 67.23127455305835554, -235.8551265064784559 ) ) ;
#112344=DIRECTION ( 'NONE',  ( 0.000000000000000000, 0.8490545835447252943, 0.5283051335749948674 ) ) ;
#112347=ORIENTED_EDGE ( 'NONE', *, *, #36276, .F. ) ;
#112353=ORIENTED_EDGE ( 'NONE', *, *, #237420, .T. ) ;
#112356=CIRCLE ( 'NONE', #83, 0.09999999999999609201 ) ;
#112384=DIRECTION ( 'NONE',  ( -1.000000000000000000, 1.207181226542539700E-16, -2.694675058168174199E-16 ) ) ;
#112401=ORIENTED_EDGE ( 'NONE', *, *, #189115, .F. ) ;
#112429=CARTESIAN_POINT ( 'NONE',  ( -20.94999999999999929, 38.23914636435922176, -236.1324109481172968 ) ) ;
#112443=VECTOR ( 'NONE', #90348, 1000.000000000000114 ) ;
#112508=DIRECTION ( 'NONE',  ( -0.7071067811864846231, -0.2890913453341779626, 0.6453109281989296564 ) ) ;
#112581=CARTESIAN_POINT ( 'NONE',  ( 18.59999999999997655, 67.23127455305835554, -235.8551265064784559 ) ) ;
#112617=ORIENTED_EDGE ( 'NONE', *, *, #36417, .F. ) ;
#112644=EDGE_CURVE ( 'NONE', #9598, #185818, #70951, .T. ) ;
#112656=AXIS2_PLACEMENT_3D ( 'NONE', #44156, #220231, #179824 ) ;
#112658=CARTESIAN_POINT ( 'NONE',  ( 20.94999999999999929, 74.34961279258810407, -232.6661986760551315 ) ) ;
#112659=EDGE_CURVE ( 'NONE', #84649, #4376, #4261, .T. ) ;
#112679=CIRCLE ( 'NONE', #46025, 0.09999999999999939493 ) ;
#112708=LINE ( 'NONE', #9741, #189548 ) ;
#112720=CARTESIAN_POINT ( 'NONE',  ( -23.25000000000000000, 67.23127455305835554, -235.8551265064784559 ) ) ;
#112735=EDGE_LOOP ( 'NONE', ( #164296, #127087, #116439, #170564 ) ) ;
#112752=DIRECTION ( 'NONE',  ( 1.000000000000000000, 0.000000000000000000, 0.000000000000000000 ) ) ;
#112756=CYLINDRICAL_SURFACE ( 'NONE', #224416, 0.1000000000000024342 ) ;
#112770=DIRECTION ( 'NONE',  ( 1.000000000000000000, 0.000000000000000000, 0.000000000000000000 ) ) ;
#112780=ORIENTED_EDGE ( 'NONE', *, *, #26181, .F. ) ;
#112784=EDGE_CURVE ( 'NONE', #151804, #10431, #167005, .T. ) ;
#112789=CARTESIAN_POINT ( 'NONE',  ( -21.05000000000000071, 30.78798680020884504, -252.2006866936654319 ) ) ;
#112797=AXIS2_PLACEMENT_3D ( 'NONE', #231818, #250084, #230527 ) ;
#112802=CARTESIAN_POINT ( 'NONE',  ( -21.14999999999999858, 31.94635157770351341, -238.7871412784868994 ) ) ;
#112807=FACE_OUTER_BOUND ( 'NONE', #136798, .T. ) ;
#112809=PLANE ( 'NONE',  #211453 ) ;
#112820=ORIENTED_EDGE ( 'NONE', *, *, #15226, .F. ) ;
#112824=CARTESIAN_POINT ( 'NONE',  ( -23.15000000000000213, 62.33780030268294325, -247.9091949332902516 ) ) ;
#112862=ADVANCED_FACE ( 'NONE', ( #93572 ), #174449, .F. ) ;
#112886=FACE_OUTER_BOUND ( 'NONE', #73438, .T. ) ;
#112899=ORIENTED_EDGE ( 'NONE', *, *, #88591, .F. ) ;
#112915=LINE ( 'NONE', #13815, #160156 ) ;
#112920=ADVANCED_FACE ( 'NONE', ( #176997 ), #231821, .T. ) ;
#112927=AXIS2_PLACEMENT_3D ( 'NONE', #202636, #24026, #103520 ) ;
#112941=DIRECTION ( 'NONE',  ( 1.000000000000000000, -0.000000000000000000, -0.000000000000000000 ) ) ;
#112954=VERTEX_POINT ( 'NONE', #197798 ) ;
#112974=EDGE_CURVE ( 'NONE', #2697, #3155, #123408, .T. ) ;
#113000=LINE ( 'NONE', #248654, #143897 ) ;
#113010=ADVANCED_FACE ( 'NONE', ( #140385 ), #38745, .F. ) ;
#113019=EDGE_CURVE ( 'NONE', #118580, #33783, #100473, .T. ) ;
#113040=EDGE_LOOP ( 'NONE', ( #207510, #171262, #235598, #132707 ) ) ;
#113045=EDGE_LOOP ( 'NONE', ( #30398, #127749, #32874, #225397 ) ) ;
#113046=CARTESIAN_POINT ( 'NONE',  ( 21.05000000000000071, 40.88152484246180052, -238.0427780438910474 ) ) ;
#113060=CARTESIAN_POINT ( 'NONE',  ( 21.08750232978087524, 43.43435178450272360, -234.7639638145086849 ) ) ;
#113081=CARTESIAN_POINT ( 'NONE',  ( 18.39999999999999858, 77.17949092533254429, -241.9177572069595783 ) ) ;
#113083=CARTESIAN_POINT ( 'NONE',  ( 21.05000000000000071, 44.05869416168422958, -258.6139110589941197 ) ) ;
#113110=DIRECTION ( 'NONE',  ( 1.000000000000000000, -1.335000415235278971E-16, 2.979993593738921214E-16 ) ) ;
#113127=ORIENTED_EDGE ( 'NONE', *, *, #77722, .T. ) ;
#113170=DIRECTION ( 'NONE',  ( 0.000000000000000000, -0.4088369013363280513, 0.9126074666063769270 ) ) ;
#113190=DIRECTION ( 'NONE',  ( 0.000000000000000000, -0.9126074666063660468, -0.4088369013363524762 ) ) ;
#113195=EDGE_CURVE ( 'NONE', #152685, #44054, #33927, .T. ) ;
#113214=CIRCLE ( 'NONE', #125695, 0.09999999999999950595 ) ;
#113217=EDGE_LOOP ( 'NONE', ( #254999, #30653, #37686, #100873 ) ) ;
#113222=EDGE_CURVE ( 'NONE', #72558, #102432, #187835, .T. ) ;
#113232=DIRECTION ( 'NONE',  ( 0.000000000000000000, -0.9126074666063769270, -0.4088369013363281623 ) ) ;
#113244=EDGE_CURVE ( 'NONE', #7959, #48558, #54715, .T. ) ;
#113298=ORIENTED_EDGE ( 'NONE', *, *, #125362, .F. ) ;
#113331=VECTOR ( 'NONE', #6143, 1000.000000000000114 ) ;
#113335=DIRECTION ( 'NONE',  ( -0.000000000000000000, 0.9126074666063770380, 0.4088369013363281068 ) ) ;
#113361=CARTESIAN_POINT ( 'NONE',  ( 20.94999999999999574, 39.15282200719421013, -236.7930294976410437 ) ) ;
#113366=ORIENTED_EDGE ( 'NONE', *, *, #131358, .F. ) ;
#113381=CARTESIAN_POINT ( 'NONE',  ( 21.22070241538126467, 30.71396139465468167, -252.1060412414022949 ) ) ;
#113439=DIRECTION ( 'NONE',  ( 1.000000000000000000, 0.000000000000000000, 0.000000000000000000 ) ) ;
#113441=LINE ( 'NONE', #195569, #155021 ) ;
#113486=AXIS2_PLACEMENT_3D ( 'NONE', #48258, #109503, #70432 ) ;
#113489=FACE_OUTER_BOUND ( 'NONE', #119211, .T. ) ;
#113510=DIRECTION ( 'NONE',  ( 1.000000000000000000, 0.000000000000000000, 0.000000000000000000 ) ) ;
#113511=ORIENTED_EDGE ( 'NONE', *, *, #2239, .F. ) ;
#113515=CARTESIAN_POINT ( 'NONE',  ( -20.64999999999999858, 46.05992536685982230, -240.5730681801377102 ) ) ;
#113541=DIRECTION ( 'NONE',  ( 0.000000000000000000, 0.9126074666063772600, 0.4088369013363276627 ) ) ;
#113585=CYLINDRICAL_SURFACE ( 'NONE', #15623, 0.09999999999999609201 ) ;
#113588=DIRECTION ( 'NONE',  ( -0.000000000000000000, 0.4088369013363276072, -0.9126074666063772600 ) ) ;
#113614=ORIENTED_EDGE ( 'NONE', *, *, #229524, .F. ) ;
#113661=AXIS2_PLACEMENT_3D ( 'NONE', #84752, #125213, #67795 ) ;
#113666=AXIS2_PLACEMENT_3D ( 'NONE', #109091, #188637, #83078 ) ;
#113673=CARTESIAN_POINT ( 'NONE',  ( -18.50000000000000000, 52.27009174976920747, -232.4217594817395138 ) ) ;
#113678=ADVANCED_FACE ( 'NONE', ( #165464 ), #102881, .T. ) ;
#113770=CARTESIAN_POINT ( 'NONE',  ( 18.49999999999999645, 78.48087866980282001, -232.8271061603568910 ) ) ;
#113810=CARTESIAN_POINT ( 'NONE',  ( 21.05000000000000071, 30.78880722230112710, -252.2904790204486574 ) ) ;
#113816=DIRECTION ( 'NONE',  ( 1.000000000000000000, -1.207181226542539700E-16, 2.694675058168174199E-16 ) ) ;
#113852=DIRECTION ( 'NONE',  ( -4.391705002472924160E-16, -0.4088369013363268301, 0.9126074666063775931 ) ) ;
#113871=AXIS2_PLACEMENT_3D ( 'NONE', #85635, #187359, #47809 ) ;
#113884=CYLINDRICAL_SURFACE ( 'NONE', #54617, 0.1000000000000214190 ) ;
#113930=ORIENTED_EDGE ( 'NONE', *, *, #37667, .F. ) ;
#113939=CIRCLE ( 'NONE', #80598, 0.09999999999999063804 ) ;
#113990=CYLINDRICAL_SURFACE ( 'NONE', #78465, 0.1000000000000142025 ) ;
#114002=VECTOR ( 'NONE', #17020, 1000.000000000000000 ) ;
#114036=DIRECTION ( 'NONE',  ( -0.000000000000000000, 0.8103668758649523740, -0.5859227990963290500 ) ) ;
#114042=ORIENTED_EDGE ( 'NONE', *, *, #184687, .T. ) ;
#114053=CARTESIAN_POINT ( 'NONE',  ( -21.11833042828143547, 30.77367799691945294, -252.1799001274110310 ) ) ;
#114058=AXIS2_PLACEMENT_3D ( 'NONE', #221302, #64811, #257830 ) ;
#114074=CYLINDRICAL_SURFACE ( 'NONE', #183452, 0.09999999999999609201 ) ;
#114080=ORIENTED_EDGE ( 'NONE', *, *, #140931, .F. ) ;
#114081=EDGE_CURVE ( 'NONE', #93242, #206465, #159165, .T. ) ;
#114084=DIRECTION ( 'NONE',  ( 0.000000000000000000, 0.9126074666063765939, 0.4088369013363289950 ) ) ;
#114090=DIRECTION ( 'NONE',  ( 1.000000000000000000, -2.986185139342070877E-16, 6.665775143889692774E-16 ) ) ;
#114094=EDGE_CURVE ( 'NONE', #244838, #2789, #218675, .T. ) ;
#114099=CYLINDRICAL_SURFACE ( 'NONE', #182970, 0.8750000000000007772 ) ;
#114102=AXIS2_PLACEMENT_3D ( 'NONE', #92364, #57064, #251444 ) ;
#114119=ORIENTED_EDGE ( 'NONE', *, *, #191183, .F. ) ;
#114121=DIRECTION ( 'NONE',  ( 1.000000000000000000, 0.000000000000000000, 0.000000000000000000 ) ) ;
#114154=DIRECTION ( 'NONE',  ( 0.000000000000000000, 0.9126074666063770380, 0.4088369013363278848 ) ) ;
#114178=ORIENTED_EDGE ( 'NONE', *, *, #120988, .T. ) ;
#114185=CARTESIAN_POINT ( 'NONE',  ( 20.95512820512820440, 39.31056039967181448, -236.7220595557971023 ) ) ;
#114195=CARTESIAN_POINT ( 'NONE',  ( 21.14999999999999858, 43.45833571831320796, -234.7657887233443716 ) ) ;
#114202=DIRECTION ( 'NONE',  ( 2.952720810173289112E-16, 0.4088369013363246096, -0.9126074666063785923 ) ) ;
#114216=DIRECTION ( 'NONE',  ( 0.000000000000000000, -0.9126074666063773710, -0.4088369013363274962 ) ) ;
#114229=EDGE_CURVE ( 'NONE', #182399, #221407, #167721, .T. ) ;
#114233=CARTESIAN_POINT ( 'NONE',  ( 21.05000000000000071, 30.91371304215671145, -252.1483800927532002 ) ) ;
#114261=AXIS2_PLACEMENT_3D ( 'NONE', #169329, #145855, #164156 ) ;
#114267=DIRECTION ( 'NONE',  ( 0.000000000000000000, -0.9126074666063769270, -0.4088369013363280513 ) ) ;
#114274=DIRECTION ( 'NONE',  ( -0.000000000000000000, -0.4088369013363281623, 0.9126074666063771490 ) ) ;
#114311=CARTESIAN_POINT ( 'NONE',  ( -20.94999999999999929, 69.08367151115869831, -247.5088222940653679 ) ) ;
#114329=ADVANCED_FACE ( 'NONE', ( #13766 ), #97110, .F. ) ;
#114365=DIRECTION ( 'NONE',  ( 1.000000000000000000, 0.000000000000000000, 0.000000000000000000 ) ) ;
#114388=DIRECTION ( 'NONE',  ( 0.000000000000000000, 0.4088369013363281623, -0.9126074666063771490 ) ) ;
#114436=CARTESIAN_POINT ( 'NONE',  ( -18.59999999999999787, 74.93036000061670165, -233.6816308724374949 ) ) ;
#114444=LINE ( 'NONE', #173185, #223171 ) ;
#114455=TOROIDAL_SURFACE ( 'NONE', #93608, 11.65000000000000036, 0.1000000000000000056 ) ;
#114472=CYLINDRICAL_SURFACE ( 'NONE', #40641, 0.1000000000000024342 ) ;
#114488=AXIS2_PLACEMENT_3D ( 'NONE', #256098, #140047, #200053 ) ;
#114525=ORIENTED_EDGE ( 'NONE', *, *, #172195, .F. ) ;
#114526=VERTEX_POINT ( 'NONE', #75771 ) ;
#114527=CARTESIAN_POINT ( 'NONE',  ( -23.15000000000000213, 46.10080905699345521, -240.6643289267983334 ) ) ;
#114588=AXIS2_PLACEMENT_3D ( 'NONE', #248980, #191593, #132881 ) ;
#114601=DIRECTION ( 'NONE',  ( 0.000000000000000000, -0.9126074666063770380, -0.4088369013363281068 ) ) ;
#114603=ORIENTED_EDGE ( 'NONE', *, *, #237494, .F. ) ;
#114604=DIRECTION ( 'NONE',  ( 0.000000000000000000, 0.9126074666063769270, 0.4088369013363282733 ) ) ;
#114645=ORIENTED_EDGE ( 'NONE', *, *, #59673, .F. ) ;
#114665=FACE_OUTER_BOUND ( 'NONE', #18558, .T. ) ;
#114709=ORIENTED_EDGE ( 'NONE', *, *, #223994, .T. ) ;
#114710=ORIENTED_EDGE ( 'NONE', *, *, #5873, .F. ) ;
#114742=CARTESIAN_POINT ( 'NONE',  ( 19.97071067811863898, 54.41629874617179041, -228.7529758933203539 ) ) ;
#114766=CARTESIAN_POINT ( 'NONE',  ( -22.50000000000000000, 31.82071903192811746, -238.9531407059545813 ) ) ;
#114781=ORIENTED_EDGE ( 'NONE', *, *, #123759, .T. ) ;
#114803=ADVANCED_FACE ( 'NONE', ( #168182 ), #165583, .T. ) ;
#114806=CARTESIAN_POINT ( 'NONE',  ( 21.05000000000000071, 42.98415524044398950, -233.9519173640447889 ) ) ;
#114811=ORIENTED_EDGE ( 'NONE', *, *, #112659, .F. ) ;
#114819=CARTESIAN_POINT ( 'NONE',  ( -22.57320508075687115, 31.89597452117654086, -238.9192857152811484 ) ) ;
#114855=CARTESIAN_POINT ( 'NONE',  ( -21.45000000000000284, 52.90028168070691095, -233.8284721206281915 ) ) ;
#114879=VERTEX_POINT ( 'NONE', #28677 ) ;
#114887=VERTEX_POINT ( 'NONE', #108171 ) ;
#114901=ORIENTED_EDGE ( 'NONE', *, *, #79135, .F. ) ;
#114932=ORIENTED_EDGE ( 'NONE', *, *, #53704, .F. ) ;
#114933=ORIENTED_EDGE ( 'NONE', *, *, #226791, .T. ) ;
#114960=VERTEX_POINT ( 'NONE', #172027 ) ;
#114961=DIRECTION ( 'NONE',  ( -0.000000000000000000, 0.4088369013363281068, -0.9126074666063770380 ) ) ;
#114968=EDGE_CURVE ( 'NONE', #116784, #206263, #173322, .T. ) ;
#114995=ADVANCED_FACE ( 'NONE', ( #175853 ), #170758, .F. ) ;
#115012=EDGE_CURVE ( 'NONE', #172097, #101237, #242885, .T. ) ;
#115030=DIRECTION ( 'NONE',  ( 0.000000000000000000, -0.2818822000685679008, 0.9594490217226259166 ) ) ;
#115031=FACE_OUTER_BOUND ( 'NONE', #42140, .T. ) ;
#115042=ADVANCED_FACE ( 'NONE', ( #37628 ), #134718, .T. ) ;
#115071=VECTOR ( 'NONE', #251470, 1000.000000000000000 ) ;
#115073=DIRECTION ( 'NONE',  ( 0.000000000000000000, 0.9126074666063771490, 0.4088369013363281623 ) ) ;
#115078=CARTESIAN_POINT ( 'NONE',  ( -22.50000000000000000, 36.61804073161109585, -249.4599019545848364 ) ) ;
#115095=DIRECTION ( 'NONE',  ( 1.000000000000000000, 0.000000000000000000, 0.000000000000000000 ) ) ;
#115099=CARTESIAN_POINT ( 'NONE',  ( -20.64999999999999858, 46.15118611352045974, -240.5321844900040844 ) ) ;
#115101=PLANE ( 'NONE',  #131273 ) ;
#115115=CARTESIAN_POINT ( 'NONE',  ( 20.94999999999999929, 53.70241689174373079, -235.9987767062293074 ) ) ;
#115131=DIRECTION ( 'NONE',  ( 1.000000000000000000, 0.000000000000000000, 0.000000000000000000 ) ) ;
#115145=ORIENTED_EDGE ( 'NONE', *, *, #217073, .F. ) ;
#115149=DIRECTION ( 'NONE',  ( 1.000000000000000000, 0.000000000000000000, 0.000000000000000000 ) ) ;
#115166=VECTOR ( 'NONE', #134878, 1000.000000000000000 ) ;
#115171=CARTESIAN_POINT ( 'NONE',  ( -23.25000000000000000, 44.25095746879271985, -258.9156452930671435 ) ) ;
#115176=ADVANCED_FACE ( 'NONE', ( #183541 ), #184809, .F. ) ;
#115190=ORIENTED_EDGE ( 'NONE', *, *, #14856, .F. ) ;
#115209=AXIS2_PLACEMENT_3D ( 'NONE', #154599, #134973, #193700 ) ;
#115212=VECTOR ( 'NONE', #256317, 1000.000000000000114 ) ;
#115231=DIRECTION ( 'NONE',  ( -2.557131231893036985E-16, 0.1022405907414164900, 0.9947597004326451664 ) ) ;
#115250=ORIENTED_EDGE ( 'NONE', *, *, #25557, .T. ) ;
#115259=AXIS2_PLACEMENT_3D ( 'NONE', #100811, #223361, #23921 ) ;
#115277=FACE_OUTER_BOUND ( 'NONE', #21070, .T. ) ;
#115289=AXIS2_PLACEMENT_3D ( 'NONE', #13364, #109869, #147736 ) ;
#115294=EDGE_CURVE ( 'NONE', #114960, #222885, #142898, .T. ) ;
#115313=ORIENTED_EDGE ( 'NONE', *, *, #105712, .T. ) ;
#115344=ADVANCED_FACE ( 'NONE', ( #85048 ), #92658, .T. ) ;
#115357=CARTESIAN_POINT ( 'NONE',  ( -18.60000000000000142, 77.40559867739671063, -241.7331358027584827 ) ) ;
#115396=CIRCLE ( 'NONE', #165496, 0.09999999999999695244 ) ;
#115404=DIRECTION ( 'NONE',  ( 1.000000000000000000, 0.000000000000000000, 0.000000000000000000 ) ) ;
#115409=CARTESIAN_POINT ( 'NONE',  ( 21.05000000000000071, 69.56804783242856161, -248.4091712263733882 ) ) ;
#115464=ORIENTED_EDGE ( 'NONE', *, *, #218653, .F. ) ;
#115504=CARTESIAN_POINT ( 'NONE',  ( 21.05000000000000071, 30.86266526676358879, -252.1316881318525986 ) ) ;
#115506=CIRCLE ( 'NONE', #3073, 0.09999999999999854838 ) ;
#115508=CIRCLE ( 'NONE', #64100, 0.09999999999999939493 ) ;
#115513=EDGE_CURVE ( 'NONE', #197418, #242821, #143091, .T. ) ;
#115552=CARTESIAN_POINT ( 'NONE',  ( 20.87600722750343252, 68.10911674539558192, -224.1414149070238864 ) ) ;
#115557=DIRECTION ( 'NONE',  ( 1.000000000000000000, 0.000000000000000000, 0.000000000000000000 ) ) ;
#115586=CARTESIAN_POINT ( 'NONE',  ( -18.59999999999999787, 67.85909929089923764, -227.8797997985275856 ) ) ;
#115617=ORIENTED_EDGE ( 'NONE', *, *, #256209, .F. ) ;
#115629=CARTESIAN_POINT ( 'NONE',  ( -22.47007471830799119, 33.50241300269673417, -242.5051845127899526 ) ) ;
#115637=VERTEX_POINT ( 'NONE', #97890 ) ;
#115638=VECTOR ( 'NONE', #221474, 1000.000000000000000 ) ;
#115670=VERTEX_POINT ( 'NONE', #37979 ) ;
#115724=DIRECTION ( 'NONE',  ( 0.000000000000000000, 0.9126074666063545004, 0.4088369013363783999 ) ) ;
#115734=ORIENTED_EDGE ( 'NONE', *, *, #73612, .T. ) ;
#115752=ORIENTED_EDGE ( 'NONE', *, *, #70303, .T. ) ;
#115759=DIRECTION ( 'NONE',  ( 0.000000000000000000, 0.9126074666063774821, 0.4088369013363273297 ) ) ;
#115774=ORIENTED_EDGE ( 'NONE', *, *, #122194, .T. ) ;
#115828=AXIS2_PLACEMENT_3D ( 'NONE', #53542, #207499, #133085 ) ;
#115860=B_SPLINE_CURVE_WITH_KNOTS ( 'NONE', 3,
 ( #196218, #175409, #179256, #57976, #159678, #239204, #160968, #35891 ),
 .UNSPECIFIED., .F., .F.,
 ( 4, 2, 2, 4 ),
 ( 0.000000000000000000, 0.0002181133598169259869, 0.0003271700397253583651, 0.0004362267196337907705 ),
 .UNSPECIFIED. ) ;
#115884=CARTESIAN_POINT ( 'NONE',  ( -23.25000000000000000, 42.94327155031035659, -233.8606566173841372 ) ) ;
#115896=CARTESIAN_POINT ( 'NONE',  ( -21.55000000000000426, 52.79208635511305658, -233.8315543717827154 ) ) ;
#115899=ORIENTED_EDGE ( 'NONE', *, *, #158928, .T. ) ;
#115903=FACE_OUTER_BOUND ( 'NONE', #120663, .T. ) ;
#115948=ADVANCED_FACE ( 'NONE', ( #148619 ), #6753, .T. ) ;
#115969=CYLINDRICAL_SURFACE ( 'NONE', #42880, 0.09999999999999609201 ) ;
#116034=ADVANCED_FACE ( 'NONE', ( #115903 ), #146984, .T. ) ;
#116035=DIRECTION ( 'NONE',  ( 0.000000000000000000, -0.4088369013363283844, 0.9126074666063768159 ) ) ;
#116074=VERTEX_POINT ( 'NONE', #196706 ) ;
#116077=DIRECTION ( 'NONE',  ( 1.000000000000000000, 0.000000000000000000, 0.000000000000000000 ) ) ;
#116082=DIRECTION ( 'NONE',  ( 1.000000000000000000, 0.000000000000000000, 0.000000000000000000 ) ) ;
#116099=EDGE_CURVE ( 'NONE', #233797, #143749, #41515, .T. ) ;
#116115=ORIENTED_EDGE ( 'NONE', *, *, #66536, .T. ) ;
#116118=EDGE_CURVE ( 'NONE', #169719, #132474, #84606, .T. ) ;
#116143=EDGE_CURVE ( 'NONE', #222885, #89898, #184598, .T. ) ;
#116153=ORIENTED_EDGE ( 'NONE', *, *, #135001, .F. ) ;
#116178=EDGE_LOOP ( 'NONE', ( #12310, #131085, #106832, #148971 ) ) ;
#116186=AXIS2_PLACEMENT_3D ( 'NONE', #109520, #229488, #92522 ) ;
#116212=ORIENTED_EDGE ( 'NONE', *, *, #150456, .T. ) ;
#116250=EDGE_CURVE ( 'NONE', #74869, #203555, #72202, .T. ) ;
#116272=CONICAL_SURFACE ( 'NONE', #145463, 4.050000000000006040, 0.7853981633974604915 ) ;
#116274=EDGE_CURVE ( 'NONE', #57537, #246198, #147194, .T. ) ;
#116323=CARTESIAN_POINT ( 'NONE',  ( 18.49362639424905552, 77.26503896671080440, -241.7069646862937304 ) ) ;
#116334=DIRECTION ( 'NONE',  ( 1.000000000000000000, 0.000000000000000000, 0.000000000000000000 ) ) ;
#116355=AXIS2_PLACEMENT_3D ( 'NONE', #146852, #68633, #227687 ) ;
#116366=DIRECTION ( 'NONE',  ( 0.000000000000000000, 0.4088369013363287729, -0.9126074666063767049 ) ) ;
#116377=CARTESIAN_POINT ( 'NONE',  ( 18.49999999999945999, 54.99804363260582818, -230.1039092834927828 ) ) ;
#116395=TOROIDAL_SURFACE ( 'NONE', #199613, 12.97499999999999787, 0.1000000000000000056 ) ;
#116406=CARTESIAN_POINT ( 'NONE',  ( 18.59999999999999787, 78.45218979564165807, -232.7313097695096076 ) ) ;
#116439=ORIENTED_EDGE ( 'NONE', *, *, #60452, .F. ) ;
#116441=FACE_OUTER_BOUND ( 'NONE', #222016, .T. ) ;
#116444=CARTESIAN_POINT ( 'NONE',  ( -21.05000000000000071, 55.49311008795314137, -234.6486875357297492 ) ) ;
#116467=DIRECTION ( 'NONE',  ( 0.000000000000000000, 0.9947597004326491632, -0.1022405907413782566 ) ) ;
#116510=ORIENTED_EDGE ( 'NONE', *, *, #23725, .T. ) ;
#116523=ORIENTED_EDGE ( 'NONE', *, *, #246878, .F. ) ;
#116543=EDGE_LOOP ( 'NONE', ( #206207, #182511, #7541, #229024 ) ) ;
#116570=EDGE_CURVE ( 'NONE', #252130, #191945, #99838, .T. ) ;
#116573=DIRECTION ( 'NONE',  ( 0.000000000000000000, -0.5283051335749160415, 0.8490545835447742551 ) ) ;
#116589=DIRECTION ( 'NONE',  ( 0.000000000000000000, 0.2868887416116073785, -0.9579639084728132081 ) ) ;
#116627=ORIENTED_EDGE ( 'NONE', *, *, #217818, .T. ) ;
#116629=ORIENTED_EDGE ( 'NONE', *, *, #117776, .T. ) ;
#116638=CARTESIAN_POINT ( 'NONE',  ( 18.52928932188133970, 55.00560498697586098, -230.0684277855484652 ) ) ;
#116668=CARTESIAN_POINT ( 'NONE',  ( -20.94999999999999929, 47.95459712139159336, -246.5019368548292675 ) ) ;
#116671=CARTESIAN_POINT ( 'NONE',  ( -20.64999999999999858, 49.36776662947724503, -253.7196102226803021 ) ) ;
#116704=AXIS2_PLACEMENT_3D ( 'NONE', #83274, #2470, #218957 ) ;
#116722=VERTEX_POINT ( 'NONE', #24209 ) ;
#116784=VERTEX_POINT ( 'NONE', #154447 ) ;
#116789=CARTESIAN_POINT ( 'NONE',  ( -21.05000000000000071, 43.52285900727589762, -245.0935880436369985 ) ) ;
#116794=FACE_OUTER_BOUND ( 'NONE', #26320, .T. ) ;
#116816=EDGE_CURVE ( 'NONE', #785, #85465, #253494, .T. ) ;
#116864=AXIS2_PLACEMENT_3D ( 'NONE', #144287, #182175, #180890 ) ;
#116877=DIRECTION ( 'NONE',  ( -1.000000000000000000, -0.000000000000000000, 0.000000000000000000 ) ) ;
#116889=AXIS2_PLACEMENT_3D ( 'NONE', #226653, #49309, #171869 ) ;
#116916=ORIENTED_EDGE ( 'NONE', *, *, #59341, .F. ) ;
#116922=CARTESIAN_POINT ( 'NONE',  ( -23.15000000000000213, 40.44624540816119662, -247.8544895606997329 ) ) ;
#116951=ORIENTED_EDGE ( 'NONE', *, *, #187832, .T. ) ;
#116986=FACE_OUTER_BOUND ( 'NONE', #84175, .T. ) ;
#116992=CIRCLE ( 'NONE', #4540, 0.09999999999999939493 ) ;
#116995=CARTESIAN_POINT ( 'NONE',  ( -22.47886152344871391, 26.01172603257827731, -254.2798843218626530 ) ) ;
#116997=ORIENTED_EDGE ( 'NONE', *, *, #32878, .F. ) ;
#117005=CARTESIAN_POINT ( 'NONE',  ( 23.14999999999999858, 36.65892442174472876, -249.5511627012454596 ) ) ;
#117013=CARTESIAN_POINT ( 'NONE',  ( -18.33981767444349131, 77.36688828064514212, -241.8004678266106851 ) ) ;
#117044=EDGE_CURVE ( 'NONE', #94097, #149671, #226661, .T. ) ;
#117046=LINE ( 'NONE', #15390, #36679 ) ;
#117057=CIRCLE ( 'NONE', #146265, 0.09999999999999714673 ) ;
#117071=EDGE_CURVE ( 'NONE', #34161, #208409, #64181, .T. ) ;
#117072=CARTESIAN_POINT ( 'NONE',  ( -23.25000000000000000, 45.96866462019919197, -240.6139518702713360 ) ) ;
#117074=CARTESIAN_POINT ( 'NONE',  ( -21.14999999999999858, 38.04609728753136011, -236.0545303518866547 ) ) ;
#117075=DIRECTION ( 'NONE',  ( 0.000000000000000000, -0.5283051335750404975, 0.8490545835446967615 ) ) ;
#117078=AXIS2_PLACEMENT_3D ( 'NONE', #10647, #51014, #212705 ) ;
#117094=EDGE_CURVE ( 'NONE', #148712, #68027, #184981, .T. ) ;
#117155=EDGE_CURVE ( 'NONE', #47266, #2253, #118349, .T. ) ;
#117161=DIRECTION ( 'NONE',  ( 1.000000000000000000, 0.000000000000000000, 0.000000000000000000 ) ) ;
#117163=CARTESIAN_POINT ( 'NONE',  ( -18.59999999999999787, 78.48087866980282001, -232.8271061603568910 ) ) ;
#117184=CARTESIAN_POINT ( 'NONE',  ( 23.14999999999999858, 67.23127455305835554, -235.8551265064784559 ) ) ;
#117239=FACE_OUTER_BOUND ( 'NONE', #252162, .T. ) ;
#117250=EDGE_CURVE ( 'NONE', #164531, #241241, #31080, .T. ) ;
#117262=LINE ( 'NONE', #18152, #141120 ) ;
#117275=CARTESIAN_POINT ( 'NONE',  ( 21.14999999999999503, 36.65892442174472876, -249.5511627012454596 ) ) ;
#117281=CARTESIAN_POINT ( 'NONE',  ( 20.94999999999999929, 78.48087866980282001, -232.8271061603568910 ) ) ;
#117288=CIRCLE ( 'NONE', #4819, 0.2000000000000048683 ) ;
#117296=CARTESIAN_POINT ( 'NONE',  ( -21.05000000000000071, 67.23127455305835554, -235.8551265064784559 ) ) ;
#117318=CARTESIAN_POINT ( 'NONE',  ( -21.05000000000000071, 47.95459712139159336, -246.5019368548292675 ) ) ;
#117329=CARTESIAN_POINT ( 'NONE',  ( 21.14999999999999858, 34.07612324756792077, -243.5412266404783566 ) ) ;
#117336=ORIENTED_EDGE ( 'NONE', *, *, #171881, .T. ) ;
#117337=CARTESIAN_POINT ( 'NONE',  ( 23.25000000000000000, 62.12679871018153932, -248.6611778639222337 ) ) ;
#117340=EDGE_CURVE ( 'NONE', #19019, #14729, #230976, .T. ) ;
#117359=DIRECTION ( 'NONE',  ( 0.000000000000000000, 0.9126074666063777041, 0.4088369013363265525 ) ) ;
#117403=ORIENTED_EDGE ( 'NONE', *, *, #40124, .T. ) ;
#117438=ADVANCED_FACE ( 'NONE', ( #21988 ), #101921, .T. ) ;
#117449=EDGE_CURVE ( 'NONE', #233797, #139650, #68639, .T. ) ;
#117467=DIRECTION ( 'NONE',  ( 0.000000000000000000, 0.4088369013363281623, -0.9126074666063771490 ) ) ;
#117510=ORIENTED_EDGE ( 'NONE', *, *, #68582, .T. ) ;
#117516=CIRCLE ( 'NONE', #146699, 4.149999999999996803 ) ;
#117554=EDGE_CURVE ( 'NONE', #33224, #254767, #1972, .T. ) ;
#117575=ORIENTED_EDGE ( 'NONE', *, *, #208898, .T. ) ;
#117669=DIRECTION ( 'NONE',  ( 0.000000000000000000, 0.9126074666064696306, 0.4088369013361213278 ) ) ;
#117672=EDGE_LOOP ( 'NONE', ( #196338, #90517, #25278, #53818 ) ) ;
#117673=DIRECTION ( 'NONE',  ( 1.000000000000000000, 0.000000000000000000, 0.000000000000000000 ) ) ;
#117691=AXIS2_PLACEMENT_3D ( 'NONE', #36154, #58249, #234327 ) ;
#117695=FACE_OUTER_BOUND ( 'NONE', #36056, .T. ) ;
#117722=EDGE_LOOP ( 'NONE', ( #194086, #89230, #41614, #238888 ) ) ;
#117747=EDGE_CURVE ( 'NONE', #70387, #74900, #29338, .T. ) ;
#117776=EDGE_CURVE ( 'NONE', #76006, #169429, #99996, .T. ) ;
#117777=CIRCLE ( 'NONE', #84403, 0.1000000000000121764 ) ;
#117783=CIRCLE ( 'NONE', #39274, 0.09999999999999854838 ) ;
#117861=EDGE_CURVE ( 'NONE', #87416, #28439, #237596, .T. ) ;
#117897=VERTEX_POINT ( 'NONE', #25523 ) ;
#117925=CARTESIAN_POINT ( 'NONE',  ( -21.55000000000000071, 52.95562111564758823, -234.1965973584252652 ) ) ;
#117934=EDGE_CURVE ( 'NONE', #254767, #30904, #257808, .T. ) ;
#117944=ORIENTED_EDGE ( 'NONE', *, *, #162500, .T. ) ;
#117961=DIRECTION ( 'NONE',  ( 1.000000000000000000, 0.000000000000000000, 0.000000000000000000 ) ) ;
#117968=ORIENTED_EDGE ( 'NONE', *, *, #124735, .F. ) ;
#117979=ADVANCED_FACE ( 'NONE', ( #162041 ), #104580, .F. ) ;
#117988=VECTOR ( 'NONE', #95006, 1000.000000000000114 ) ;
#117994=ORIENTED_EDGE ( 'NONE', *, *, #192932, .F. ) ;
#117999=ORIENTED_EDGE ( 'NONE', *, *, #171255, .F. ) ;
#118004=ORIENTED_EDGE ( 'NONE', *, *, #218611, .T. ) ;
#118022=CARTESIAN_POINT ( 'NONE',  ( 18.59999999999999787, 65.76686835164943545, -247.8575435273897938 ) ) ;
#118032=FACE_OUTER_BOUND ( 'NONE', #161859, .T. ) ;
#118038=VERTEX_POINT ( 'NONE', #227114 ) ;
#118051=CYLINDRICAL_SURFACE ( 'NONE', #257079, 0.4999999999999944489 ) ;
#118065=EDGE_LOOP ( 'NONE', ( #170051, #122123, #87431, #47527 ) ) ;
#118088=CARTESIAN_POINT ( 'NONE',  ( 18.53317502108576775, 68.08564185115264422, -224.1612363371343122 ) ) ;
#118100=AXIS2_PLACEMENT_3D ( 'NONE', #30822, #110329, #129882 ) ;
#118125=AXIS2_PLACEMENT_3D ( 'NONE', #244208, #65592, #198681 ) ;
#118186=ORIENTED_EDGE ( 'NONE', *, *, #237494, .T. ) ;
#118198=FACE_OUTER_BOUND ( 'NONE', #55796, .T. ) ;
#118223=ORIENTED_EDGE ( 'NONE', *, *, #250161, .T. ) ;
#118225=VERTEX_POINT ( 'NONE', #195514 ) ;
#118226=DIRECTION ( 'NONE',  ( 0.000000000000000000, 0.9126074666063769270, 0.4088369013363280513 ) ) ;
#118243=DIRECTION ( 'NONE',  ( -2.952720810173289112E-16, -0.4088369013363282733, 0.9126074666063769270 ) ) ;
#118246=ORIENTED_EDGE ( 'NONE', *, *, #239912, .T. ) ;
#118261=AXIS2_PLACEMENT_3D ( 'NONE', #168807, #50084, #69676 ) ;
#118264=ADVANCED_FACE ( 'NONE', ( #114665 ), #75566, .F. ) ;
#118284=DIRECTION ( 'NONE',  ( 0.000000000000000000, 0.9955484899852913294, -0.09425075112701486457 ) ) ;
#118303=CARTESIAN_POINT ( 'NONE',  ( -18.48408745364668349, 77.28143348823819281, -241.9425700404712529 ) ) ;
#118310=ORIENTED_EDGE ( 'NONE', *, *, #60038, .F. ) ;
#118315=CIRCLE ( 'NONE', #109909, 7.799999999999999822 ) ;
#118325=DIRECTION ( 'NONE',  ( 0.000000000000000000, -0.4088369013363783999, 0.9126074666063545004 ) ) ;
#118349=CIRCLE ( 'NONE', #5884, 11.79999999999999716 ) ;
#118351=CARTESIAN_POINT ( 'NONE',  ( 21.14999999999999858, 33.98486250090727623, -243.5821103306120108 ) ) ;
#118367=AXIS2_PLACEMENT_3D ( 'NONE', #34703, #13837, #232907 ) ;
#118375=UNCERTAINTY_MEASURE_WITH_UNIT (LENGTH_MEASURE( 1.000000000000000082E-05 ), #194642, 'distance_accuracy_value', 'NONE');
#118379=DIRECTION ( 'NONE',  ( 0.000000000000000000, 0.9126074666063844765, 0.4088369013363114535 ) ) ;
#118405=FACE_OUTER_BOUND ( 'NONE', #13787, .T. ) ;
#118460=CIRCLE ( 'NONE', #180996, 11.65000000000000213 ) ;
#118461=DIRECTION ( 'NONE',  ( 0.000000000000000000, 0.9126074666063660468, 0.4088369013363524762 ) ) ;
#118484=ORIENTED_EDGE ( 'NONE', *, *, #194826, .T. ) ;
#118487=DIRECTION ( 'NONE',  ( -1.000000000000000000, -0.000000000000000000, -0.000000000000000000 ) ) ;
#118516=DIRECTION ( 'NONE',  ( 0.000000000000000000, 0.9126074666064696306, 0.4088369013361213278 ) ) ;
#118550=ORIENTED_EDGE ( 'NONE', *, *, #198043, .T. ) ;
#118552=CARTESIAN_POINT ( 'NONE',  ( -21.05000000000000071, 69.34766280046808617, -247.6726305063181144 ) ) ;
#118580=VERTEX_POINT ( 'NONE', #477 ) ;
#118587=STYLED_ITEM ( 'NONE', ( #43686 ), #103691 ) ;
#118598=DIRECTION ( 'NONE',  ( -1.000000000000000000, -0.000000000000000000, 0.000000000000000000 ) ) ;
#118616=FACE_OUTER_BOUND ( 'NONE', #253932, .T. ) ;
#118628=DIRECTION ( 'NONE',  ( 0.000000000000000000, 0.9126074666063804797, 0.4088369013363203908 ) ) ;
#118631=ORIENTED_EDGE ( 'NONE', *, *, #197223, .T. ) ;
#118633=DIRECTION ( 'NONE',  ( 0.000000000000000000, -0.9126074666063773710, -0.4088369013363274962 ) ) ;
#118664=DIRECTION ( 'NONE',  ( -7.304098846218134667E-16, 0.4088369013363281068, -0.9126074666063770380 ) ) ;
#118669=EDGE_CURVE ( 'NONE', #243814, #228447, #23941, .T. ) ;
#118718=AXIS2_PLACEMENT_3D ( 'NONE', #248725, #209596, #130035 ) ;
#118733=CARTESIAN_POINT ( 'NONE',  ( -23.25000000000000000, 54.22301550979020845, -237.0256805049050115 ) ) ;
#118738=EDGE_CURVE ( 'NONE', #152713, #220102, #137415, .T. ) ;
#118749=ORIENTED_EDGE ( 'NONE', *, *, #137670, .T. ) ;
#118767=VERTEX_POINT ( 'NONE', #5605 ) ;
#118770=CARTESIAN_POINT ( 'NONE',  ( -18.39999999999999858, 29.77885356168128794, -262.9335064780472635 ) ) ;
#118772=ORIENTED_EDGE ( 'NONE', *, *, #108014, .T. ) ;
#118782=ORIENTED_EDGE ( 'NONE', *, *, #233599, .T. ) ;
#118806=FACE_OUTER_BOUND ( 'NONE', #56521, .T. ) ;
#118839=CARTESIAN_POINT ( 'NONE',  ( -21.05000000000000071, 30.90801580390628800, -252.0203440857197279 ) ) ;
#118878=CARTESIAN_POINT ( 'NONE',  ( 23.14999999999999858, 36.65892442174472876, -249.5511627012454596 ) ) ;
#118896=DIRECTION ( 'NONE',  ( 0.000000000000000000, 0.9126074666063734853, 0.4088369013363359894 ) ) ;
#118901=CARTESIAN_POINT ( 'NONE',  ( 18.46858270002951841, 47.01368633151875542, -255.2938221613214580 ) ) ;
#118903=DIRECTION ( 'NONE',  ( -0.000000000000000000, -0.4088369013363281068, 0.9126074666063770380 ) ) ;
#118916=CARTESIAN_POINT ( 'NONE',  ( -23.15000000000000213, 69.09936979046463534, -247.6075824278584889 ) ) ;
#118935=DIRECTION ( 'NONE',  ( 1.000000000000000000, -1.207181226542539700E-16, 2.694675058168174199E-16 ) ) ;
#118947=CIRCLE ( 'NONE', #152276, 0.09999999999999326095 ) ;
#118948=CARTESIAN_POINT ( 'NONE',  ( 18.49999999999999289, 55.01933066900991776, -229.9591340285290073 ) ) ;
#118967=ORIENTED_EDGE ( 'NONE', *, *, #254731, .T. ) ;
#118987=CIRCLE ( 'NONE', #98090, 0.1000000000000121764 ) ;
#118998=DIRECTION ( 'NONE',  ( 1.000000000000000000, 0.000000000000000000, 0.000000000000000000 ) ) ;
#119000=DIRECTION ( 'NONE',  ( 1.000000000000000000, 0.000000000000000000, 0.000000000000000000 ) ) ;
#119001=CARTESIAN_POINT ( 'NONE',  ( -20.54999999999999716, 36.65892442174472876, -249.5511627012454596 ) ) ;
#119071=DIRECTION ( 'NONE',  ( -0.7071067811865685560, -0.2890913453344204909, 0.6453109281987288171 ) ) ;
#119079=ADVANCED_FACE ( 'NONE', ( #183973 ), #203541, .T. ) ;
#119120=VERTEX_POINT ( 'NONE', #82272 ) ;
#119148=LINE ( 'NONE', #124288, #186821 ) ;
#119151=DIRECTION ( 'NONE',  ( -1.000000000000000000, -0.000000000000000000, -0.000000000000000000 ) ) ;
#119156=CYLINDRICAL_SURFACE ( 'NONE', #214373, 0.09999999999999950595 ) ;
#119157=FACE_OUTER_BOUND ( 'NONE', #110176, .T. ) ;
#119159=ORIENTED_EDGE ( 'NONE', *, *, #224465, .T. ) ;
#119169=EDGE_CURVE ( 'NONE', #227500, #185809, #209972, .T. ) ;
#119181=CARTESIAN_POINT ( 'NONE',  ( 21.05000000000000071, 65.49732036650624423, -236.6319166190174883 ) ) ;
#119185=CARTESIAN_POINT ( 'NONE',  ( 18.49999999999999645, 46.62132166459547733, -243.0426574061995950 ) ) ;
#119198=CARTESIAN_POINT ( 'NONE',  ( -21.52071067811865746, 44.74916609337672924, -237.4025894497016225 ) ) ;
#119211=EDGE_LOOP ( 'NONE', ( #28628, #86380, #245575 ) ) ;
#119221=VERTEX_POINT ( 'NONE', #91303 ) ;
#119233=DIRECTION ( 'NONE',  ( -1.000000000000000000, -0.000000000000000000, 0.000000000000000000 ) ) ;
#119256=ORIENTED_EDGE ( 'NONE', *, *, #111161, .T. ) ;
#119270=DIRECTION ( 'NONE',  ( 0.000000000000000000, 0.9126074666063622720, 0.4088369013363611360 ) ) ;
#119271=CARTESIAN_POINT ( 'NONE',  ( 21.00000000000000000, 51.97441255244040548, -232.0063394385699667 ) ) ;
#119282=DIRECTION ( 'NONE',  ( -0.000000000000000000, -0.9126074666063770380, -0.4088369013363281068 ) ) ;
#119319=VECTOR ( 'NONE', #147498, 1000.000000000000000 ) ;
#119374=CYLINDRICAL_SURFACE ( 'NONE', #202211, 2.000000000000012879 ) ;
#119406=CARTESIAN_POINT ( 'NONE',  ( 22.42196299218230493, 26.02640355241475589, -254.3117255616162424 ) ) ;
#119407=VECTOR ( 'NONE', #77457, 1000.000000000000114 ) ;
#119408=ADVANCED_FACE ( 'NONE', ( #80695 ), #121166, .T. ) ;
#119433=VERTEX_POINT ( 'NONE', #198096 ) ;
#119445=CIRCLE ( 'NONE', #252695, 0.1000000000000074579 ) ;
#119478=DIRECTION ( 'NONE',  ( 0.000000000000000000, 0.9126074666063769270, 0.4088369013363282733 ) ) ;
#119494=AXIS2_PLACEMENT_3D ( 'NONE', #216091, #136547, #115724 ) ;
#119498=CARTESIAN_POINT ( 'NONE',  ( -18.50000000000000000, 77.38471025844603446, -241.6066692018393098 ) ) ;
#119512=CARTESIAN_POINT ( 'NONE',  ( -20.85000000000000142, 69.38854649060172619, -247.7638912529787660 ) ) ;
#119518=COLOUR_RGB ( '', 0.08235294, 0.09019608, 0.10196078) ;
#119521=CIRCLE ( 'NONE', #190845, 0.09999999999999240052 ) ;
#119527=DIRECTION ( 'NONE',  ( -0.000000000000000000, 0.4088369013363281623, -0.9126074666063771490 ) ) ;
#119565=VERTEX_POINT ( 'NONE', #169283 ) ;
#119581=DIRECTION ( 'NONE',  ( -1.000000000000000000, 0.000000000000000000, 0.000000000000000000 ) ) ;
#119600=CARTESIAN_POINT ( 'NONE',  ( -18.52309608778534056, 77.30126544915781039, -241.9097476308881483 ) ) ;
#119614=AXIS2_PLACEMENT_3D ( 'NONE', #103867, #46468, #221254 ) ;
#119616=DIRECTION ( 'NONE',  ( 1.000000000000000000, -1.207181226542539700E-16, 2.694675058168174199E-16 ) ) ;
#119643=EDGE_CURVE ( 'NONE', #14385, #20995, #50547, .T. ) ;
#119648=ORIENTED_EDGE ( 'NONE', *, *, #81712, .F. ) ;
#119651=TOROIDAL_SURFACE ( 'NONE', #231906, 0.2000000000000000111, 0.1000000000000000056 ) ;
#119654=ORIENTED_EDGE ( 'NONE', *, *, #201915, .F. ) ;
#119685=EDGE_CURVE ( 'NONE', #114887, #18598, #229572, .T. ) ;
#119697=PRODUCT_DEFINITION_FORMATION_WITH_SPECIFIED_SOURCE ( 'ANY', '', #30667, .NOT_KNOWN. ) ;
#119720=DIRECTION ( 'NONE',  ( 1.000000000000000000, -0.000000000000000000, 0.000000000000000000 ) ) ;
#119795=ORIENTED_EDGE ( 'NONE', *, *, #211278, .F. ) ;
#119799=VECTOR ( 'NONE', #35934, 1000.000000000000000 ) ;
#119865=ORIENTED_EDGE ( 'NONE', *, *, #182744, .T. ) ;
#119899=EDGE_CURVE ( 'NONE', #215487, #90768, #80374, .T. ) ;
#119904=EDGE_CURVE ( 'NONE', #171099, #74869, #137958, .T. ) ;
#119952=LINE ( 'NONE', #199476, #31947 ) ;
#120002=CARTESIAN_POINT ( 'NONE',  ( 20.94999999999999929, 45.16048418391989117, -238.5653317536036582 ) ) ;
#120005=ORIENTED_EDGE ( 'NONE', *, *, #28390, .F. ) ;
#120020=CIRCLE ( 'NONE', #174194, 0.09999999999999681366 ) ;
#120046=VERTEX_POINT ( 'NONE', #133651 ) ;
#120090=CYLINDRICAL_SURFACE ( 'NONE', #104061, 0.09999999999999609201 ) ;
#120098=DIRECTION ( 'NONE',  ( 0.000000000000000000, -0.9126074666063660468, -0.4088369013363524762 ) ) ;
#120130=AXIS2_PLACEMENT_3D ( 'NONE', #116668, #141364, #18848 ) ;
#120133=CLOSED_SHELL ( 'NONE', ( #192124, #214677, #24678, #60923, #250528, #120275, #75359, #145926, #10296, #217970, #137890, #233437, #94708, #23212, #63912, #208947, #242782, #187570, #16119, #225237, #146263, #251595, #103189, #16277, #20754, #4516, #107907, #152826, #129796, #52915, #167817, #86253, #165663, #19818, #9454, #101507, #160571, #185699, #242946, #171942, #41874, #120397, #23584, #76193, #110253, #173743, #159294, #41512, #2944, #190451, #251624, #222701, #115176, #35948, #233720, #122629, #37795, #22854, #228360, #246002, #151160, #33850, #129422, #74292, #232787, #213334, #256885, #108666, #26704, #30179, #67948, #186849, #143225, #256756, #190129, #22538, #142632, #126210, #33490, #53165, #150572, #86250, #165958, #150282, #53156, #30321, #29919, #124442, #197624, #205308, #75646, #133957, #161144, #202147, #110598, #114329, #109744, #106702, #145141, #175658, #177688, #139687, #198769, #72215, #248117, #94448, #65388, #143566, #187419, #15907, #105875, #5684, #252319, #119079, #195033, #141484, #156234, #60748, #136538, #25726, #168429, #38382, #219936, #128931, #2652, #73685, #40117, #154808, #89716, #197704, #172256, #194766, #15249, #42991, #214083, #110539, #159872, #197638, #144538, #74053, #95357, #125087, #97563, #2845, #16225, #175759, #143824, #241775, #82384, #78230, #42505, #20200, #187848, #180326, #191586, #98995, #231843, #238711, #147208, #188151, #124986, #95856, #137317, #230603, #2518, #136209, #29707, #113010, #36335, #184528, #102773, #92053, #233190, #93781, #139484, #96001, #60344, #228301, #153484, #212394, #252217, #45483, #70760, #76322, #65239, #138764, #203996, #67805, #114995, #14368, #120654, #106415, #180499, #246811, #43478, #247178, #91487, #219899, #170420, #172466, #52608, #92000, #24149, #131500, #239278, #21974, #116034, #81546, #135535, #156711, #18679, #210529, #114803, #136446, #60732, #80601, #252705, #21490, #172825, #2511, #160433, #110018, #39505, #180452, #219128, #88874, #25981, #26110, #233180, #140791, #31725, #144359, #8129, #231043, #248965, #27785, #229737, #58669, #82515, #218406, #50214, #255045, #198971, #139116, #89631, #86127, #74488, #56578, #31113, #174763, #65781, #231768, #112862, #165433, #90698, #136974, #91821, #5089, #225760, #210724, #55946, #257746, #195462, #178655, #51473, #76757, #77619, #202726, #256889, #228689, #236914, #220273, #220460, #201716, #174767, #154473, #44437, #118264, #112920, #216051, #75660, #39984, #63416, #13715, #235386, #154223, #111291, #18850, #42138, #156811, #200204, #229207, #36216, #4502, #217795, #54198, #63218, #102730, #55512, #49297, #61046, #202447, #78220, #50178, #86384, #59316, #130670, #87391, #68224, #117438, #134943, #14903, #178989, #141757, #40291, #9945, #220268, #202956, #127476, #36830, #140290, #157896, #125355, #123097, #113678, #24716, #133828, #46026, #89594, #248491, #198691, #181733, #235156, #104264, #102004, #202046, #58324, #226838, #81745, #115344, #129991, #135894, #108904, #223030, #62900, #39254, #3603, #26130, #193146, #83429, #62094, #221174, #64543, #89693, #110432, #32594, #212988, #197657, #103800, #76256, #190737, #237976, #181346, #59902, #156174, #213322, #232025, #150899, #186342, #216300, #92926, #107847, #245542, #151857, #199902, #95992, #59816, #150083, #62621, #210218, #205839, #204897, #25954, #205264, #132463, #257791, #744, #22575, #136906, #125093, #15285, #115042, #153212, #232139, #239581, #233749, #126948, #151991, #257973, #247967, #89058, #127701, #153686, #163241, #79062, #145949, #41589, #255756, #28796, #7025, #172238, #149799, #46662, #23712, #151257, #119408, #128062, #227441, #75982, #40758, #127480, #245742, #126915, #191768, #55394, #154861, #106234, #74597, #217941, #231856, #14911, #236434, #250155, #170249, #49044, #156243, #231695, #192863, #112011, #96306, #216350, #88457, #35109, #77653, #18684, #117979, #23759, #217439, #145572, #91714, #173575, #41103, #84304, #75852, #165584, #75921, #194016, #237798, #158233, #122919, #174375, #110315, #96509, #183622, #175681, #173715, #103585, #91952, #195439, #223642, #115948, #69126, #102130, #6922, #201079, #129179, #71207, #127314 ) ) ;
#120152=ORIENTED_EDGE ( 'NONE', *, *, #175028, .F. ) ;
#120163=CARTESIAN_POINT ( 'NONE',  ( 22.50000000000000000, 36.65892442174472876, -249.5511627012454596 ) ) ;
#120204=EDGE_LOOP ( 'NONE', ( #90531, #234277, #117994, #7819 ) ) ;
#120221=VECTOR ( 'NONE', #9531, 1000.000000000000114 ) ;
#120275=ADVANCED_FACE ( 'NONE', ( #229570 ), #42307, .T. ) ;
#120283=ORIENTED_EDGE ( 'NONE', *, *, #166119, .T. ) ;
#120293=AXIS2_PLACEMENT_3D ( 'NONE', #181731, #244251, #46060 ) ;
#120306=VECTOR ( 'NONE', #14313, 1000.000000000000000 ) ;
#120356=CARTESIAN_POINT ( 'NONE',  ( 18.59999999999999076, 51.96945017402672562, -231.5060697639786440 ) ) ;
#120357=ORIENTED_EDGE ( 'NONE', *, *, #205372, .F. ) ;
#120397=ADVANCED_FACE ( 'NONE', ( #233435 ), #121623, .F. ) ;
#120401=ORIENTED_EDGE ( 'NONE', *, *, #171954, .T. ) ;
#120409=VERTEX_POINT ( 'NONE', #15680 ) ;
#120435=VERTEX_POINT ( 'NONE', #117318 ) ;
#120454=CARTESIAN_POINT ( 'NONE',  ( 21.05000000000000071, 64.58471289989986985, -237.0407535203538316 ) ) ;
#120464=DIRECTION ( 'NONE',  ( -1.000000000000000000, 0.000000000000000000, 0.000000000000000000 ) ) ;
#120469=ORIENTED_EDGE ( 'NONE', *, *, #248664, .T. ) ;
#120502=TOROIDAL_SURFACE ( 'NONE', #149535, 11.65000000000000036, 0.1000000000000000056 ) ;
#120522=EDGE_LOOP ( 'NONE', ( #250331, #81027, #141673, #90328 ) ) ;
#120556=CIRCLE ( 'NONE', #191300, 2.000000000000003109 ) ;
#120622=AXIS2_PLACEMENT_3D ( 'NONE', #32764, #247911, #112279 ) ;
#120645=AXIS2_PLACEMENT_3D ( 'NONE', #86759, #62092, #161195 ) ;
#120654=ADVANCED_FACE ( 'NONE', ( #209693 ), #111889, .T. ) ;
#120663=EDGE_LOOP ( 'NONE', ( #39073, #73299, #167531, #109686 ) ) ;
#120670=CARTESIAN_POINT ( 'NONE',  ( 23.25000000000000000, 69.16514130714681130, -247.7543978865853660 ) ) ;
#120675=ORIENTED_EDGE ( 'NONE', *, *, #156473, .F. ) ;
#120682=CARTESIAN_POINT ( 'NONE',  ( 18.50016250449482413, 68.01715840423111104, -224.2192812407674580 ) ) ;
#120690=CARTESIAN_POINT ( 'NONE',  ( -20.94999999999999929, 67.23127455305835554, -235.8551265064784559 ) ) ;
#120692=CARTESIAN_POINT ( 'NONE',  ( -18.59999999999999787, 62.42744096235649920, -225.1319887738535499 ) ) ;
#120693=ORIENTED_EDGE ( 'NONE', *, *, #183670, .F. ) ;
#120696=CARTESIAN_POINT ( 'NONE',  ( -21.14999999999999858, 44.06843597547145208, -258.9974126733344519 ) ) ;
#120699=CARTESIAN_POINT ( 'NONE',  ( 21.05000000000000071, 67.23127455305835554, -235.8551265064784559 ) ) ;
#120717=B_SPLINE_CURVE_WITH_KNOTS ( 'NONE', 3,
 ( #101806, #219207, #4018, #5275, #84806, #121438 ),
 .UNSPECIFIED., .F., .F.,
 ( 4, 2, 4 ),
 ( 0.000000000000000000, 0.0001895189928937367218, 0.0003790379857874734437 ),
 .UNSPECIFIED. ) ;
#120777=DIRECTION ( 'NONE',  ( 0.000000000000000000, 0.9126074666063804797, 0.4088369013363203908 ) ) ;
#120786=VERTEX_POINT ( 'NONE', #36209 ) ;
#120788=CARTESIAN_POINT ( 'NONE',  ( 20.22894356738407851, 40.41144770130940600, -237.7030586605688711 ) ) ;
#120816=DIRECTION ( 'NONE',  ( -1.000000000000000000, -0.000000000000000000, 0.000000000000000000 ) ) ;
#120823=EDGE_CURVE ( 'NONE', #229414, #10431, #77864, .T. ) ;
#120876=CIRCLE ( 'NONE', #8420, 0.1000000000000065836 ) ;
#120910=AXIS2_PLACEMENT_3D ( 'NONE', #161175, #217266, #179469 ) ;
#120933=AXIS2_PLACEMENT_3D ( 'NONE', #49947, #68239, #166088 ) ;
#120934=DIRECTION ( 'NONE',  ( 0.000000000000000000, 0.9126074666063768159, 0.4088369013363282178 ) ) ;
#120958=CARTESIAN_POINT ( 'NONE',  ( 21.09316766718127667, 34.01873860631857838, -243.7537655525922276 ) ) ;
#120966=EDGE_LOOP ( 'NONE', ( #126907, #171387, #22554, #30512, #253849, #78310, #224801, #88251, #114933, #221790, #124150 ) ) ;
#120979=CIRCLE ( 'NONE', #241747, 0.1000000000000065836 ) ;
#120988=EDGE_CURVE ( 'NONE', #201532, #97383, #92722, .T. ) ;
#120991=EDGE_LOOP ( 'NONE', ( #244369, #31906, #126199, #239064 ) ) ;
#121001=DIRECTION ( 'NONE',  ( 0.000000000000000000, 0.9126074666063771490, 0.4088369013363281623 ) ) ;
#121015=CARTESIAN_POINT ( 'NONE',  ( 18.50000000000000355, 47.11985028124983899, -255.1884644111641194 ) ) ;
#121020=CIRCLE ( 'NONE', #41908, 0.09999999999999108213 ) ;
#121022=AXIS2_PLACEMENT_3D ( 'NONE', #175700, #255154, #34927 ) ;
#121045=EDGE_LOOP ( 'NONE', ( #44382, #221073 ) ) ;
#121085=EDGE_LOOP ( 'NONE', ( #229738, #46362, #130226, #244735 ) ) ;
#121110=DIRECTION ( 'NONE',  ( 0.000000000000000000, 0.9126074666063545004, 0.4088369013363783999 ) ) ;
#121149=CARTESIAN_POINT ( 'NONE',  ( 18.49999999999999289, 54.98105481382776816, -230.1569079895687366 ) ) ;
#121158=CARTESIAN_POINT ( 'NONE',  ( 18.54271179734040942, 77.31781020912761448, -241.8821825064762834 ) ) ;
#121166=CYLINDRICAL_SURFACE ( 'NONE', #166876, 0.09999999999999939493 ) ;
#121176=VERTEX_POINT ( 'NONE', #35901 ) ;
#121194=ORIENTED_EDGE ( 'NONE', *, *, #14122, .T. ) ;
#121238=DIRECTION ( 'NONE',  ( -1.000000000000000000, 0.000000000000000000, 0.000000000000000000 ) ) ;
#121301=CARTESIAN_POINT ( 'NONE',  ( -22.14074124539699895, 29.87418771707450205, -252.4821028181641225 ) ) ;
#121304=CARTESIAN_POINT ( 'NONE',  ( 23.15000000000000213, 49.61306877027904250, -254.2671747026441551 ) ) ;
#121341=ORIENTED_EDGE ( 'NONE', *, *, #31314, .T. ) ;
#121350=DIRECTION ( 'NONE',  ( 0.000000000000000000, -0.9126074666063771490, -0.4088369013363281623 ) ) ;
#121374=EDGE_CURVE ( 'NONE', #201532, #18598, #86530, .T. ) ;
#121385=EDGE_CURVE ( 'NONE', #68445, #71022, #227350, .T. ) ;
#121403=SPHERICAL_SURFACE ( 'NONE', #229807, 0.1000000000000000056 ) ;
#121426=ORIENTED_EDGE ( 'NONE', *, *, #33763, .T. ) ;
#121433=ORIENTED_EDGE ( 'NONE', *, *, #170319, .T. ) ;
#121438=CARTESIAN_POINT ( 'NONE',  ( 21.05000000000000071, 34.01125473725045367, -243.8802146427659352 ) ) ;
#121505=CARTESIAN_POINT ( 'NONE',  ( 23.24999999999999289, 53.42432843990430058, -234.7536552047824330 ) ) ;
#121518=ORIENTED_EDGE ( 'NONE', *, *, #224602, .F. ) ;
#121548=DIRECTION ( 'NONE',  ( 0.000000000000000000, -0.9126074666063913599, -0.4088369013362965210 ) ) ;
#121579=DIRECTION ( 'NONE',  ( 0.000000000000000000, -0.4088369013362398441, 0.9126074666064164509 ) ) ;
#121581=ORIENTED_EDGE ( 'NONE', *, *, #61789, .F. ) ;
#121587=EDGE_CURVE ( 'NONE', #251907, #177565, #133152, .T. ) ;
#121595=CARTESIAN_POINT ( 'NONE',  ( -22.59999999999999787, 31.80488924422933295, -238.9605610896540213 ) ) ;
#121623=CONICAL_SURFACE ( 'NONE', #9173, 4.050000000000006040, 0.7853981633974604915 ) ;
#121624=DIRECTION ( 'NONE',  ( 1.000000000000000000, 0.000000000000000000, 0.000000000000000000 ) ) ;
#121646=B_SPLINE_CURVE_WITH_KNOTS ( 'NONE', 3,
 ( #28882, #103208, #62821, #86206 ),
 .UNSPECIFIED., .F., .F.,
 ( 4, 4 ),
 ( 0.000000000000000000, 0.0001048066582182356256 ),
 .UNSPECIFIED. ) ;
#121659=EDGE_CURVE ( 'NONE', #99817, #138284, #34678, .T. ) ;
#121660=ORIENTED_EDGE ( 'NONE', *, *, #44668, .F. ) ;
#121679=CARTESIAN_POINT ( 'NONE',  ( -20.95000000000002416, 56.23643450586806125, -227.9054833905874773 ) ) ;
#121695=CARTESIAN_POINT ( 'NONE',  ( 20.94999999999999929, 69.56804783242856161, -248.4091712263733882 ) ) ;
#121697=CYLINDRICAL_SURFACE ( 'NONE', #24053, 0.09999999999999939493 ) ;
#121725=LINE ( 'NONE', #216936, #126106 ) ;
#121826=AXIS2_PLACEMENT_3D ( 'NONE', #202635, #117961, #123114 ) ;
#121882=DIRECTION ( 'NONE',  ( 0.000000000000000000, 0.5859227990963362664, 0.8103668758649469339 ) ) ;
#121883=EDGE_LOOP ( 'NONE', ( #196462, #197904, #77150, #247257, #44150, #2149, #72203, #27835 ) ) ;
#121907=AXIS2_PLACEMENT_3D ( 'NONE', #67202, #47615, #249696 ) ;
#121939=VERTEX_POINT ( 'NONE', #48772 ) ;
#121960=CARTESIAN_POINT ( 'NONE',  ( -23.15000000000000213, 48.31748480764120046, -244.3282712866738962 ) ) ;
#121969=CARTESIAN_POINT ( 'NONE',  ( 22.49806830649813350, 25.99547786654754589, -254.2433729751658120 ) ) ;
#121980=SPHERICAL_SURFACE ( 'NONE', #101155, 0.1000000000000000056 ) ;
#121986=CARTESIAN_POINT ( 'NONE',  ( 18.50000000000000000, 65.76686835164943545, -247.8575435273897938 ) ) ;
#121988=CIRCLE ( 'NONE', #101080, 12.97499999999999787 ) ;
#121995=CIRCLE ( 'NONE', #5449, 0.1000000000000024342 ) ;
#122007=EDGE_CURVE ( 'NONE', #192936, #181336, #113939, .T. ) ;
#122010=DIRECTION ( 'NONE',  ( 1.000000000000000000, -1.207181226542539700E-16, 2.694675058168174199E-16 ) ) ;
#122021=CARTESIAN_POINT ( 'NONE',  ( -18.39999999999999858, 47.00127771169579916, -255.4372249185379928 ) ) ;
#122047=CARTESIAN_POINT ( 'NONE',  ( 20.97250901189795513, 39.30993059825905078, -236.7215534631462788 ) ) ;
#122076=LINE ( 'NONE', #182050, #5442 ) ;
#122082=EDGE_CURVE ( 'NONE', #25855, #4376, #198552, .T. ) ;
#122094=ORIENTED_EDGE ( 'NONE', *, *, #160028, .T. ) ;
#122123=ORIENTED_EDGE ( 'NONE', *, *, #3552, .T. ) ;
#122126=CARTESIAN_POINT ( 'NONE',  ( 20.94999999999999574, 36.65892442174472876, -249.5511627012454596 ) ) ;
#122130=DIRECTION ( 'NONE',  ( 0.000000000000000000, -0.4088369013363281623, 0.9126074666063771490 ) ) ;
#122133=CARTESIAN_POINT ( 'NONE',  ( -22.39999999999999858, 26.02743912001966464, -254.3139371321002216 ) ) ;
#122135=CIRCLE ( 'NONE', #126402, 0.1000000000000078465 ) ;
#122137=EDGE_CURVE ( 'NONE', #3155, #226069, #155853, .T. ) ;
#122161=FACE_OUTER_BOUND ( 'NONE', #150876, .T. ) ;
#122169=CARTESIAN_POINT ( 'NONE',  ( -20.64999999999999858, 48.50000630096246823, -244.2465039064066161 ) ) ;
#122194=EDGE_CURVE ( 'NONE', #215594, #80413, #35067, .T. ) ;
#122197=LINE ( 'NONE', #201717, #231270 ) ;
#122198=CARTESIAN_POINT ( 'NONE',  ( 20.99780126800934354, 56.17802974602408739, -228.0901074916681353 ) ) ;
#122235=ORIENTED_EDGE ( 'NONE', *, *, #41985, .F. ) ;
#122248=ORIENTED_EDGE ( 'NONE', *, *, #197000, .F. ) ;
#122265=CARTESIAN_POINT ( 'NONE',  ( -22.00356870067735215, 30.03864867784057680, -252.5169646700133796 ) ) ;
#122270=EDGE_CURVE ( 'NONE', #217247, #170976, #22566, .T. ) ;
#122280=ORIENTED_EDGE ( 'NONE', *, *, #168521, .F. ) ;
#122309=VECTOR ( 'NONE', #107495, 1000.000000000000114 ) ;
#122311=CIRCLE ( 'NONE', #26659, 0.09999999999999609201 ) ;
#122347=EDGE_CURVE ( 'NONE', #73589, #101099, #97528, .T. ) ;
#122352=DIRECTION ( 'NONE',  ( 1.000000000000000000, 0.000000000000000000, 0.000000000000000000 ) ) ;
#122354=ORIENTED_EDGE ( 'NONE', *, *, #180666, .F. ) ;
#122363=DIRECTION ( 'NONE',  ( -3.265361837132812600E-16, -0.4088369013363267745, 0.9126074666063774821 ) ) ;
#122368=DIRECTION ( 'NONE',  ( 0.000000000000000000, 0.9061079809440786281, 0.4230464831072883181 ) ) ;
#122392=CARTESIAN_POINT ( 'NONE',  ( -20.94999675878240808, 68.00468331834514402, -224.2298952291173464 ) ) ;
#122472=DIRECTION ( 'NONE',  ( 0.000000000000000000, 0.4088369013363281068, -0.9126074666063770380 ) ) ;
#122487=ORIENTED_EDGE ( 'NONE', *, *, #249071, .T. ) ;
#122513=DIRECTION ( 'NONE',  ( -1.000000000000000000, 7.510212038922846022E-17, -1.676432719286211941E-16 ) ) ;
#122524=FACE_OUTER_BOUND ( 'NONE', #94091, .T. ) ;
#122527=AXIS2_PLACEMENT_3D ( 'NONE', #52298, #130564, #227095 ) ;
#122547=CARTESIAN_POINT ( 'NONE',  ( 21.05000000000000071, 62.04503132991427350, -248.4786563706009588 ) ) ;
#122558=DIRECTION ( 'NONE',  ( 0.000000000000000000, 0.9126074666063769270, 0.4088369013363282733 ) ) ;
#122590=DIRECTION ( 'NONE',  ( 1.000000000000000000, 0.000000000000000000, 0.000000000000000000 ) ) ;
#122600=ORIENTED_EDGE ( 'NONE', *, *, #136896, .F. ) ;
#122603=AXIS2_PLACEMENT_3D ( 'NONE', #61320, #224231, #5159 ) ;
#122612=EDGE_CURVE ( 'NONE', #185818, #132466, #30564, .T. ) ;
#122629=ADVANCED_FACE ( 'NONE', ( #87268 ), #51990, .F. ) ;
#122642=ORIENTED_EDGE ( 'NONE', *, *, #131358, .T. ) ;
#122643=CIRCLE ( 'NONE', #18577, 0.09999999999999939493 ) ;
#122691=CARTESIAN_POINT ( 'NONE',  ( 21.05000000000000071, 53.86595165227826243, -236.3638196928718855 ) ) ;
#122726=AXIS2_PLACEMENT_3D ( 'NONE', #243827, #166903, #229415 ) ;
#122752=CARTESIAN_POINT ( 'NONE',  ( 20.94999999999999929, 36.65892442174472876, -249.5511627012454596 ) ) ;
#122758=CARTESIAN_POINT ( 'NONE',  ( 18.39999999999999858, 46.96039402156216624, -255.3459641718773128 ) ) ;
#122765=CARTESIAN_POINT ( 'NONE',  ( 21.05000000000000071, 62.08148826970417389, -247.6553521922769221 ) ) ;
#122791=DIRECTION ( 'NONE',  ( 0.000000000000000000, 0.9126074666063771490, 0.4088369013363281623 ) ) ;
#122811=DIRECTION ( 'NONE',  ( -3.265361837132813093E-16, -0.4088369013363053472, 0.9126074666063872520 ) ) ;
#122844=DIRECTION ( 'NONE',  ( 0.000000000000000000, 0.9126074666063770380, 0.4088369013363281068 ) ) ;
#122859=LINE ( 'NONE', #160724, #160709 ) ;
#122862=ORIENTED_EDGE ( 'NONE', *, *, #14937, .F. ) ;
#122911=CARTESIAN_POINT ( 'NONE',  ( 20.85000000000000142, 78.48087866980282001, -232.8271061603568910 ) ) ;
#122919=ADVANCED_FACE ( 'NONE', ( #59684 ), #79248, .T. ) ;
#122954=EDGE_CURVE ( 'NONE', #9026, #136054, #164909, .T. ) ;
#122993=EDGE_CURVE ( 'NONE', #49603, #118225, #85339, .T. ) ;
#123002=DIRECTION ( 'NONE',  ( -1.000000000000000000, 0.000000000000000000, 0.000000000000000000 ) ) ;
#123008=CARTESIAN_POINT ( 'NONE',  ( 21.09096482362050651, 34.02127186812258941, -243.7598725113532794 ) ) ;
#123028=CIRCLE ( 'NONE', #160473, 0.1000000000000056677 ) ;
#123045=DIRECTION ( 'NONE',  ( 0.000000000000000000, 0.4088369013363283289, -0.9126074666063768159 ) ) ;
#123047=FACE_OUTER_BOUND ( 'NONE', #7499, .T. ) ;
#123050=CYLINDRICAL_SURFACE ( 'NONE', #152024, 0.09999999999999609201 ) ;
#123064=ORIENTED_EDGE ( 'NONE', *, *, #207278, .F. ) ;
#123097=ADVANCED_FACE ( 'NONE', ( #130915 ), #22382, .T. ) ;
#123103=CARTESIAN_POINT ( 'NONE',  ( -18.39999999999999858, 46.93047535494665823, -255.3593673659106855 ) ) ;
#123105=CIRCLE ( 'NONE', #156459, 0.09999999999999609201 ) ;
#123110=DIRECTION ( 'NONE',  ( 0.000000000000000000, 0.9126074666063660468, 0.4088369013363524762 ) ) ;
#123112=FACE_OUTER_BOUND ( 'NONE', #9774, .T. ) ;
#123114=DIRECTION ( 'NONE',  ( 0.000000000000000000, 0.9126074666063641594, 0.4088369013363568061 ) ) ;
#123127=DIRECTION ( 'NONE',  ( -0.000000000000000000, -0.9126074666063770380, -0.4088369013363282178 ) ) ;
#123138=EDGE_LOOP ( 'NONE', ( #146669, #160710, #232513, #4394 ) ) ;
#123141=CARTESIAN_POINT ( 'NONE',  ( -21.12230431290519306, 34.01407833148830662, -243.6600691369628180 ) ) ;
#123168=CARTESIAN_POINT ( 'NONE',  ( 20.94999999999999929, 36.65892442174472876, -249.5511627012454596 ) ) ;
#123209=VECTOR ( 'NONE', #251903, 1000.000000000000114 ) ;
#123230=ORIENTED_EDGE ( 'NONE', *, *, #105279, .F. ) ;
#123248=CARTESIAN_POINT ( 'NONE',  ( -20.94999999999999929, 44.55458850188623643, -247.3966190010231969 ) ) ;
#123266=VERTEX_POINT ( 'NONE', #242852 ) ;
#123268=AXIS2_PLACEMENT_3D ( 'NONE', #156348, #158906, #221394 ) ;
#123324=ORIENTED_EDGE ( 'NONE', *, *, #227497, .F. ) ;
#123326=CARTESIAN_POINT ( 'NONE',  ( 18.49999999999999645, 43.57568952063339651, -245.1784935019914826 ) ) ;
#123362=CARTESIAN_POINT ( 'NONE',  ( -20.64999999999999858, 65.49732036650624423, -236.6319166190174883 ) ) ;
#123380=CARTESIAN_POINT ( 'NONE',  ( 20.94999999999999574, 44.09392520544991356, -258.8097135244738638 ) ) ;
#123400=CARTESIAN_POINT ( 'NONE',  ( -23.15000000000000213, 42.98415524044398950, -233.9519173640447889 ) ) ;
#123408=LINE ( 'NONE', #141675, #25501 ) ;
#123424=DIRECTION ( 'NONE',  ( 0.000000000000000000, -0.4088369013363281068, 0.9126074666063770380 ) ) ;
#123473=EDGE_CURVE ( 'NONE', #40222, #97414, #85036, .T. ) ;
#123475=DIRECTION ( 'NONE',  ( 0.000000000000000000, -0.9126074666063770380, -0.4088369013363281068 ) ) ;
#123486=CIRCLE ( 'NONE', #210983, 0.09999999999999939493 ) ;
#123496=FACE_OUTER_BOUND ( 'NONE', #216116, .T. ) ;
#123502=LINE ( 'NONE', #220033, #75403 ) ;
#123537=EDGE_CURVE ( 'NONE', #21929, #80413, #251478, .T. ) ;
#123541=ORIENTED_EDGE ( 'NONE', *, *, #169557, .T. ) ;
#123551=CIRCLE ( 'NONE', #111079, 0.09999999999999609201 ) ;
#123558=ORIENTED_EDGE ( 'NONE', *, *, #9721, .T. ) ;
#123585=AXIS2_PLACEMENT_3D ( 'NONE', #236291, #118935, #116366 ) ;
#123600=DIRECTION ( 'NONE',  ( -6.938893903907225222E-15, -0.4088369013363281068, 0.9126074666063770380 ) ) ;
#123645=VERTEX_POINT ( 'NONE', #204694 ) ;
#123718=CARTESIAN_POINT ( 'NONE',  ( -20.64999999999999858, 52.99650480578122824, -234.2878581050858884 ) ) ;
#123729=AXIS2_PLACEMENT_3D ( 'NONE', #43231, #21123, #237582 ) ;
#123733=CIRCLE ( 'NONE', #227756, 7.799999999999992717 ) ;
#123758=DIRECTION ( 'NONE',  ( 0.000000000000000000, 0.9126074666063660468, 0.4088369013363524762 ) ) ;
#123759=EDGE_CURVE ( 'NONE', #228170, #142241, #131588, .T. ) ;
#123771=ORIENTED_EDGE ( 'NONE', *, *, #17357, .T. ) ;
#123782=CARTESIAN_POINT ( 'NONE',  ( -22.39999999999999858, 31.85509083104287598, -238.8280249686205536 ) ) ;
#123785=AXIS2_PLACEMENT_3D ( 'NONE', #134085, #213634, #75441 ) ;
#123789=CARTESIAN_POINT ( 'NONE',  ( -20.94999999999999929, 67.85909929089923764, -227.8797997985275856 ) ) ;
#123795=AXIS2_PLACEMENT_3D ( 'NONE', #178502, #199334, #256671 ) ;
#123800=CARTESIAN_POINT ( 'NONE',  ( -21.44999999999999929, 44.92467540951147953, -237.7943620901849613 ) ) ;
#123849=CARTESIAN_POINT ( 'NONE',  ( -18.59999999999999787, 36.65892442174472876, -249.5511627012454596 ) ) ;
#123861=CARTESIAN_POINT ( 'NONE',  ( -21.07933241753356413, 30.84517785335011908, -252.0533277889904866 ) ) ;
#123872=FACE_OUTER_BOUND ( 'NONE', #249455, .T. ) ;
#123911=CIRCLE ( 'NONE', #236320, 0.09999999999999939493 ) ;
#123947=EDGE_CURVE ( 'NONE', #93920, #215460, #1840, .T. ) ;
#123961=DIRECTION ( 'NONE',  ( 1.000000000000000000, 0.000000000000000000, 0.000000000000000000 ) ) ;
#124022=ORIENTED_EDGE ( 'NONE', *, *, #19615, .F. ) ;
#124033=AXIS2_PLACEMENT_3D ( 'NONE', #62434, #141953, #198080 ) ;
#124039=CARTESIAN_POINT ( 'NONE',  ( -20.00857864376270001, 44.18876898710608003, -236.1516686502934590 ) ) ;
#124050=CIRCLE ( 'NONE', #24109, 4.099999999999998757 ) ;
#124080=DIRECTION ( 'NONE',  ( 0.000000000000000000, -0.4088369013363281068, 0.9126074666063770380 ) ) ;
#124082=CARTESIAN_POINT ( 'NONE',  ( 18.59999999999999432, 54.95667902235472013, -229.8578999281555468 ) ) ;
#124101=CARTESIAN_POINT ( 'NONE',  ( -18.51991288638587463, 47.01789743104386332, -255.2023397431154592 ) ) ;
#124103=DIRECTION ( 'NONE',  ( 0.000000000000000000, 0.9126074666063770380, 0.4088369013363281068 ) ) ;
#124129=DIRECTION ( 'NONE',  ( -0.000000000000000000, -0.4088369013363296611, 0.9126074666063764829 ) ) ;
#124141=AXIS2_PLACEMENT_3D ( 'NONE', #96093, #113110, #118243 ) ;
#124142=ORIENTED_EDGE ( 'NONE', *, *, #94560, .T. ) ;
#124150=ORIENTED_EDGE ( 'NONE', *, *, #248751, .T. ) ;
#124192=ORIENTED_EDGE ( 'NONE', *, *, #73227, .F. ) ;
#124194=ORIENTED_EDGE ( 'NONE', *, *, #1862, .F. ) ;
#124211=EDGE_CURVE ( 'NONE', #37046, #110542, #143701, .T. ) ;
#124214=AXIS2_PLACEMENT_3D ( 'NONE', #81093, #198487, #95535 ) ;
#124220=ORIENTED_EDGE ( 'NONE', *, *, #197931, .T. ) ;
#124248=CARTESIAN_POINT ( 'NONE',  ( -20.94999999999999929, 67.75954444190071513, -227.8703747234148693 ) ) ;
#124263=ORIENTED_EDGE ( 'NONE', *, *, #91808, .T. ) ;
#124267=ORIENTED_EDGE ( 'NONE', *, *, #27222, .T. ) ;
#124288=CARTESIAN_POINT ( 'NONE',  ( -23.15000000000000213, 21.13195309841794867, -243.6318585593224100 ) ) ;
#124297=CARTESIAN_POINT ( 'NONE',  ( 21.11747605621531321, 44.24434441712620014, -236.5336189637216933 ) ) ;
#124348=ORIENTED_EDGE ( 'NONE', *, *, #95556, .F. ) ;
#124363=LINE ( 'NONE', #203880, #141638 ) ;
#124376=VERTEX_POINT ( 'NONE', #37332 ) ;
#124388=ORIENTED_EDGE ( 'NONE', *, *, #187832, .F. ) ;
#124418=AXIS2_PLACEMENT_3D ( 'NONE', #85873, #126307, #123758 ) ;
#124430=DIRECTION ( 'NONE',  ( 4.408576920032447355E-17, 0.9594490217226103734, 0.2818822000686205254 ) ) ;
#124442=ADVANCED_FACE ( 'NONE', ( #103675 ), #4587, .T. ) ;
#124460=ORIENTED_EDGE ( 'NONE', *, *, #187492, .T. ) ;
#124481=AXIS2_PLACEMENT_3D ( 'NONE', #48125, #208512, #46827 ) ;
#124523=EDGE_CURVE ( 'NONE', #74900, #49355, #85579, .T. ) ;
#124547=CARTESIAN_POINT ( 'NONE',  ( 22.47110162079220785, 26.01533245542389849, -254.2878056764235737 ) ) ;
#124555=CARTESIAN_POINT ( 'NONE',  ( -18.50000000000000000, 38.29773864426885410, -236.0513742605307925 ) ) ;
#124557=EDGE_LOOP ( 'NONE', ( #3302, #1193, #81231 ) ) ;
#124641=ORIENTED_EDGE ( 'NONE', *, *, #61932, .F. ) ;
#124662=DIRECTION ( 'NONE',  ( 1.000000000000000000, 0.000000000000000000, 0.000000000000000000 ) ) ;
#124666=CARTESIAN_POINT ( 'NONE',  ( -20.54999999999999716, 45.00644278977874535, -237.9768835835062077 ) ) ;
#124721=CIRCLE ( 'NONE', #132918, 0.09999999999999609201 ) ;
#124733=CARTESIAN_POINT ( 'NONE',  ( -23.15000000000000213, 55.48145342050125350, -241.1189016111836736 ) ) ;
#124735=EDGE_CURVE ( 'NONE', #187157, #143336, #210528, .T. ) ;
#124766=DIRECTION ( 'NONE',  ( 1.000000000000000000, 0.000000000000000000, 0.000000000000000000 ) ) ;
#124771=CARTESIAN_POINT ( 'NONE',  ( -23.15000000000000213, 67.23127455305835554, -235.8551265064784559 ) ) ;
#124781=ORIENTED_EDGE ( 'NONE', *, *, #251674, .T. ) ;
#124784=ORIENTED_EDGE ( 'NONE', *, *, #171838, .F. ) ;
#124831=VERTEX_POINT ( 'NONE', #24861 ) ;
#124836=CARTESIAN_POINT ( 'NONE',  ( -21.93340585899782980, 29.97485316283794177, -252.5455442746994947 ) ) ;
#124854=FACE_OUTER_BOUND ( 'NONE', #233818, .T. ) ;
#124866=CARTESIAN_POINT ( 'NONE',  ( 20.94999999999999929, 48.98768910550767686, -253.5949463715719787 ) ) ;
#124898=EDGE_CURVE ( 'NONE', #2024, #150106, #206037, .T. ) ;
#124902=CARTESIAN_POINT ( 'NONE',  ( -22.57848426163146627, 25.93747689298670878, -254.3589117886994586 ) ) ;
#124903=CIRCLE ( 'NONE', #129011, 0.4999999999999944489 ) ;
#124905=DIRECTION ( 'NONE',  ( 1.000000000000000000, 0.000000000000000000, 0.000000000000000000 ) ) ;
#124907=AXIS2_PLACEMENT_3D ( 'NONE', #168645, #129468, #208998 ) ;
#124911=VERTEX_POINT ( 'NONE', #202184 ) ;
#124953=ORIENTED_EDGE ( 'NONE', *, *, #67323, .F. ) ;
#124960=EDGE_CURVE ( 'NONE', #52160, #171102, #173167, .T. ) ;
#124969=DIRECTION ( 'NONE',  ( -0.000000000000000000, 0.9126074666063771490, 0.4088369013363281623 ) ) ;
#124976=DIRECTION ( 'NONE',  ( -1.000000000000000000, -0.000000000000000000, -0.000000000000000000 ) ) ;
#124983=ORIENTED_EDGE ( 'NONE', *, *, #176169, .F. ) ;
#124986=ADVANCED_FACE ( 'NONE', ( #226875 ), #89923, .T. ) ;
#125004=DIRECTION ( 'NONE',  ( 0.000000000000000000, 0.9126074666063772600, 0.4088369013363274407 ) ) ;
#125037=DIRECTION ( 'NONE',  ( 2.952720810173289112E-16, 0.4088369013363388205, -0.9126074666063722640 ) ) ;
#125070=CARTESIAN_POINT ( 'NONE',  ( 18.49999999999999289, 51.95251559509352290, -231.4682683249995137 ) ) ;
#125085=DIRECTION ( 'NONE',  ( 1.000000000000000000, 0.000000000000000000, 0.000000000000000000 ) ) ;
#125087=ADVANCED_FACE ( 'NONE', ( #8668, #247261 ), #106450, .F. ) ;
#125093=ADVANCED_FACE ( 'NONE', ( #6085 ), #85766, .T. ) ;
#125095=ORIENTED_EDGE ( 'NONE', *, *, #233599, .F. ) ;
#125147=CARTESIAN_POINT ( 'NONE',  ( -21.13498764882296044, 30.73029760849721015, -252.2052994570879036 ) ) ;
#125165=VECTOR ( 'NONE', #58173, 1000.000000000000114 ) ;
#125186=VERTEX_POINT ( 'NONE', #73804 ) ;
#125204=ORIENTED_EDGE ( 'NONE', *, *, #257772, .F. ) ;
#125213=DIRECTION ( 'NONE',  ( 1.000000000000000000, 2.986185139342072849E-16, -6.665775143889690802E-16 ) ) ;
#125226=VERTEX_POINT ( 'NONE', #208169 ) ;
#125236=CARTESIAN_POINT ( 'NONE',  ( -21.44999999999999929, 52.99650480578122824, -234.2878581050858884 ) ) ;
#125257=VECTOR ( 'NONE', #197161, 1000.000000000000000 ) ;
#125269=CARTESIAN_POINT ( 'NONE',  ( 20.12500000000000000, 40.07562767317620711, -237.3368484665046765 ) ) ;
#125355=ADVANCED_FACE ( 'NONE', ( #137222 ), #62822, .T. ) ;
#125356=DIRECTION ( 'NONE',  ( 2.940209281316622988E-16, 0.4088369013363260529, -0.9126074666063779262 ) ) ;
#125362=EDGE_CURVE ( 'NONE', #173652, #154226, #69258, .T. ) ;
#125365=DIRECTION ( 'NONE',  ( -1.000000000000000000, -0.000000000000000000, -0.000000000000000000 ) ) ;
#125392=CARTESIAN_POINT ( 'NONE',  ( -18.59999999999999787, 43.07541598710462694, -233.9110336739111631 ) ) ;
#125433=ORIENTED_EDGE ( 'NONE', *, *, #228741, .F. ) ;
#125456=EDGE_CURVE ( 'NONE', #120409, #152713, #65389, .T. ) ;
#125464=AXIS2_PLACEMENT_3D ( 'NONE', #195331, #97452, #173226 ) ;
#125467=DIRECTION ( 'NONE',  ( 0.000000000000000000, 0.9126074666063771490, 0.4088369013363281623 ) ) ;
#125474=DIRECTION ( 'NONE',  ( -0.000000000000000000, 0.9579639084728149845, 0.2868887416116019384 ) ) ;
#125482=ORIENTED_EDGE ( 'NONE', *, *, #205372, .T. ) ;
#125493=ORIENTED_EDGE ( 'NONE', *, *, #154511, .F. ) ;
#125505=CARTESIAN_POINT ( 'NONE',  ( -20.85000000106584750, 56.18110340670160952, -227.9302710413118973 ) ) ;
#125514=CARTESIAN_POINT ( 'NONE',  ( -18.59999999999999787, 62.46832465249013921, -225.2232495205141731 ) ) ;
#125540=CARTESIAN_POINT ( 'NONE',  ( 20.95512820512820795, 43.44946199836419254, -234.8678826325710531 ) ) ;
#125581=CARTESIAN_POINT ( 'NONE',  ( 20.94999999999999929, 67.23127455305835554, -235.8551265064784559 ) ) ;
#125585=DIRECTION ( 'NONE',  ( 1.000000000000000000, 0.000000000000000000, 0.000000000000000000 ) ) ;
#125602=CIRCLE ( 'NONE', #187981, 0.09999999999999538425 ) ;
#125628=CARTESIAN_POINT ( 'NONE',  ( 18.59999999999999787, 48.05114133249968944, -246.4758750954581785 ) ) ;
#125631=DIRECTION ( 'NONE',  ( 0.000000000000000000, 0.8371762388950346745, 0.5469332180710581026 ) ) ;
#125695=AXIS2_PLACEMENT_3D ( 'NONE', #219371, #61594, #155599 ) ;
#125699=CARTESIAN_POINT ( 'NONE',  ( 21.14999999999999858, 44.24607648097409651, -236.5241869975821487 ) ) ;
#125707=FACE_OUTER_BOUND ( 'NONE', #161572, .T. ) ;
#125718=EDGE_CURVE ( 'NONE', #224475, #70441, #84599, .T. ) ;
#125739=EDGE_LOOP ( 'NONE', ( #20105, #148777, #44446, #133960 ) ) ;
#125753=SPHERICAL_SURFACE ( 'NONE', #225170, 0.1000000000000000056 ) ;
#125784=CARTESIAN_POINT ( 'NONE',  ( -18.50000000000000000, 44.18876898710608003, -236.1516686502934590 ) ) ;
#125789=EDGE_CURVE ( 'NONE', #131079, #110771, #184962, .T. ) ;
#125792=DIRECTION ( 'NONE',  ( 0.000000000000000000, 0.3999834006488773852, 0.9165223833629813077 ) ) ;
#125816=EDGE_CURVE ( 'NONE', #97714, #172097, #82042, .T. ) ;
#125817=CARTESIAN_POINT ( 'NONE',  ( 20.85000000000000142, 67.84340367245323478, -228.0791829662263410 ) ) ;
#125826=CARTESIAN_POINT ( 'NONE',  ( 23.14999999999999858, 65.63681063784667913, -232.2959573867136100 ) ) ;
#125859=EDGE_CURVE ( 'NONE', #133755, #91918, #203318, .T. ) ;
#125890=EDGE_CURVE ( 'NONE', #133755, #251907, #227629, .T. ) ;
#125928=CARTESIAN_POINT ( 'NONE',  ( -23.25000000000000000, 46.23295349378772556, -240.7147059833253309 ) ) ;
#125956=ORIENTED_EDGE ( 'NONE', *, *, #136034, .T. ) ;
#125962=AXIS2_PLACEMENT_3D ( 'NONE', #148212, #249882, #167807 ) ;
#125977=CARTESIAN_POINT ( 'NONE',  ( -21.07954640115351808, 34.01103892604695034, -243.8019938780049642 ) ) ;
#126006=DIRECTION ( 'NONE',  ( 0.000000000000000000, 0.9126074666063660468, 0.4088369013363524762 ) ) ;
#126008=EDGE_LOOP ( 'NONE', ( #229582, #114901, #83458, #62848 ) ) ;
#126019=CARTESIAN_POINT ( 'NONE',  ( -23.15000000000000213, 63.58084468663284383, -237.4904741118237723 ) ) ;
#126054=ORIENTED_EDGE ( 'NONE', *, *, #122137, .T. ) ;
#126056=CARTESIAN_POINT ( 'NONE',  ( -23.15000000000000213, 54.27339256631721298, -236.8935360681107625 ) ) ;
#126057=DIRECTION ( 'NONE',  ( 0.000000000000000000, 0.4088369013363280513, -0.9126074666063769270 ) ) ;
#126059=VERTEX_POINT ( 'NONE', #102254 ) ;
#126067=DIRECTION ( 'NONE',  ( 1.000000000000000000, 0.000000000000000000, -0.000000000000000000 ) ) ;
#126070=AXIS2_PLACEMENT_3D ( 'NONE', #92672, #13154, #172264 ) ;
#126079=EDGE_LOOP ( 'NONE', ( #26717, #43132, #139708, #132538 ) ) ;
#126091=FACE_OUTER_BOUND ( 'NONE', #144764, .T. ) ;
#126097=ORIENTED_EDGE ( 'NONE', *, *, #107694, .T. ) ;
#126106=VECTOR ( 'NONE', #22626, 1000.000000000000114 ) ;
#126176=EDGE_CURVE ( 'NONE', #139213, #125226, #206975, .T. ) ;
#126177=ORIENTED_EDGE ( 'NONE', *, *, #39750, .F. ) ;
#126195=EDGE_CURVE ( 'NONE', #10431, #215970, #240304, .T. ) ;
#126199=ORIENTED_EDGE ( 'NONE', *, *, #83648, .F. ) ;
#126210=ADVANCED_FACE ( 'NONE', ( #72178 ), #51278, .F. ) ;
#126216=ORIENTED_EDGE ( 'NONE', *, *, #142390, .F. ) ;
#126259=VERTEX_POINT ( 'NONE', #55129 ) ;
#126264=DIRECTION ( 'NONE',  ( -0.000000000000000000, 0.4088369013363281623, -0.9126074666063771490 ) ) ;
#126278=CARTESIAN_POINT ( 'NONE',  ( -20.54999999999999716, 54.70975502726918194, -239.2730902609777104 ) ) ;
#126287=DIRECTION ( 'NONE',  ( -1.000000000000000000, -0.000000000000000000, 0.000000000000000000 ) ) ;
#126307=DIRECTION ( 'NONE',  ( -1.000000000000000000, -0.000000000000000000, -0.000000000000000000 ) ) ;
#126331=CIRCLE ( 'NONE', #184586, 11.70000000000000462 ) ;
#126345=LINE ( 'NONE', #25978, #74365 ) ;
#126349=( BOUNDED_SURFACE ( )  B_SPLINE_SURFACE ( 3, 2, ( 
 ( #173066, #170508, #249993 ),
 ( #130016, #53065, #229151 ),
 ( #51759, #29688, #190020 ),
 ( #71373, #111766, #212158 ),
 ( #253823, #169201, #149629 ),
 ( #15245, #233018, #109175 ) ),
 .UNSPECIFIED., .F., .F., .F. ) 
 B_SPLINE_SURFACE_WITH_KNOTS ( ( 4, 2, 4 ),
 ( 3, 3 ),
 ( 0.0001342700090130142393, 0.0002909192928057479071, 0.0004475685765984815478 ),
 ( 0.000000000000000000, 1.000000000000000000 ),
 .UNSPECIFIED. ) 
 GEOMETRIC_REPRESENTATION_ITEM ( )  RATIONAL_B_SPLINE_SURFACE ( (
 ( 1.000000000000000000, 0.7250110520819876836, 1.000000000000000000),
 ( 1.000000000000000000, 0.7257599279130237946, 1.000000000000000000),
 ( 1.000000000000000000, 0.7137594617289112486, 1.000000000000000000),
 ( 1.000000000000000000, 0.6959270178805850859, 1.000000000000000000),
 ( 1.000000000000000000, 0.6919879549343305181, 1.000000000000000000),
 ( 1.000000000000000000, 0.7071067811865487940, 1.000000000000000000) ) ) 
 REPRESENTATION_ITEM ( '' )  SURFACE ( )  );
#126351=EDGE_CURVE ( 'NONE', #70690, #133508, #11344, .T. ) ;
#126360=DIRECTION ( 'NONE',  ( 1.000000000000000000, 0.000000000000000000, 0.000000000000000000 ) ) ;
#126387=EDGE_LOOP ( 'NONE', ( #124220, #129035 ) ) ;
#126402=AXIS2_PLACEMENT_3D ( 'NONE', #178677, #254301, #75702 ) ;
#126406=CARTESIAN_POINT ( 'NONE',  ( -21.44999999999999929, 44.83341466285084209, -237.8352457803185871 ) ) ;
#126411=CARTESIAN_POINT ( 'NONE',  ( -21.10320863425827298, 30.80775347085393889, -252.1449967823172642 ) ) ;
#126417=CARTESIAN_POINT ( 'NONE',  ( -20.64999999999999858, 54.18117728009210055, -239.0715820348696923 ) ) ;
#126437=CARTESIAN_POINT ( 'NONE',  ( 19.97071067811864609, 54.45410018515091366, -228.7360413143871654 ) ) ;
#126445=CIRCLE ( 'NONE', #163866, 0.5999999999999934275 ) ;
#126462=AXIS2_PLACEMENT_3D ( 'NONE', #146504, #108686, #111261 ) ;
#126517=ORIENTED_EDGE ( 'NONE', *, *, #121659, .T. ) ;
#126535=CIRCLE ( 'NONE', #93200, 0.09999999999999609201 ) ;
#126536=CARTESIAN_POINT ( 'NONE',  ( 23.14999999999999858, 67.23127455305835554, -235.8551265064784559 ) ) ;
#126575=CARTESIAN_POINT ( 'NONE',  ( 23.14999999999999858, 66.41360075038569732, -234.0299115732657071 ) ) ;
#126634=AXIS2_PLACEMENT_3D ( 'NONE', #118770, #61348, #78329 ) ;
#126670=CARTESIAN_POINT ( 'NONE',  ( -21.14999999999999858, 31.94635157770351341, -238.7871412784868994 ) ) ;
#126673=CARTESIAN_POINT ( 'NONE',  ( 20.85000000000000142, 67.23127455305835554, -235.8551265064784559 ) ) ;
#126697=DIRECTION ( 'NONE',  ( 0.000000000000000000, -0.9126074666063769270, -0.4088369013363282733 ) ) ;
#126705=ORIENTED_EDGE ( 'NONE', *, *, #17861, .T. ) ;
#126814=CARTESIAN_POINT ( 'NONE',  ( 19.97071067695875968, 54.38679851776535656, -228.7661916334623413 ) ) ;
#126825=ORIENTED_EDGE ( 'NONE', *, *, #20362, .T. ) ;
#126880=CARTESIAN_POINT ( 'NONE',  ( 20.04142135623730070, 21.13195309841794867, -243.6318585593224100 ) ) ;
#126896=FACE_OUTER_BOUND ( 'NONE', #170646, .T. ) ;
#126906=CIRCLE ( 'NONE', #110322, 0.1000000000000024342 ) ;
#126907=ORIENTED_EDGE ( 'NONE', *, *, #171923, .T. ) ;
#126915=ADVANCED_FACE ( 'NONE', ( #170697 ), #190217, .T. ) ;
#126948=ADVANCED_FACE ( 'NONE', ( #209776 ), #3984, .F. ) ;
#126951=DIRECTION ( 'NONE',  ( 0.000000000000000000, 0.5283051335750404975, -0.8490545835446967615 ) ) ;
#126967=DIRECTION ( 'NONE',  ( 1.836970198721030427E-16, 0.4088369013363281623, -0.9126074666063771490 ) ) ;
#126968=ORIENTED_EDGE ( 'NONE', *, *, #232167, .F. ) ;
#126986=PLANE ( 'NONE',  #53999 ) ;
#127000=ORIENTED_EDGE ( 'NONE', *, *, #168521, .T. ) ;
#127037=VERTEX_POINT ( 'NONE', #177088 ) ;
#127040=ORIENTED_EDGE ( 'NONE', *, *, #179152, .F. ) ;
#127054=CARTESIAN_POINT ( 'NONE',  ( -21.05000000000000071, 44.52640028187936849, -247.3006740988509193 ) ) ;
#127059=CYLINDRICAL_SURFACE ( 'NONE', #249731, 0.4999999999999944489 ) ;
#127071=DIRECTION ( 'NONE',  ( 0.000000000000000000, 0.4088369013363311599, -0.9126074666063757057 ) ) ;
#127087=ORIENTED_EDGE ( 'NONE', *, *, #117071, .T. ) ;
#127089=EDGE_CURVE ( 'NONE', #143749, #213386, #108055, .T. ) ;
#127153=CARTESIAN_POINT ( 'NONE',  ( 20.95595012432476167, 39.25550045643235109, -236.7682787779284581 ) ) ;
#127205=EDGE_LOOP ( 'NONE', ( #90374, #171076, #136785, #162042 ) ) ;
#127242=DIRECTION ( 'NONE',  ( -7.304098846218443309E-16, -0.4088369013363783999, 0.9126074666063545004 ) ) ;
#127266=DIRECTION ( 'NONE',  ( 0.000000000000000000, 0.9126074666063772600, 0.4088369013363276627 ) ) ;
#127277=EDGE_CURVE ( 'NONE', #228417, #150739, #195742, .T. ) ;
#127301=EDGE_CURVE ( 'NONE', #112216, #142489, #95728, .T. ) ;
#127308=CARTESIAN_POINT ( 'NONE',  ( 20.85000000000000142, 78.57213941646344324, -232.7862224702232652 ) ) ;
#127314=ADVANCED_FACE ( 'NONE', ( #109062 ), #49089, .T. ) ;
#127416=AXIS2_PLACEMENT_3D ( 'NONE', #161847, #140989, #220521 ) ;
#127454=ORIENTED_EDGE ( 'NONE', *, *, #68866, .T. ) ;
#127471=ORIENTED_EDGE ( 'NONE', *, *, #151493, .T. ) ;
#127476=ADVANCED_FACE ( 'NONE', ( #61623 ), #162029, .T. ) ;
#127480=ADVANCED_FACE ( 'NONE', ( #37261 ), #33242, .T. ) ;
#127504=DIRECTION ( 'NONE',  ( -1.000000000000000000, 1.207181226542539700E-16, -2.694675058168174199E-16 ) ) ;
#127506=ORIENTED_EDGE ( 'NONE', *, *, #167990, .F. ) ;
#127533=ORIENTED_EDGE ( 'NONE', *, *, #39884, .F. ) ;
#127547=ORIENTED_EDGE ( 'NONE', *, *, #169591, .T. ) ;
#127563=FACE_OUTER_BOUND ( 'NONE', #94159, .T. ) ;
#127629=CARTESIAN_POINT ( 'NONE',  ( 21.14999999999999858, 52.64219947837469959, -255.2660483925003803 ) ) ;
#127645=DIRECTION ( 'NONE',  ( 0.000000000000000000, -0.9126074666063770380, -0.4088369013363281068 ) ) ;
#127651=DIRECTION ( 'NONE',  ( 0.000000000000000000, 0.9126074666063791474, 0.4088369013363231663 ) ) ;
#127691=CARTESIAN_POINT ( 'NONE',  ( 22.50000000000000000, 25.98655542988603173, -254.2226763854395983 ) ) ;
#127701=ADVANCED_FACE ( 'NONE', ( #51007 ), #113585, .F. ) ;
#127702=EDGE_CURVE ( 'NONE', #785, #149628, #36467, .T. ) ;
#127723=CIRCLE ( 'NONE', #236038, 4.099999999999998757 ) ;
#127749=ORIENTED_EDGE ( 'NONE', *, *, #48944, .T. ) ;
#127767=CARTESIAN_POINT ( 'NONE',  ( 22.59999999999999432, 25.89494711235934687, -254.2627752153468350 ) ) ;
#127774=ORIENTED_EDGE ( 'NONE', *, *, #7795, .F. ) ;
#127839=CARTESIAN_POINT ( 'NONE',  ( -22.39999999999999858, 29.50811709945089945, -252.6450601445781103 ) ) ;
#127872=CARTESIAN_POINT ( 'NONE',  ( -23.15000000000000213, 51.28888318656201761, -230.2315015618842153 ) ) ;
#127882=CYLINDRICAL_SURFACE ( 'NONE', #195652, 0.09999999999999939493 ) ;
#127887=DIRECTION ( 'NONE',  ( 0.000000000000000000, 0.9126074666063774821, 0.4088369013363268301 ) ) ;
#127898=EDGE_CURVE ( 'NONE', #218531, #19219, #19695, .T. ) ;
#127921=FACE_OUTER_BOUND ( 'NONE', #231812, .T. ) ;
#127938=FACE_OUTER_BOUND ( 'NONE', #66081, .T. ) ;
#127944=FACE_OUTER_BOUND ( 'NONE', #258081, .T. ) ;
#127952=DIRECTION ( 'NONE',  ( 1.000000000000000000, -1.335000415235278971E-16, 2.979993593738921214E-16 ) ) ;
#127957=AXIS2_PLACEMENT_3D ( 'NONE', #165944, #45965, #153787 ) ;
#128008=CIRCLE ( 'NONE', #252890, 0.1000000000000024342 ) ;
#128049=FACE_OUTER_BOUND ( 'NONE', #225641, .T. ) ;
#128058=EDGE_LOOP ( 'NONE', ( #96573, #185097, #115464, #225147 ) ) ;
#128062=ADVANCED_FACE ( 'NONE', ( #179682 ), #74068, .T. ) ;
#128071=ORIENTED_EDGE ( 'NONE', *, *, #236877, .T. ) ;
#128087=CIRCLE ( 'NONE', #98820, 4.299999999999953637 ) ;
#128096=CARTESIAN_POINT ( 'NONE',  ( 18.59999999999999076, 43.10494791715829166, -239.6505508802563327 ) ) ;
#128130=DIRECTION ( 'NONE',  ( 0.000000000000000000, -0.9126074666063769270, -0.4088369013363282733 ) ) ;
#128156=CARTESIAN_POINT ( 'NONE',  ( 22.39999999999999503, 26.06832281015329755, -254.4051978787608732 ) ) ;
#128166=DIRECTION ( 'NONE',  ( -1.000000000000000000, -0.000000000000000000, 0.000000000000000000 ) ) ;
#128178=DIRECTION ( 'NONE',  ( 0.000000000000000000, -0.9126074666063622720, -0.4088369013363611360 ) ) ;
#128188=AXIS2_PLACEMENT_3D ( 'NONE', #219941, #238211, #76577 ) ;
#128192=EDGE_LOOP ( 'NONE', ( #32515, #135116, #64157, #3244 ) ) ;
#128220=LINE ( 'NONE', #111218, #23812 ) ;
#128263=DIRECTION ( 'NONE',  ( 0.000000000000000000, -0.8103668758649577031, 0.5859227990963212784 ) ) ;
#128293=DIRECTION ( 'NONE',  ( 0.000000000000000000, -0.9126074666063769270, -0.4088369013363280513 ) ) ;
#128313=CARTESIAN_POINT ( 'NONE',  ( 23.15000000000000213, 69.19063053712525857, -247.5666987377248631 ) ) ;
#128322=CARTESIAN_POINT ( 'NONE',  ( 21.05000000000000071, 69.20602499728043711, -247.8456586332460176 ) ) ;
#128324=CARTESIAN_POINT ( 'NONE',  ( 21.05000000000000071, 39.23476235320398331, -236.9756760510740037 ) ) ;
#128331=AXIS2_PLACEMENT_3D ( 'NONE', #123400, #84207, #4709 ) ;
#128450=EDGE_LOOP ( 'NONE', ( #220531, #164008, #214572, #144979 ) ) ;
#128463=SPHERICAL_SURFACE ( 'NONE', #163407, 0.1000000000000000056 ) ;
#128477=CIRCLE ( 'NONE', #149348, 0.09999999999999939493 ) ;
#128484=CARTESIAN_POINT ( 'NONE',  ( -21.05000000000000071, 36.52237217006333481, -249.3317055962219229 ) ) ;
#128495=DIRECTION ( 'NONE',  ( 1.000000000000000000, 0.000000000000000000, -0.000000000000000000 ) ) ;
#128505=EDGE_LOOP ( 'NONE', ( #150789, #175188, #234335, #34056 ) ) ;
#128526=EDGE_CURVE ( 'NONE', #62147, #176943, #174208, .T. ) ;
#128553=FACE_OUTER_BOUND ( 'NONE', #225309, .T. ) ;
#128561=DIRECTION ( 'NONE',  ( 0.000000000000000000, 0.9126074666063660468, 0.4088369013363524762 ) ) ;
#128583=CARTESIAN_POINT ( 'NONE',  ( -20.64999999999999858, 49.36776662947724503, -253.7196102226803021 ) ) ;
#128642=ORIENTED_EDGE ( 'NONE', *, *, #236387, .T. ) ;
#128652=DIRECTION ( 'NONE',  ( 0.000000000000000000, -0.4088369013363280513, 0.9126074666063769270 ) ) ;
#128677=EDGE_LOOP ( 'NONE', ( #221890, #182396, #167691, #144897 ) ) ;
#128708=DIRECTION ( 'NONE',  ( -7.304098846218134667E-16, 0.4088369013363281068, -0.9126074666063770380 ) ) ;
#128717=CARTESIAN_POINT ( 'NONE',  ( -21.07928932188134041, 33.98134083355423485, -243.8161431329846778 ) ) ;
#128733=VERTEX_POINT ( 'NONE', #175263 ) ;
#128791=DIRECTION ( 'NONE',  ( -1.000000000000000000, -0.000000000000000000, -0.000000000000000000 ) ) ;
#128834=DIRECTION ( 'NONE',  ( 0.000000000000000000, 0.9126074666063780372, 0.4088369013363259419 ) ) ;
#128853=CARTESIAN_POINT ( 'NONE',  ( -20.64999999999999858, 48.89266972451527948, -253.5637804087949121 ) ) ;
#128876=EDGE_CURVE ( 'NONE', #158029, #41121, #181655, .T. ) ;
#128892=DIRECTION ( 'NONE',  ( -0.000000000000000000, -0.9126074666063770380, -0.4088369013363281068 ) ) ;
#128895=CARTESIAN_POINT ( 'NONE',  ( 18.59999999999999076, 54.48300931968434213, -228.8005724072070564 ) ) ;
#128900=ORIENTED_EDGE ( 'NONE', *, *, #104417, .T. ) ;
#128907=ORIENTED_EDGE ( 'NONE', *, *, #207621, .F. ) ;
#128931=ADVANCED_FACE ( 'NONE', ( #59084 ), #138627, .F. ) ;
#128974=CONICAL_SURFACE ( 'NONE', #74831, 7.750000000000023981, 0.7853981633974531640 ) ;
#128997=EDGE_LOOP ( 'NONE', ( #207719, #223026, #26195, #129054 ) ) ;
#129006=CARTESIAN_POINT ( 'NONE',  ( -20.54999999999999716, 44.87429835298446790, -237.9265065269792103 ) ) ;
#129011=AXIS2_PLACEMENT_3D ( 'NONE', #77814, #158685, #200350 ) ;
#129013=VECTOR ( 'NONE', #2212, 1000.000000000000114 ) ;
#129017=DIRECTION ( 'NONE',  ( 1.000000000000000000, 0.000000000000000000, -0.000000000000000000 ) ) ;
#129035=ORIENTED_EDGE ( 'NONE', *, *, #257772, .T. ) ;
#129054=ORIENTED_EDGE ( 'NONE', *, *, #109448, .F. ) ;
#129055=VERTEX_POINT ( 'NONE', #164658 ) ;
#129060=DIRECTION ( 'NONE',  ( 0.000000000000000000, -0.9126074666063770380, -0.4088369013363281068 ) ) ;
#129071=CARTESIAN_POINT ( 'NONE',  ( -21.44999999999999929, 53.04688186230822566, -234.1557136682916394 ) ) ;
#129136=CARTESIAN_POINT ( 'NONE',  ( 18.59999999999999432, 48.14768554360777841, -246.4498133360871179 ) ) ;
#129148=EDGE_CURVE ( 'NONE', #112295, #206700, #66392, .T. ) ;
#129179=ADVANCED_FACE ( 'NONE', ( #80595 ), #3642, .T. ) ;
#129207=ORIENTED_EDGE ( 'NONE', *, *, #72390, .F. ) ;
#129225=CARTESIAN_POINT ( 'NONE',  ( -18.48550754431968457, 46.96068962191068863, -255.3057266380914712 ) ) ;
#129251=CARTESIAN_POINT ( 'NONE',  ( -20.54999999999999716, 46.19206980365409265, -240.6234452366647076 ) ) ;
#129257=CARTESIAN_POINT ( 'NONE',  ( -18.53317502108577131, 68.08564185115265843, -224.1612363371343122 ) ) ;
#129281=EDGE_CURVE ( 'NONE', #169429, #216161, #55211, .T. ) ;
#129290=ORIENTED_EDGE ( 'NONE', *, *, #255289, .T. ) ;
#129299=AXIS2_PLACEMENT_3D ( 'NONE', #242713, #4111, #64088 ) ;
#129307=DIRECTION ( 'NONE',  ( 0.000000000000000000, -0.9126074666063773710, -0.4088369013363272741 ) ) ;
#129328=CIRCLE ( 'NONE', #254210, 0.1000000000000024342 ) ;
#129332=VERTEX_POINT ( 'NONE', #50453 ) ;
#129359=CIRCLE ( 'NONE', #145915, 0.1000000000000024342 ) ;
#129361=AXIS2_PLACEMENT_3D ( 'NONE', #16623, #74047, #212257 ) ;
#129380=CARTESIAN_POINT ( 'NONE',  ( 19.75857864376269291, 54.44212562955072343, -228.7093116605464047 ) ) ;
#129422=ADVANCED_FACE ( 'NONE', ( #10071, #149608 ), #132595, .T. ) ;
#129432=CARTESIAN_POINT ( 'NONE',  ( 20.50589344625223731, 39.28418211382209790, -236.8880073202264782 ) ) ;
#129439=DIRECTION ( 'NONE',  ( 0.000000000000000000, -0.9126074666063773710, -0.4088369013363271631 ) ) ;
#129468=DIRECTION ( 'NONE',  ( 1.000000000000000000, 0.000000000000000000, 0.000000000000000000 ) ) ;
#129472=EDGE_CURVE ( 'NONE', #179534, #178504, #61725, .T. ) ;
#129476=EDGE_LOOP ( 'NONE', ( #27301, #234154, #219076, #220955 ) ) ;
#129499=DIRECTION ( 'NONE',  ( -0.000000000000000000, 0.9126074666063770380, 0.4088369013363281068 ) ) ;
#129512=DIRECTION ( 'NONE',  ( 0.000000000000000000, -0.9126074666063769270, -0.4088369013363280513 ) ) ;
#129527=DIRECTION ( 'NONE',  ( 1.000000000000000000, 0.000000000000000000, 0.000000000000000000 ) ) ;
#129561=ORIENTED_EDGE ( 'NONE', *, *, #144677, .T. ) ;
#129571=FACE_OUTER_BOUND ( 'NONE', #58010, .T. ) ;
#129596=VERTEX_POINT ( 'NONE', #94736 ) ;
#129597=FACE_OUTER_BOUND ( 'NONE', #26736, .T. ) ;
#129605=DIRECTION ( 'NONE',  ( -2.342056488767302165E-15, -0.8490545835447238510, -0.5283051335749973099 ) ) ;
#129610=AXIS2_PLACEMENT_3D ( 'NONE', #193889, #180738, #102437 ) ;
#129671=DIRECTION ( 'NONE',  ( -1.000000000000000000, 2.986185139342070877E-16, -6.665775143889692774E-16 ) ) ;
#129706=CARTESIAN_POINT ( 'NONE',  ( 23.25000000000000000, 69.20602499728043711, -247.8456586332460176 ) ) ;
#129742=DIRECTION ( 'NONE',  ( 0.000000000000000000, -0.4088369013363280513, 0.9126074666063769270 ) ) ;
#129745=DIRECTION ( 'NONE',  ( -1.000000000000000000, -0.000000000000000000, 0.000000000000000000 ) ) ;
#129747=ORIENTED_EDGE ( 'NONE', *, *, #206140, .F. ) ;
#129782=DIRECTION ( 'NONE',  ( 0.000000000000000000, 0.9126074666063772600, 0.4088369013363274407 ) ) ;
#129796=ADVANCED_FACE ( 'NONE', ( #149302 ), #7178, .F. ) ;
#129824=CARTESIAN_POINT ( 'NONE',  ( -21.05000000000000071, 36.65892442174472876, -249.5511627012454596 ) ) ;
#129864=DIRECTION ( 'NONE',  ( 0.000000000000000000, -0.9126074666063769270, -0.4088369013363280513 ) ) ;
#129882=DIRECTION ( 'NONE',  ( 0.000000000000000000, -0.1569827930593259702, 0.9876013379310970564 ) ) ;
#129902=CARTESIAN_POINT ( 'NONE',  ( -21.64999999999999858, 44.83341466285084209, -237.8352457803185871 ) ) ;
#129960=DIRECTION ( 'NONE',  ( 1.000000000000000000, -0.000000000000000000, -0.000000000000000000 ) ) ;
#129968=DIRECTION ( 'NONE',  ( -0.000000000000000000, 0.9969158384938637818, -0.07847809223010315804 ) ) ;
#129972=CARTESIAN_POINT ( 'NONE',  ( -18.59999999999999787, 47.16152503674116048, -255.1462838189583238 ) ) ;
#129983=VECTOR ( 'NONE', #77252, 1000.000000000000000 ) ;
#129991=ADVANCED_FACE ( 'NONE', ( #172742 ), #113990, .T. ) ;
#129995=EDGE_LOOP ( 'NONE', ( #178300, #64396, #74874 ) ) ;
#130016=CARTESIAN_POINT ( 'NONE',  ( 20.95512840106804120, 43.45157668952643348, -234.8669352659592846 ) ) ;
#130019=VERTEX_POINT ( 'NONE', #22629 ) ;
#130034=CARTESIAN_POINT ( 'NONE',  ( 21.05193202509564543, 43.38332961584228542, -234.7878372896277881 ) ) ;
#130035=DIRECTION ( 'NONE',  ( -1.000000000000000000, 0.000000000000000000, 0.000000000000000000 ) ) ;
#130043=LINE ( 'NONE', #145758, #109517 ) ;
#130053=ORIENTED_EDGE ( 'NONE', *, *, #165815, .T. ) ;
#130079=EDGE_CURVE ( 'NONE', #198869, #62294, #119148, .T. ) ;
#130085=EDGE_LOOP ( 'NONE', ( #88565, #220471, #75447, #230727 ) ) ;
#130088=CARTESIAN_POINT ( 'NONE',  ( -22.39999999999999858, 31.76383008438224564, -238.8689086587541510 ) ) ;
#130112=AXIS2_PLACEMENT_3D ( 'NONE', #100638, #194677, #219329 ) ;
#130117=PLANE ( 'NONE',  #111078 ) ;
#130136=CARTESIAN_POINT ( 'NONE',  ( -21.05000000000000071, 43.39316802731212874, -245.2602608822587342 ) ) ;
#130151=ORIENTED_EDGE ( 'NONE', *, *, #182937, .F. ) ;
#130153=CIRCLE ( 'NONE', #196787, 0.09999999999999993616 ) ;
#130178=CARTESIAN_POINT ( 'NONE',  ( -23.25000000000000000, 67.23127455305835554, -235.8551265064784559 ) ) ;
#130226=ORIENTED_EDGE ( 'NONE', *, *, #200044, .T. ) ;
#130250=AXIS2_PLACEMENT_3D ( 'NONE', #199593, #220422, #41799 ) ;
#130251=EDGE_CURVE ( 'NONE', #11074, #222021, #141199, .T. ) ;
#130265=DIRECTION ( 'NONE',  ( -0.000000000000000000, 0.4088369013363281068, -0.9126074666063770380 ) ) ;
#130277=CARTESIAN_POINT ( 'NONE',  ( -20.64999999999999858, 44.87429835298446790, -237.9265065269792103 ) ) ;
#130280=B_SPLINE_CURVE_WITH_KNOTS ( 'NONE', 3,
 ( #158351, #237848, #81306, #183029, #43511, #223405, #65624, #83865, #107319, #22682 ),
 .UNSPECIFIED., .F., .F.,
 ( 4, 3, 3, 4 ),
 ( 0.000000000000000000, 3.394313611811697806E-05, 6.779740500700335930E-05, 0.0001049857339142755560 ),
 .UNSPECIFIED. ) ;
#130281=DIRECTION ( 'NONE',  ( -0.000000000000000000, 0.9165223833629858596, -0.3999834006488672267 ) ) ;
#130298=ORIENTED_EDGE ( 'NONE', *, *, #133235, .F. ) ;
#130307=DIRECTION ( 'NONE',  ( 1.000000000000000000, 0.000000000000000000, 0.000000000000000000 ) ) ;
#130335=EDGE_LOOP ( 'NONE', ( #81971, #136047, #36617, #99070 ) ) ;
#130357=CARTESIAN_POINT ( 'NONE',  ( 21.05000000000000071, 31.89597452117650533, -238.9192857152811484 ) ) ;
#130358=CARTESIAN_POINT ( 'NONE',  ( -20.64999999999999858, 45.00644278977874535, -237.9768835835062077 ) ) ;
#130390=DIRECTION ( 'NONE',  ( -1.000000000000000000, -0.000000000000000000, 0.000000000000000000 ) ) ;
#130391=CIRCLE ( 'NONE', #242991, 11.74999999999999822 ) ;
#130393=EDGE_LOOP ( 'NONE', ( #37962, #160283, #106448, #42589 ) ) ;
#130432=ORIENTED_EDGE ( 'NONE', *, *, #81712, .T. ) ;
#130442=CARTESIAN_POINT ( 'NONE',  ( 18.50000000000000000, 47.16152503674118890, -255.1462838189583806 ) ) ;
#130444=CARTESIAN_POINT ( 'NONE',  ( 21.46681500598917580, 30.40070853532387929, -252.3547663145410240 ) ) ;
#130449=TOROIDAL_SURFACE ( 'NONE', #97078, 0.2000000000000000111, 0.1000000000000000056 ) ;
#130455=AXIS2_PLACEMENT_3D ( 'NONE', #209836, #76719, #214957 ) ;
#130456=ORIENTED_EDGE ( 'NONE', *, *, #96928, .T. ) ;
#130493=ORIENTED_EDGE ( 'NONE', *, *, #12817, .T. ) ;
#130527=CARTESIAN_POINT ( 'NONE',  ( -18.52643265882458579, 68.07764576057050476, -224.1679995073710359 ) ) ;
#130541=EDGE_LOOP ( 'NONE', ( #57720, #252832, #84802, #211731, #158999, #5298 ) ) ;
#130543=EDGE_CURVE ( 'NONE', #111624, #200814, #191296, .T. ) ;
#130553=CIRCLE ( 'NONE', #188821, 0.1000000000000024342 ) ;
#130564=DIRECTION ( 'NONE',  ( -1.000000000000000000, -0.000000000000000000, -0.000000000000000000 ) ) ;
#130572=DIRECTION ( 'NONE',  ( 1.000000000000000000, 0.000000000000000000, 0.000000000000000000 ) ) ;
#130591=DIRECTION ( 'NONE',  ( 0.000000000000000000, -0.9126074666063545004, -0.4088369013363783999 ) ) ;
#130596=EDGE_CURVE ( 'NONE', #216161, #86809, #157998, .T. ) ;
#130598=AXIS2_PLACEMENT_3D ( 'NONE', #111140, #228536, #91579 ) ;
#130605=DIRECTION ( 'NONE',  ( -0.000000000000000000, 0.5283051335749948674, -0.8490545835447252943 ) ) ;
#130610=CARTESIAN_POINT ( 'NONE',  ( -21.55000000000000426, 52.80902093404626640, -233.8693558107618173 ) ) ;
#130627=EDGE_LOOP ( 'NONE', ( #47144, #98527, #145244, #224525 ) ) ;
#130629=VERTEX_POINT ( 'NONE', #251629 ) ;
#130634=ORIENTED_EDGE ( 'NONE', *, *, #129148, .F. ) ;
#130635=DIRECTION ( 'NONE',  ( 0.000000000000000000, 0.9126074666063660468, 0.4088369013363524762 ) ) ;
#130668=DIRECTION ( 'NONE',  ( 0.000000000000000000, -0.5283051335750404975, 0.8490545835446967615 ) ) ;
#130670=ADVANCED_FACE ( 'NONE', ( #211215 ), #249712, .T. ) ;
#130694=CIRCLE ( 'NONE', #218162, 0.1000000000000074579 ) ;
#130751=ORIENTED_EDGE ( 'NONE', *, *, #235822, .F. ) ;
#130760=ORIENTED_EDGE ( 'NONE', *, *, #48944, .F. ) ;
#130770=ORIENTED_EDGE ( 'NONE', *, *, #63995, .F. ) ;
#130776=CIRCLE ( 'NONE', #193156, 0.4000000000000033529 ) ;
#130789=CIRCLE ( 'NONE', #47572, 11.74999999999999822 ) ;
#130798=FACE_OUTER_BOUND ( 'NONE', #106675, .T. ) ;
#130840=DIRECTION ( 'NONE',  ( 1.734723475976817823E-14, 0.9126074666063771490, 0.4088369013363281623 ) ) ;
#130872=DIRECTION ( 'NONE',  ( 0.7070776581709139474, 0.2891032514073391679, -0.6453375049857563717 ) ) ;
#130889=LINE ( 'NONE', #150475, #83259 ) ;
#130915=FACE_OUTER_BOUND ( 'NONE', #7776, .T. ) ;
#130917=AXIS2_PLACEMENT_3D ( 'NONE', #50687, #168144, #228082 ) ;
#130926=DIRECTION ( 'NONE',  ( 0.000000000000000000, -0.4088369013363280513, 0.9126074666063769270 ) ) ;
#130932=EDGE_LOOP ( 'NONE', ( #257832, #204403, #241682, #173828 ) ) ;
#130991=VECTOR ( 'NONE', #122844, 1000.000000000000114 ) ;
#131041=DIRECTION ( 'NONE',  ( 0.000000000000000000, 0.8412123295017488456, 0.5407049257166434142 ) ) ;
#131051=ORIENTED_EDGE ( 'NONE', *, *, #208423, .T. ) ;
#131070=DIRECTION ( 'NONE',  ( 1.000000000000000000, 0.000000000000000000, 0.000000000000000000 ) ) ;
#131078=CARTESIAN_POINT ( 'NONE',  ( -22.50000000000000000, 31.80488924422933295, -238.9605610896540213 ) ) ;
#131079=VERTEX_POINT ( 'NONE', #76186 ) ;
#131085=ORIENTED_EDGE ( 'NONE', *, *, #205887, .F. ) ;
#131092=ORIENTED_EDGE ( 'NONE', *, *, #86128, .T. ) ;
#131097=CARTESIAN_POINT ( 'NONE',  ( -18.59999999999999787, 44.47083028126616000, -247.4212268238128161 ) ) ;
#131110=CARTESIAN_POINT ( 'NONE',  ( 22.49436431346199683, 31.83493791481901880, -238.9466831125989756 ) ) ;
#131126=AXIS2_PLACEMENT_3D ( 'NONE', #239658, #220092, #20625 ) ;
#131205=CARTESIAN_POINT ( 'NONE',  ( -18.39999999999999858, 77.17949092533254429, -241.9177572069595783 ) ) ;
#131233=EDGE_CURVE ( 'NONE', #69371, #217944, #149965, .T. ) ;
#131239=CARTESIAN_POINT ( 'NONE',  ( 18.59999999999999787, 74.95904887477786360, -233.7774272632847783 ) ) ;
#131241=CARTESIAN_POINT ( 'NONE',  ( -20.85000000000000142, 67.32498692201720303, -236.1680459564915679 ) ) ;
#131262=CIRCLE ( 'NONE', #68730, 12.87499999999999289 ) ;
#131273=AXIS2_PLACEMENT_3D ( 'NONE', #75974, #56389, #13441 ) ;
#131290=EDGE_CURVE ( 'NONE', #82665, #167448, #112356, .T. ) ;
#131308=DIRECTION ( 'NONE',  ( -1.000000000000000000, 0.000000000000000000, 0.000000000000000000 ) ) ;
#131314=CARTESIAN_POINT ( 'NONE',  ( 22.39999999999999503, 31.89597452117651244, -238.9192857152811484 ) ) ;
#131318=ORIENTED_EDGE ( 'NONE', *, *, #47806, .T. ) ;
#131332=CARTESIAN_POINT ( 'NONE',  ( 21.14999999999999858, 43.45833571831320796, -234.7657887233443716 ) ) ;
#131340=CARTESIAN_POINT ( 'NONE',  ( -23.15000000000000213, 51.38014393322265505, -230.1906178717505611 ) ) ;
#131354=TOROIDAL_SURFACE ( 'NONE', #235395, 0.2000000000000000111, 0.1000000000000000056 ) ;
#131358=EDGE_CURVE ( 'NONE', #9091, #37194, #171028, .T. ) ;
#131384=ORIENTED_EDGE ( 'NONE', *, *, #186560, .T. ) ;
#131403=DIRECTION ( 'NONE',  ( -3.890533409366484652E-14, 0.9579639084728162057, 0.2868887416115976086 ) ) ;
#131460=CIRCLE ( 'NONE', #152530, 0.2000000000000118627 ) ;
#131475=DIRECTION ( 'NONE',  ( -0.000000000000000000, -0.4088369013363281068, 0.9126074666063770380 ) ) ;
#131492=FACE_OUTER_BOUND ( 'NONE', #118065, .T. ) ;
#131500=ADVANCED_FACE ( 'NONE', ( #232430 ), #133313, .T. ) ;
#131506=DIRECTION ( 'NONE',  ( 0.000000000000000000, 0.3970902486047481750, -0.9177795674686920480 ) ) ;
#131537=VECTOR ( 'NONE', #99927, 1000.000000000000114 ) ;
#131543=CARTESIAN_POINT ( 'NONE',  ( -21.37071067811865532, 44.53876154244880325, -237.1775198342045314 ) ) ;
#131559=DIRECTION ( 'NONE',  ( 0.000000000000000000, -0.9126074666063729302, -0.4088369013363370996 ) ) ;
#131579=CARTESIAN_POINT ( 'NONE',  ( -20.64999999999999858, 47.91013932883114990, -242.3192343197862044 ) ) ;
#131588=LINE ( 'NONE', #190299, #89334 ) ;
#131642=CARTESIAN_POINT ( 'NONE',  ( -21.07928932188134041, 30.84304088367084162, -252.0482413927653340 ) ) ;
#131654=DIRECTION ( 'NONE',  ( 0.000000000000000000, -0.9126074666063660468, -0.4088369013363524762 ) ) ;
#131668=ORIENTED_EDGE ( 'NONE', *, *, #198490, .T. ) ;
#131689=FACE_OUTER_BOUND ( 'NONE', #92536, .T. ) ;
#131691=CIRCLE ( 'NONE', #139861, 0.2000000000000118627 ) ;
#131789=CYLINDRICAL_SURFACE ( 'NONE', #115828, 2.000000000000012879 ) ;
#131815=CARTESIAN_POINT ( 'NONE',  ( -18.50000000000000000, 68.00366762990590530, -224.2307594727497815 ) ) ;
#131817=CARTESIAN_POINT ( 'NONE',  ( 21.05000000000000071, 62.24653955602229161, -247.9500786234238490 ) ) ;
#131835=DIRECTION ( 'NONE',  ( 1.000000000000000000, -1.335000415235278971E-16, 2.979993593738921214E-16 ) ) ;
#131862=DIRECTION ( 'NONE',  ( 1.000000000000000000, 0.000000000000000000, -0.000000000000000000 ) ) ;
#131870=DIRECTION ( 'NONE',  ( -1.836970198721029934E-16, -0.4088369013363281068, 0.9126074666063770380 ) ) ;
#131894=VERTEX_POINT ( 'NONE', #58581 ) ;
#131920=EDGE_LOOP ( 'NONE', ( #180317, #115899, #1720, #114781 ) ) ;
#132026=DIRECTION ( 'NONE',  ( 0.000000000000000000, 0.9126074666063660468, 0.4088369013363524762 ) ) ;
#132043=AXIS2_PLACEMENT_3D ( 'NONE', #211484, #228493, #49834 ) ;
#132057=CARTESIAN_POINT ( 'NONE',  ( 23.24999999999999289, 56.06656052939784729, -228.0911609752645290 ) ) ;
#132060=DIRECTION ( 'NONE',  ( 0.000000000000000000, 0.4088369013361243254, -0.9126074666064684093 ) ) ;
#132068=ORIENTED_EDGE ( 'NONE', *, *, #49358, .T. ) ;
#132134=DIRECTION ( 'NONE',  ( 1.000000000000000000, 0.000000000000000000, 0.000000000000000000 ) ) ;
#132135=DIRECTION ( 'NONE',  ( 0.000000000000000000, -0.9955484899852801162, 0.09425075112713271475 ) ) ;
#132187=VECTOR ( 'NONE', #88578, 1000.000000000000114 ) ;
#132200=PLANE ( 'NONE',  #215381 ) ;
#132201=DIRECTION ( 'NONE',  ( -1.000000000000000000, -0.000000000000000000, 0.000000000000000000 ) ) ;
#132252=FACE_OUTER_BOUND ( 'NONE', #61071, .T. ) ;
#132255=DIRECTION ( 'NONE',  ( 0.000000000000000000, 0.9126074666063769270, 0.4088369013363280513 ) ) ;
#132265=ORIENTED_EDGE ( 'NONE', *, *, #54609, .T. ) ;
#132305=DIRECTION ( 'NONE',  ( 1.000000000000000000, 0.000000000000000000, 0.000000000000000000 ) ) ;
#132323=DIRECTION ( 'NONE',  ( 0.000000000000000000, -0.4088369013363280513, 0.9126074666063769270 ) ) ;
#132340=CARTESIAN_POINT ( 'NONE',  ( -21.04999999999999716, 30.86294145740712125, -252.1314134296355007 ) ) ;
#132375=EDGE_CURVE ( 'NONE', #217944, #95060, #108813, .T. ) ;
#132386=DIRECTION ( 'NONE',  ( 0.000000000000000000, -0.8371762388950346745, -0.5469332180710581026 ) ) ;
#132400=DIRECTION ( 'NONE',  ( 1.000000000000000000, 0.000000000000000000, 0.000000000000000000 ) ) ;
#132404=EDGE_LOOP ( 'NONE', ( #11678, #188606, #94697, #65833 ) ) ;
#132419=DIRECTION ( 'NONE',  ( 0.000000000000000000, 0.9126074666063660468, 0.4088369013363524762 ) ) ;
#132426=AXIS2_PLACEMENT_3D ( 'NONE', #85433, #81584, #120777 ) ;
#132431=CARTESIAN_POINT ( 'NONE',  ( -20.95613430942438882, 38.11298866354308501, -236.0245638395625463 ) ) ;
#132463=ADVANCED_FACE ( 'NONE', ( #232578 ), #113884, .T. ) ;
#132465=EDGE_CURVE ( 'NONE', #198148, #91918, #21338, .T. ) ;
#132466=VERTEX_POINT ( 'NONE', #74802 ) ;
#132473=AXIS2_PLACEMENT_3D ( 'NONE', #182844, #218068, #44598 ) ;
#132474=VERTEX_POINT ( 'NONE', #154344 ) ;
#132490=DIRECTION ( 'NONE',  ( -1.000000000000000000, 0.000000000000000000, 0.000000000000000000 ) ) ;
#132538=ORIENTED_EDGE ( 'NONE', *, *, #120823, .F. ) ;
#132544=TOROIDAL_SURFACE ( 'NONE', #78362, 0.2000000000000000111, 0.1000000000000000056 ) ;
#132552=CIRCLE ( 'NONE', #224121, 11.64999999999999503 ) ;
#132595=PLANE ( 'NONE',  #20428 ) ;
#132616=EDGE_LOOP ( 'NONE', ( #116916, #62676, #55933 ) ) ;
#132632=EDGE_CURVE ( 'NONE', #92460, #99525, #159071, .T. ) ;
#132649=VECTOR ( 'NONE', #177950, 1000.000000000000114 ) ;
#132707=ORIENTED_EDGE ( 'NONE', *, *, #123947, .F. ) ;
#132722=EDGE_CURVE ( 'NONE', #249163, #2024, #38250, .T. ) ;
#132757=CARTESIAN_POINT ( 'NONE',  ( 21.14999999999999858, 44.33733722763473395, -236.4833033074485513 ) ) ;
#132781=AXIS2_PLACEMENT_3D ( 'NONE', #144986, #8075, #68034 ) ;
#132795=FACE_OUTER_BOUND ( 'NONE', #39853, .T. ) ;
#132805=CARTESIAN_POINT ( 'NONE',  ( -20.94999999999999929, 38.25685495413521409, -235.9601135138701693 ) ) ;
#132840=CIRCLE ( 'NONE', #20413, 0.1999999999999893807 ) ;
#132863=DIRECTION ( 'NONE',  ( 0.000000000000000000, 0.9126074666064177832, 0.4088369013362369020 ) ) ;
#132881=DIRECTION ( 'NONE',  ( -1.000000000000000000, 0.000000000000000000, 0.000000000000000000 ) ) ;
#132906=CIRCLE ( 'NONE', #191180, 0.09999999999999939493 ) ;
#132918=AXIS2_PLACEMENT_3D ( 'NONE', #41609, #195549, #215085 ) ;
#132939=CYLINDRICAL_SURFACE ( 'NONE', #181938, 7.899999999999995914 ) ;
#132958=ORIENTED_EDGE ( 'NONE', *, *, #119169, .F. ) ;
#132976=VERTEX_POINT ( 'NONE', #236084 ) ;
#132978=ORIENTED_EDGE ( 'NONE', *, *, #97833, .F. ) ;
#132984=AXIS2_PLACEMENT_3D ( 'NONE', #136567, #156177, #235671 ) ;
#133018=DIRECTION ( 'NONE',  ( 0.000000000000000000, 0.9126074666063813678, 0.4088369013363182813 ) ) ;
#133027=PLANE ( 'NONE',  #228723 ) ;
#133061=DIRECTION ( 'NONE',  ( -0.000000000000000000, 0.4088369013363281068, -0.9126074666063770380 ) ) ;
#133085=DIRECTION ( 'NONE',  ( 0.000000000000000000, -0.9126074666063753726, -0.4088369013363320481 ) ) ;
#133086=CARTESIAN_POINT ( 'NONE',  ( -18.59999999999999787, 38.29773864426885410, -236.0513742605307925 ) ) ;
#133091=DIRECTION ( 'NONE',  ( -0.000000000000000000, -0.4088369013363281623, 0.9126074666063771490 ) ) ;
#133131=ORIENTED_EDGE ( 'NONE', *, *, #182801, .T. ) ;
#133134=CIRCLE ( 'NONE', #257976, 11.65000000000000213 ) ;
#133142=ORIENTED_EDGE ( 'NONE', *, *, #46394, .T. ) ;
#133150=CIRCLE ( 'NONE', #66513, 0.09999999999999939493 ) ;
#133152=B_SPLINE_CURVE_WITH_KNOTS ( 'NONE', 3,
 ( #178983, #156842, #236344, #58959, #177690, #199810, #18591 ),
 .UNSPECIFIED., .F., .F.,
 ( 4, 3, 4 ),
 ( 0.000000000000000000, 1.860045280645600797E-05, 5.251155757304835946E-05 ),
 .UNSPECIFIED. ) ;
#133162=ORIENTED_EDGE ( 'NONE', *, *, #232768, .T. ) ;
#133199=TOROIDAL_SURFACE ( 'NONE', #237433, 11.70000000000000462, 0.1000000000000000056 ) ;
#133200=EDGE_LOOP ( 'NONE', ( #227208, #14107, #1269, #106559 ) ) ;
#133235=EDGE_CURVE ( 'NONE', #55374, #7110, #12910, .T. ) ;
#133270=DIRECTION ( 'NONE',  ( 0.000000000000000000, 0.4088369013363241100, -0.9126074666063788143 ) ) ;
#133300=ORIENTED_EDGE ( 'NONE', *, *, #23161, .F. ) ;
#133308=CARTESIAN_POINT ( 'NONE',  ( 18.39999999999999858, 77.43243075322052960, -241.6948671442531520 ) ) ;
#133313=CYLINDRICAL_SURFACE ( 'NONE', #12589, 0.09999999999999609201 ) ;
#133345=LINE ( 'NONE', #48655, #194794 ) ;
#133361=( NAMED_UNIT ( * ) PLANE_ANGLE_UNIT ( ) SI_UNIT ( $, .RADIAN. ) );
#133380=AXIS2_PLACEMENT_3D ( 'NONE', #235093, #58978, #18605 ) ;
#133388=DIRECTION ( 'NONE',  ( -1.000000000000000000, -0.000000000000000000, -0.000000000000000000 ) ) ;
#133394=DIRECTION ( 'NONE',  ( 4.026293107431335996E-15, -0.09425075112712516523, -0.9955484899852807823 ) ) ;
#133422=CARTESIAN_POINT ( 'NONE',  ( -23.25000000000000000, 67.74990736105834799, -227.9721689390126755 ) ) ;
#133508=VERTEX_POINT ( 'NONE', #4832 ) ;
#133521=DIRECTION ( 'NONE',  ( 0.000000000000000000, 0.4088369013363281623, -0.9126074666063771490 ) ) ;
#133541=EDGE_CURVE ( 'NONE', #173788, #84389, #47819, .T. ) ;
#133547=ORIENTED_EDGE ( 'NONE', *, *, #78740, .T. ) ;
#133573=DIRECTION ( 'NONE',  ( 0.000000000000000000, 0.5859227990963362664, 0.8103668758649469339 ) ) ;
#133582=CIRCLE ( 'NONE', #154472, 0.1000000000000024342 ) ;
#133651=CARTESIAN_POINT ( 'NONE',  ( -18.50000000000000000, 46.62132166459547733, -243.0426574061995950 ) ) ;
#133691=VERTEX_POINT ( 'NONE', #213319 ) ;
#133751=DIRECTION ( 'NONE',  ( -0.000000000000000000, -0.9126074666063770380, -0.4088369013363281068 ) ) ;
#133755=VERTEX_POINT ( 'NONE', #212069 ) ;
#133778=AXIS2_PLACEMENT_3D ( 'NONE', #160931, #104755, #99623 ) ;
#133807=CARTESIAN_POINT ( 'NONE',  ( -18.50000000000000000, 22.19492904189240079, -246.0046379724989549 ) ) ;
#133817=ORIENTED_EDGE ( 'NONE', *, *, #123759, .F. ) ;
#133826=DIRECTION ( 'NONE',  ( -1.000000000000000000, -0.000000000000000000, 0.000000000000000000 ) ) ;
#133828=ADVANCED_FACE ( 'NONE', ( #60659 ), #230315, .T. ) ;
#133868=CARTESIAN_POINT ( 'NONE',  ( -21.05000000000000071, 34.01125473725046078, -243.8802146427659352 ) ) ;
#133869=CARTESIAN_POINT ( 'NONE',  ( 20.94999999999999574, 42.96458825698139350, -239.5490660745215337 ) ) ;
#133897=CARTESIAN_POINT ( 'NONE',  ( 21.14261333020286315, 43.45739530927919247, -234.7636895383062949 ) ) ;
#133898=ORIENTED_EDGE ( 'NONE', *, *, #51948, .F. ) ;
#133907=DIRECTION ( 'NONE',  ( 0.000000000000000000, -0.4088369013363276072, 0.9126074666063772600 ) ) ;
#133947=FACE_OUTER_BOUND ( 'NONE', #40620, .T. ) ;
#133957=ADVANCED_FACE ( 'NONE', ( #251835 ), #73242, .F. ) ;
#133958=CYLINDRICAL_SURFACE ( 'NONE', #196542, 0.4999999999999944489 ) ;
#133960=ORIENTED_EDGE ( 'NONE', *, *, #148291, .F. ) ;
#133963=CARTESIAN_POINT ( 'NONE',  ( -21.00857864376268935, 38.23914636435921466, -236.1324109481172684 ) ) ;
#133995=ORIENTED_EDGE ( 'NONE', *, *, #101296, .T. ) ;
#134032=CARTESIAN_POINT ( 'NONE',  ( -21.44999999999999929, 44.96555909964510533, -237.8856228368455845 ) ) ;
#134057=DIRECTION ( 'NONE',  ( -1.000000000000000000, 0.000000000000000000, 0.000000000000000000 ) ) ;
#134059=ORIENTED_EDGE ( 'NONE', *, *, #52623, .F. ) ;
#134064=DIRECTION ( 'NONE',  ( 2.428612866367594051E-13, 0.4205162045344795763, -0.9072850278296868964 ) ) ;
#134069=CARTESIAN_POINT ( 'NONE',  ( 21.05000000000000071, 67.23127455305835554, -235.8551265064784559 ) ) ;
#134085=CARTESIAN_POINT ( 'NONE',  ( -21.14999999999999858, 41.42187432231295219, -260.1830396872097140 ) ) ;
#134109=FACE_OUTER_BOUND ( 'NONE', #241510, .T. ) ;
#134124=EDGE_CURVE ( 'NONE', #12219, #233644, #138336, .T. ) ;
#134127=DIRECTION ( 'NONE',  ( 1.875376730785737966E-16, 0.4088369013363281068, -0.9126074666063770380 ) ) ;
#134140=EDGE_LOOP ( 'NONE', ( #51483, #236739, #194235, #207290 ) ) ;
#134156=AXIS2_PLACEMENT_3D ( 'NONE', #98971, #157751, #163803 ) ;
#134164=EDGE_LOOP ( 'NONE', ( #253993, #195336, #90234, #2343 ) ) ;
#134216=EDGE_CURVE ( 'NONE', #225601, #41121, #130553, .T. ) ;
#134218=FACE_OUTER_BOUND ( 'NONE', #236176, .T. ) ;
#134284=DIRECTION ( 'NONE',  ( -1.000000000000000000, 7.510212038922847255E-17, -1.676432719286211941E-16 ) ) ;
#134305=CARTESIAN_POINT ( 'NONE',  ( -22.59066674512241235, 31.82725254005515936, -238.8404961800037256 ) ) ;
#134345=CIRCLE ( 'NONE', #121907, 0.1000000000000024342 ) ;
#134363=DIRECTION ( 'NONE',  ( -1.000000000000000000, -0.000000000000000000, -0.000000000000000000 ) ) ;
#134368=DIRECTION ( 'NONE',  ( 0.000000000000000000, -0.9126074666063769270, -0.4088369013363280513 ) ) ;
#134393=DIRECTION ( 'NONE',  ( 0.000000000000000000, -0.9126074666063769270, -0.4088369013363280513 ) ) ;
#134457=VERTEX_POINT ( 'NONE', #230701 ) ;
#134471=CIRCLE ( 'NONE', #1197, 0.09999999999999771572 ) ;
#134481=LINE ( 'NONE', #229752, #233904 ) ;
#134499=DIRECTION ( 'NONE',  ( 1.000000000000000000, 0.000000000000000000, 0.000000000000000000 ) ) ;
#134509=ORIENTED_EDGE ( 'NONE', *, *, #205952, .F. ) ;
#134528=CARTESIAN_POINT ( 'NONE',  ( -20.94999999999999929, 44.06843597547145208, -258.9974126733344519 ) ) ;
#134548=ORIENTED_EDGE ( 'NONE', *, *, #66326, .T. ) ;
#134572=CARTESIAN_POINT ( 'NONE',  ( -20.94999999999999929, 47.95459712139159336, -246.5019368548292675 ) ) ;
#134609=AXIS2_PLACEMENT_3D ( 'NONE', #4959, #178526, #158964 ) ;
#134633=CARTESIAN_POINT ( 'NONE',  ( 21.05000000000000071, 30.73075574124490217, -252.3164853687435709 ) ) ;
#134674=AXIS2_PLACEMENT_3D ( 'NONE', #78666, #198624, #143782 ) ;
#134700=ORIENTED_EDGE ( 'NONE', *, *, #233119, .F. ) ;
#134718=TOROIDAL_SURFACE ( 'NONE', #63831, 2.100000000000002309, 0.1000000000000000056 ) ;
#134749=AXIS2_PLACEMENT_3D ( 'NONE', #233869, #250847, #211750 ) ;
#134798=FACE_OUTER_BOUND ( 'NONE', #222311, .T. ) ;
#134828=CARTESIAN_POINT ( 'NONE',  ( -23.15000000000000213, 67.23127455305835554, -235.8551265064784559 ) ) ;
#134841=TOROIDAL_SURFACE ( 'NONE', #205795, 0.2000000000000000111, 0.1000000000000000056 ) ;
#134869=DIRECTION ( 'NONE',  ( 0.000000000000000000, 0.9126074666063813678, 0.4088369013363182813 ) ) ;
#134878=DIRECTION ( 'NONE',  ( -2.840903330521632762E-16, 0.09425075112713271475, 0.9955484899852801162 ) ) ;
#134889=ORIENTED_EDGE ( 'NONE', *, *, #206192, .F. ) ;
#134895=DIRECTION ( 'NONE',  ( -0.7071067811865475727, 0.2890913453342130457, -0.6453109281988448354 ) ) ;
#134901=DIRECTION ( 'NONE',  ( -1.000000000000000000, -8.623019343401623015E-17, -8.389849937938898203E-16 ) ) ;
#134913=ORIENTED_EDGE ( 'NONE', *, *, #78851, .T. ) ;
#134919=EDGE_LOOP ( 'NONE', ( #171260, #192045, #17491, #79838 ) ) ;
#134926=AXIS2_PLACEMENT_3D ( 'NONE', #37550, #72841, #117075 ) ;
#134933=DIRECTION ( 'NONE',  ( 0.000000000000000000, 0.9126074666063769270, 0.4088369013363282733 ) ) ;
#134943=ADVANCED_FACE ( 'NONE', ( #54288 ), #213362, .T. ) ;
#134960=DIRECTION ( 'NONE',  ( -1.000000000000000000, -2.986185139342066933E-16, 6.665775143889695732E-16 ) ) ;
#134964=CARTESIAN_POINT ( 'NONE',  ( -21.05000000000000071, 44.47083028126616000, -247.4212268238128161 ) ) ;
#134973=DIRECTION ( 'NONE',  ( 7.304098846218134667E-16, -0.4088369013363281068, 0.9126074666063770380 ) ) ;
#134999=ORIENTED_EDGE ( 'NONE', *, *, #36417, .T. ) ;
#135001=EDGE_CURVE ( 'NONE', #9598, #186768, #255195, .T. ) ;
#135012=ORIENTED_EDGE ( 'NONE', *, *, #49583, .T. ) ;
#135028=EDGE_CURVE ( 'NONE', #197595, #245185, #192757, .T. ) ;
#135058=CARTESIAN_POINT ( 'NONE',  ( 18.59117750673696179, 68.11287320386161070, -224.1382462126928488 ) ) ;
#135060=CIRCLE ( 'NONE', #55759, 0.09999999999999609201 ) ;
#135085=ORIENTED_EDGE ( 'NONE', *, *, #122993, .F. ) ;
#135094=FACE_OUTER_BOUND ( 'NONE', #232153, .T. ) ;
#135102=CARTESIAN_POINT ( 'NONE',  ( 20.84999999999998721, 68.11287320386161070, -224.1382462126928488 ) ) ;
#135116=ORIENTED_EDGE ( 'NONE', *, *, #138635, .F. ) ;
#135160=DIRECTION ( 'NONE',  ( 0.000000000000000000, 0.000000000000000000, 1.000000000000000000 ) ) ;
#135167=ORIENTED_EDGE ( 'NONE', *, *, #150456, .F. ) ;
#135205=VECTOR ( 'NONE', #162343, 1000.000000000000000 ) ;
#135239=ORIENTED_EDGE ( 'NONE', *, *, #156055, .T. ) ;
#135240=SPHERICAL_SURFACE ( 'NONE', #128331, 0.1000000000000000056 ) ;
#135242=PLANE ( 'NONE',  #182055 ) ;
#135330=DIRECTION ( 'NONE',  ( 0.1538461538461656786, -0.4039696218773441982, 0.9017427047373420823 ) ) ;
#135460=ORIENTED_EDGE ( 'NONE', *, *, #64305, .T. ) ;
#135535=ADVANCED_FACE ( 'NONE', ( #171124 ), #164413, .T. ) ;
#135573=DIRECTION ( 'NONE',  ( 0.000000000000000000, -0.9126074666063545004, -0.4088369013363783999 ) ) ;
#135583=EDGE_CURVE ( 'NONE', #64123, #932, #2403, .T. ) ;
#135585=ORIENTED_EDGE ( 'NONE', *, *, #206725, .T. ) ;
#135591=CARTESIAN_POINT ( 'NONE',  ( -22.50014994443984406, 31.77938584364020258, -238.8622469772241175 ) ) ;
#135654=DIRECTION ( 'NONE',  ( 0.000000000000000000, 0.9126074666063660468, 0.4088369013363524762 ) ) ;
#135670=CARTESIAN_POINT ( 'NONE',  ( -21.04999999999999716, 30.84067272007213134, -252.2516193862038278 ) ) ;
#135676=DIRECTION ( 'NONE',  ( -1.000000000000000000, 1.207181226542539700E-16, -2.694675058168174199E-16 ) ) ;
#135679=VECTOR ( 'NONE', #27441, 1000.000000000000000 ) ;
#135693=EDGE_CURVE ( 'NONE', #24027, #41411, #161479, .T. ) ;
#135762=ORIENTED_EDGE ( 'NONE', *, *, #155446, .T. ) ;
#135807=DIRECTION ( 'NONE',  ( 0.000000000000000000, 0.9126074666063772600, 0.4088369013363273852 ) ) ;
#135818=EDGE_CURVE ( 'NONE', #7171, #24438, #243142, .T. ) ;
#135841=CYLINDRICAL_SURFACE ( 'NONE', #241404, 0.09999999999999939493 ) ;
#135864=DIRECTION ( 'NONE',  ( 0.000000000000000000, 0.9126074666063773710, 0.4088369013363272741 ) ) ;
#135866=AXIS2_PLACEMENT_3D ( 'NONE', #155850, #114121, #132419 ) ;
#135894=ADVANCED_FACE ( 'NONE', ( #118032 ), #162315, .F. ) ;
#135901=EDGE_LOOP ( 'NONE', ( #150501, #73265, #41425, #188500 ) ) ;
#135917=CARTESIAN_POINT ( 'NONE',  ( 18.39999999999999858, 77.26488334054519669, -241.9697969554615611 ) ) ;
#135925=EDGE_CURVE ( 'NONE', #10431, #91860, #139249, .T. ) ;
#135926=ORIENTED_EDGE ( 'NONE', *, *, #224798, .T. ) ;
#135944=EDGE_CURVE ( 'NONE', #60871, #85465, #18483, .T. ) ;
#135958=DIRECTION ( 'NONE',  ( 0.000000000000000000, -0.4088369013363280513, 0.9126074666063769270 ) ) ;
#135960=ORIENTED_EDGE ( 'NONE', *, *, #63146, .F. ) ;
#136026=EDGE_CURVE ( 'NONE', #133691, #21323, #202704, .T. ) ;
#136034=EDGE_CURVE ( 'NONE', #15348, #64826, #36936, .T. ) ;
#136047=ORIENTED_EDGE ( 'NONE', *, *, #63315, .T. ) ;
#136054=VERTEX_POINT ( 'NONE', #243114 ) ;
#136077=TOROIDAL_SURFACE ( 'NONE', #202738, 0.2000000000000000111, 0.1000000000000000056 ) ;
#136081=VERTEX_POINT ( 'NONE', #217745 ) ;
#136098=AXIS2_PLACEMENT_3D ( 'NONE', #34446, #158254, #193502 ) ;
#136121=LINE ( 'NONE', #235247, #248649 ) ;
#136133=CARTESIAN_POINT ( 'NONE',  ( 18.50000000000000000, 46.96039402156216624, -255.3459641718773128 ) ) ;
#136181=( BOUNDED_CURVE ( )  B_SPLINE_CURVE ( 3, ( #199572, #57447, #237390, #58718 ),
 .UNSPECIFIED., .F., .F. ) 
 B_SPLINE_CURVE_WITH_KNOTS ( ( 4, 4 ),
 ( 4.712388980384690562, 6.283185307179586232 ),
 .UNSPECIFIED. ) 
 CURVE ( )  GEOMETRIC_REPRESENTATION_ITEM ( )  RATIONAL_B_SPLINE_CURVE ( ( 1.000000000000000000, 0.8047378541243652705, 0.8047378541243652705, 1.000000000000000000 ) ) 
 REPRESENTATION_ITEM ( '' )  );
#136190=CARTESIAN_POINT ( 'NONE',  ( -21.05000000000000071, 36.65892442174472876, -249.5511627012454596 ) ) ;
#136209=ADVANCED_FACE ( 'NONE', ( #162953 ), #89379, .F. ) ;
#136219=EDGE_CURVE ( 'NONE', #36016, #228170, #93666, .T. ) ;
#136232=DIRECTION ( 'NONE',  ( 1.000000000000000000, 0.000000000000000000, 0.000000000000000000 ) ) ;
#136238=ORIENTED_EDGE ( 'NONE', *, *, #118669, .T. ) ;
#136258=DIRECTION ( 'NONE',  ( 0.000000000000000000, 0.9126074666063891394, 0.4088369013363010729 ) ) ;
#136281=DIRECTION ( 'NONE',  ( 0.000000000000000000, 0.9126074666064812879, 0.4088369013360954596 ) ) ;
#136338=EDGE_LOOP ( 'NONE', ( #11476, #156908, #200282, #47609 ) ) ;
#136341=DIRECTION ( 'NONE',  ( -1.000000000000000000, -0.000000000000000000, 0.000000000000000000 ) ) ;
#136382=CARTESIAN_POINT ( 'NONE',  ( 21.05000000000000071, 43.51422117117169108, -240.0698702536254530 ) ) ;
#136395=CARTESIAN_POINT ( 'NONE',  ( 22.39999999999999503, 25.97741635855165754, -254.4468634167653249 ) ) ;
#136396=AXIS2_PLACEMENT_3D ( 'NONE', #248718, #116589, #177864 ) ;
#136400=CARTESIAN_POINT ( 'NONE',  ( -20.94999999999999929, 69.20602499728043711, -247.8456586332460176 ) ) ;
#136432=CARTESIAN_POINT ( 'NONE',  ( -23.25000000000000000, 67.23127455305835554, -235.8551265064784559 ) ) ;
#136436=CIRCLE ( 'NONE', #40830, 0.1000000000000024342 ) ;
#136445=FACE_OUTER_BOUND ( 'NONE', #190863, .T. ) ;
#136446=ADVANCED_FACE ( 'NONE', ( #194067 ), #31163, .T. ) ;
#136451=ORIENTED_EDGE ( 'NONE', *, *, #93828, .F. ) ;
#136481=AXIS2_PLACEMENT_3D ( 'NONE', #107345, #65653, #185609 ) ;
#136514=AXIS2_PLACEMENT_3D ( 'NONE', #101969, #159423, #98113 ) ;
#136515=CARTESIAN_POINT ( 'NONE',  ( 20.94999999999999574, 40.74071615341952679, -237.9411309446948337 ) ) ;
#136518=DIRECTION ( 'NONE',  ( 0.000000000000000000, -0.09425075112712516523, -0.9955484899852807823 ) ) ;
#136525=DIRECTION ( 'NONE',  ( 0.000000000000000000, 0.9126074666063773710, 0.4088369013363269966 ) ) ;
#136533=CARTESIAN_POINT ( 'NONE',  ( -22.49917693094574034, 25.99238864986915942, -254.2362476092667123 ) ) ;
#136534=CIRCLE ( 'NONE', #36636, 0.09999999999999538425 ) ;
#136538=ADVANCED_FACE ( 'NONE', ( #41410 ), #235726, .F. ) ;
#136547=DIRECTION ( 'NONE',  ( 1.000000000000000000, 0.000000000000000000, 0.000000000000000000 ) ) ;
#136552=CARTESIAN_POINT ( 'NONE',  ( -18.58744394320989102, 77.36894789412127693, -241.7960489703176563 ) ) ;
#136558=( BOUNDED_SURFACE ( )  B_SPLINE_SURFACE ( 3, 2, ( 
 ( #65657, #145186, #224722 ),
 ( #9532, #6968, #206459 ),
 ( #89066, #87772, #48659 ),
 ( #30406, #188188, #107349 ),
 ( #186925, #185614, #163483 ),
 ( #8272, #244287, #167363 ) ),
 .UNSPECIFIED., .F., .F., .T. ) 
 B_SPLINE_SURFACE_WITH_KNOTS ( ( 4, 2, 4 ),
 ( 3, 3 ),
 ( 0.0001381104793128072085, 0.0002947094729387660984, 0.0004513084665647249883 ),
 ( 0.000000000000000000, 1.000000000000000000 ),
 .UNSPECIFIED. ) 
 GEOMETRIC_REPRESENTATION_ITEM ( )  RATIONAL_B_SPLINE_SURFACE ( (
 ( 1.000000000000000000, 0.7071067811866307284, 1.000000000000000000),
 ( 1.000000000000000000, 0.6919563088109071947, 1.000000000000000000),
 ( 1.000000000000000000, 0.6959445945703722769, 1.000000000000000000),
 ( 1.000000000000000000, 0.7137882985326097218, 1.000000000000000000),
 ( 1.000000000000000000, 0.7257496306086942406, 1.000000000000000000),
 ( 1.000000000000000000, 0.7250110520819876836, 1.000000000000000000) ) ) 
 REPRESENTATION_ITEM ( '' )  SURFACE ( )  );
#136559=CIRCLE ( 'NONE', #244902, 0.1000000000000024342 ) ;
#136567=CARTESIAN_POINT ( 'NONE',  ( -20.85000000000000142, 78.48087866980282001, -232.8271061603568910 ) ) ;
#136568=VERTEX_POINT ( 'NONE', #77935 ) ;
#136573=DIRECTION ( 'NONE',  ( 1.000000000000000000, 0.000000000000000000, 0.000000000000000000 ) ) ;
#136599=CARTESIAN_POINT ( 'NONE',  ( 20.94999999999999929, 56.27731819600170837, -227.9967441372480437 ) ) ;
#136643=VECTOR ( 'NONE', #44839, 1000.000000000000114 ) ;
#136658=ORIENTED_EDGE ( 'NONE', *, *, #95176, .T. ) ;
#136675=CARTESIAN_POINT ( 'NONE',  ( -22.47007471830799474, 29.61294623328925013, -252.7076741202934898 ) ) ;
#136682=ORIENTED_EDGE ( 'NONE', *, *, #194948, .T. ) ;
#136686=AXIS2_PLACEMENT_3D ( 'NONE', #161474, #257927, #179743 ) ;
#136696=DIRECTION ( 'NONE',  ( 1.000000000000000000, 0.000000000000000000, 0.000000000000000000 ) ) ;
#136732=DIRECTION ( 'NONE',  ( 0.000000000000000000, 0.9126074666063107577, 0.4088369013364760440 ) ) ;
#136742=CIRCLE ( 'NONE', #203412, 0.09999999999999609201 ) ;
#136753=EDGE_CURVE ( 'NONE', #220739, #126259, #146878, .T. ) ;
#136772=DIRECTION ( 'NONE',  ( -1.000000000000000000, 0.000000000000000000, 0.000000000000000000 ) ) ;
#136779=CARTESIAN_POINT ( 'NONE',  ( 22.24259225415828212, 29.78122419289665146, -252.5237351003267179 ) ) ;
#136784=DIRECTION ( 'NONE',  ( 1.000000000000000000, 0.000000000000000000, 0.000000000000000000 ) ) ;
#136785=ORIENTED_EDGE ( 'NONE', *, *, #9217, .F. ) ;
#136798=EDGE_LOOP ( 'NONE', ( #157737, #110277, #41588, #38664 ) ) ;
#136804=CARTESIAN_POINT ( 'NONE',  ( -18.50000000000000000, 25.65398771707549841, -256.3298696899526021 ) ) ;
#136829=EDGE_LOOP ( 'NONE', ( #100800, #109625, #49721, #13024 ) ) ;
#136845=ORIENTED_EDGE ( 'NONE', *, *, #144736, .F. ) ;
#136888=DIRECTION ( 'NONE',  ( 0.000000000000000000, 0.9126074666063385132, 0.4088369013364143156 ) ) ;
#136891=CARTESIAN_POINT ( 'NONE',  ( -22.48660254037843131, 31.85034414784621148, -238.9397275603479898 ) ) ;
#136896=EDGE_CURVE ( 'NONE', #79382, #219396, #222841, .T. ) ;
#136900=DIRECTION ( 'NONE',  ( 1.000000000000000000, 0.000000000000000000, 0.000000000000000000 ) ) ;
#136906=ADVANCED_FACE ( 'NONE', ( #219389 ), #64616, .T. ) ;
#136916=AXIS2_PLACEMENT_3D ( 'NONE', #86705, #209244, #30639 ) ;
#136940=ORIENTED_EDGE ( 'NONE', *, *, #53851, .F. ) ;
#136974=ADVANCED_FACE ( 'NONE', ( #138553 ), #59010, .T. ) ;
#136980=CARTESIAN_POINT ( 'NONE',  ( 20.85000000000000142, 71.99422445362657186, -246.4870034924427671 ) ) ;
#137024=ORIENTED_EDGE ( 'NONE', *, *, #173080, .T. ) ;
#137055=ORIENTED_EDGE ( 'NONE', *, *, #159800, .F. ) ;
#137076=ORIENTED_EDGE ( 'NONE', *, *, #42962, .F. ) ;
#137080=ORIENTED_EDGE ( 'NONE', *, *, #175385, .T. ) ;
#137114=DIRECTION ( 'NONE',  ( 1.000000000000000000, 0.000000000000000000, 0.000000000000000000 ) ) ;
#137130=CARTESIAN_POINT ( 'NONE',  ( -21.07928932188134041, 36.65892442174472876, -249.5511627012454596 ) ) ;
#137142=DIRECTION ( 'NONE',  ( 0.000000000000000000, 0.2818822000686748708, -0.9594490217225944972 ) ) ;
#137145=DIRECTION ( 'NONE',  ( 1.000000000000000000, 0.000000000000000000, -0.000000000000000000 ) ) ;
#137168=LINE ( 'NONE', #139718, #35906 ) ;
#137185=DIRECTION ( 'NONE',  ( 1.000000000000000000, 0.000000000000000000, 0.000000000000000000 ) ) ;
#137202=CARTESIAN_POINT ( 'NONE',  ( 23.14999999999999858, 54.46551753941606222, -236.3409998116131021 ) ) ;
#137206=CARTESIAN_POINT ( 'NONE',  ( -20.94999999999999929, 44.06843597547145208, -258.9974126733344519 ) ) ;
#137222=FACE_OUTER_BOUND ( 'NONE', #80944, .T. ) ;
#137234=FACE_OUTER_BOUND ( 'NONE', #162970, .T. ) ;
#137244=ORIENTED_EDGE ( 'NONE', *, *, #38628, .T. ) ;
#137265=ORIENTED_EDGE ( 'NONE', *, *, #67567, .T. ) ;
#137316=EDGE_CURVE ( 'NONE', #38307, #246198, #168905, .T. ) ;
#137317=ADVANCED_FACE ( 'NONE', ( #23502 ), #102980, .F. ) ;
#137324=VERTEX_POINT ( 'NONE', #80846 ) ;
#137353=EDGE_CURVE ( 'NONE', #91403, #225601, #196953, .T. ) ;
#137404=VECTOR ( 'NONE', #134960, 1000.000000000000000 ) ;
#137413=DIRECTION ( 'NONE',  ( 0.000000000000000000, -0.2818822000685679008, 0.9594490217226259166 ) ) ;
#137415=CIRCLE ( 'NONE', #95899, 4.050000000000014921 ) ;
#137419=DIRECTION ( 'NONE',  ( -1.000000000000000000, -0.000000000000000000, -0.000000000000000000 ) ) ;
#137481=ORIENTED_EDGE ( 'NONE', *, *, #209252, .F. ) ;
#137487=VECTOR ( 'NONE', #253696, 1000.000000000000000 ) ;
#137536=AXIS2_PLACEMENT_3D ( 'NONE', #100276, #179859, #27220 ) ;
#137542=DIRECTION ( 'NONE',  ( 1.000000000000000000, 0.000000000000000000, -0.000000000000000000 ) ) ;
#137580=AXIS2_PLACEMENT_3D ( 'NONE', #181685, #195173, #215968 ) ;
#137637=CIRCLE ( 'NONE', #129299, 6.329289321881371500 ) ;
#137638=DIRECTION ( 'NONE',  ( 0.000000000000000000, -0.9126074666063768159, -0.4088369013363282178 ) ) ;
#137670=EDGE_CURVE ( 'NONE', #221119, #211199, #23176, .T. ) ;
#137726=ORIENTED_EDGE ( 'NONE', *, *, #18121, .F. ) ;
#137728=DIRECTION ( 'NONE',  ( 1.000000000000000000, 0.000000000000000000, 0.000000000000000000 ) ) ;
#137735=DIRECTION ( 'NONE',  ( 1.000000000000000000, -1.207181226542539700E-16, 2.694675058168174199E-16 ) ) ;
#137740=CARTESIAN_POINT ( 'NONE',  ( -23.25000000000000000, 67.23127455305835554, -235.8551265064784559 ) ) ;
#137768=DIRECTION ( 'NONE',  ( 0.000000000000000000, 0.9126074666063660468, 0.4088369013363524762 ) ) ;
#137770=ORIENTED_EDGE ( 'NONE', *, *, #204752, .F. ) ;
#137798=ORIENTED_EDGE ( 'NONE', *, *, #90470, .T. ) ;
#137810=CARTESIAN_POINT ( 'NONE',  ( 23.14999999999999858, 66.37271706025207152, -233.9386508266050839 ) ) ;
#137820=CYLINDRICAL_SURFACE ( 'NONE', #249000, 0.09999999999999939493 ) ;
#137823=EDGE_CURVE ( 'NONE', #212713, #100153, #64831, .T. ) ;
#137830=CARTESIAN_POINT ( 'NONE',  ( 21.05000000000000071, 34.07612324756792077, -243.5412266404783566 ) ) ;
#137837=CARTESIAN_POINT ( 'NONE',  ( -18.50000000000000000, 77.44184265367995579, -241.6694879557322793 ) ) ;
#137851=CARTESIAN_POINT ( 'NONE',  ( -18.46856557590792036, 47.01365916724044780, -255.2938488308768115 ) ) ;
#137862=ORIENTED_EDGE ( 'NONE', *, *, #3453, .T. ) ;
#137883=FACE_OUTER_BOUND ( 'NONE', #192218, .T. ) ;
#137890=ADVANCED_FACE ( 'NONE', ( #244747 ), #17986, .F. ) ;
#137910=CARTESIAN_POINT ( 'NONE',  ( 22.47071067811865319, 36.65892442174472876, -249.5511627012454596 ) ) ;
#137935=ORIENTED_EDGE ( 'NONE', *, *, #1983, .T. ) ;
#137950=ORIENTED_EDGE ( 'NONE', *, *, #183595, .F. ) ;
#137958=CIRCLE ( 'NONE', #54765, 0.1000000000000024342 ) ;
#137962=DIRECTION ( 'NONE',  ( 0.000000000000000000, 0.9126074666063774821, 0.4088369013363268301 ) ) ;
#137979=DIRECTION ( 'NONE',  ( 0.000000000000000000, -0.9656312546561486299, -0.2599159095384356855 ) ) ;
#137994=ORIENTED_EDGE ( 'NONE', *, *, #233798, .T. ) ;
#138077=ORIENTED_EDGE ( 'NONE', *, *, #145536, .F. ) ;
#138111=ORIENTED_EDGE ( 'NONE', *, *, #229565, .T. ) ;
#138132=DIRECTION ( 'NONE',  ( -2.812466655313720057E-14, -0.9594490217226113726, -0.2818822000686178608 ) ) ;
#138213=CARTESIAN_POINT ( 'NONE',  ( -18.44448725179913851, 77.16080881524374036, -241.8056823530271231 ) ) ;
#138246=DIRECTION ( 'NONE',  ( 1.000000000000000000, 0.000000000000000000, 0.000000000000000000 ) ) ;
#138250=EDGE_LOOP ( 'NONE', ( #39260, #116997, #234728, #123230 ) ) ;
#138264=CYLINDRICAL_SURFACE ( 'NONE', #31572, 0.09999999999999939493 ) ;
#138284=VERTEX_POINT ( 'NONE', #170103 ) ;
#138290=ORIENTED_EDGE ( 'NONE', *, *, #128876, .T. ) ;
#138293=CARTESIAN_POINT ( 'NONE',  ( 22.39999999999999503, 29.54900078958455367, -252.7363208912387051 ) ) ;
#138308=ORIENTED_EDGE ( 'NONE', *, *, #173834, .F. ) ;
#138328=CARTESIAN_POINT ( 'NONE',  ( -18.59999999999999787, 38.29773864426885410, -236.0513742605307925 ) ) ;
#138336=CIRCLE ( 'NONE', #5619, 12.87499999999999112 ) ;
#138345=CARTESIAN_POINT ( 'NONE',  ( 18.59999999999999432, 43.57568952063339651, -245.1784935019914826 ) ) ;
#138346=ORIENTED_EDGE ( 'NONE', *, *, #68311, .T. ) ;
#138375=AXIS2_PLACEMENT_3D ( 'NONE', #138513, #218058, #118998 ) ;
#138397=CARTESIAN_POINT ( 'NONE',  ( 18.49999999999999645, 47.89822068137787170, -246.3100470504847692 ) ) ;
#138414=CARTESIAN_POINT ( 'NONE',  ( 18.49505832270840244, 47.08691893723204913, -255.2213761142054125 ) ) ;
#138426=AXIS2_PLACEMENT_3D ( 'NONE', #156454, #39054, #36496 ) ;
#138438=ORIENTED_EDGE ( 'NONE', *, *, #238528, .T. ) ;
#138459=EDGE_CURVE ( 'NONE', #66990, #43171, #213817, .T. ) ;
#138483=CIRCLE ( 'NONE', #217594, 0.09999999999999542588 ) ;
#138513=CARTESIAN_POINT ( 'NONE',  ( -18.59999999999999787, 43.57568952063339651, -245.1784935019914826 ) ) ;
#138521=CARTESIAN_POINT ( 'NONE',  ( 23.14999999999999858, 53.86595165227826243, -236.3638196928718855 ) ) ;
#138553=FACE_OUTER_BOUND ( 'NONE', #70316, .T. ) ;
#138623=LINE ( 'NONE', #124248, #24183 ) ;
#138627=CYLINDRICAL_SURFACE ( 'NONE', #161905, 0.4999999999999944489 ) ;
#138635=EDGE_CURVE ( 'NONE', #178504, #198869, #251529, .T. ) ;
#138666=DIRECTION ( 'NONE',  ( -1.000000000000000000, -0.000000000000000000, 0.000000000000000000 ) ) ;
#138671=DIRECTION ( 'NONE',  ( 2.342056488767302165E-15, 0.9594490217226113726, 0.2818822000686178608 ) ) ;
#138672=CARTESIAN_POINT ( 'NONE',  ( 21.08832698747859169, 44.23125050195789498, -236.5431486773145480 ) ) ;
#138691=DIRECTION ( 'NONE',  ( 1.000000000000000000, -7.667232114526941871E-17, 1.711482807214921537E-16 ) ) ;
#138706=CARTESIAN_POINT ( 'NONE',  ( -21.04999999999999716, 34.09556617704311776, -243.7880827679370270 ) ) ;
#138744=FACE_OUTER_BOUND ( 'NONE', #40621, .T. ) ;
#138764=ADVANCED_FACE ( 'NONE', ( #41494 ), #179714, .F. ) ;
#138786=LINE ( 'NONE', #78833, #75578 ) ;
#138798=CARTESIAN_POINT ( 'NONE',  ( -18.50000000000000000, 52.13794731297493712, -232.3713824252124880 ) ) ;
#138800=LINE ( 'NONE', #7034, #62199 ) ;
#138818=DIRECTION ( 'NONE',  ( -0.000000000000000000, 0.9126074666063770380, 0.4088369013363281068 ) ) ;
#138867=ORIENTED_EDGE ( 'NONE', *, *, #176831, .F. ) ;
#138897=DIRECTION ( 'NONE',  ( -1.000000000000000000, -0.000000000000000000, 0.000000000000000000 ) ) ;
#138910=DIRECTION ( 'NONE',  ( 1.713247197920696931E-14, -0.2606175937107791940, 0.9654421110809303652 ) ) ;
#138918=CARTESIAN_POINT ( 'NONE',  ( 23.25000000000000000, 61.88149656937974896, -248.1136133839584090 ) ) ;
#138948=CARTESIAN_POINT ( 'NONE',  ( 20.94999999999999574, 35.88801296822693843, -234.5558624753690538 ) ) ;
#138992=EDGE_LOOP ( 'NONE', ( #207125, #245668, #203238, #244635 ) ) ;
#139024=CARTESIAN_POINT ( 'NONE',  ( -20.85000000000000142, 67.85909929089923764, -227.8797997985275856 ) ) ;
#139025=ORIENTED_EDGE ( 'NONE', *, *, #92649, .T. ) ;
#139036=ORIENTED_EDGE ( 'NONE', *, *, #174273, .T. ) ;
#139088=ORIENTED_EDGE ( 'NONE', *, *, #107609, .F. ) ;
#139095=EDGE_CURVE ( 'NONE', #145909, #100153, #247499, .T. ) ;
#139099=CARTESIAN_POINT ( 'NONE',  ( -18.50000000000000000, 77.35494420175976416, -241.6200040285045532 ) ) ;
#139116=ADVANCED_FACE ( 'NONE', ( #192542 ), #173021, .T. ) ;
#139139=CARTESIAN_POINT ( 'NONE',  ( 23.24999999999999645, 53.62064951147646497, -235.8162552129080609 ) ) ;
#139152=CARTESIAN_POINT ( 'NONE',  ( 20.94999999999999929, 56.23643450586807546, -227.9054833905874204 ) ) ;
#139168=CARTESIAN_POINT ( 'NONE',  ( 22.59999985501178799, 31.79527822860963582, -238.8549629533907819 ) ) ;
#139204=FACE_OUTER_BOUND ( 'NONE', #53384, .T. ) ;
#139213=VERTEX_POINT ( 'NONE', #101077 ) ;
#139217=AXIS2_PLACEMENT_3D ( 'NONE', #220246, #24630, #237231 ) ;
#139249=CIRCLE ( 'NONE', #210032, 0.09999999999999609201 ) ;
#139261=VECTOR ( 'NONE', #28355, 1000.000000000000114 ) ;
#139267=EDGE_CURVE ( 'NONE', #249181, #114887, #77699, .T. ) ;
#139288=CIRCLE ( 'NONE', #47721, 0.09999999999999939493 ) ;
#139295=DIRECTION ( 'NONE',  ( 0.000000000000000000, -0.4230464831072829335, 0.9061079809440810706 ) ) ;
#139307=ORIENTED_EDGE ( 'NONE', *, *, #89458, .T. ) ;
#139320=ORIENTED_EDGE ( 'NONE', *, *, #16719, .T. ) ;
#139334=ORIENTED_EDGE ( 'NONE', *, *, #209252, .T. ) ;
#139340=VERTEX_POINT ( 'NONE', #146656 ) ;
#139363=EDGE_LOOP ( 'NONE', ( #210877, #154066, #13563, #57074 ) ) ;
#139428=TOROIDAL_SURFACE ( 'NONE', #122726, 0.2000000000000000111, 0.1000000000000000056 ) ;
#139435=DIRECTION ( 'NONE',  ( -1.000000000000000000, -0.000000000000000000, 0.000000000000000000 ) ) ;
#139479=DIRECTION ( 'NONE',  ( 0.7071359030028202541, 0.6452843503173477657, 0.2890794387705640789 ) ) ;
#139484=ADVANCED_FACE ( 'NONE', ( #134798 ), #151849, .T. ) ;
#139496=EDGE_CURVE ( 'NONE', #78948, #124831, #30612, .T. ) ;
#139516=ORIENTED_EDGE ( 'NONE', *, *, #152237, .T. ) ;
#139538=ORIENTED_EDGE ( 'NONE', *, *, #243675, .T. ) ;
#139586=ORIENTED_EDGE ( 'NONE', *, *, #169591, .F. ) ;
#139600=ORIENTED_EDGE ( 'NONE', *, *, #115012, .T. ) ;
#139624=DIRECTION ( 'NONE',  ( -0.000000000000000000, -0.9126074666063771490, -0.4088369013363281623 ) ) ;
#139650=VERTEX_POINT ( 'NONE', #175275 ) ;
#139662=VECTOR ( 'NONE', #130572, 1000.000000000000000 ) ;
#139687=ADVANCED_FACE ( 'NONE', ( #236486 ), #158282, .F. ) ;
#139691=DIRECTION ( 'NONE',  ( 0.000000000000000000, 0.9126074666063769270, 0.4088369013363280513 ) ) ;
#139708=ORIENTED_EDGE ( 'NONE', *, *, #135925, .F. ) ;
#139709=CARTESIAN_POINT ( 'NONE',  ( 18.50000000000000000, 47.16152503674118890, -255.1462838189583806 ) ) ;
#139718=CARTESIAN_POINT ( 'NONE',  ( -23.15000000000000213, 21.13195309841794867, -243.6318585593224100 ) ) ;
#139723=EDGE_CURVE ( 'NONE', #214500, #170250, #151401, .T. ) ;
#139755=DIRECTION ( 'NONE',  ( 0.000000000000000000, 0.9126074666063844765, 0.4088369013363114535 ) ) ;
#139779=EDGE_LOOP ( 'NONE', ( #198881, #54843, #93779, #246124 ) ) ;
#139812=AXIS2_PLACEMENT_3D ( 'NONE', #237366, #59985, #181261 ) ;
#139816=CARTESIAN_POINT ( 'NONE',  ( 21.05000000000000071, 30.90801580390627734, -252.0203440857197279 ) ) ;
#139820=LINE ( 'NONE', #236364, #162129 ) ;
#139832=AXIS2_PLACEMENT_3D ( 'NONE', #181511, #221872, #238905 ) ;
#139861=AXIS2_PLACEMENT_3D ( 'NONE', #85700, #165279, #201839 ) ;
#139949=VERTEX_POINT ( 'NONE', #30212 ) ;
#139950=ORIENTED_EDGE ( 'NONE', *, *, #13846, .F. ) ;
#139960=DIRECTION ( 'NONE',  ( -0.000000000000000000, -0.9126074666063770380, -0.4088369013363281068 ) ) ;
#139988=CIRCLE ( 'NONE', #227490, 0.4000000000000033529 ) ;
#139996=CARTESIAN_POINT ( 'NONE',  ( 21.05000000000000071, 40.74071615341952679, -237.9411309446948053 ) ) ;
#140008=CARTESIAN_POINT ( 'NONE',  ( -21.05000000000000071, 34.06366114622594665, -243.8432908520872786 ) ) ;
#140009=DIRECTION ( 'NONE',  ( -0.000000000000000000, -0.9126074666063771490, -0.4088369013363281623 ) ) ;
#140047=DIRECTION ( 'NONE',  ( 0.000000000000000000, -0.4088369013363280513, 0.9126074666063769270 ) ) ;
#140063=LINE ( 'NONE', #109619, #47003 ) ;
#140085=CARTESIAN_POINT ( 'NONE',  ( 18.59999999999999076, 53.32357432685029153, -235.0179440783709879 ) ) ;
#140102=ORIENTED_EDGE ( 'NONE', *, *, #147397, .T. ) ;
#140107=DIRECTION ( 'NONE',  ( 1.000000000000000000, 0.000000000000000000, 0.000000000000000000 ) ) ;
#140123=VERTEX_POINT ( 'NONE', #56159 ) ;
#140140=CIRCLE ( 'NONE', #135866, 0.1000000000000024342 ) ;
#140181=CIRCLE ( 'NONE', #106880, 0.5999999999999968692 ) ;
#140193=CARTESIAN_POINT ( 'NONE',  ( 18.52643265882457868, 68.07764576057049055, -224.1679995073710359 ) ) ;
#140202=EDGE_CURVE ( 'NONE', #5885, #126059, #136181, .T. ) ;
#140205=DIRECTION ( 'NONE',  ( 0.000000000000000000, 0.9126074666063770380, 0.4088369013363281068 ) ) ;
#140237=EDGE_CURVE ( 'NONE', #5240, #143749, #60025, .T. ) ;
#140290=ADVANCED_FACE ( 'NONE', ( #123872 ), #51614, .F. ) ;
#140350=AXIS2_PLACEMENT_3D ( 'NONE', #234986, #96716, #216693 ) ;
#140380=DIRECTION ( 'NONE',  ( -1.000000000000000000, -0.000000000000000000, 0.000000000000000000 ) ) ;
#140385=FACE_OUTER_BOUND ( 'NONE', #135901, .T. ) ;
#140410=CARTESIAN_POINT ( 'NONE',  ( -18.47130263965429720, 77.20275754622504394, -241.7661513169259422 ) ) ;
#140414=EDGE_CURVE ( 'NONE', #80413, #74293, #248954, .T. ) ;
#140415=EDGE_CURVE ( 'NONE', #244854, #249043, #143426, .T. ) ;
#140473=DIRECTION ( 'NONE',  ( 1.000000000000000000, 0.000000000000000000, 0.000000000000000000 ) ) ;
#140492=CARTESIAN_POINT ( 'NONE',  ( -20.64999999999999858, 65.40605961984560679, -236.6728003091511425 ) ) ;
#140495=CYLINDRICAL_SURFACE ( 'NONE', #235102, 0.09999999999999063804 ) ;
#140530=FACE_OUTER_BOUND ( 'NONE', #254386, .T. ) ;
#140539=CIRCLE ( 'NONE', #107796, 0.1000000000000028227 ) ;
#140550=DIRECTION ( 'NONE',  ( 2.952720810173289112E-16, 0.4088369013363280513, -0.9126074666063769270 ) ) ;
#140568=CIRCLE ( 'NONE', #257061, 6.329289321881348407 ) ;
#140580=ORIENTED_EDGE ( 'NONE', *, *, #141465, .T. ) ;
#140623=VERTEX_POINT ( 'NONE', #244443 ) ;
#140629=DIRECTION ( 'NONE',  ( 0.000000000000000000, 0.9126074666063770380, 0.4088369013363281068 ) ) ;
#140642=DIRECTION ( 'NONE',  ( 0.000000000000000000, 0.4088369013363287729, -0.9126074666063767049 ) ) ;
#140658=CARTESIAN_POINT ( 'NONE',  ( -20.92356734117541706, 68.07764576057049055, -224.1679995073710359 ) ) ;
#140691=AXIS2_PLACEMENT_3D ( 'NONE', #30060, #109550, #189109 ) ;
#140710=DIRECTION ( 'NONE',  ( 0.000000000000000000, 0.5283051335750404975, -0.8490545835446967615 ) ) ;
#140750=ORIENTED_EDGE ( 'NONE', *, *, #206842, .F. ) ;
#140764=CARTESIAN_POINT ( 'NONE',  ( 21.05000000000000071, 69.06797323185276127, -247.4100621602722470 ) ) ;
#140791=ADVANCED_FACE ( 'NONE', ( #95638 ), #73556, .T. ) ;
#140835=CARTESIAN_POINT ( 'NONE',  ( 20.94999999999999929, 47.95459712139159336, -246.5019368548292675 ) ) ;
#140841=AXIS2_PLACEMENT_3D ( 'NONE', #66973, #146491, #126951 ) ;
#140854=ORIENTED_EDGE ( 'NONE', *, *, #153109, .F. ) ;
#140879=DIRECTION ( 'NONE',  ( 0.000000000000000000, 0.9126074666063660468, 0.4088369013363524762 ) ) ;
#140881=FACE_OUTER_BOUND ( 'NONE', #64783, .T. ) ;
#140902=TOROIDAL_SURFACE ( 'NONE', #190815, 11.90000000000000213, 0.1000000000000000056 ) ;
#140931=EDGE_CURVE ( 'NONE', #126259, #178504, #38256, .T. ) ;
#140943=B_SPLINE_CURVE_WITH_KNOTS ( 'NONE', 3,
 ( #234170, #196333, #256237, #60660, #120682, #217166, #99777, #36000, #197612, #140193, #118088, #158523, #41145, #219744, #55505, #17687, #95940, #135058, #97190 ),
 .UNSPECIFIED., .F., .F.,
 ( 4, 3, 3, 3, 3, 3, 4 ),
 ( -2.000416914671369846E-06, 0.000000000000000000, 4.714008503745774695E-05, 9.979203887777935550E-05, 0.0001372215519229537709, 0.0001635031576221019581, 0.0001900083748504146253 ),
 .UNSPECIFIED. ) ;
#140945=ORIENTED_EDGE ( 'NONE', *, *, #98241, .T. ) ;
#140989=DIRECTION ( 'NONE',  ( 0.000000000000000000, 0.4088369013363280513, -0.9126074666063769270 ) ) ;
#140990=DIRECTION ( 'NONE',  ( 0.000000000000000000, -0.4088369013363296611, 0.9126074666063762608 ) ) ;
#140992=DIRECTION ( 'NONE',  ( 0.000000000000000000, -0.4088369013363281623, 0.9126074666063771490 ) ) ;
#140994=LINE ( 'NONE', #160568, #36915 ) ;
#141004=FACE_OUTER_BOUND ( 'NONE', #249756, .T. ) ;
#141006=FACE_OUTER_BOUND ( 'NONE', #129476, .T. ) ;
#141011=AXIS2_PLACEMENT_3D ( 'NONE', #171962, #131506, #32448 ) ;
#141030=DIRECTION ( 'NONE',  ( 0.000000000000000000, 0.9126074666063844765, 0.4088369013363114535 ) ) ;
#141058=DIRECTION ( 'NONE',  ( 0.000000000000000000, -0.9126074666063771490, -0.4088369013363281623 ) ) ;
#141070=CARTESIAN_POINT ( 'NONE',  ( 18.56308993302884147, 54.99211411440564490, -229.9633593191885836 ) ) ;
#141077=DIRECTION ( 'NONE',  ( -1.000000000000000000, 0.000000000000000000, 0.000000000000000000 ) ) ;
#141094=VECTOR ( 'NONE', #131475, 1000.000000000000114 ) ;
#141099=ORIENTED_EDGE ( 'NONE', *, *, #71085, .T. ) ;
#141106=ORIENTED_EDGE ( 'NONE', *, *, #29027, .F. ) ;
#141114=ORIENTED_EDGE ( 'NONE', *, *, #26092, .T. ) ;
#141120=VECTOR ( 'NONE', #255428, 1000.000000000000000 ) ;
#141130=DIRECTION ( 'NONE',  ( 0.000000000000000000, -0.9126074666063769270, -0.4088369013363280513 ) ) ;
#141133=DIRECTION ( 'NONE',  ( -1.000000000000000000, -0.000000000000000000, -0.000000000000000000 ) ) ;
#141144=ORIENTED_EDGE ( 'NONE', *, *, #168463, .T. ) ;
#141187=DIRECTION ( 'NONE',  ( -1.000000000000000000, 0.000000000000000000, 0.000000000000000000 ) ) ;
#141195=ORIENTED_EDGE ( 'NONE', *, *, #201969, .T. ) ;
#141199=CIRCLE ( 'NONE', #232798, 0.09999999999999609201 ) ;
#141230=DIRECTION ( 'NONE',  ( -1.000000000000000000, -0.000000000000000000, 0.000000000000000000 ) ) ;
#141236=EDGE_CURVE ( 'NONE', #173788, #191945, #189596, .T. ) ;
#141253=CARTESIAN_POINT ( 'NONE',  ( 22.45305468355009992, 25.97741635855175346, -254.4468634167663197 ) ) ;
#141273=CARTESIAN_POINT ( 'NONE',  ( -20.54999999999999716, 49.36776662947724503, -253.7196102226803021 ) ) ;
#141274=CARTESIAN_POINT ( 'NONE',  ( 21.15000000000000213, 33.98486250090727623, -243.5821103306120108 ) ) ;
#141333=AXIS2_PLACEMENT_3D ( 'NONE', #67310, #210675, #50301 ) ;
#141364=DIRECTION ( 'NONE',  ( 1.000000000000000000, 0.000000000000000000, 0.000000000000000000 ) ) ;
#141385=DIRECTION ( 'NONE',  ( -2.252264143451594314E-15, 0.9579639084728162057, 0.2868887416115976086 ) ) ;
#141413=DIRECTION ( 'NONE',  ( 0.000000000000000000, 0.9126074666063769270, 0.4088369013363280513 ) ) ;
#141437=DIRECTION ( 'NONE',  ( 0.000000000000000000, -0.9126074666063622720, -0.4088369013363611360 ) ) ;
#141465=EDGE_CURVE ( 'NONE', #155635, #198535, #156489, .T. ) ;
#141466=DIRECTION ( 'NONE',  ( 0.000000000000000000, -0.5283051335750404975, 0.8490545835446967615 ) ) ;
#141480=ORIENTED_EDGE ( 'NONE', *, *, #229842, .T. ) ;
#141484=ADVANCED_FACE ( 'NONE', ( #247695 ), #70377, .F. ) ;
#141513=ORIENTED_EDGE ( 'NONE', *, *, #125362, .T. ) ;
#141520=CARTESIAN_POINT ( 'NONE',  ( 22.40736611211992368, 26.02743912001966464, -254.3139371321002216 ) ) ;
#141544=ORIENTED_EDGE ( 'NONE', *, *, #179573, .T. ) ;
#141556=AXIS2_PLACEMENT_3D ( 'NONE', #154833, #197776, #98637 ) ;
#141558=ORIENTED_EDGE ( 'NONE', *, *, #30246, .T. ) ;
#141571=DIRECTION ( 'NONE',  ( -0.000000000000000000, -0.4088369013363281623, 0.9126074666063771490 ) ) ;
#141590=EDGE_CURVE ( 'NONE', #145938, #5729, #185677, .T. ) ;
#141601=CARTESIAN_POINT ( 'NONE',  ( 20.22483756094572271, 40.20239933964113277, -237.5519095886356240 ) ) ;
#141638=VECTOR ( 'NONE', #86477, 1000.000000000000000 ) ;
#141652=CARTESIAN_POINT ( 'NONE',  ( 18.49999999999999289, 21.13195309841794867, -243.6318585593224100 ) ) ;
#141664=DIRECTION ( 'NONE',  ( 0.000000000000000000, 0.9126074666063770380, 0.4088369013363281068 ) ) ;
#141673=ORIENTED_EDGE ( 'NONE', *, *, #121374, .T. ) ;
#141675=CARTESIAN_POINT ( 'NONE',  ( -23.25000000000000000, 40.35498466150055918, -247.8953732508333587 ) ) ;
#141697=CARTESIAN_POINT ( 'NONE',  ( -18.31331870001099915, 77.39837993464469434, -241.7498918423547991 ) ) ;
#141707=EDGE_CURVE ( 'NONE', #213386, #177788, #1040, .T. ) ;
#141721=ORIENTED_EDGE ( 'NONE', *, *, #8537, .F. ) ;
#141736=AXIS2_PLACEMENT_3D ( 'NONE', #147740, #26516, #167321 ) ;
#141740=FACE_OUTER_BOUND ( 'NONE', #254356, .T. ) ;
#141741=CARTESIAN_POINT ( 'NONE',  ( 20.99551997958262106, 56.17759395754559648, -227.9318432312958294 ) ) ;
#141757=ADVANCED_FACE ( 'NONE', ( #62335 ), #48299, .T. ) ;
#141765=CARTESIAN_POINT ( 'NONE',  ( -23.25000000000000000, 78.48087866980282001, -232.8271061603568910 ) ) ;
#141766=EDGE_CURVE ( 'NONE', #192597, #18074, #181594, .T. ) ;
#141816=DIRECTION ( 'NONE',  ( 0.000000000000000000, -0.9126074666063771490, -0.4088369013363281623 ) ) ;
#141818=CARTESIAN_POINT ( 'NONE',  ( 18.49713797159835948, 46.97446046665651664, -255.2810199801895408 ) ) ;
#141823=AXIS2_PLACEMENT_3D ( 'NONE', #92954, #13436, #228644 ) ;
#141838=CARTESIAN_POINT ( 'NONE',  ( -21.05000000000000071, 36.65892442174472876, -249.5511627012454596 ) ) ;
#141857=CARTESIAN_POINT ( 'NONE',  ( -18.59999999999999787, 46.45388641681647357, -243.1520440498138385 ) ) ;
#141863=EDGE_CURVE ( 'NONE', #209494, #228778, #131691, .T. ) ;
#141891=ORIENTED_EDGE ( 'NONE', *, *, #139095, .T. ) ;
#141908=CARTESIAN_POINT ( 'NONE',  ( 18.59999999999999076, 67.23127455305835554, -235.8551265064784559 ) ) ;
#141930=ORIENTED_EDGE ( 'NONE', *, *, #178101, .T. ) ;
#141942=CARTESIAN_POINT ( 'NONE',  ( -20.86777300164945004, 68.11153784908182729, -224.1393723182492579 ) ) ;
#141953=DIRECTION ( 'NONE',  ( 1.000000000000000000, 0.000000000000000000, 0.000000000000000000 ) ) ;
#141959=CARTESIAN_POINT ( 'NONE',  ( 18.58725287972329454, 77.36873348216533941, -241.7964099312725637 ) ) ;
#142007=DIRECTION ( 'NONE',  ( 1.000000000000000000, 2.986185139342070877E-16, -6.665775143889692774E-16 ) ) ;
#142012=CARTESIAN_POINT ( 'NONE',  ( -22.50000000000000000, 30.95512775545487472, -252.1063933345974988 ) ) ;
#142019=ORIENTED_EDGE ( 'NONE', *, *, #237504, .F. ) ;
#142032=DIRECTION ( 'NONE',  ( 0.000000000000000000, -0.9126074666063772600, -0.4088369013363274407 ) ) ;
#142068=AXIS2_PLACEMENT_3D ( 'NONE', #8188, #147691, #128130 ) ;
#142078=DIRECTION ( 'NONE',  ( 0.000000000000000000, 0.9126074666063770380, 0.4088369013363278848 ) ) ;
#142098=CARTESIAN_POINT ( 'NONE',  ( -22.42357213249529124, 29.61603862786154906, -252.5977130990568753 ) ) ;
#142148=CARTESIAN_POINT ( 'NONE',  ( 21.05000000000000071, 47.92640890138473253, -246.4059919526569900 ) ) ;
#142151=CARTESIAN_POINT ( 'NONE',  ( -20.54999999999999716, 54.18213181965657554, -236.9344197582443883 ) ) ;
#142155=VECTOR ( 'NONE', #73871, 1000.000000000000114 ) ;
#142156=FACE_BOUND ( 'NONE', #248084, .T. ) ;
#142159=AXIS2_PLACEMENT_3D ( 'NONE', #222140, #119233, #59201 ) ;
#142191=ORIENTED_EDGE ( 'NONE', *, *, #124960, .T. ) ;
#142193=DIRECTION ( 'NONE',  ( -1.000000000000000000, 0.000000000000000000, 0.000000000000000000 ) ) ;
#142241=VERTEX_POINT ( 'NONE', #208916 ) ;
#142266=( BOUNDED_SURFACE ( )  B_SPLINE_SURFACE ( 3, 2, ( 
 ( #185565, #139996, #219540 ),
 ( #100843, #104702, #224677 ),
 ( #4343, #180434, #202560 ),
 ( #203836, #241687, #21383 ) ),
 .UNSPECIFIED., .F., .F., .F. ) 
 B_SPLINE_SURFACE_WITH_KNOTS ( ( 4, 4 ),
 ( 3, 3 ),
 ( 0.0002700421466196669426, 0.0004789321604330889072 ),
 ( 0.000000000000000000, 1.000000000000000000 ),
 .UNSPECIFIED. ) 
 GEOMETRIC_REPRESENTATION_ITEM ( )  RATIONAL_B_SPLINE_SURFACE ( (
 ( 1.000000000000000000, 0.7071067811865475727, 1.000000000000000000),
 ( 1.000000000000000000, 0.7163411249511604240, 1.000000000000000000),
 ( 1.000000000000000000, 0.7221957104842396946, 1.000000000000000000),
 ( 1.000000000000000000, 0.7250110520819882387, 1.000000000000000000) ) ) 
 REPRESENTATION_ITEM ( '' )  SURFACE ( )  );
#142282=ORIENTED_EDGE ( 'NONE', *, *, #21343, .T. ) ;
#142301=ORIENTED_EDGE ( 'NONE', *, *, #58861, .F. ) ;
#142330=LINE ( 'NONE', #41979, #208430 ) ;
#142341=CIRCLE ( 'NONE', #46657, 0.4999999999999995004 ) ;
#142380=VECTOR ( 'NONE', #20514, 1000.000000000000114 ) ;
#142382=AXIS2_PLACEMENT_3D ( 'NONE', #123168, #203976, #202692 ) ;
#142390=EDGE_CURVE ( 'NONE', #225601, #58341, #94269, .T. ) ;
#142440=EDGE_LOOP ( 'NONE', ( #176198, #22771, #48163, #59398 ) ) ;
#142450=CARTESIAN_POINT ( 'NONE',  ( 20.94999999999999929, 43.51422117117169108, -240.0698702536254530 ) ) ;
#142454=CARTESIAN_POINT ( 'NONE',  ( 18.50000000000000000, 46.88959166481302532, -255.2681066192500339 ) ) ;
#142489=VERTEX_POINT ( 'NONE', #3986 ) ;
#142523=ORIENTED_EDGE ( 'NONE', *, *, #100494, .F. ) ;
#142537=CARTESIAN_POINT ( 'NONE',  ( -21.65000000000000213, 44.76114064897694789, -237.4293191035423831 ) ) ;
#142540=CARTESIAN_POINT ( 'NONE',  ( 18.59999999999999076, 53.24180694658302571, -234.8354225850497130 ) ) ;
#142542=FACE_OUTER_BOUND ( 'NONE', #212519, .T. ) ;
#142563=CIRCLE ( 'NONE', #146651, 11.90000000000000213 ) ;
#142632=ADVANCED_FACE ( 'NONE', ( #249038 ), #132939, .T. ) ;
#142637=CIRCLE ( 'NONE', #126070, 0.09999999999999542588 ) ;
#142687=CIRCLE ( 'NONE', #30297, 0.1000000000000024342 ) ;
#142719=DIRECTION ( 'NONE',  ( 5.421010862427555697E-16, 0.4088369013363311044, -0.9126074666063758167 ) ) ;
#142724=ORIENTED_EDGE ( 'NONE', *, *, #129281, .F. ) ;
#142750=B_SPLINE_CURVE_WITH_KNOTS ( 'NONE', 3,
 ( #22681, #97012, #140008, #138706, #1788, #78755, #200014, #102153 ),
 .UNSPECIFIED., .F., .F.,
 ( 4, 2, 2, 4 ),
 ( 0.000000000000000000, 9.550056980121915124E-05, 0.0001910011396024383025, 0.0003820022792049600885 ),
 .UNSPECIFIED. ) ;
#142754=DIRECTION ( 'NONE',  ( 0.000000000000000000, 0.9126074666063765939, 0.4088369013363289950 ) ) ;
#142755=CARTESIAN_POINT ( 'NONE',  ( -20.94999999999999929, 74.98773774893902555, -233.8732236541320333 ) ) ;
#142796=CARTESIAN_POINT ( 'NONE',  ( 20.94403535211772294, 68.04082873524789932, -224.1991862745062178 ) ) ;
#142828=DIRECTION ( 'NONE',  ( 0.000000000000000000, -0.9126074666063660468, -0.4088369013363524762 ) ) ;
#142861=DIRECTION ( 'NONE',  ( 0.7071067811865474617, 0.2890913453342131012, -0.6453109281988449464 ) ) ;
#142864=ORIENTED_EDGE ( 'NONE', *, *, #171881, .F. ) ;
#142870=CIRCLE ( 'NONE', #188685, 0.09999999999999950595 ) ;
#142876=DIRECTION ( 'NONE',  ( -1.000000000000000000, -0.000000000000000000, -0.000000000000000000 ) ) ;
#142898=CIRCLE ( 'NONE', #97096, 3.999999999999989786 ) ;
#142956=LINE ( 'NONE', #245946, #221639 ) ;
#142970=AXIS2_PLACEMENT_3D ( 'NONE', #176331, #177625, #39396 ) ;
#142982=DIRECTION ( 'NONE',  ( 0.000000000000000000, 0.4088369013363062909, -0.9126074666063868079 ) ) ;
#143065=EDGE_CURVE ( 'NONE', #61601, #65298, #244654, .T. ) ;
#143091=CIRCLE ( 'NONE', #97272, 0.09999999999999993616 ) ;
#143096=CIRCLE ( 'NONE', #84623, 11.65000000000000391 ) ;
#143127=DIRECTION ( 'NONE',  ( 0.000000000000000000, -0.4088369013363280513, 0.9126074666063769270 ) ) ;
#143134=CIRCLE ( 'NONE', #93074, 0.1000000000000024342 ) ;
#143167=LINE ( 'NONE', #226545, #162910 ) ;
#143207=EDGE_LOOP ( 'NONE', ( #99393, #88304, #81244, #239472 ) ) ;
#143225=ADVANCED_FACE ( 'NONE', ( #195185 ), #15248, .T. ) ;
#143235=DIRECTION ( 'NONE',  ( -3.265361837132812600E-16, -0.4088369013363246096, 0.9126074666063785923 ) ) ;
#143290=ORIENTED_EDGE ( 'NONE', *, *, #35736, .T. ) ;
#143294=DIRECTION ( 'NONE',  ( -0.000000000000000000, 0.9579639084728162057, 0.2868887416115976086 ) ) ;
#143305=CARTESIAN_POINT ( 'NONE',  ( -21.65000000000000213, 44.77807522791015060, -237.4671205425215135 ) ) ;
#143332=DIRECTION ( 'NONE',  ( -1.000000000000000000, -0.000000000000000000, -0.000000000000000000 ) ) ;
#143336=VERTEX_POINT ( 'NONE', #123326 ) ;
#143345=DIRECTION ( 'NONE',  ( 0.000000000000000000, 0.9126074666063545004, 0.4088369013363783999 ) ) ;
#143348=DIRECTION ( 'NONE',  ( 0.000000000000000000, -0.4088369013363283289, 0.9126074666063768159 ) ) ;
#143355=EDGE_CURVE ( 'NONE', #245692, #87416, #228116, .T. ) ;
#143361=DIRECTION ( 'NONE',  ( 1.000000000000000000, 0.000000000000000000, -0.000000000000000000 ) ) ;
#143366=AXIS2_PLACEMENT_3D ( 'NONE', #5633, #43514, #68211 ) ;
#143384=CARTESIAN_POINT ( 'NONE',  ( -21.76363531954647357, 30.21839054580515693, -252.3279600990519498 ) ) ;
#143394=AXIS2_PLACEMENT_3D ( 'NONE', #10326, #29899, #92398 ) ;
#143406=DIRECTION ( 'NONE',  ( -1.000000000000000000, -0.000000000000000000, -0.000000000000000000 ) ) ;
#143409=CARTESIAN_POINT ( 'NONE',  ( -21.09813707148783379, 30.81905141938414516, -252.1330000948349834 ) ) ;
#143426=CIRCLE ( 'NONE', #31034, 11.65000000000000924 ) ;
#143429=TOROIDAL_SURFACE ( 'NONE', #214164, 0.2000000000000000111, 0.1000000000000000056 ) ;
#143445=CARTESIAN_POINT ( 'NONE',  ( 22.39999999999999503, 33.47376623175147614, -242.4412390690852988 ) ) ;
#143456=AXIS2_PLACEMENT_3D ( 'NONE', #141908, #221427, #122363 ) ;
#143469=DIRECTION ( 'NONE',  ( -1.000000000000000000, 0.000000000000000000, 0.000000000000000000 ) ) ;
#143480=CARTESIAN_POINT ( 'NONE',  ( -21.05000000000000071, 69.34766280046808617, -247.6726305063181144 ) ) ;
#143511=VERTEX_POINT ( 'NONE', #28097 ) ;
#143566=ADVANCED_FACE ( 'NONE', ( #171471 ), #67195, .F. ) ;
#143621=CARTESIAN_POINT ( 'NONE',  ( 18.49999999999822720, 54.99329599893192722, -229.8977671155099358 ) ) ;
#143638=CARTESIAN_POINT ( 'NONE',  ( -18.54159361262917827, 46.96088360856536070, -255.3053464615296377 ) ) ;
#143646=CARTESIAN_POINT ( 'NONE',  ( -21.05000000000000071, 63.48958393997221350, -237.5313578019574265 ) ) ;
#143659=VERTEX_POINT ( 'NONE', #189029 ) ;
#143661=TOROIDAL_SURFACE ( 'NONE', #239342, 0.2000000000000000111, 0.1000000000000000056 ) ;
#143662=EDGE_LOOP ( 'NONE', ( #49296, #38190, #16547, #157855, #220530, #26078, #33518, #118749, #60122, #80199, #91223, #47417, #183837, #199025 ) ) ;
#143664=CARTESIAN_POINT ( 'NONE',  ( 21.05000000000000071, 42.92370456684775348, -239.4578053278609104 ) ) ;
#143682=DIRECTION ( 'NONE',  ( 1.000000000000000000, 0.000000000000000000, -0.000000000000000000 ) ) ;
#143685=EDGE_LOOP ( 'NONE', ( #57173, #220851, #227199 ) ) ;
#143701=CIRCLE ( 'NONE', #147810, 0.1000000000000003386 ) ;
#143712=DIRECTION ( 'NONE',  ( 0.000000000000000000, 0.9126074666063545004, 0.4088369013363783999 ) ) ;
#143726=ORIENTED_EDGE ( 'NONE', *, *, #141707, .F. ) ;
#143737=AXIS2_PLACEMENT_3D ( 'NONE', #1625, #83700, #44627 ) ;
#143749=VERTEX_POINT ( 'NONE', #194181 ) ;
#143754=CARTESIAN_POINT ( 'NONE',  ( -23.15000000000000213, 51.38014393322265505, -230.1906178717505611 ) ) ;
#143762=ORIENTED_EDGE ( 'NONE', *, *, #158632, .T. ) ;
#143775=CARTESIAN_POINT ( 'NONE',  ( -21.05000000000000071, 56.02567683926420727, -227.9999002286039058 ) ) ;
#143782=DIRECTION ( 'NONE',  ( 0.000000000000000000, 0.9126074666063660468, 0.4088369013363524762 ) ) ;
#143789=DIRECTION ( 'NONE',  ( 0.000000000000000000, -0.4088369013363281623, 0.9126074666063771490 ) ) ;
#143817=CARTESIAN_POINT ( 'NONE',  ( -18.59999999999999787, 42.98415524044399660, -233.9519173640447889 ) ) ;
#143824=ADVANCED_FACE ( 'NONE', ( #19379, #101425 ), #98874, .T. ) ;
#143825=LINE ( 'NONE', #79983, #48760 ) ;
#143830=PLANE ( 'NONE',  #147094 ) ;
#143838=EDGE_LOOP ( 'NONE', ( #59107, #45651, #26446, #121660 ) ) ;
#143851=DIRECTION ( 'NONE',  ( 0.000000000000000000, -0.4088369013363280513, 0.9126074666063769270 ) ) ;
#143859=EDGE_CURVE ( 'NONE', #119221, #224911, #253400, .T. ) ;
#143860=DIRECTION ( 'NONE',  ( 1.000000000000000000, -2.986185139342071370E-16, 6.665775143889693760E-16 ) ) ;
#143870=FACE_OUTER_BOUND ( 'NONE', #128505, .T. ) ;
#143872=DIRECTION ( 'NONE',  ( 1.000000000000000000, 0.000000000000000000, -0.000000000000000000 ) ) ;
#143894=EDGE_CURVE ( 'NONE', #155635, #245692, #177197, .T. ) ;
#143897=VECTOR ( 'NONE', #153457, 1000.000000000000000 ) ;
#143901=FACE_OUTER_BOUND ( 'NONE', #155122, .T. ) ;
#143909=CARTESIAN_POINT ( 'NONE',  ( 23.15000000000000213, 62.12679871018153932, -248.6611778639222337 ) ) ;
#143916=AXIS2_PLACEMENT_3D ( 'NONE', #202107, #143406, #1313 ) ;
#143999=AXIS2_PLACEMENT_3D ( 'NONE', #185911, #7264, #110218 ) ;
#144000=CIRCLE ( 'NONE', #177370, 0.1000000000000024342 ) ;
#144015=AXIS2_PLACEMENT_3D ( 'NONE', #91609, #210286, #169912 ) ;
#144054=ORIENTED_EDGE ( 'NONE', *, *, #63315, .F. ) ;
#144123=CARTESIAN_POINT ( 'NONE',  ( 21.04999999999999716, 39.25007626008504502, -236.7661609525534629 ) ) ;
#144127=CARTESIAN_POINT ( 'NONE',  ( 23.14999999999999147, 38.35559756229049100, -253.3384836876619204 ) ) ;
#144138=VERTEX_POINT ( 'NONE', #94741 ) ;
#144142=VERTEX_POINT ( 'NONE', #53049 ) ;
#144155=EDGE_LOOP ( 'NONE', ( #243515, #109184, #84824, #160815 ) ) ;
#144169=EDGE_CURVE ( 'NONE', #32720, #172675, #15535, .T. ) ;
#144175=VERTEX_POINT ( 'NONE', #12671 ) ;
#144251=CIRCLE ( 'NONE', #98432, 0.1000000000000051820 ) ;
#144278=DIRECTION ( 'NONE',  ( 0.000000000000000000, 0.1022405907414165593, 0.9947597004326453884 ) ) ;
#144287=CARTESIAN_POINT ( 'NONE',  ( 23.14999999999999503, 56.06656052939784729, -228.0911609752645290 ) ) ;
#144311=CARTESIAN_POINT ( 'NONE',  ( -23.25000000000000000, 54.34471204062663219, -239.4366250215122420 ) ) ;
#144315=DIRECTION ( 'NONE',  ( 1.000000000000000000, 0.000000000000000000, 0.000000000000000000 ) ) ;
#144323=CARTESIAN_POINT ( 'NONE',  ( -21.05000000000000071, 43.51422117117169108, -240.0698702536254530 ) ) ;
#144330=AXIS2_PLACEMENT_3D ( 'NONE', #161148, #141571, #221099 ) ;
#144347=DIRECTION ( 'NONE',  ( -1.000000000000000000, -0.000000000000000000, -0.000000000000000000 ) ) ;
#144359=ADVANCED_FACE ( 'NONE', ( #163717 ), #232956, .F. ) ;
#144365=CARTESIAN_POINT ( 'NONE',  ( 18.42595409746855495, 46.93054525149890566, -255.3593358477256743 ) ) ;
#144396=DIRECTION ( 'NONE',  ( 0.000000000000000000, 0.9126074666063770380, 0.4088369013363278848 ) ) ;
#144418=DIRECTION ( 'NONE',  ( 0.000000000000000000, -0.9126074666063769270, -0.4088369013363280513 ) ) ;
#144463=CARTESIAN_POINT ( 'NONE',  ( -21.05000000000000071, 43.57568952063339651, -245.1784935019914826 ) ) ;
#144496=TOROIDAL_SURFACE ( 'NONE', #94438, 0.2000000000000000111, 0.1000000000000000056 ) ;
#144516=CARTESIAN_POINT ( 'NONE',  ( 18.59999996954842771, 77.40622708283223119, -241.7320322634360252 ) ) ;
#144526=CIRCLE ( 'NONE', #227934, 6.258578643762714222 ) ;
#144527=DIRECTION ( 'NONE',  ( 0.000000000000000000, -0.9126074666063763718, -0.4088369013363293836 ) ) ;
#144538=ADVANCED_FACE ( 'NONE', ( #461 ), #220807, .T. ) ;
#144553=CARTESIAN_POINT ( 'NONE',  ( 18.44444291854882323, 77.16076536701955035, -241.8057231467951738 ) ) ;
#144567=CARTESIAN_POINT ( 'NONE',  ( -23.25000000000000000, 74.44087353924872730, -232.6253149859214773 ) ) ;
#144569=AXIS2_PLACEMENT_3D ( 'NONE', #98656, #140380, #87779 ) ;
#144589=ORIENTED_EDGE ( 'NONE', *, *, #215664, .F. ) ;
#144604=CARTESIAN_POINT ( 'NONE',  ( 18.59999999999999076, 53.28269063671665151, -234.9266833317103647 ) ) ;
#144623=VERTEX_POINT ( 'NONE', #239098 ) ;
#144668=DIRECTION ( 'NONE',  ( 1.000000000000000000, 0.000000000000000000, -0.000000000000000000 ) ) ;
#144677=EDGE_CURVE ( 'NONE', #62507, #178487, #223961, .T. ) ;
#144698=ORIENTED_EDGE ( 'NONE', *, *, #176818, .F. ) ;
#144716=DIRECTION ( 'NONE',  ( 0.000000000000000000, 0.9126074666063660468, 0.4088369013363524762 ) ) ;
#144736=EDGE_CURVE ( 'NONE', #168134, #108295, #253191, .T. ) ;
#144764=EDGE_LOOP ( 'NONE', ( #50318, #191590, #190677, #70837, #25078, #147445 ) ) ;
#144830=EDGE_CURVE ( 'NONE', #81533, #236784, #193643, .T. ) ;
#144836=CIRCLE ( 'NONE', #153087, 0.09999999999999609201 ) ;
#144856=DIRECTION ( 'NONE',  ( 0.000000000000000000, 0.9126074666063771490, 0.4088369013363281623 ) ) ;
#144872=AXIS2_PLACEMENT_3D ( 'NONE', #55175, #36972, #18656 ) ;
#144897=ORIENTED_EDGE ( 'NONE', *, *, #96928, .F. ) ;
#144911=AXIS2_PLACEMENT_3D ( 'NONE', #256429, #40054, #118284 ) ;
#144912=CARTESIAN_POINT ( 'NONE',  ( -18.43599941264851338, 46.91436743304934254, -255.3877617659306338 ) ) ;
#144916=DIRECTION ( 'NONE',  ( 0.000000000000000000, 0.9126074666063622720, 0.4088369013363611360 ) ) ;
#144979=ORIENTED_EDGE ( 'NONE', *, *, #51170, .T. ) ;
#144981=AXIS2_PLACEMENT_3D ( 'NONE', #73128, #246584, #90068 ) ;
#144986=CARTESIAN_POINT ( 'NONE',  ( 23.15000000000000213, 61.88149656937974896, -248.1136133839584090 ) ) ;
#145014=ORIENTED_EDGE ( 'NONE', *, *, #187203, .T. ) ;
#145025=EDGE_CURVE ( 'NONE', #132976, #154226, #199042, .T. ) ;
#145029=FACE_OUTER_BOUND ( 'NONE', #45375, .T. ) ;
#145040=EDGE_CURVE ( 'NONE', #219396, #144623, #45097, .T. ) ;
#145069=DIRECTION ( 'NONE',  ( 0.000000000000000000, -0.9126074666063660468, -0.4088369013363524762 ) ) ;
#145103=DIRECTION ( 'NONE',  ( -1.000000000000000000, 6.938893903907270030E-14, -2.775557561562908012E-13 ) ) ;
#145109=CARTESIAN_POINT ( 'NONE',  ( 21.07928932188134397, 33.98134083355422774, -243.8161431329846494 ) ) ;
#145129=DIRECTION ( 'NONE',  ( -1.000000000000000000, -0.000000000000000000, -0.000000000000000000 ) ) ;
#145137=CARTESIAN_POINT ( 'NONE',  ( -18.59999999999999787, 35.94660524813657076, -234.4748257877825495 ) ) ;
#145141=ADVANCED_FACE ( 'NONE', ( #45725 ), #106970, .F. ) ;
#145148=FACE_OUTER_BOUND ( 'NONE', #155154, .T. ) ;
#145186=CARTESIAN_POINT ( 'NONE',  ( 21.13461538461538680, 44.20567951878638269, -236.4340127271084384 ) ) ;
#145244=ORIENTED_EDGE ( 'NONE', *, *, #136896, .T. ) ;
#145246=ORIENTED_EDGE ( 'NONE', *, *, #42462, .F. ) ;
#145306=LINE ( 'NONE', #103599, #91889 ) ;
#145309=CARTESIAN_POINT ( 'NONE',  ( 23.14999999999999858, 68.86662215840367196, -239.5055563729039534 ) ) ;
#145310=DIRECTION ( 'NONE',  ( 0.000000000000000000, -0.8490545835447254053, -0.5283051335749948674 ) ) ;
#145362=CARTESIAN_POINT ( 'NONE',  ( 18.49999999999999289, 51.96945017402672562, -231.5060697639786440 ) ) ;
#145396=DIRECTION ( 'NONE',  ( -1.000000000000000000, 1.207181226542539700E-16, -2.694675058168174199E-16 ) ) ;
#145417=VECTOR ( 'NONE', #197024, 1000.000000000000114 ) ;
#145420=CARTESIAN_POINT ( 'NONE',  ( 21.05000000000000071, 39.14563005184295719, -236.8629343064758075 ) ) ;
#145422=DIRECTION ( 'NONE',  ( 0.000000000000000000, 0.9126074666063770380, 0.4088369013363281068 ) ) ;
#145439=ORIENTED_EDGE ( 'NONE', *, *, #62854, .F. ) ;
#145446=DIRECTION ( 'NONE',  ( -1.000000000000000000, 1.207181226542539700E-16, -2.694675058168174199E-16 ) ) ;
#145460=FACE_OUTER_BOUND ( 'NONE', #58170, .T. ) ;
#145463=AXIS2_PLACEMENT_3D ( 'NONE', #22354, #204798, #47001 ) ;
#145464=DIRECTION ( 'NONE',  ( 0.000000000000000000, 0.9126074666063805907, 0.4088369013363201132 ) ) ;
#145477=CARTESIAN_POINT ( 'NONE',  ( 20.85000000000000142, 62.46832465249013921, -225.2232495205141731 ) ) ;
#145484=EDGE_CURVE ( 'NONE', #185809, #183191, #33268, .T. ) ;
#145494=DIRECTION ( 'NONE',  ( -0.000000000000000000, 0.9126074666063770380, 0.4088369013363281068 ) ) ;
#145500=LINE ( 'NONE', #26875, #77334 ) ;
#145535=CARTESIAN_POINT ( 'NONE',  ( -21.05000000000000071, 33.99373157816623348, -243.8426824212930342 ) ) ;
#145536=EDGE_CURVE ( 'NONE', #256823, #45859, #253552, .T. ) ;
#145543=ORIENTED_EDGE ( 'NONE', *, *, #135028, .T. ) ;
#145572=ADVANCED_FACE ( 'NONE', ( #95748 ), #151920, .F. ) ;
#145585=DIRECTION ( 'NONE',  ( 0.000000000000000000, -0.9126074666063545004, -0.4088369013363783999 ) ) ;
#145608=DIRECTION ( 'NONE',  ( -1.836970198721030427E-16, -0.4088369013363281623, 0.9126074666063771490 ) ) ;
#145615=CARTESIAN_POINT ( 'NONE',  ( 23.25000000000000000, 49.61306877027904250, -254.2671747026441551 ) ) ;
#145650=EDGE_CURVE ( 'NONE', #57263, #147844, #142750, .T. ) ;
#145726=DIRECTION ( 'NONE',  ( 1.000000000000000000, 0.000000000000000000, 0.000000000000000000 ) ) ;
#145758=CARTESIAN_POINT ( 'NONE',  ( -23.25000000000000000, 78.45218979564165807, -232.7313097695096076 ) ) ;
#145759=EDGE_LOOP ( 'NONE', ( #151944, #147976, #222384, #15950 ) ) ;
#145763=FACE_OUTER_BOUND ( 'NONE', #130335, .T. ) ;
#145795=ORIENTED_EDGE ( 'NONE', *, *, #156509, .F. ) ;
#145825=DIRECTION ( 'NONE',  ( 0.000000000000000000, -0.03803313543129139412, 0.9992764785629977276 ) ) ;
#145838=VECTOR ( 'NONE', #67565, 1000.000000000000000 ) ;
#145847=LINE ( 'NONE', #46747, #152208 ) ;
#145850=ORIENTED_EDGE ( 'NONE', *, *, #229524, .T. ) ;
#145855=DIRECTION ( 'NONE',  ( -3.440080580676165868E-14, 0.9579639084728162057, 0.2868887416115976086 ) ) ;
#145899=DIRECTION ( 'NONE',  ( 0.000000000000000000, 0.8103668758649577031, -0.5859227990963212784 ) ) ;
#145909=VERTEX_POINT ( 'NONE', #202576 ) ;
#145915=AXIS2_PLACEMENT_3D ( 'NONE', #59553, #21768, #179563 ) ;
#145926=ADVANCED_FACE ( 'NONE', ( #126896 ), #116395, .F. ) ;
#145937=DIRECTION ( 'NONE',  ( 1.000000000000000000, 0.000000000000000000, 0.000000000000000000 ) ) ;
#145938=VERTEX_POINT ( 'NONE', #208995 ) ;
#145949=ADVANCED_FACE ( 'NONE', ( #249419 ), #91451, .F. ) ;
#145967=DIRECTION ( 'NONE',  ( 0.000000000000000000, 0.9126074666063783702, 0.4088369013363252757 ) ) ;
#145990=CARTESIAN_POINT ( 'NONE',  ( -21.05000000000000071, 34.04175893161810507, -243.6660727135796662 ) ) ;
#145994=DIRECTION ( 'NONE',  ( 0.000000000000000000, 0.9126074666063769270, 0.4088369013363280513 ) ) ;
#146000=CARTESIAN_POINT ( 'NONE',  ( -18.43569575749026512, 46.91436717984745997, -255.3877622108296634 ) ) ;
#146014=ORIENTED_EDGE ( 'NONE', *, *, #183292, .F. ) ;
#146022=ORIENTED_EDGE ( 'NONE', *, *, #178367, .T. ) ;
#146051=ORIENTED_EDGE ( 'NONE', *, *, #147731, .F. ) ;
#146097=DIRECTION ( 'NONE',  ( 0.000000000000000000, 0.4088369013363281623, -0.9126074666063771490 ) ) ;
#146101=EDGE_CURVE ( 'NONE', #170976, #57537, #54016, .T. ) ;
#146112=VECTOR ( 'NONE', #162866, 1000.000000000000000 ) ;
#146133=EDGE_LOOP ( 'NONE', ( #138346, #173880, #137798, #107934 ) ) ;
#146150=DIRECTION ( 'NONE',  ( -1.000000000000000000, 0.000000000000000000, 0.000000000000000000 ) ) ;
#146191=EDGE_LOOP ( 'NONE', ( #208185, #84106, #16401, #182276 ) ) ;
#146197=LINE ( 'NONE', #247874, #24404 ) ;
#146202=CARTESIAN_POINT ( 'NONE',  ( -18.43473496883443374, 46.97092634935879829, -255.3357148657918856 ) ) ;
#146263=ADVANCED_FACE ( 'NONE', ( #65328 ), #66686, .T. ) ;
#146265=AXIS2_PLACEMENT_3D ( 'NONE', #174872, #226096, #189580 ) ;
#146296=DIRECTION ( 'NONE',  ( -1.000000000000000000, 0.000000000000000000, 0.000000000000000000 ) ) ;
#146315=CYLINDRICAL_SURFACE ( 'NONE', #212433, 11.80000000000000249 ) ;
#146357=CARTESIAN_POINT ( 'NONE',  ( 19.80993210785419834, 54.45774741499781868, -228.7023132931329030 ) ) ;
#146365=DIRECTION ( 'NONE',  ( 1.000000000000000000, -1.207181226542539700E-16, 2.694675058168174199E-16 ) ) ;
#146371=VECTOR ( 'NONE', #123424, 1000.000000000000114 ) ;
#146383=DIRECTION ( 'NONE',  ( -3.265361837132812600E-16, -0.4088369013363246096, 0.9126074666063785923 ) ) ;
#146396=ORIENTED_EDGE ( 'NONE', *, *, #247005, .F. ) ;
#146401=CARTESIAN_POINT ( 'NONE',  ( 20.22516295850462598, 39.83048402819590450, -237.2830021754640200 ) ) ;
#146402=DIRECTION ( 'NONE',  ( 1.000000000000000000, 0.000000000000000000, 0.000000000000000000 ) ) ;
#146430=CARTESIAN_POINT ( 'NONE',  ( 21.14999999999999858, 45.06922343725926083, -238.6062154437373124 ) ) ;
#146432=DIRECTION ( 'NONE',  ( 0.000000000000000000, 0.9126074666063769270, 0.4088369013363280513 ) ) ;
#146447=ORIENTED_EDGE ( 'NONE', *, *, #125718, .T. ) ;
#146457=DIRECTION ( 'NONE',  ( 0.000000000000000000, 0.9126074666063660468, 0.4088369013363524762 ) ) ;
#146491=DIRECTION ( 'NONE',  ( 0.000000000000000000, -0.8490545835447238510, -0.5283051335749973099 ) ) ;
#146504=CARTESIAN_POINT ( 'NONE',  ( 20.94999999999999929, 43.16354019706792400, -239.5695141926698284 ) ) ;
#146513=( BOUNDED_CURVE ( )  B_SPLINE_CURVE ( 3, ( #170362, #33409, #71232, #114185 ),
 .UNSPECIFIED., .F., .F. ) 
 B_SPLINE_CURVE_WITH_KNOTS ( ( 4, 4 ),
 ( 4.712388980384689674, 6.231880751915385375 ),
 .UNSPECIFIED. ) 
 CURVE ( )  GEOMETRIC_REPRESENTATION_ITEM ( )  RATIONAL_B_SPLINE_CURVE ( ( 1.000000000000000000, 0.8166740347213230500, 0.8166740347213230500, 1.000000000000000000 ) ) 
 REPRESENTATION_ITEM ( '' )  );
#146530=LINE ( 'NONE', #203954, #162797 ) ;
#146534=DIRECTION ( 'NONE',  ( 0.000000000000000000, -0.9594490217226032680, -0.2818822000686448392 ) ) ;
#146575=ORIENTED_EDGE ( 'NONE', *, *, #209131, .F. ) ;
#146583=FACE_OUTER_BOUND ( 'NONE', #60623, .T. ) ;
#146592=CARTESIAN_POINT ( 'NONE',  ( 22.39999999999999503, 25.97741635855165754, -254.4468634167653249 ) ) ;
#146603=DIRECTION ( 'NONE',  ( 1.000000000000000000, 0.000000000000000000, 0.000000000000000000 ) ) ;
#146615=CIRCLE ( 'NONE', #196524, 12.87499999999999289 ) ;
#146639=CYLINDRICAL_SURFACE ( 'NONE', #174536, 0.09999999999999108213 ) ;
#146648=DIRECTION ( 'NONE',  ( 0.000000000000000000, 0.9126074666063660468, 0.4088369013363524762 ) ) ;
#146651=AXIS2_PLACEMENT_3D ( 'NONE', #35211, #75608, #232106 ) ;
#146656=CARTESIAN_POINT ( 'NONE',  ( -23.25000000000000000, 48.31748480764120046, -244.3282712866738962 ) ) ;
#146669=ORIENTED_EDGE ( 'NONE', *, *, #9084, .T. ) ;
#146684=CARTESIAN_POINT ( 'NONE',  ( 21.04999999999660432, 39.27454047675113458, -236.7319953479758965 ) ) ;
#146699=AXIS2_PLACEMENT_3D ( 'NONE', #10082, #145726, #164029 ) ;
#146709=DIRECTION ( 'NONE',  ( -2.561896900575096800E-15, -0.4948392722769219265, -0.8689845192018362807 ) ) ;
#146738=DIRECTION ( 'NONE',  ( 1.000000000000000000, 0.000000000000000000, 0.000000000000000000 ) ) ;
#146741=ORIENTED_EDGE ( 'NONE', *, *, #63303, .T. ) ;
#146781=VECTOR ( 'NONE', #239538, 1000.000000000000114 ) ;
#146783=EDGE_CURVE ( 'NONE', #206263, #136054, #220, .T. ) ;
#146818=DIRECTION ( 'NONE',  ( 1.000000000000000000, 0.000000000000000000, 0.000000000000000000 ) ) ;
#146825=AXIS2_PLACEMENT_3D ( 'NONE', #29514, #149448, #146836 ) ;
#146834=( BOUNDED_CURVE ( )  B_SPLINE_CURVE ( 3, ( #98968, #160293, #177292, #79418 ),
 .UNSPECIFIED., .F., .F. ) 
 B_SPLINE_CURVE_WITH_KNOTS ( ( 4, 4 ),
 ( 3.141592653589791784, 4.712388980384661252 ),
 .UNSPECIFIED. ) 
 CURVE ( )  GEOMETRIC_REPRESENTATION_ITEM ( )  RATIONAL_B_SPLINE_CURVE ( ( 1.000000000000000000, 0.8047378541243714878, 0.8047378541243714878, 1.000000000000000000 ) ) 
 REPRESENTATION_ITEM ( '' )  );
#146835=CARTESIAN_POINT ( 'NONE',  ( 20.94999999999999929, 61.88149656937974896, -248.1136133839584090 ) ) ;
#146836=DIRECTION ( 'NONE',  ( 0.000000000000000000, 0.9126074666063660468, 0.4088369013363524762 ) ) ;
#146851=VERTEX_POINT ( 'NONE', #148428 ) ;
#146852=CARTESIAN_POINT ( 'NONE',  ( 21.05000000000000071, 67.23127455305835554, -235.8551265064784559 ) ) ;
#146878=LINE ( 'NONE', #236400, #227121 ) ;
#146937=EDGE_CURVE ( 'NONE', #28183, #174500, #120876, .T. ) ;
#146984=TOROIDAL_SURFACE ( 'NONE', #34430, 11.89999999999999858, 0.1000000000000000056 ) ;
#146987=AXIS2_PLACEMENT_3D ( 'NONE', #63903, #121350, #3932 ) ;
#146999=FACE_BOUND ( 'NONE', #184206, .T. ) ;
#147011=VERTEX_POINT ( 'NONE', #65843 ) ;
#147032=CARTESIAN_POINT ( 'NONE',  ( -20.85000000000000142, 62.42744096235649920, -225.1319887738535499 ) ) ;
#147072=ORIENTED_EDGE ( 'NONE', *, *, #97624, .T. ) ;
#147090=ORIENTED_EDGE ( 'NONE', *, *, #217240, .F. ) ;
#147094=AXIS2_PLACEMENT_3D ( 'NONE', #164701, #205083, #26482 ) ;
#147102=ORIENTED_EDGE ( 'NONE', *, *, #21700, .T. ) ;
#147131=CARTESIAN_POINT ( 'NONE',  ( 21.05000000000000071, 31.98723526783714988, -238.8784020251475511 ) ) ;
#147147=CARTESIAN_POINT ( 'NONE',  ( 23.15000000000000213, 49.36776662947724503, -253.7196102226803021 ) ) ;
#147154=DIRECTION ( 'NONE',  ( 1.000000000000000000, 0.000000000000000000, 0.000000000000000000 ) ) ;
#147165=AXIS2_PLACEMENT_3D ( 'NONE', #31918, #110141, #111432 ) ;
#147194=CIRCLE ( 'NONE', #213648, 0.1000000000000024342 ) ;
#147199=AXIS2_PLACEMENT_3D ( 'NONE', #120696, #140205, #106214 ) ;
#147208=ADVANCED_FACE ( 'NONE', ( #76119 ), #96933, .F. ) ;
#147220=CARTESIAN_POINT ( 'NONE',  ( -20.94999999999999929, 74.73788286442776041, -233.7359682632885267 ) ) ;
#147239=FACE_OUTER_BOUND ( 'NONE', #4474, .T. ) ;
#147274=DIRECTION ( 'NONE',  ( 0.000000000000000000, 0.9126074666063844765, 0.4088369013363114535 ) ) ;
#147278=DIRECTION ( 'NONE',  ( 4.239556034732057360E-17, 0.9579639084728132081, 0.2868887416116073785 ) ) ;
#147280=AXIS2_PLACEMENT_3D ( 'NONE', #72945, #196697, #114604 ) ;
#147298=DIRECTION ( 'NONE',  ( 0.000000000000000000, 0.9090645160163607352, 0.4166553800443956734 ) ) ;
#147397=EDGE_CURVE ( 'NONE', #150102, #169429, #173274, .T. ) ;
#147425=DIRECTION ( 'NONE',  ( 1.000000000000000000, 0.000000000000000000, 0.000000000000000000 ) ) ;
#147429=DIRECTION ( 'NONE',  ( 1.000000000000000000, 0.000000000000000000, 0.000000000000000000 ) ) ;
#147439=DIRECTION ( 'NONE',  ( 0.000000000000000000, 0.9126074666063772600, 0.4088369013363274407 ) ) ;
#147441=DIRECTION ( 'NONE',  ( 0.000000000000000000, 0.9126074666063660468, 0.4088369013363524762 ) ) ;
#147444=FACE_OUTER_BOUND ( 'NONE', #180919, .T. ) ;
#147445=ORIENTED_EDGE ( 'NONE', *, *, #194948, .F. ) ;
#147454=SPHERICAL_SURFACE ( 'NONE', #21219, 0.1000000000000000056 ) ;
#147458=CARTESIAN_POINT ( 'NONE',  ( 23.25000000000000000, 29.86062094194855376, -263.1160279713685100 ) ) ;
#147487=ORIENTED_EDGE ( 'NONE', *, *, #78851, .F. ) ;
#147498=DIRECTION ( 'NONE',  ( 1.000000000000000000, 0.000000000000000000, 0.000000000000000000 ) ) ;
#147500=CARTESIAN_POINT ( 'NONE',  ( -18.45037301276714459, 46.93868734354772698, -255.3449505252505389 ) ) ;
#147523=AXIS2_PLACEMENT_3D ( 'NONE', #137910, #38843, #14160 ) ;
#147533=CARTESIAN_POINT ( 'NONE',  ( -18.58222699835055280, 68.11153784908182729, -224.1393723182492579 ) ) ;
#147554=AXIS2_PLACEMENT_3D ( 'NONE', #38433, #98357, #119270 ) ;
#147565=AXIS2_PLACEMENT_3D ( 'NONE', #229736, #250573, #27725 ) ;
#147583=DIRECTION ( 'NONE',  ( 0.000000000000000000, -0.9654421110809058293, -0.2606175937108693996 ) ) ;
#147584=CARTESIAN_POINT ( 'NONE',  ( -21.05000000000000071, 67.23127455305835554, -235.8551265064784559 ) ) ;
#147601=AXIS2_PLACEMENT_3D ( 'NONE', #189605, #10961, #13532 ) ;
#147605=ORIENTED_EDGE ( 'NONE', *, *, #208626, .T. ) ;
#147624=ORIENTED_EDGE ( 'NONE', *, *, #104717, .T. ) ;
#147643=AXIS2_PLACEMENT_3D ( 'NONE', #59937, #39140, #1251 ) ;
#147658=EDGE_CURVE ( 'NONE', #52160, #27038, #77980, .T. ) ;
#147680=CIRCLE ( 'NONE', #130917, 0.09999999999999939493 ) ;
#147691=DIRECTION ( 'NONE',  ( -1.000000000000000000, -0.000000000000000000, 0.000000000000000000 ) ) ;
#147712=ORIENTED_EDGE ( 'NONE', *, *, #156772, .F. ) ;
#147719=VECTOR ( 'NONE', #104703, 1000.000000000000114 ) ;
#147731=EDGE_CURVE ( 'NONE', #220241, #60562, #102357, .T. ) ;
#147736=DIRECTION ( 'NONE',  ( 0.000000000000000000, 0.9126074666063769270, 0.4088369013363280513 ) ) ;
#147739=EDGE_CURVE ( 'NONE', #24027, #183601, #102178, .T. ) ;
#147740=CARTESIAN_POINT ( 'NONE',  ( 18.59999999999999076, 54.57427006634497957, -228.7596887170734306 ) ) ;
#147744=VECTOR ( 'NONE', #233956, 1000.000000000000114 ) ;
#147752=AXIS2_PLACEMENT_3D ( 'NONE', #90921, #110485, #50490 ) ;
#147777=EDGE_CURVE ( 'NONE', #57597, #149628, #194187, .T. ) ;
#147781=FACE_OUTER_BOUND ( 'NONE', #33062, .T. ) ;
#147810=AXIS2_PLACEMENT_3D ( 'NONE', #129972, #30930, #212114 ) ;
#147813=LINE ( 'NONE', #87799, #222566 ) ;
#147844=VERTEX_POINT ( 'NONE', #187376 ) ;
#147846=DIRECTION ( 'NONE',  ( 3.265361837132813093E-16, 0.4088369013363281068, -0.9126074666063770380 ) ) ;
#147858=CARTESIAN_POINT ( 'NONE',  ( 20.94999999999999929, 52.46376478296784285, -232.8540772485547450 ) ) ;
#147877=DIRECTION ( 'NONE',  ( 1.000000000000000000, 0.000000000000000000, 0.000000000000000000 ) ) ;
#147885=CARTESIAN_POINT ( 'NONE',  ( 21.05000000000000426, 39.20539516596018359, -236.6597403278730383 ) ) ;
#147928=CARTESIAN_POINT ( 'NONE',  ( 20.85000000000000142, 62.42744096235649920, -225.1319887738535499 ) ) ;
#147942=ORIENTED_EDGE ( 'NONE', *, *, #210197, .T. ) ;
#147973=DIRECTION ( 'NONE',  ( 0.000000000000000000, 0.4088369013363783999, -0.9126074666063545004 ) ) ;
#147976=ORIENTED_EDGE ( 'NONE', *, *, #12975, .F. ) ;
#148001=CARTESIAN_POINT ( 'NONE',  ( -18.59999999999999787, 78.48087866980282001, -232.8271061603568910 ) ) ;
#148012=ORIENTED_EDGE ( 'NONE', *, *, #155678, .F. ) ;
#148038=TOROIDAL_SURFACE ( 'NONE', #60538, 0.2000000000000000111, 0.1000000000000000056 ) ;
#148050=CARTESIAN_POINT ( 'NONE',  ( -20.94999999999999929, 46.59314322379660922, -243.1831726892433210 ) ) ;
#148072=EDGE_CURVE ( 'NONE', #229408, #131894, #202537, .T. ) ;
#148116=DIRECTION ( 'NONE',  ( 1.000000000000000000, 0.000000000000000000, 0.000000000000000000 ) ) ;
#148120=DIRECTION ( 'NONE',  ( -0.7071067811865475727, 0.2890913453342130457, -0.6453109281988448354 ) ) ;
#148135=DIRECTION ( 'NONE',  ( 0.000000000000000000, 0.9126074666063660468, 0.4088369013363524762 ) ) ;
#148146=CARTESIAN_POINT ( 'NONE',  ( -20.54999999999999716, 45.00644278977874535, -237.9768835835062077 ) ) ;
#148153=CARTESIAN_POINT ( 'NONE',  ( -20.94999999999999929, 46.45388641681647357, -243.1520440498138385 ) ) ;
#148158=DIRECTION ( 'NONE',  ( 1.000000000000000000, 0.000000000000000000, -0.000000000000000000 ) ) ;
#148171=DIRECTION ( 'NONE',  ( 0.000000000000000000, 0.9126074666063769270, 0.4088369013363280513 ) ) ;
#148181=EDGE_CURVE ( 'NONE', #198338, #170976, #144251, .T. ) ;
#148190=CARTESIAN_POINT ( 'NONE',  ( 21.08078803292165659, 33.99748930211067943, -243.8039819374040178 ) ) ;
#148193=DIRECTION ( 'NONE',  ( 0.000000000000000000, -0.9126074666063660468, -0.4088369013363524762 ) ) ;
#148212=CARTESIAN_POINT ( 'NONE',  ( -20.64999999999999858, 49.53130139001177668, -254.0846532093228802 ) ) ;
#148219=CARTESIAN_POINT ( 'NONE',  ( -23.15000000000000213, 40.35498466150055918, -247.8953732508333587 ) ) ;
#148222=VERTEX_POINT ( 'NONE', #125784 ) ;
#148241=EDGE_LOOP ( 'NONE', ( #116510, #111711, #58941, #198355 ) ) ;
#148291=EDGE_CURVE ( 'NONE', #36945, #47998, #72253, .T. ) ;
#148299=CARTESIAN_POINT ( 'NONE',  ( -20.64999999999999858, 54.70975502726918194, -239.2730902609777104 ) ) ;
#148338=ORIENTED_EDGE ( 'NONE', *, *, #215419, .F. ) ;
#148341=CARTESIAN_POINT ( 'NONE',  ( -20.54999999999999716, 67.23127455305835554, -235.8551265064784559 ) ) ;
#148343=LINE ( 'NONE', #32274, #213573 ) ;
#148363=DIRECTION ( 'NONE',  ( 1.000000000000000000, 0.000000000000000000, 0.000000000000000000 ) ) ;
#148372=CARTESIAN_POINT ( 'NONE',  ( 18.49999999999999289, 55.04793976901536467, -229.8170162380219494 ) ) ;
#148383=VERTEX_POINT ( 'NONE', #112658 ) ;
#148384=CARTESIAN_POINT ( 'NONE',  ( -20.54999999999999716, 49.02191564284679970, -236.1780012176263881 ) ) ;
#148403=DIRECTION ( 'NONE',  ( 0.000000000000000000, -0.9126074666063660468, -0.4088369013363524762 ) ) ;
#148408=CIRCLE ( 'NONE', #202554, 0.1000000000000024342 ) ;
#148428=CARTESIAN_POINT ( 'NONE',  ( -20.85000000000000142, 67.85125148167622910, -227.9794913823769491 ) ) ;
#148468=EDGE_LOOP ( 'NONE', ( #116212, #256978, #102696, #45847 ) ) ;
#148485=VERTEX_POINT ( 'NONE', #4240 ) ;
#148492=CARTESIAN_POINT ( 'NONE',  ( -20.64999999999999858, 48.40874555430183079, -244.2873875965402704 ) ) ;
#148494=CARTESIAN_POINT ( 'NONE',  ( 20.95575313997065336, 39.27455013993715482, -236.7483772272189810 ) ) ;
#148498=ORIENTED_EDGE ( 'NONE', *, *, #9708, .F. ) ;
#148517=CARTESIAN_POINT ( 'NONE',  ( -23.25000000000000000, 69.14775023293175593, -234.9965690136722003 ) ) ;
#148543=CYLINDRICAL_SURFACE ( 'NONE', #243345, 12.87499999999999822 ) ;
#148561=CARTESIAN_POINT ( 'NONE',  ( 19.97071067811864609, 51.35123479868923368, -230.1260867789306701 ) ) ;
#148573=CARTESIAN_POINT ( 'NONE',  ( -21.13435531349763963, 34.00405162396337033, -243.6249443725523918 ) ) ;
#148577=ORIENTED_EDGE ( 'NONE', *, *, #2239, .T. ) ;
#148619=FACE_OUTER_BOUND ( 'NONE', #207768, .T. ) ;
#148634=DIRECTION ( 'NONE',  ( 1.000000000000000000, 0.000000000000000000, 0.000000000000000000 ) ) ;
#148637=FACE_OUTER_BOUND ( 'NONE', #128192, .T. ) ;
#148660=ORIENTED_EDGE ( 'NONE', *, *, #106727, .F. ) ;
#148712=VERTEX_POINT ( 'NONE', #124866 ) ;
#148743=CARTESIAN_POINT ( 'NONE',  ( 21.00023020733502932, 30.82656943040776554, -252.1639858803266918 ) ) ;
#148755=CARTESIAN_POINT ( 'NONE',  ( 18.59999999999999432, 78.48087866980282001, -232.8271061603568910 ) ) ;
#148771=EDGE_LOOP ( 'NONE', ( #166133, #3400, #167561, #133898 ) ) ;
#148777=ORIENTED_EDGE ( 'NONE', *, *, #28010, .F. ) ;
#148781=AXIS2_PLACEMENT_3D ( 'NONE', #193970, #111860, #110562 ) ;
#148794=CARTESIAN_POINT ( 'NONE',  ( -18.46946985241332939, 46.92276463528965280, -255.3730311325347770 ) ) ;
#148821=DIRECTION ( 'NONE',  ( 0.000000000000000000, -0.9126074666063660468, -0.4088369013363524762 ) ) ;
#148831=CARTESIAN_POINT ( 'NONE',  ( -18.59117750673696889, 68.11287320386161070, -224.1382462126928488 ) ) ;
#148844=AXIS2_PLACEMENT_3D ( 'NONE', #168755, #69614, #228691 ) ;
#148860=AXIS2_PLACEMENT_3D ( 'NONE', #157786, #221527, #118628 ) ;
#148890=ORIENTED_EDGE ( 'NONE', *, *, #217815, .F. ) ;
#148946=ORIENTED_EDGE ( 'NONE', *, *, #221852, .F. ) ;
#148971=ORIENTED_EDGE ( 'NONE', *, *, #252854, .F. ) ;
#148972=CARTESIAN_POINT ( 'NONE',  ( 23.14999999999999503, 53.33306769324366314, -234.7945388949160872 ) ) ;
#148989=CARTESIAN_POINT ( 'NONE',  ( -23.15000000000000213, 51.38014393322265505, -230.1906178717505611 ) ) ;
#149016=DIRECTION ( 'NONE',  ( 2.952720810173289605E-16, 0.4088369013363286064, -0.9126074666063768159 ) ) ;
#149018=ORIENTED_EDGE ( 'NONE', *, *, #253487, .F. ) ;
#149026=AXIS2_PLACEMENT_3D ( 'NONE', #230961, #171015, #56127 ) ;
#149039=SPHERICAL_SURFACE ( 'NONE', #77806, 0.1000000000000000056 ) ;
#149052=CIRCLE ( 'NONE', #144911, 0.09999999999999681366 ) ;
#149066=FACE_OUTER_BOUND ( 'NONE', #192632, .T. ) ;
#149074=CARTESIAN_POINT ( 'NONE',  ( -21.05000000000000071, 46.45388641681647357, -243.1520440498138385 ) ) ;
#149088=ORIENTED_EDGE ( 'NONE', *, *, #141236, .T. ) ;
#149090=CARTESIAN_POINT ( 'NONE',  ( 20.94999999999999929, 53.66153320161009788, -235.9075159595686841 ) ) ;
#149094=ORIENTED_EDGE ( 'NONE', *, *, #94197, .F. ) ;
#149113=AXIS2_PLACEMENT_3D ( 'NONE', #58934, #176375, #159370 ) ;
#149115=DIRECTION ( 'NONE',  ( 0.000000000000000000, 0.4088369013363205573, -0.9126074666063803686 ) ) ;
#149117=DIRECTION ( 'NONE',  ( -1.000000000000000000, 0.000000000000000000, 0.000000000000000000 ) ) ;
#149174=VECTOR ( 'NONE', #50525, 1000.000000000000000 ) ;
#149185=EDGE_CURVE ( 'NONE', #228315, #25987, #166287, .T. ) ;
#149204=DIRECTION ( 'NONE',  ( 0.000000000000000000, 0.9126074666063545004, 0.4088369013363783999 ) ) ;
#149213=VECTOR ( 'NONE', #101656, 1000.000000000000000 ) ;
#149302=FACE_OUTER_BOUND ( 'NONE', #128677, .T. ) ;
#149348=AXIS2_PLACEMENT_3D ( 'NONE', #33607, #140009, #219554 ) ;
#149359=EDGE_LOOP ( 'NONE', ( #248506, #10492, #140580, #27729 ) ) ;
#149365=CYLINDRICAL_SURFACE ( 'NONE', #81793, 0.09999999999999939493 ) ;
#149372=DIRECTION ( 'NONE',  ( 0.000000000000000000, 0.9126074666063660468, 0.4088369013363524762 ) ) ;
#149387=DIRECTION ( 'NONE',  ( 1.000000000000000000, 2.986185139342073343E-16, -6.665775143889692774E-16 ) ) ;
#149396=CARTESIAN_POINT ( 'NONE',  ( 23.14999999999999503, 56.45527679911575802, -225.2871936083021467 ) ) ;
#149425=DIRECTION ( 'NONE',  ( -1.000000000000000000, 0.000000000000000000, 0.000000000000000000 ) ) ;
#149426=FACE_OUTER_BOUND ( 'NONE', #121085, .T. ) ;
#149427=SPHERICAL_SURFACE ( 'NONE', #177945, 0.1000000000000000056 ) ;
#149443=CYLINDRICAL_SURFACE ( 'NONE', #180143, 0.4999999999999944489 ) ;
#149448=DIRECTION ( 'NONE',  ( 0.000000000000000000, 0.4088369013363281623, -0.9126074666063771490 ) ) ;
#149452=SPHERICAL_SURFACE ( 'NONE', #232982, 0.1000000000000000056 ) ;
#149455=DIRECTION ( 'NONE',  ( -3.265361837132813093E-16, -0.4088369013363281068, 0.9126074666063770380 ) ) ;
#149457=FACE_OUTER_BOUND ( 'NONE', #95146, .T. ) ;
#149495=TOROIDAL_SURFACE ( 'NONE', #220228, 11.65000000000000036, 0.1000000000000000056 ) ;
#149531=ORIENTED_EDGE ( 'NONE', *, *, #150307, .F. ) ;
#149535=AXIS2_PLACEMENT_3D ( 'NONE', #182171, #100022, #120934 ) ;
#149608=FACE_OUTER_BOUND ( 'NONE', #99291, .T. ) ;
#149609=AXIS2_PLACEMENT_3D ( 'NONE', #225242, #144418, #223970 ) ;
#149626=ORIENTED_EDGE ( 'NONE', *, *, #7795, .T. ) ;
#149628=VERTEX_POINT ( 'NONE', #69432 ) ;
#149629=CARTESIAN_POINT ( 'NONE',  ( 21.12400247839527978, 43.45502593803676206, -234.7584006177618221 ) ) ;
#149640=CARTESIAN_POINT ( 'NONE',  ( 21.13507111622890022, 43.45582266793360304, -234.7622126887535785 ) ) ;
#149642=DIRECTION ( 'NONE',  ( 1.000000000000000000, 0.000000000000000000, 0.000000000000000000 ) ) ;
#149646=CARTESIAN_POINT ( 'NONE',  ( -21.05000000000000071, 43.44873802792533724, -245.1397081572968659 ) ) ;
#149658=DIRECTION ( 'NONE',  ( 0.000000000000000000, 0.1022405907414166287, 0.9947597004326452774 ) ) ;
#149671=VERTEX_POINT ( 'NONE', #148972 ) ;
#149684=VECTOR ( 'NONE', #92031, 1000.000000000000114 ) ;
#149717=DIRECTION ( 'NONE',  ( -0.000000000000000000, -0.9126074666063770380, -0.4088369013363281068 ) ) ;
#149739=CARTESIAN_POINT ( 'NONE',  ( 23.14999999999999858, 67.23127455305835554, -235.8551265064784559 ) ) ;
#149766=AXIS2_PLACEMENT_3D ( 'NONE', #178370, #257822, #2251 ) ;
#149799=ADVANCED_FACE ( 'NONE', ( #216620 ), #40437, .F. ) ;
#149803=CARTESIAN_POINT ( 'NONE',  ( -23.15000000000000213, 54.34471204062663219, -239.4366250215122420 ) ) ;
#149828=DIRECTION ( 'NONE',  ( 1.000000000000000000, 0.000000000000000000, 0.000000000000000000 ) ) ;
#149862=CARTESIAN_POINT ( 'NONE',  ( -23.25000000000000000, 46.15118611352045974, -240.5321844900040844 ) ) ;
#149864=DIRECTION ( 'NONE',  ( 0.000000000000000000, -0.9126074666063660468, -0.4088369013363524762 ) ) ;
#149868=EDGE_CURVE ( 'NONE', #239804, #187157, #119521, .T. ) ;
#149908=ORIENTED_EDGE ( 'NONE', *, *, #48951, .T. ) ;
#149921=ORIENTED_EDGE ( 'NONE', *, *, #208054, .F. ) ;
#149951=ORIENTED_EDGE ( 'NONE', *, *, #174805, .F. ) ;
#149954=ORIENTED_EDGE ( 'NONE', *, *, #141236, .F. ) ;
#149965=CIRCLE ( 'NONE', #12405, 0.1000000000000024342 ) ;
#149970=ORIENTED_EDGE ( 'NONE', *, *, #240682, .F. ) ;
#149976=ORIENTED_EDGE ( 'NONE', *, *, #98409, .F. ) ;
#150008=DIRECTION ( 'NONE',  ( 0.000000000000000000, 0.9126074666063757057, 0.4088369013363309379 ) ) ;
#150035=FACE_OUTER_BOUND ( 'NONE', #67194, .T. ) ;
#150067=DIRECTION ( 'NONE',  ( 1.000000000000000000, 0.000000000000000000, 0.000000000000000000 ) ) ;
#150083=ADVANCED_FACE ( 'NONE', ( #110792 ), #96346, .F. ) ;
#150102=VERTEX_POINT ( 'NONE', #131642 ) ;
#150105=DIRECTION ( 'NONE',  ( 0.000000000000000000, 0.4088369013363783999, -0.9126074666063545004 ) ) ;
#150106=VERTEX_POINT ( 'NONE', #112104 ) ;
#150110=EDGE_CURVE ( 'NONE', #55374, #90768, #182051, .T. ) ;
#150122=DIRECTION ( 'NONE',  ( 0.5000000000001141309, 0.7903412497644213275, 0.3540631425617453143 ) ) ;
#150131=DIRECTION ( 'NONE',  ( 1.000000000000000000, 0.000000000000000000, 0.000000000000000000 ) ) ;
#150144=EDGE_LOOP ( 'NONE', ( #110511, #154653, #78662 ) ) ;
#150151=EDGE_CURVE ( 'NONE', #111166, #38307, #192911, .T. ) ;
#150227=CIRCLE ( 'NONE', #62733, 11.74999999999999822 ) ;
#150257=ORIENTED_EDGE ( 'NONE', *, *, #82646, .F. ) ;
#150262=EDGE_LOOP ( 'NONE', ( #41583, #215453, #130634, #101674 ) ) ;
#150282=ADVANCED_FACE ( 'NONE', ( #37707 ), #42816, .T. ) ;
#150287=AXIS2_PLACEMENT_3D ( 'NONE', #106645, #102790, #83224 ) ;
#150307=EDGE_CURVE ( 'NONE', #206012, #38559, #115396, .T. ) ;
#150386=PLANE ( 'NONE',  #214236 ) ;
#150389=CARTESIAN_POINT ( 'NONE',  ( 21.04999999999999361, 30.92254191997125190, -252.0827843769733931 ) ) ;
#150445=DIRECTION ( 'NONE',  ( 1.000000000000000000, 2.986185139342066440E-16, -6.665775143889694746E-16 ) ) ;
#150456=EDGE_CURVE ( 'NONE', #228447, #213386, #198782, .T. ) ;
#150475=CARTESIAN_POINT ( 'NONE',  ( 22.39999999999999503, 31.85509083104287598, -238.8280249686205536 ) ) ;
#150480=CYLINDRICAL_SURFACE ( 'NONE', #85203, 0.4999999999999944489 ) ;
#150501=ORIENTED_EDGE ( 'NONE', *, *, #240682, .T. ) ;
#150542=EDGE_LOOP ( 'NONE', ( #156730, #168842, #73284, #211472 ) ) ;
#150570=DIRECTION ( 'NONE',  ( -1.000000000000000000, 1.207181226542539700E-16, -2.694675058168174199E-16 ) ) ;
#150572=ADVANCED_FACE ( 'NONE', ( #89624 ), #98262, .F. ) ;
#150599=DIRECTION ( 'NONE',  ( 0.000000000000000000, 0.8689845192018014197, -0.4948392722769828778 ) ) ;
#150650=DIRECTION ( 'NONE',  ( 1.000000000000000000, -0.000000000000000000, -0.000000000000000000 ) ) ;
#150673=AXIS2_PLACEMENT_3D ( 'NONE', #87573, #167166, #221937 ) ;
#150675=CYLINDRICAL_SURFACE ( 'NONE', #62666, 0.09999999999999771572 ) ;
#150691=DIRECTION ( 'NONE',  ( 1.000000000000000000, 0.000000000000000000, 0.000000000000000000 ) ) ;
#150739=VERTEX_POINT ( 'NONE', #27793 ) ;
#150759=ORIENTED_EDGE ( 'NONE', *, *, #245437, .T. ) ;
#150779=DIRECTION ( 'NONE',  ( 0.000000000000000000, -0.9126074666063545004, -0.4088369013363783999 ) ) ;
#150789=ORIENTED_EDGE ( 'NONE', *, *, #155085, .T. ) ;
#150837=ORIENTED_EDGE ( 'NONE', *, *, #11361, .F. ) ;
#150842=CARTESIAN_POINT ( 'NONE',  ( -20.54999999999999716, 49.36776662947724503, -253.7196102226803021 ) ) ;
#150876=EDGE_LOOP ( 'NONE', ( #39390, #18594, #112347, #229814 ) ) ;
#150899=ADVANCED_FACE ( 'NONE', ( #194661 ), #17290, .T. ) ;
#150917=CARTESIAN_POINT ( 'NONE',  ( -23.25000000000000000, 31.85509083104287598, -238.8280249686205536 ) ) ;
#150945=AXIS2_PLACEMENT_3D ( 'NONE', #134964, #76291, #56703 ) ;
#151001=ORIENTED_EDGE ( 'NONE', *, *, #197000, .T. ) ;
#151010=DIRECTION ( 'NONE',  ( 0.000000000000000000, 0.9126074666063545004, 0.4088369013363783999 ) ) ;
#151021=CIRCLE ( 'NONE', #167595, 11.74999999999999822 ) ;
#151025=DIRECTION ( 'NONE',  ( 1.000000000000000000, 0.000000000000000000, 0.000000000000000000 ) ) ;
#151036=ORIENTED_EDGE ( 'NONE', *, *, #9084, .F. ) ;
#151072=CIRCLE ( 'NONE', #96857, 3.999999999999989786 ) ;
#151080=CARTESIAN_POINT ( 'NONE',  ( -23.25000000000000000, 62.42906104934358069, -247.8683112431566258 ) ) ;
#151088=DIRECTION ( 'NONE',  ( 0.000000000000000000, 0.9126074666063751506, 0.4088369013363318816 ) ) ;
#151100=CARTESIAN_POINT ( 'NONE',  ( -23.15000000000000213, 41.42187432231295219, -260.1830396872097140 ) ) ;
#151159=VERTEX_POINT ( 'NONE', #189198 ) ;
#151160=ADVANCED_FACE ( 'NONE', ( #127938 ), #10564, .T. ) ;
#151174=ORIENTED_EDGE ( 'NONE', *, *, #99196, .F. ) ;
#151182=ORIENTED_EDGE ( 'NONE', *, *, #65809, .F. ) ;
#151198=CARTESIAN_POINT ( 'NONE',  ( -22.50047199488185257, 25.91738416313705429, -254.3140340802643209 ) ) ;
#151208=ORIENTED_EDGE ( 'NONE', *, *, #248812, .F. ) ;
#151229=DIRECTION ( 'NONE',  ( 1.000000000000000000, 0.000000000000000000, -0.000000000000000000 ) ) ;
#151257=ADVANCED_FACE ( 'NONE', ( #233474 ), #91015, .T. ) ;
#151276=CIRCLE ( 'NONE', #9596, 4.300000000000029132 ) ;
#151307=DIRECTION ( 'NONE',  ( 0.000000000000000000, 0.9126074666063844765, 0.4088369013363113980 ) ) ;
#151329=CARTESIAN_POINT ( 'NONE',  ( 20.85000000000000142, 67.75954444190071513, -227.8703747234148693 ) ) ;
#151343=ORIENTED_EDGE ( 'NONE', *, *, #252639, .F. ) ;
#151364=CARTESIAN_POINT ( 'NONE',  ( -23.25000000000000000, 69.16514130714681130, -247.7543978865853660 ) ) ;
#151397=SPHERICAL_SURFACE ( 'NONE', #81692, 0.1000000000000000056 ) ;
#151401=LINE ( 'NONE', #73161, #114002 ) ;
#151438=ORIENTED_EDGE ( 'NONE', *, *, #213526, .F. ) ;
#151467=ORIENTED_EDGE ( 'NONE', *, *, #158357, .F. ) ;
#151474=LINE ( 'NONE', #36673, #30804 ) ;
#151492=CARTESIAN_POINT ( 'NONE',  ( -23.25000000000000000, 26.06832281015329755, -254.4051978787608732 ) ) ;
#151493=EDGE_CURVE ( 'NONE', #83103, #70449, #51910, .T. ) ;
#151518=VERTEX_POINT ( 'NONE', #229303 ) ;
#151530=EDGE_LOOP ( 'NONE', ( #195725, #141195, #23943 ) ) ;
#151536=DIRECTION ( 'NONE',  ( -0.000000000000000000, 0.4088369013363281623, -0.9126074666063771490 ) ) ;
#151540=CARTESIAN_POINT ( 'NONE',  ( 21.05000000000000071, 40.73935534331184272, -238.0635479304912678 ) ) ;
#151549=ORIENTED_EDGE ( 'NONE', *, *, #201915, .T. ) ;
#151584=DIRECTION ( 'NONE',  ( 0.000000000000000000, 0.9126074666063844765, 0.4088369013363113980 ) ) ;
#151665=( NAMED_UNIT ( * ) PLANE_ANGLE_UNIT ( ) SI_UNIT ( $, .RADIAN. ) );
#151678=TOROIDAL_SURFACE ( 'NONE', #147554, 0.2000000000000000111, 0.1000000000000000056 ) ;
#151687=DIRECTION ( 'NONE',  ( -3.265361837132812600E-16, -0.4088369013363282178, 0.9126074666063768159 ) ) ;
#151715=AXIS2_PLACEMENT_3D ( 'NONE', #165587, #228123, #109428 ) ;
#151738=CARTESIAN_POINT ( 'NONE',  ( 21.05000000000000071, 62.33780030268294325, -247.9091949332902516 ) ) ;
#151767=VECTOR ( 'NONE', #6711, 999.9999999999998863 ) ;
#151804=VERTEX_POINT ( 'NONE', #48731 ) ;
#151816=ORIENTED_EDGE ( 'NONE', *, *, #250161, .F. ) ;
#151849=CYLINDRICAL_SURFACE ( 'NONE', #59629, 0.09999999999999939493 ) ;
#151857=ADVANCED_FACE ( 'NONE', ( #129571 ), #193410, .F. ) ;
#151920=SPHERICAL_SURFACE ( 'NONE', #16269, 0.1000000000000000056 ) ;
#151931=EDGE_LOOP ( 'NONE', ( #137265, #226640, #111297, #53716 ) ) ;
#151939=CARTESIAN_POINT ( 'NONE',  ( -21.04999999999999361, 30.88834551968416164, -252.0800683362990355 ) ) ;
#151944=ORIENTED_EDGE ( 'NONE', *, *, #115513, .T. ) ;
#151974=TOROIDAL_SURFACE ( 'NONE', #243517, 0.6000000000000009770, 0.1000000000000000056 ) ;
#151978=LINE ( 'NONE', #131097, #223941 ) ;
#151987=DIRECTION ( 'NONE',  ( 0.000000000000000000, -0.9126074666063769270, -0.4088369013363280513 ) ) ;
#151991=ADVANCED_FACE ( 'NONE', ( #99400 ), #153791, .F. ) ;
#152001=FACE_OUTER_BOUND ( 'NONE', #84570, .T. ) ;
#152018=CIRCLE ( 'NONE', #97786, 12.97500000000000675 ) ;
#152020=EDGE_CURVE ( 'NONE', #2253, #215594, #139820, .T. ) ;
#152024=AXIS2_PLACEMENT_3D ( 'NONE', #202581, #223408, #244254 ) ;
#152036=DIRECTION ( 'NONE',  ( 0.000000000000000000, 0.9126074666064696306, 0.4088369013361213278 ) ) ;
#152073=CARTESIAN_POINT ( 'NONE',  ( 23.14999999999999503, 53.24180694658302571, -234.8354225850497130 ) ) ;
#152116=CARTESIAN_POINT ( 'NONE',  ( 21.14999999999999858, 36.69980811187836878, -249.6424234479061113 ) ) ;
#152149=CARTESIAN_POINT ( 'NONE',  ( -21.17356465864818560, 33.94277835663822174, -243.7301031769779343 ) ) ;
#152169=DIRECTION ( 'NONE',  ( -1.000000000000000000, -0.000000000000000000, -0.000000000000000000 ) ) ;
#152202=CARTESIAN_POINT ( 'NONE',  ( 21.07016717456946964, 34.07469055596557439, -243.7826248964179854 ) ) ;
#152208=VECTOR ( 'NONE', #126287, 1000.000000000000000 ) ;
#152210=ORIENTED_EDGE ( 'NONE', *, *, #62846, .F. ) ;
#152237=EDGE_CURVE ( 'NONE', #25987, #213658, #58030, .T. ) ;
#152276=AXIS2_PLACEMENT_3D ( 'NONE', #48045, #224108, #8928 ) ;
#152284=ORIENTED_EDGE ( 'NONE', *, *, #83205, .T. ) ;
#152290=CYLINDRICAL_SURFACE ( 'NONE', #116889, 0.1000000000000076245 ) ;
#152327=CARTESIAN_POINT ( 'NONE',  ( 23.14999999999999858, 67.23127455305835554, -235.8551265064784559 ) ) ;
#152350=VECTOR ( 'NONE', #133061, 1000.000000000000114 ) ;
#152380=DIRECTION ( 'NONE',  ( 0.000000000000000000, 0.9126074666063769270, 0.4088369013363280513 ) ) ;
#152410=DIRECTION ( 'NONE',  ( -0.000000000000000000, -0.9126074666063770380, -0.4088369013363281068 ) ) ;
#152445=CARTESIAN_POINT ( 'NONE',  ( 21.05000000000000071, 69.19063053712525857, -247.5666987377248631 ) ) ;
#152461=AXIS2_PLACEMENT_3D ( 'NONE', #182965, #146365, #83801 ) ;
#152476=COLOUR_RGB ( '', 0.08235294, 0.09019608, 0.10196078) ;
#152501=DIRECTION ( 'NONE',  ( -1.000000000000000000, 0.000000000000000000, 0.000000000000000000 ) ) ;
#152506=ORIENTED_EDGE ( 'NONE', *, *, #86643, .F. ) ;
#152521=FACE_OUTER_BOUND ( 'NONE', #172413, .T. ) ;
#152530=AXIS2_PLACEMENT_3D ( 'NONE', #58315, #38789, #19218 ) ;
#152554=ORIENTED_EDGE ( 'NONE', *, *, #232314, .F. ) ;
#152567=AXIS2_PLACEMENT_3D ( 'NONE', #123789, #7701, #246302 ) ;
#152571=DIRECTION ( 'NONE',  ( 0.7071067811865476838, -0.2890913453342132122, 0.6453109281988448354 ) ) ;
#152593=LINE ( 'NONE', #194283, #193132 ) ;
#152594=DIRECTION ( 'NONE',  ( -0.000000000000000000, 0.09425075112713271475, 0.9955484899852801162 ) ) ;
#152626=AXIS2_PLACEMENT_3D ( 'NONE', #66616, #173476, #133018 ) ;
#152667=CARTESIAN_POINT ( 'NONE',  ( -18.50000000000000355, 47.07326788871597500, -255.0992659944397758 ) ) ;
#152685=VERTEX_POINT ( 'NONE', #70291 ) ;
#152693=DIRECTION ( 'NONE',  ( 0.000000000000000000, -0.4088369013363280513, 0.9126074666063769270 ) ) ;
#152713=VERTEX_POINT ( 'NONE', #9000 ) ;
#152752=ORIENTED_EDGE ( 'NONE', *, *, #23112, .F. ) ;
#152761=LINE ( 'NONE', #109728, #245606 ) ;
#152773=EDGE_CURVE ( 'NONE', #241027, #68027, #66630, .T. ) ;
#152783=ORIENTED_EDGE ( 'NONE', *, *, #111592, .T. ) ;
#152810=CIRCLE ( 'NONE', #202655, 0.4000000000000033529 ) ;
#152826=ADVANCED_FACE ( 'NONE', ( #85616 ), #64803, .T. ) ;
#152849=VECTOR ( 'NONE', #5076, 1000.000000000000114 ) ;
#152910=DIRECTION ( 'NONE',  ( 0.000000000000000000, 0.9126074666063660468, 0.4088369013363524762 ) ) ;
#152911=CARTESIAN_POINT ( 'NONE',  ( 21.05000000000000071, 36.65892442174472876, -249.5511627012454596 ) ) ;
#152975=CIRCLE ( 'NONE', #148860, 2.000000000000001776 ) ;
#152980=CARTESIAN_POINT ( 'NONE',  ( 21.04999999999999716, 30.92067721666403912, -252.0498334655604253 ) ) ;
#153009=FACE_OUTER_BOUND ( 'NONE', #198513, .T. ) ;
#153026=EDGE_CURVE ( 'NONE', #1847, #14385, #54309, .T. ) ;
#153042=FACE_OUTER_BOUND ( 'NONE', #126008, .T. ) ;
#153048=CARTESIAN_POINT ( 'NONE',  ( 20.95512820512820440, 44.11820694106860685, -236.4833523840364933 ) ) ;
#153087=AXIS2_PLACEMENT_3D ( 'NONE', #78110, #53427, #73031 ) ;
#153093=ORIENTED_EDGE ( 'NONE', *, *, #52623, .T. ) ;
#153103=DIRECTION ( 'NONE',  ( 1.000000000000000000, 0.000000000000000000, 0.000000000000000000 ) ) ;
#153109=EDGE_CURVE ( 'NONE', #240937, #157687, #178052, .T. ) ;
#153168=CYLINDRICAL_SURFACE ( 'NONE', #13895, 7.899999999999995914 ) ;
#153212=ADVANCED_FACE ( 'NONE', ( #34691 ), #170917, .F. ) ;
#153255=ORIENTED_EDGE ( 'NONE', *, *, #32037, .F. ) ;
#153277=AXIS2_PLACEMENT_3D ( 'NONE', #60478, #200015, #39679 ) ;
#153280=CYLINDRICAL_SURFACE ( 'NONE', #170101, 0.1000000000000024342 ) ;
#153313=CARTESIAN_POINT ( 'NONE',  ( -21.03571358705564975, 38.08373427723915228, -236.0376694442006169 ) ) ;
#153324=EDGE_CURVE ( 'NONE', #20493, #54257, #165504, .T. ) ;
#153329=ORIENTED_EDGE ( 'NONE', *, *, #201726, .T. ) ;
#153401=EDGE_CURVE ( 'NONE', #246455, #9598, #14513, .T. ) ;
#153404=CARTESIAN_POINT ( 'NONE',  ( 21.05000000000000071, 30.90801580390118630, -252.0203440857215469 ) ) ;
#153417=EDGE_CURVE ( 'NONE', #178795, #127037, #204334, .T. ) ;
#153456=ORIENTED_EDGE ( 'NONE', *, *, #186875, .T. ) ;
#153457=DIRECTION ( 'NONE',  ( -1.000000000000000000, -0.000000000000000000, 0.000000000000000000 ) ) ;
#153465=ORIENTED_EDGE ( 'NONE', *, *, #248744, .F. ) ;
#153484=ADVANCED_FACE ( 'NONE', ( #7094 ), #125753, .F. ) ;
#153493=AXIS2_PLACEMENT_3D ( 'NONE', #21596, #204058, #85366 ) ;
#153513=CARTESIAN_POINT ( 'NONE',  ( 0.000000000000000000, 0.000000000000000000, 0.000000000000000000 ) ) ;
#153514=CARTESIAN_POINT ( 'NONE',  ( 20.04142135623730070, 51.38014393322265505, -230.1906178717505611 ) ) ;
#153554=CARTESIAN_POINT ( 'NONE',  ( -20.94999999999999929, 56.27731819600170837, -227.9967441372480721 ) ) ;
#153596=VECTOR ( 'NONE', #109653, 1000.000000000000000 ) ;
#153616=VECTOR ( 'NONE', #25241, 1000.000000000000000 ) ;
#153618=DIRECTION ( 'NONE',  ( 0.000000000000000000, 0.9126074666063660468, 0.4088369013363524762 ) ) ;
#153634=CIRCLE ( 'NONE', #174483, 0.1000000000000024342 ) ;
#153663=TOROIDAL_SURFACE ( 'NONE', #45460, 0.2000000000000000111, 0.1000000000000000056 ) ;
#153686=ADVANCED_FACE ( 'NONE', ( #6465 ), #245085, .F. ) ;
#153691=ORIENTED_EDGE ( 'NONE', *, *, #182937, .T. ) ;
#153693=DIRECTION ( 'NONE',  ( -1.000000000000000000, -0.000000000000000000, -0.000000000000000000 ) ) ;
#153695=VERTEX_POINT ( 'NONE', #24788 ) ;
#153710=ORIENTED_EDGE ( 'NONE', *, *, #238528, .F. ) ;
#153729=AXIS2_PLACEMENT_3D ( 'NONE', #175437, #154597, #30792 ) ;
#153752=CARTESIAN_POINT ( 'NONE',  ( -21.05000000000000071, 36.65892442174472876, -249.5511627012454596 ) ) ;
#153761=ORIENTED_EDGE ( 'NONE', *, *, #192089, .F. ) ;
#153766=PLANE ( 'NONE',  #97569 ) ;
#153768=ORIENTED_EDGE ( 'NONE', *, *, #25153, .T. ) ;
#153787=DIRECTION ( 'NONE',  ( 0.000000000000000000, 0.9126074666063660468, 0.4088369013363524762 ) ) ;
#153791=TOROIDAL_SURFACE ( 'NONE', #187072, 0.9750000000000019762, 0.1000000000000000056 ) ;
#153810=CARTESIAN_POINT ( 'NONE',  ( 20.94999999999999929, 55.99424519013661694, -234.9720658648265896 ) ) ;
#153841=DIRECTION ( 'NONE',  ( -1.000000000000000000, -0.000000000000000000, 0.000000000000000000 ) ) ;
#153849=AXIS2_PLACEMENT_3D ( 'NONE', #222547, #84279, #221265 ) ;
#153877=ORIENTED_EDGE ( 'NONE', *, *, #163455, .F. ) ;
#153889=EDGE_CURVE ( 'NONE', #174500, #241398, #252773, .T. ) ;
#153942=CARTESIAN_POINT ( 'NONE',  ( -22.59999985501179154, 31.79527822860976016, -238.8549629533907250 ) ) ;
#153957=ORIENTED_EDGE ( 'NONE', *, *, #59158, .F. ) ;
#154005=CARTESIAN_POINT ( 'NONE',  ( -20.54999999999999716, 61.88149656937975607, -248.1136133839584090 ) ) ;
#154028=EDGE_LOOP ( 'NONE', ( #208202, #225644, #176298, #242795 ) ) ;
#154031=AXIS2_PLACEMENT_3D ( 'NONE', #10786, #254190, #36476 ) ;
#154066=ORIENTED_EDGE ( 'NONE', *, *, #180666, .T. ) ;
#154070=ORIENTED_EDGE ( 'NONE', *, *, #244905, .F. ) ;
#154125=ORIENTED_EDGE ( 'NONE', *, *, #193634, .T. ) ;
#154162=CARTESIAN_POINT ( 'NONE',  ( -21.05000000000000071, 44.55458850188623643, -247.3966190010231969 ) ) ;
#154171=CIRCLE ( 'NONE', #95835, 0.09999999999999939493 ) ;
#154182=LINE ( 'NONE', #233682, #57092 ) ;
#154205=ORIENTED_EDGE ( 'NONE', *, *, #140202, .F. ) ;
#154223=ADVANCED_FACE ( 'NONE', ( #206934 ), #251168, .T. ) ;
#154226=VERTEX_POINT ( 'NONE', #109100 ) ;
#154249=DIRECTION ( 'NONE',  ( 1.000000000000000000, 0.000000000000000000, 0.000000000000000000 ) ) ;
#154252=EDGE_CURVE ( 'NONE', #186873, #144175, #217353, .T. ) ;
#154262=DIRECTION ( 'NONE',  ( 1.000000000000000000, 0.000000000000000000, 0.000000000000000000 ) ) ;
#154285=DIRECTION ( 'NONE',  ( 0.000000000000000000, -0.4088369013363281068, 0.9126074666063770380 ) ) ;
#154320=EDGE_LOOP ( 'NONE', ( #136658, #218269, #110761, #164671 ) ) ;
#154323=ORIENTED_EDGE ( 'NONE', *, *, #32733, .T. ) ;
#154334=DIRECTION ( 'NONE',  ( 0.000000000000000000, -0.9126074666063769270, -0.4088369013363280513 ) ) ;
#154344=CARTESIAN_POINT ( 'NONE',  ( -18.59999999999999787, 43.48442877397276618, -245.2193771921251084 ) ) ;
#154390=EDGE_CURVE ( 'NONE', #137324, #79014, #167512, .T. ) ;
#154447=CARTESIAN_POINT ( 'NONE',  ( -20.64999999999999858, 44.91518204311810081, -238.0177672736398620 ) ) ;
#154449=DIRECTION ( 'NONE',  ( 1.000000000000000000, 0.000000000000000000, 0.000000000000000000 ) ) ;
#154460=CARTESIAN_POINT ( 'NONE',  ( 23.24999999999999289, 21.17283678855157802, -243.7231193059830048 ) ) ;
#154472=AXIS2_PLACEMENT_3D ( 'NONE', #7313, #228937, #29488 ) ;
#154473=ADVANCED_FACE ( 'NONE', ( #209057 ), #246588, .T. ) ;
#154476=VECTOR ( 'NONE', #240924, 1000.000000000000000 ) ;
#154511=EDGE_CURVE ( 'NONE', #236784, #21148, #105089, .T. ) ;
#154553=AXIS2_PLACEMENT_3D ( 'NONE', #170774, #112048, #232000 ) ;
#154558=EDGE_CURVE ( 'NONE', #248454, #233399, #42588, .T. ) ;
#154597=DIRECTION ( 'NONE',  ( 1.000000000000000000, 0.000000000000000000, 0.000000000000000000 ) ) ;
#154599=CARTESIAN_POINT ( 'NONE',  ( -22.39999999999999858, 31.80471377451587500, -238.9601694054148027 ) ) ;
#154653=ORIENTED_EDGE ( 'NONE', *, *, #215664, .T. ) ;
#154713=CARTESIAN_POINT ( 'NONE',  ( -21.05000000000000071, 38.08698097766499302, -236.1457910985472779 ) ) ;
#154721=DIRECTION ( 'NONE',  ( -1.000000000000000000, 1.335000415235278971E-16, -2.979993593738921214E-16 ) ) ;
#154730=EDGE_LOOP ( 'NONE', ( #58564, #179119, #81896, #238773 ) ) ;
#154742=CARTESIAN_POINT ( 'NONE',  ( -18.59999999999999787, 42.98415524044398950, -233.9519173640448173 ) ) ;
#154755=ORIENTED_EDGE ( 'NONE', *, *, #227876, .T. ) ;
#154757=DIRECTION ( 'NONE',  ( 0.000000000000000000, 0.9126074666063770380, 0.4088369013363281068 ) ) ;
#154783=CARTESIAN_POINT ( 'NONE',  ( -21.07016717456946964, 34.07469055596557439, -243.7826248964179854 ) ) ;
#154792=LINE ( 'NONE', #252566, #35249 ) ;
#154800=DIRECTION ( 'NONE',  ( 1.000000000000000000, 0.000000000000000000, 0.000000000000000000 ) ) ;
#154808=ADVANCED_FACE ( 'NONE', ( #112807 ), #13696, .F. ) ;
#154833=CARTESIAN_POINT ( 'NONE',  ( -20.54999999999999716, 46.10080905699345521, -240.6643289267983334 ) ) ;
#154858=CIRCLE ( 'NONE', #29957, 0.09999999999999939493 ) ;
#154861=ADVANCED_FACE ( 'NONE', ( #220875 ), #63087, .T. ) ;
#154865=EDGE_CURVE ( 'NONE', #121176, #184585, #71267, .T. ) ;
#154878=DIRECTION ( 'NONE',  ( 1.000000000000000000, 0.000000000000000000, -0.000000000000000000 ) ) ;
#154897=DIRECTION ( 'NONE',  ( 1.000000000000000000, -1.207181226542539700E-16, 2.694675058168174199E-16 ) ) ;
#154974=DIRECTION ( 'NONE',  ( 0.000000000000000000, 0.9126074666063844765, 0.4088369013363114535 ) ) ;
#154995=AXIS2_PLACEMENT_3D ( 'NONE', #51572, #172891, #249817 ) ;
#155001=ORIENTED_EDGE ( 'NONE', *, *, #44968, .T. ) ;
#155021=VECTOR ( 'NONE', #192991, 1000.000000000000000 ) ;
#155029=DIRECTION ( 'NONE',  ( -0.000000000000000000, 0.2599159095383575813, -0.9656312546561697241 ) ) ;
#155032=ORIENTED_EDGE ( 'NONE', *, *, #123537, .T. ) ;
#155033=LINE ( 'NONE', #53336, #222628 ) ;
#155042=CARTESIAN_POINT ( 'NONE',  ( 20.95512820512820440, 52.42293488718664207, -232.7629365818759481 ) ) ;
#155072=CARTESIAN_POINT ( 'NONE',  ( -22.39999999999999858, 25.97741635855165399, -254.4468634167653249 ) ) ;
#155085=EDGE_CURVE ( 'NONE', #253877, #105957, #171254, .T. ) ;
#155097=EDGE_LOOP ( 'NONE', ( #211195, #221022, #137770, #141114 ) ) ;
#155110=CARTESIAN_POINT ( 'NONE',  ( -2.995603634470829482E-16, 53.24180694658302571, -234.8354225850497130 ) ) ;
#155120=LINE ( 'NONE', #234617, #217821 ) ;
#155122=EDGE_LOOP ( 'NONE', ( #156481, #124142, #63810, #249093, #73066 ) ) ;
#155143=ORIENTED_EDGE ( 'NONE', *, *, #55570, .T. ) ;
#155154=EDGE_LOOP ( 'NONE', ( #76180, #246440, #96782, #42355 ) ) ;
#155218=AXIS2_PLACEMENT_3D ( 'NONE', #38956, #2361, #20681 ) ;
#155220=CIRCLE ( 'NONE', #213421, 0.4999999999999944489 ) ;
#155299=FACE_OUTER_BOUND ( 'NONE', #148468, .T. ) ;
#155315=CARTESIAN_POINT ( 'NONE',  ( -21.45000000000000284, 52.90028168070691095, -233.8284721206281915 ) ) ;
#155318=DIRECTION ( 'NONE',  ( 0.000000000000000000, 0.4088369013363280513, -0.9126074666063769270 ) ) ;
#155354=CYLINDRICAL_SURFACE ( 'NONE', #25369, 0.09999999999999108213 ) ;
#155373=ORIENTED_EDGE ( 'NONE', *, *, #76422, .T. ) ;
#155404=ORIENTED_EDGE ( 'NONE', *, *, #965, .T. ) ;
#155433=DIRECTION ( 'NONE',  ( -1.000000000000000000, -0.000000000000000000, 0.000000000000000000 ) ) ;
#155435=EDGE_LOOP ( 'NONE', ( #214602, #84208, #82779, #25177 ) ) ;
#155446=EDGE_CURVE ( 'NONE', #86798, #24027, #229583, .T. ) ;
#155462=CARTESIAN_POINT ( 'NONE',  ( 20.94999999999999929, 53.86595165227826243, -236.3638196928718855 ) ) ;
#155538=FACE_OUTER_BOUND ( 'NONE', #36985, .T. ) ;
#155566=CIRCLE ( 'NONE', #209694, 0.09999999999999108213 ) ;
#155599=DIRECTION ( 'NONE',  ( 0.000000000000000000, 0.5859227990963362664, 0.8103668758649469339 ) ) ;
#155621=DIRECTION ( 'NONE',  ( -1.000000000000000000, -0.000000000000000000, 0.000000000000000000 ) ) ;
#155629=ORIENTED_EDGE ( 'NONE', *, *, #71997, .F. ) ;
#155635=VERTEX_POINT ( 'NONE', #217681 ) ;
#155678=EDGE_CURVE ( 'NONE', #182258, #172675, #88322, .T. ) ;
#155696=DIRECTION ( 'NONE',  ( 0.000000000000000000, -0.9126074666063769270, -0.4088369013363280513 ) ) ;
#155700=EDGE_CURVE ( 'NONE', #62294, #60194, #175870, .T. ) ;
#155715=AXIS2_PLACEMENT_3D ( 'NONE', #142151, #101711, #82151 ) ;
#155719=AXIS2_PLACEMENT_3D ( 'NONE', #229919, #185655, #109961 ) ;
#155725=EDGE_CURVE ( 'NONE', #115637, #241027, #238191, .T. ) ;
#155743=EDGE_CURVE ( 'NONE', #223565, #59699, #250661, .T. ) ;
#155744=VERTEX_POINT ( 'NONE', #46763 ) ;
#155747=CIRCLE ( 'NONE', #251569, 0.09999999999999939493 ) ;
#155777=CARTESIAN_POINT ( 'NONE',  ( -20.64999999999999858, 47.57365439703043108, -242.5355162900727919 ) ) ;
#155792=CARTESIAN_POINT ( 'NONE',  ( 18.59999999999999076, 54.95667902235472013, -229.8578999281555753 ) ) ;
#155850=CARTESIAN_POINT ( 'NONE',  ( -21.44999999999999929, 45.00644278977874535, -237.9768835835062077 ) ) ;
#155853=CIRCLE ( 'NONE', #210007, 4.049999999999974953 ) ;
#155892=AXIS2_PLACEMENT_3D ( 'NONE', #123849, #144668, #104250 ) ;
#155923=FACE_OUTER_BOUND ( 'NONE', #46952, .T. ) ;
#155945=AXIS2_PLACEMENT_3D ( 'NONE', #54293, #230375, #115557 ) ;
#155952=AXIS2_PLACEMENT_3D ( 'NONE', #21645, #239405, #42474 ) ;
#155984=DIRECTION ( 'NONE',  ( 1.000000000000000000, 0.000000000000000000, 0.000000000000000000 ) ) ;
#155991=DIRECTION ( 'NONE',  ( -0.000000000000000000, -0.2606175937107957918, 0.9654421110809259243 ) ) ;
#155999=AXIS2_PLACEMENT_3D ( 'NONE', #187050, #206584, #244420 ) ;
#156018=ORIENTED_EDGE ( 'NONE', *, *, #182744, .F. ) ;
#156023=EDGE_CURVE ( 'NONE', #169719, #62507, #180852, .T. ) ;
#156039=CIRCLE ( 'NONE', #27054, 0.1000000000000078465 ) ;
#156055=EDGE_CURVE ( 'NONE', #226018, #242431, #142687, .T. ) ;
#156076=CARTESIAN_POINT ( 'NONE',  ( 19.97071067811864609, 54.36283943849028333, -228.7769250045207912 ) ) ;
#156093=ORIENTED_EDGE ( 'NONE', *, *, #237427, .F. ) ;
#156094=ORIENTED_EDGE ( 'NONE', *, *, #209631, .T. ) ;
#156103=DIRECTION ( 'NONE',  ( 0.000000000000000000, 0.9126074666063545004, 0.4088369013363783999 ) ) ;
#156137=CARTESIAN_POINT ( 'NONE',  ( -20.94999999999999929, 38.23914636435922176, -236.1324109481172968 ) ) ;
#156154=DIRECTION ( 'NONE',  ( 1.000000000000000000, 0.000000000000000000, 0.000000000000000000 ) ) ;
#156174=ADVANCED_FACE ( 'NONE', ( #122161 ), #84249, .F. ) ;
#156177=DIRECTION ( 'NONE',  ( -0.000000000000000000, 0.9579639084728068799, 0.2868887416116283617 ) ) ;
#156185=DIRECTION ( 'NONE',  ( -0.000000000000000000, -0.4088369013363281623, 0.9126074666063771490 ) ) ;
#156200=FACE_OUTER_BOUND ( 'NONE', #54416, .T. ) ;
#156223=CARTESIAN_POINT ( 'NONE',  ( 20.85000000000000142, 67.23127455305835554, -235.8551265064784559 ) ) ;
#156234=ADVANCED_FACE ( 'NONE', ( #77251 ), #149443, .F. ) ;
#156243=ADVANCED_FACE ( 'NONE', ( #137234 ), #257133, .F. ) ;
#156282=EDGE_LOOP ( 'NONE', ( #180292, #160444, #249121, #237020 ) ) ;
#156290=CARTESIAN_POINT ( 'NONE',  ( -22.47071067811865319, 29.57301391503005661, -252.6169816238249552 ) ) ;
#156294=TOROIDAL_SURFACE ( 'NONE', #10524, 11.65000000000000036, 0.1000000000000000056 ) ;
#156302=VECTOR ( 'NONE', #57786, 1000.000000000000114 ) ;
#156303=SPHERICAL_SURFACE ( 'NONE', #212659, 0.1000000000000000056 ) ;
#156309=UNCERTAINTY_MEASURE_WITH_UNIT (LENGTH_MEASURE( 1.000000000000000082E-05 ), #60655, 'distance_accuracy_value', 'NONE');
#156324=DIRECTION ( 'NONE',  ( -7.304098846218134667E-16, -0.4088369013363281068, 0.9126074666063770380 ) ) ;
#156348=CARTESIAN_POINT ( 'NONE',  ( -23.15000000000000213, 54.18213181965657554, -236.9344197582443883 ) ) ;
#156360=DIRECTION ( 'NONE',  ( 0.000000000000000000, -0.9947597004326491632, 0.1022405907413782566 ) ) ;
#156371=CARTESIAN_POINT ( 'NONE',  ( 20.94999999999999574, 43.97124485275623584, -258.7804622366496119 ) ) ;
#156419=DIRECTION ( 'NONE',  ( 0.000000000000000000, -0.4088369013363281623, 0.9126074666063771490 ) ) ;
#156453=CIRCLE ( 'NONE', #181377, 0.2000000000000048683 ) ;
#156454=CARTESIAN_POINT ( 'NONE',  ( 21.14999999999999858, 30.90801580390627734, -252.0203440857197279 ) ) ;
#156458=LINE ( 'NONE', #37778, #215136 ) ;
#156459=AXIS2_PLACEMENT_3D ( 'NONE', #81734, #202995, #145585 ) ;
#156473=EDGE_CURVE ( 'NONE', #183612, #244854, #165813, .T. ) ;
#156481=ORIENTED_EDGE ( 'NONE', *, *, #233943, .F. ) ;
#156484=DIRECTION ( 'NONE',  ( 0.000000000000000000, 0.9126074666063770380, 0.4088369013363281068 ) ) ;
#156489=CIRCLE ( 'NONE', #98144, 0.09999999999999609201 ) ;
#156490=ORIENTED_EDGE ( 'NONE', *, *, #201969, .F. ) ;
#156503=LINE ( 'NONE', #14415, #152350 ) ;
#156509=EDGE_CURVE ( 'NONE', #60290, #97714, #208779, .T. ) ;
#156553=EDGE_CURVE ( 'NONE', #171102, #221915, #1697, .T. ) ;
#156554=CARTESIAN_POINT ( 'NONE',  ( 20.94999999999999929, 56.27731819600170837, -227.9967441372480437 ) ) ;
#156569=ORIENTED_EDGE ( 'NONE', *, *, #135583, .T. ) ;
#156575=LINE ( 'NONE', #256866, #263 ) ;
#156588=FACE_OUTER_BOUND ( 'NONE', #75705, .T. ) ;
#156614=EDGE_LOOP ( 'NONE', ( #49, #50030, #100485, #253953 ) ) ;
#156622=AXIS2_PLACEMENT_3D ( 'NONE', #236061, #251777, #52271 ) ;
#156650=ORIENTED_EDGE ( 'NONE', *, *, #3102, .F. ) ;
#156664=CYLINDRICAL_SURFACE ( 'NONE', #89718, 0.09999999999999609201 ) ;
#156711=ADVANCED_FACE ( 'NONE', ( #222876 ), #177379, .F. ) ;
#156720=DIRECTION ( 'NONE',  ( 0.7071067811865475727, -0.2890913453342130457, 0.6453109281988449464 ) ) ;
#156730=ORIENTED_EDGE ( 'NONE', *, *, #116118, .T. ) ;
#156749=CARTESIAN_POINT ( 'NONE',  ( 18.48197441911733208, 77.41062428956240637, -241.7243103415940766 ) ) ;
#156769=ORIENTED_EDGE ( 'NONE', *, *, #83205, .F. ) ;
#156772=EDGE_CURVE ( 'NONE', #7959, #30904, #198185, .T. ) ;
#156774=EDGE_CURVE ( 'NONE', #248466, #19155, #62535, .T. ) ;
#156810=DIRECTION ( 'NONE',  ( 0.000000000000000000, -0.9594490217226104845, -0.2818822000686205809 ) ) ;
#156811=ADVANCED_FACE ( 'NONE', ( #83343 ), #162938, .F. ) ;
#156817=FACE_OUTER_BOUND ( 'NONE', #179887, .T. ) ;
#156819=LINE ( 'NONE', #176374, #182002 ) ;
#156821=EDGE_CURVE ( 'NONE', #231797, #243814, #180974, .T. ) ;
#156842=CARTESIAN_POINT ( 'NONE',  ( -22.48970261584618058, 31.84544391280713072, -238.9419228052725543 ) ) ;
#156845=EDGE_CURVE ( 'NONE', #228584, #89549, #40111, .T. ) ;
#156855=DIRECTION ( 'NONE',  ( -0.000000000000000000, 0.9126074666063770380, 0.4088369013363281068 ) ) ;
#156861=CARTESIAN_POINT ( 'NONE',  ( 21.05000000000000071, 67.23127455305835554, -235.8551265064784559 ) ) ;
#156866=ORIENTED_EDGE ( 'NONE', *, *, #36347, .T. ) ;
#156908=ORIENTED_EDGE ( 'NONE', *, *, #219086, .T. ) ;
#156935=CIRCLE ( 'NONE', #86157, 1.999999999999994893 ) ;
#156941=DIRECTION ( 'NONE',  ( 0.000000000000000000, 0.9126074666063770380, 0.4088369013363281068 ) ) ;
#156973=EDGE_LOOP ( 'NONE', ( #27412, #131668, #78129, #254185 ) ) ;
#157016=CARTESIAN_POINT ( 'NONE',  ( 21.06600267594171783, 44.20901405692286090, -236.5533276467423320 ) ) ;
#157019=CARTESIAN_POINT ( 'NONE',  ( -21.45000000000000284, 52.80902093404626640, -233.8693558107618173 ) ) ;
#157032=CYLINDRICAL_SURFACE ( 'NONE', #242114, 4.049999999999994493 ) ;
#157120=DIRECTION ( 'NONE',  ( 1.000000000000000000, 0.000000000000000000, 0.000000000000000000 ) ) ;
#157186=ORIENTED_EDGE ( 'NONE', *, *, #229832, .T. ) ;
#157196=AXIS2_PLACEMENT_3D ( 'NONE', #61681, #60384, #62962 ) ;
#157210=EDGE_CURVE ( 'NONE', #177788, #97714, #77087, .T. ) ;
#157280=DIRECTION ( 'NONE',  ( 0.000000000000000000, 0.9126074666063545004, 0.4088369013363783999 ) ) ;
#157335=CIRCLE ( 'NONE', #48965, 11.70000000000000462 ) ;
#157359=PLANE ( 'NONE',  #60218 ) ;
#157394=TOROIDAL_SURFACE ( 'NONE', #144872, 0.2000000000000000111, 0.1000000000000000056 ) ;
#157441=CARTESIAN_POINT ( 'NONE',  ( -22.44366136229477249, 26.02348510400886639, -254.3054723516606259 ) ) ;
#157455=DIRECTION ( 'NONE',  ( -1.000000000000000000, -0.000000000000000000, -0.000000000000000000 ) ) ;
#157458=CARTESIAN_POINT ( 'NONE',  ( -18.41809261886931992, 77.26488344959624044, -241.9697967765189048 ) ) ;
#157461=VECTOR ( 'NONE', #223211, 1000.000000000000227 ) ;
#157490=DIRECTION ( 'NONE',  ( 1.000000000000000000, 0.000000000000000000, 0.000000000000000000 ) ) ;
#157522=AXIS2_PLACEMENT_3D ( 'NONE', #16850, #250308, #15579 ) ;
#157590=FACE_OUTER_BOUND ( 'NONE', #26367, .T. ) ;
#157599=DIRECTION ( 'NONE',  ( 1.000000000000000000, 0.000000000000000000, 0.000000000000000000 ) ) ;
#157647=DIRECTION ( 'NONE',  ( -0.000000000000000000, -0.09425075112713271475, -0.9955484899852801162 ) ) ;
#157652=VERTEX_POINT ( 'NONE', #128322 ) ;
#157660=DIRECTION ( 'NONE',  ( 2.952720810173288619E-16, 0.4088369013363286064, -0.9126074666063768159 ) ) ;
#157679=CARTESIAN_POINT ( 'NONE',  ( 21.14999999999999858, 31.98723526783714988, -238.8784020251475511 ) ) ;
#157687=VERTEX_POINT ( 'NONE', #47464 ) ;
#157691=DIRECTION ( 'NONE',  ( -1.000000000000000000, 0.000000000000000000, 0.000000000000000000 ) ) ;
#157711=CARTESIAN_POINT ( 'NONE',  ( -20.89192007715127630, 68.10318897902124036, -224.1464165264002872 ) ) ;
#157737=ORIENTED_EDGE ( 'NONE', *, *, #221440, .F. ) ;
#157750=ORIENTED_EDGE ( 'NONE', *, *, #112644, .T. ) ;
#157751=DIRECTION ( 'NONE',  ( -0.7070776581708965169, 0.2891032514073239024, -0.6453375049857822399 ) ) ;
#157786=CARTESIAN_POINT ( 'NONE',  ( -23.15000000000000213, 67.23127455305835554, -235.8551265064784559 ) ) ;
#157835=VECTOR ( 'NONE', #211061, 1000.000000000000114 ) ;
#157846=CARTESIAN_POINT ( 'NONE',  ( 21.05000000000000071, 56.16603649944111254, -228.1013850343386480 ) ) ;
#157855=ORIENTED_EDGE ( 'NONE', *, *, #251674, .F. ) ;
#157890=CARTESIAN_POINT ( 'NONE',  ( -20.64999999999999858, 54.18213181965657554, -236.9344197582443883 ) ) ;
#157896=ADVANCED_FACE ( 'NONE', ( #129597 ), #208707, .F. ) ;
#157959=FACE_OUTER_BOUND ( 'NONE', #37193, .T. ) ;
#157961=CARTESIAN_POINT ( 'NONE',  ( -20.64999999999999858, 67.23127455305835554, -235.8551265064784559 ) ) ;
#157998=CIRCLE ( 'NONE', #212125, 0.09999999999999939493 ) ;
#158012=DIRECTION ( 'NONE',  ( -1.000000000000000000, 0.000000000000000000, 0.000000000000000000 ) ) ;
#158029=VERTEX_POINT ( 'NONE', #127872 ) ;
#158049=CARTESIAN_POINT ( 'NONE',  ( -20.94999999999999929, 67.23127455305835554, -235.8551265064784559 ) ) ;
#158060=CYLINDRICAL_SURFACE ( 'NONE', #249985, 0.09999999999999609201 ) ;
#158083=ORIENTED_EDGE ( 'NONE', *, *, #111407, .F. ) ;
#158106=CARTESIAN_POINT ( 'NONE',  ( 18.49999999999999289, 55.01984530832636011, -230.0610957569644199 ) ) ;
#158112=DIRECTION ( 'NONE',  ( 0.7071067811865475727, -0.2890913453342130457, 0.6453109281988448354 ) ) ;
#158130=LINE ( 'NONE', #238909, #57547 ) ;
#158167=LINE ( 'NONE', #241508, #157461 ) ;
#158196=DIRECTION ( 'NONE',  ( 0.000000000000000000, 0.9126074666063768159, 0.4088369013363282178 ) ) ;
#158218=CARTESIAN_POINT ( 'NONE',  ( 20.94999999999999929, 46.45388641681647357, -243.1520440498138385 ) ) ;
#158224=CIRCLE ( 'NONE', #54118, 11.80000000000000249 ) ;
#158233=ADVANCED_FACE ( 'NONE', ( #157959 ), #156664, .T. ) ;
#158254=DIRECTION ( 'NONE',  ( 1.000000000000000000, 0.000000000000000000, 0.000000000000000000 ) ) ;
#158282=PLANE ( 'NONE',  #76397 ) ;
#158292=TOROIDAL_SURFACE ( 'NONE', #75074, 0.9750000000000019762, 0.1000000000000000056 ) ;
#158313=CARTESIAN_POINT ( 'NONE',  ( 21.04999999999908411, 44.16625465172463549, -236.5712595585798965 ) ) ;
#158329=ORIENTED_EDGE ( 'NONE', *, *, #51023, .F. ) ;
#158351=CARTESIAN_POINT ( 'NONE',  ( 20.94999999999999574, 40.74071615341952679, -237.9411309446948337 ) ) ;
#158353=CIRCLE ( 'NONE', #79189, 0.09999999999999609201 ) ;
#158357=EDGE_CURVE ( 'NONE', #62147, #41411, #247938, .T. ) ;
#158414=CARTESIAN_POINT ( 'NONE',  ( -20.94999999999999929, 74.93036000061670165, -233.6816308724374949 ) ) ;
#158422=DIRECTION ( 'NONE',  ( -1.000000000000000000, -0.000000000000000000, -0.000000000000000000 ) ) ;
#158462=AXIS2_PLACEMENT_3D ( 'NONE', #2651, #77057, #82166 ) ;
#158493=CARTESIAN_POINT ( 'NONE',  ( 20.94999999999999929, 70.88170441948386724, -234.2197789011331679 ) ) ;
#158511=LINE ( 'NONE', #116789, #80143 ) ;
#158523=CARTESIAN_POINT ( 'NONE',  ( 18.54148534481893407, 68.09306500613196533, -224.1549646960459086 ) ) ;
#158526=TOROIDAL_SURFACE ( 'NONE', #250095, 0.2000000000000000111, 0.1000000000000000056 ) ;
#158528=EDGE_LOOP ( 'NONE', ( #255092, #195106, #147090, #38322, #195706, #135460, #216671, #127000, #123541, #178788, #135762, #228217, #33825, #51817, #177427, #256097 ) ) ;
#158540=ORIENTED_EDGE ( 'NONE', *, *, #134124, .T. ) ;
#158623=ORIENTED_EDGE ( 'NONE', *, *, #124523, .F. ) ;
#158632=EDGE_CURVE ( 'NONE', #144175, #151159, #89892, .T. ) ;
#158663=FACE_OUTER_BOUND ( 'NONE', #21936, .T. ) ;
#158666=DIRECTION ( 'NONE',  ( 1.000000000000000000, 0.000000000000000000, -0.000000000000000000 ) ) ;
#158685=DIRECTION ( 'NONE',  ( -1.000000000000000000, -0.000000000000000000, -0.000000000000000000 ) ) ;
#158702=EDGE_LOOP ( 'NONE', ( #110327, #71072, #145246, #63539 ) ) ;
#158704=DIRECTION ( 'NONE',  ( -1.000000000000000000, -0.000000000000000000, -0.000000000000000000 ) ) ;
#158719=FACE_OUTER_BOUND ( 'NONE', #238023, .T. ) ;
#158721=VECTOR ( 'NONE', #29196, 1000.000000000000000 ) ;
#158736=CARTESIAN_POINT ( 'NONE',  ( -18.31572283045078109, 77.38696040852184410, -241.7683136019773542 ) ) ;
#158744=CARTESIAN_POINT ( 'NONE',  ( 23.25000000000000000, 51.33926024308902214, -230.0993571250899095 ) ) ;
#158749=CARTESIAN_POINT ( 'NONE',  ( -18.50000000000000711, 47.12422580718823895, -255.1840357777358577 ) ) ;
#158785=ORIENTED_EDGE ( 'NONE', *, *, #66536, .F. ) ;
#158825=AXIS2_PLACEMENT_3D ( 'NONE', #38924, #101396, #19350 ) ;
#158838=DIRECTION ( 'NONE',  ( 0.000000000000000000, -0.9126074666063769270, -0.4088369013363280513 ) ) ;
#158906=DIRECTION ( 'NONE',  ( 1.000000000000000000, 0.000000000000000000, 0.000000000000000000 ) ) ;
#158928=EDGE_CURVE ( 'NONE', #61955, #108295, #37361, .T. ) ;
#158930=FACE_OUTER_BOUND ( 'NONE', #192172, .T. ) ;
#158947=CARTESIAN_POINT ( 'NONE',  ( -18.50000000000000000, 74.73788286442776041, -233.7359682632885267 ) ) ;
#158949=DIRECTION ( 'NONE',  ( 0.000000000000000000, -0.4230464831072829335, 0.9061079809440810706 ) ) ;
#158964=DIRECTION ( 'NONE',  ( 0.000000000000000000, 0.2868887416115947775, -0.9579639084728169829 ) ) ;
#158988=ORIENTED_EDGE ( 'NONE', *, *, #162121, .F. ) ;
#158989=VECTOR ( 'NONE', #199410, 1000.000000000000000 ) ;
#158999=ORIENTED_EDGE ( 'NONE', *, *, #209159, .T. ) ;
#159029=CIRCLE ( 'NONE', #13257, 0.09999999999999609201 ) ;
#159062=CARTESIAN_POINT ( 'NONE',  ( 20.94999999999999929, 74.93036000061670165, -233.6816308724374949 ) ) ;
#159071=CIRCLE ( 'NONE', #225657, 0.1000000000000056677 ) ;
#159109=CARTESIAN_POINT ( 'NONE',  ( 20.99142135623731065, 56.16603649944111254, -228.1013850343386196 ) ) ;
#159127=ORIENTED_EDGE ( 'NONE', *, *, #220382, .T. ) ;
#159147=EDGE_LOOP ( 'NONE', ( #244215, #175823, #122248, #245741 ) ) ;
#159165=CIRCLE ( 'NONE', #254757, 0.1000000000000024342 ) ;
#159168=LINE ( 'NONE', #195727, #233609 ) ;
#159194=CARTESIAN_POINT ( 'NONE',  ( 21.14999999999999858, 30.68987205111126926, -252.2252246220829193 ) ) ;
#159234=ORIENTED_EDGE ( 'NONE', *, *, #226259, .F. ) ;
#159237=ORIENTED_EDGE ( 'NONE', *, *, #20523, .T. ) ;
#159272=DIRECTION ( 'NONE',  ( 0.000000000000000000, 0.9126074666063771490, 0.4088369013363281623 ) ) ;
#159288=CARTESIAN_POINT ( 'NONE',  ( 18.49999999999999289, 21.76214302935564859, -245.0385711982110877 ) ) ;
#159294=ADVANCED_FACE ( 'NONE', ( #142542 ), #160856, .F. ) ;
#159297=DIRECTION ( 'NONE',  ( -3.469446951953749873E-14, 0.4088369013363783999, -0.9126074666063545004 ) ) ;
#159342=DIRECTION ( 'NONE',  ( 0.000000000000000000, -0.9126074666063771490, -0.4088369013363281623 ) ) ;
#159366=CARTESIAN_POINT ( 'NONE',  ( -1.820710678118657944, 63.30541909908242104, -248.4939929664152203 ) ) ;
#159369=EDGE_CURVE ( 'NONE', #973, #92460, #143825, .T. ) ;
#159370=DIRECTION ( 'NONE',  ( 0.000000000000000000, 0.9126074666063660468, 0.4088369013363524762 ) ) ;
#159372=CARTESIAN_POINT ( 'NONE',  ( -18.59999999999999787, 25.65398771707549841, -256.3298696899526021 ) ) ;
#159382=LINE ( 'NONE', #74738, #250907 ) ;
#159413=DIRECTION ( 'NONE',  ( -1.000000000000000000, -0.000000000000000000, 0.000000000000000000 ) ) ;
#159423=DIRECTION ( 'NONE',  ( -1.000000000000000000, -0.000000000000000000, -0.000000000000000000 ) ) ;
#159449=ORIENTED_EDGE ( 'NONE', *, *, #131290, .F. ) ;
#159457=CARTESIAN_POINT ( 'NONE',  ( 19.58285714285715073, 40.65800978083061779, -237.8813314257687352 ) ) ;
#159469=TOROIDAL_SURFACE ( 'NONE', #155218, 0.2000000000000000111, 0.1000000000000000056 ) ;
#159470=CIRCLE ( 'NONE', #197036, 11.65000000000000213 ) ;
#159521=CARTESIAN_POINT ( 'NONE',  ( 23.14999999999999858, 30.73962027982165424, -265.0781340245722504 ) ) ;
#159524=CARTESIAN_POINT ( 'NONE',  ( -23.25000000000000000, 54.89227652059045681, -239.1913228807104588 ) ) ;
#159525=ORIENTED_EDGE ( 'NONE', *, *, #229081, .F. ) ;
#159550=EDGE_CURVE ( 'NONE', #62719, #180643, #156935, .T. ) ;
#159557=CYLINDRICAL_SURFACE ( 'NONE', #105428, 0.09999999999999939493 ) ;
#159567=CARTESIAN_POINT ( 'NONE',  ( 21.09706851349342216, 44.23730524916371110, -236.5399123196797007 ) ) ;
#159604=DIRECTION ( 'NONE',  ( 0.000000000000000000, 0.9126074666063769270, 0.4088369013363280513 ) ) ;
#159672=AXIS2_PLACEMENT_3D ( 'NONE', #50726, #130281, #125792 ) ;
#159678=CARTESIAN_POINT ( 'NONE',  ( 18.52351027002948314, 77.30154854284161559, -241.9092773799638962 ) ) ;
#159694=AXIS2_PLACEMENT_3D ( 'NONE', #92070, #171654, #251128 ) ;
#159705=EDGE_LOOP ( 'NONE', ( #242640, #132958, #95084, #78937 ) ) ;
#159708=CARTESIAN_POINT ( 'NONE',  ( 23.14999999999999858, 45.58907629467868361, -240.2765730862633404 ) ) ;
#159717=ORIENTED_EDGE ( 'NONE', *, *, #2277, .F. ) ;
#159748=AXIS2_PLACEMENT_3D ( 'NONE', #208592, #190305, #10384 ) ;
#159764=CARTESIAN_POINT ( 'NONE',  ( 23.14999999999999503, 51.28888318656201761, -230.2315015618841869 ) ) ;
#159774=DIRECTION ( 'NONE',  ( 1.000000000000000000, 0.000000000000000000, 0.000000000000000000 ) ) ;
#159781=DIRECTION ( 'NONE',  ( -1.000000000000000000, 7.510212038922847255E-17, -1.676432719286211941E-16 ) ) ;
#159800=EDGE_CURVE ( 'NONE', #63414, #118225, #228019, .T. ) ;
#159827=CARTESIAN_POINT ( 'NONE',  ( 23.25000000000000000, 30.69873658968802133, -264.9868732779115703 ) ) ;
#159840=ORIENTED_EDGE ( 'NONE', *, *, #156509, .T. ) ;
#159847=ORIENTED_EDGE ( 'NONE', *, *, #177064, .T. ) ;
#159867=ORIENTED_EDGE ( 'NONE', *, *, #32037, .T. ) ;
#159872=ADVANCED_FACE ( 'NONE', ( #32284 ), #92218, .T. ) ;
#159909=FACE_OUTER_BOUND ( 'NONE', #26104, .T. ) ;
#159914=ORIENTED_EDGE ( 'NONE', *, *, #1108, .F. ) ;
#159924=LINE ( 'NONE', #64646, #11350 ) ;
#159941=FACE_OUTER_BOUND ( 'NONE', #130932, .T. ) ;
#159970=CARTESIAN_POINT ( 'NONE',  ( -20.54999999999999716, 44.01574086017817677, -236.0100308471058099 ) ) ;
#160013=CARTESIAN_POINT ( 'NONE',  ( -18.39999999999999858, 77.13860723519890428, -241.8264964602989266 ) ) ;
#160028=EDGE_CURVE ( 'NONE', #132474, #22954, #159924, .T. ) ;
#160045=CARTESIAN_POINT ( 'NONE',  ( 21.05000000000000071, 36.65892442174472876, -249.5511627012454596 ) ) ;
#160054=EDGE_CURVE ( 'NONE', #220241, #192597, #69996, .T. ) ;
#160055=VECTOR ( 'NONE', #192265, 1000.000000000000114 ) ;
#160066=EDGE_CURVE ( 'NONE', #228447, #111770, #184592, .T. ) ;
#160081=CARTESIAN_POINT ( 'NONE',  ( 21.09813707148777340, 34.01986380303547008, -243.7369249987247883 ) ) ;
#160120=CARTESIAN_POINT ( 'NONE',  ( -21.14999999999999858, 31.98723526783714988, -238.8784020251475511 ) ) ;
#160122=DIRECTION ( 'NONE',  ( 0.000000000000000000, -0.9126074666063545004, -0.4088369013363783999 ) ) ;
#160138=CARTESIAN_POINT ( 'NONE',  ( 18.59999999999999432, 22.88260507592945814, -249.4775442468527729 ) ) ;
#160142=AXIS2_PLACEMENT_3D ( 'NONE', #81851, #143127, #162729 ) ;
#160156=VECTOR ( 'NONE', #133751, 1000.000000000000114 ) ;
#160160=VECTOR ( 'NONE', #37499, 1000.000000000000000 ) ;
#160169=ORIENTED_EDGE ( 'NONE', *, *, #79891, .F. ) ;
#160214=VECTOR ( 'NONE', #189726, 1000.000000000000000 ) ;
#160223=ORIENTED_EDGE ( 'NONE', *, *, #228591, .F. ) ;
#160237=ORIENTED_EDGE ( 'NONE', *, *, #5960, .F. ) ;
#160274=AXIS2_PLACEMENT_3D ( 'NONE', #167099, #69261, #230910 ) ;
#160283=ORIENTED_EDGE ( 'NONE', *, *, #195427, .F. ) ;
#160293=CARTESIAN_POINT ( 'NONE',  ( -20.93284271247462058, 56.02567683926421438, -227.9999002286039058 ) ) ;
#160400=CARTESIAN_POINT ( 'NONE',  ( -18.39999999999999858, 77.13860723519891849, -241.8264964602989266 ) ) ;
#160433=ADVANCED_FACE ( 'NONE', ( #145148 ), #183026, .T. ) ;
#160444=ORIENTED_EDGE ( 'NONE', *, *, #177955, .F. ) ;
#160470=CYLINDRICAL_SURFACE ( 'NONE', #155715, 0.1000000000000024342 ) ;
#160473=AXIS2_PLACEMENT_3D ( 'NONE', #3305, #222343, #82826 ) ;
#160476=ORIENTED_EDGE ( 'NONE', *, *, #202594, .T. ) ;
#160494=CARTESIAN_POINT ( 'NONE',  ( -22.50000000000000000, 33.38250548509083160, -242.4821227592188961 ) ) ;
#160529=ORIENTED_EDGE ( 'NONE', *, *, #40825, .F. ) ;
#160543=EDGE_CURVE ( 'NONE', #20995, #171172, #166042, .T. ) ;
#160568=CARTESIAN_POINT ( 'NONE',  ( 18.59999999999999076, 53.37395138337728895, -234.8857996415767104 ) ) ;
#160571=ADVANCED_FACE ( 'NONE', ( #246826 ), #103455, .T. ) ;
#160586=CARTESIAN_POINT ( 'NONE',  ( 23.14999999999999858, 67.23127455305835554, -235.8551265064784559 ) ) ;
#160673=FACE_OUTER_BOUND ( 'NONE', #210567, .T. ) ;
#160694=LINE ( 'NONE', #240209, #53399 ) ;
#160702=DIRECTION ( 'NONE',  ( -1.000000000000000000, 1.335000415235278971E-16, -2.979993593738921214E-16 ) ) ;
#160709=VECTOR ( 'NONE', #182848, 1000.000000000000000 ) ;
#160710=ORIENTED_EDGE ( 'NONE', *, *, #110851, .F. ) ;
#160724=CARTESIAN_POINT ( 'NONE',  ( -18.50000000000000000, 47.92640890138473253, -246.4059919526569900 ) ) ;
#160814=VECTOR ( 'NONE', #9200, 1000.000000000000114 ) ;
#160815=ORIENTED_EDGE ( 'NONE', *, *, #29457, .F. ) ;
#160818=DIRECTION ( 'NONE',  ( 0.000000000000000000, 0.9126074666063759278, 0.4088369013363304383 ) ) ;
#160856=CYLINDRICAL_SURFACE ( 'NONE', #240307, 0.4999999999999944489 ) ;
#160877=DIRECTION ( 'NONE',  ( 0.000000000000000000, 0.4088369013363198357, -0.9126074666063807017 ) ) ;
#160879=DIRECTION ( 'NONE',  ( 0.000000000000000000, 0.9126074666063767049, 0.4088369013363286619 ) ) ;
#160895=DIRECTION ( 'NONE',  ( -1.000000000000000000, -0.000000000000000000, -0.000000000000000000 ) ) ;
#160899=CARTESIAN_POINT ( 'NONE',  ( -20.64999999999999858, 44.96555909964510533, -237.8856228368455845 ) ) ;
#160931=CARTESIAN_POINT ( 'NONE',  ( 20.85000000000000142, 69.34766280046808617, -247.6726305063181144 ) ) ;
#160935=AXIS2_PLACEMENT_3D ( 'NONE', #69804, #209288, #103741 ) ;
#160968=CARTESIAN_POINT ( 'NONE',  ( 18.43709777086140278, 77.26488334054519669, -241.9697969554615042 ) ) ;
#160988=CARTESIAN_POINT ( 'NONE',  ( -21.09610168723072476, 34.02031789858177291, -243.7434127162948698 ) ) ;
#161002=ORIENTED_EDGE ( 'NONE', *, *, #40219, .T. ) ;
#161079=DIRECTION ( 'NONE',  ( 2.952720810173288619E-16, 0.4088369013363239990, -0.9126074666063788143 ) ) ;
#161112=VERTEX_POINT ( 'NONE', #243327 ) ;
#161143=ORIENTED_EDGE ( 'NONE', *, *, #140414, .F. ) ;
#161144=ADVANCED_FACE ( 'NONE', ( #198115 ), #226313, .F. ) ;
#161148=CARTESIAN_POINT ( 'NONE',  ( -20.64999999999999858, 45.00644278977874535, -237.9768835835062077 ) ) ;
#161171=ORIENTED_EDGE ( 'NONE', *, *, #37480, .T. ) ;
#161175=CARTESIAN_POINT ( 'NONE',  ( -23.15000000000000213, 65.31479887318495514, -236.7136839992847399 ) ) ;
#161178=CARTESIAN_POINT ( 'NONE',  ( 20.13684514580175033, 40.20805984460254479, -237.5560023261490699 ) ) ;
#161195=DIRECTION ( 'NONE',  ( 0.000000000000000000, 0.9126074666063772600, 0.4088369013363274407 ) ) ;
#161246=ORIENTED_EDGE ( 'NONE', *, *, #208898, .F. ) ;
#161293=CARTESIAN_POINT ( 'NONE',  ( -20.64999999999999858, 62.33780030268294325, -247.9091949332902232 ) ) ;
#161300=DIRECTION ( 'NONE',  ( 0.000000000000000000, 0.9126074666063660468, 0.4088369013363524762 ) ) ;
#161334=CARTESIAN_POINT ( 'NONE',  ( 21.05000000000000071, 56.02567683926420727, -227.9999002286038774 ) ) ;
#161413=CARTESIAN_POINT ( 'NONE',  ( 18.58703555224985493, 47.00685966653406922, -255.2225155549824933 ) ) ;
#161426=CARTESIAN_POINT ( 'NONE',  ( 21.05000000000000071, 40.58313652815218830, -247.7931640254992658 ) ) ;
#161450=DIRECTION ( 'NONE',  ( 0.000000000000000000, -0.8103668758649578141, 0.5859227990963212784 ) ) ;
#161463=VERTEX_POINT ( 'NONE', #254830 ) ;
#161474=CARTESIAN_POINT ( 'NONE',  ( -2.995603634470829482E-16, 60.85566667783209738, -251.5865162804734041 ) ) ;
#161476=AXIS2_PLACEMENT_3D ( 'NONE', #136432, #137728, #119478 ) ;
#161479=LINE ( 'NONE', #201865, #230695 ) ;
#161483=ORIENTED_EDGE ( 'NONE', *, *, #122347, .T. ) ;
#161492=DIRECTION ( 'NONE',  ( 0.000000000000000000, 0.9126074666063769270, 0.4088369013363280513 ) ) ;
#161498=DIRECTION ( 'NONE',  ( 0.000000000000000000, 0.7745938767306564943, 0.6324589521315772123 ) ) ;
#161531=CARTESIAN_POINT ( 'NONE',  ( -20.94999027547553894, 68.00519115550238780, -224.2294631537215821 ) ) ;
#161553=CARTESIAN_POINT ( 'NONE',  ( 18.48413544395637587, 77.28145018450004500, -241.9425425904620681 ) ) ;
#161566=AXIS2_PLACEMENT_3D ( 'NONE', #155462, #40654, #38063 ) ;
#161571=ORIENTED_EDGE ( 'NONE', *, *, #209204, .T. ) ;
#161572=EDGE_LOOP ( 'NONE', ( #149626, #257264, #108444, #92559 ) ) ;
#161594=ORIENTED_EDGE ( 'NONE', *, *, #705, .T. ) ;
#161611=PLANE ( 'NONE',  #199443 ) ;
#161639=AXIS2_PLACEMENT_3D ( 'NONE', #130088, #72725, #50533 ) ;
#161663=ORIENTED_EDGE ( 'NONE', *, *, #17752, .F. ) ;
#161676=AXIS2_PLACEMENT_3D ( 'NONE', #220356, #219043, #142078 ) ;
#161759=FACE_OUTER_BOUND ( 'NONE', #128997, .T. ) ;
#161765=AXIS2_PLACEMENT_3D ( 'NONE', #70670, #11975, #52339 ) ;
#161788=CARTESIAN_POINT ( 'NONE',  ( 20.85000000000000142, 71.99422445362657186, -246.4870034924427671 ) ) ;
#161794=VECTOR ( 'NONE', #213338, 1000.000000000000114 ) ;
#161847=CARTESIAN_POINT ( 'NONE',  ( -18.59999999999999787, 47.93499546395150190, -254.9093547331817717 ) ) ;
#161859=EDGE_LOOP ( 'NONE', ( #166091, #46483, #85928, #88165 ) ) ;
#161876=EDGE_CURVE ( 'NONE', #171099, #108499, #117046, .T. ) ;
#161905=AXIS2_PLACEMENT_3D ( 'NONE', #79932, #27744, #90222 ) ;
#161927=ORIENTED_EDGE ( 'NONE', *, *, #126351, .F. ) ;
#161997=CARTESIAN_POINT ( 'NONE',  ( -20.85000000000000142, 67.23127455305835554, -235.8551265064784559 ) ) ;
#162029=CYLINDRICAL_SURFACE ( 'NONE', #170821, 0.1000000000000024342 ) ;
#162041=FACE_OUTER_BOUND ( 'NONE', #143685, .T. ) ;
#162042=ORIENTED_EDGE ( 'NONE', *, *, #49583, .F. ) ;
#162080=AXIS2_PLACEMENT_3D ( 'NONE', #210209, #118487, #136732 ) ;
#162088=CARTESIAN_POINT ( 'NONE',  ( -20.87155475150660777, 56.12642167632806434, -227.9547677828175836 ) ) ;
#162099=CARTESIAN_POINT ( 'NONE',  ( -20.94999999999999929, 74.93036000061670165, -233.6816308724374949 ) ) ;
#162115=ORIENTED_EDGE ( 'NONE', *, *, #212347, .F. ) ;
#162121=EDGE_CURVE ( 'NONE', #84696, #223817, #41380, .T. ) ;
#162129=VECTOR ( 'NONE', #40769, 1000.000000000000000 ) ;
#162132=ORIENTED_EDGE ( 'NONE', *, *, #117449, .F. ) ;
#162137=AXIS2_PLACEMENT_3D ( 'NONE', #134572, #116334, #152910 ) ;
#162147=CARTESIAN_POINT ( 'NONE',  ( 18.59999999999998721, 67.85125148167622910, -227.9794913823769491 ) ) ;
#162151=AXIS2_PLACEMENT_3D ( 'NONE', #36574, #118664, #39125 ) ;
#162178=LINE ( 'NONE', #1779, #110714 ) ;
#162201=VERTEX_POINT ( 'NONE', #127308 ) ;
#162222=SPHERICAL_SURFACE ( 'NONE', #224837, 0.1000000000000000056 ) ;
#162262=ORIENTED_EDGE ( 'NONE', *, *, #25604, .F. ) ;
#162264=DIRECTION ( 'NONE',  ( 0.000000000000000000, 0.9126074666064696306, 0.4088369013361212723 ) ) ;
#162279=LINE ( 'NONE', #241792, #220642 ) ;
#162315=CYLINDRICAL_SURFACE ( 'NONE', #110053, 0.1000000000000024342 ) ;
#162343=DIRECTION ( 'NONE',  ( 1.000000000000000000, 0.000000000000000000, 0.000000000000000000 ) ) ;
#162354=CARTESIAN_POINT ( 'NONE',  ( 18.59999999999999432, 78.48087866980282001, -232.8271061603568910 ) ) ;
#162378=CYLINDRICAL_SURFACE ( 'NONE', #227168, 0.1000000000000065836 ) ;
#162408=ORIENTED_EDGE ( 'NONE', *, *, #164182, .T. ) ;
#162461=AXIS2_PLACEMENT_3D ( 'NONE', #2241, #145608, #225136 ) ;
#162472=CARTESIAN_POINT ( 'NONE',  ( 20.59588692710267921, 39.39129011228262556, -236.9654500441737071 ) ) ;
#162490=TOROIDAL_SURFACE ( 'NONE', #104370, 3.899999999999999467, 0.1000000000000000056 ) ;
#162500=EDGE_CURVE ( 'NONE', #201217, #221407, #220369, .T. ) ;
#162545=DIRECTION ( 'NONE',  ( 0.000000000000000000, 0.9126074666063767049, 0.4088369013363286619 ) ) ;
#162563=ORIENTED_EDGE ( 'NONE', *, *, #207417, .T. ) ;
#162620=EDGE_CURVE ( 'NONE', #77834, #251907, #70545, .T. ) ;
#162625=EDGE_LOOP ( 'NONE', ( #32478, #119159, #162779, #131318 ) ) ;
#162632=DIRECTION ( 'NONE',  ( 0.000000000000000000, 0.9126074666063751506, 0.4088369013363322146 ) ) ;
#162644=ORIENTED_EDGE ( 'NONE', *, *, #122270, .T. ) ;
#162658=CARTESIAN_POINT ( 'NONE',  ( -21.45000000000000284, 44.77807522791015060, -237.4671205425215135 ) ) ;
#162709=FACE_OUTER_BOUND ( 'NONE', #138250, .T. ) ;
#162729=DIRECTION ( 'NONE',  ( 1.000000000000000000, 0.000000000000000000, 0.000000000000000000 ) ) ;
#162730=DIRECTION ( 'NONE',  ( 0.000000000000000000, 0.4088369013363281068, -0.9126074666063770380 ) ) ;
#162747=CIRCLE ( 'NONE', #179324, 0.09999999999999609201 ) ;
#162755=CARTESIAN_POINT ( 'NONE',  ( -22.59999999999999787, 25.89494711235935043, -254.2627752153468350 ) ) ;
#162779=ORIENTED_EDGE ( 'NONE', *, *, #110552, .F. ) ;
#162797=VECTOR ( 'NONE', #27925, 1000.000000000000114 ) ;
#162812=DIRECTION ( 'NONE',  ( 3.469446951953635646E-14, -0.9126074666063771490, -0.4088369013363281623 ) ) ;
#162835=VECTOR ( 'NONE', #25331, 1000.000000000000227 ) ;
#162866=DIRECTION ( 'NONE',  ( -1.000000000000000000, -0.000000000000000000, 0.000000000000000000 ) ) ;
#162887=ORIENTED_EDGE ( 'NONE', *, *, #72390, .T. ) ;
#162910=VECTOR ( 'NONE', #106602, 1000.000000000000114 ) ;
#162929=CYLINDRICAL_SURFACE ( 'NONE', #252909, 0.09999999999999771572 ) ;
#162938=CYLINDRICAL_SURFACE ( 'NONE', #176888, 0.09999999999999609201 ) ;
#162953=FACE_OUTER_BOUND ( 'NONE', #109655, .T. ) ;
#162970=EDGE_LOOP ( 'NONE', ( #236021, #218612, #87334, #25564, #204539 ) ) ;
#163000=CIRCLE ( 'NONE', #183824, 0.09999999999999939493 ) ;
#163067=ORIENTED_EDGE ( 'NONE', *, *, #97789, .F. ) ;
#163096=DIRECTION ( 'NONE',  ( 0.000000000000000000, 0.4088369013363281623, -0.9126074666063771490 ) ) ;
#163115=DIRECTION ( 'NONE',  ( 0.000000000000000000, 0.9126074666063545004, 0.4088369013363783999 ) ) ;
#163122=DIRECTION ( 'NONE',  ( 0.000000000000000000, 0.4088369013363281068, -0.9126074666063770380 ) ) ;
#163138=DIRECTION ( 'NONE',  ( 0.000000000000000000, -0.9126074666063770380, -0.4088369013363281068 ) ) ;
#163172=CARTESIAN_POINT ( 'NONE',  ( 18.52928932188133970, 54.95214567929435390, -230.0923768967488456 ) ) ;
#163176=EDGE_CURVE ( 'NONE', #79382, #56413, #29225, .T. ) ;
#163223=CARTESIAN_POINT ( 'NONE',  ( -18.49719636458513961, 46.97455478271485418, -255.2808495583587103 ) ) ;
#163241=ADVANCED_FACE ( 'NONE', ( #123496 ), #50024, .F. ) ;
#163245=EDGE_CURVE ( 'NONE', #236709, #25987, #179059, .T. ) ;
#163252=( BOUNDED_CURVE ( )  B_SPLINE_CURVE ( 3, ( #156137, #133963, #213502, #256416 ),
 .UNSPECIFIED., .F., .T. ) 
 B_SPLINE_CURVE_WITH_KNOTS ( ( 4, 4 ),
 ( 3.141592653589793116, 4.712388980384689674 ),
 .UNSPECIFIED. ) 
 CURVE ( )  GEOMETRIC_REPRESENTATION_ITEM ( )  RATIONAL_B_SPLINE_CURVE ( ( 1.000000000000000000, 0.8047378541243649375, 0.8047378541243649375, 1.000000000000000000 ) ) 
 REPRESENTATION_ITEM ( '' )  );
#163269=DIRECTION ( 'NONE',  ( 0.000000000000000000, 0.9090645160164306793, 0.4166553800442435729 ) ) ;
#163319=LINE ( 'NONE', #142454, #238986 ) ;
#163341=EDGE_CURVE ( 'NONE', #144138, #26148, #66606, .T. ) ;
#163357=ORIENTED_EDGE ( 'NONE', *, *, #148291, .T. ) ;
#163361=CARTESIAN_POINT ( 'NONE',  ( -20.99749315643147440, 56.02567684099302880, -227.9999002278294142 ) ) ;
#163394=AXIS2_PLACEMENT_3D ( 'NONE', #9840, #72405, #29449 ) ;
#163407=AXIS2_PLACEMENT_3D ( 'NONE', #185861, #129742, #132305 ) ;
#163415=CARTESIAN_POINT ( 'NONE',  ( 21.05000000000000071, 34.04174220360669523, -243.6657363632959914 ) ) ;
#163420=FACE_OUTER_BOUND ( 'NONE', #120522, .T. ) ;
#163430=CARTESIAN_POINT ( 'NONE',  ( 20.94999999999999929, 67.23127455305835554, -235.8551265064784559 ) ) ;
#163455=EDGE_CURVE ( 'NONE', #191031, #114960, #179334, .T. ) ;
#163459=ORIENTED_EDGE ( 'NONE', *, *, #183202, .F. ) ;
#163460=DIRECTION ( 'NONE',  ( 0.000000000000000000, 0.9126074666063660468, 0.4088369013363524762 ) ) ;
#163481=CARTESIAN_POINT ( 'NONE',  ( 23.14999999999999503, 51.38014393322265505, -230.1906178717505327 ) ) ;
#163483=CARTESIAN_POINT ( 'NONE',  ( 21.05000000000000071, 44.18296097254452803, -236.5637753386232589 ) ) ;
#163498=ORIENTED_EDGE ( 'NONE', *, *, #143065, .F. ) ;
#163513=DIRECTION ( 'NONE',  ( 1.000000000000000000, 0.000000000000000000, 0.000000000000000000 ) ) ;
#163593=CARTESIAN_POINT ( 'NONE',  ( 23.15000000000000213, 69.09936979046463534, -247.6075824278584889 ) ) ;
#163631=EDGE_CURVE ( 'NONE', #68027, #110197, #145306, .T. ) ;
#163637=( NAMED_UNIT ( * ) PLANE_ANGLE_UNIT ( ) SI_UNIT ( $, .RADIAN. ) );
#163650=CARTESIAN_POINT ( 'NONE',  ( -21.37071067811865532, 52.66096799524555649, -233.5388714123112095 ) ) ;
#163653=AXIS2_PLACEMENT_3D ( 'NONE', #209377, #226349, #245949 ) ;
#163680=ORIENTED_EDGE ( 'NONE', *, *, #188343, .F. ) ;
#163684=ORIENTED_EDGE ( 'NONE', *, *, #113019, .F. ) ;
#163717=FACE_OUTER_BOUND ( 'NONE', #25819, .T. ) ;
#163743=CARTESIAN_POINT ( 'NONE',  ( 19.75857864376268935, 54.53338637621133955, -228.6684279704127789 ) ) ;
#163771=AXIS2_PLACEMENT_3D ( 'NONE', #91814, #209187, #50108 ) ;
#163774=AXIS2_PLACEMENT_3D ( 'NONE', #178944, #2816, #164490 ) ;
#163803=DIRECTION ( 'NONE',  ( 0.7071359030027302151, 0.2890794387707354418, -0.6452843503173697481 ) ) ;
#163809=DIRECTION ( 'NONE',  ( 1.000000000000000000, -2.986185139342070877E-16, 6.665775143889692774E-16 ) ) ;
#163828=VECTOR ( 'NONE', #98798, 1000.000000000000114 ) ;
#163866=AXIS2_PLACEMENT_3D ( 'NONE', #168759, #248241, #107440 ) ;
#163887=DIRECTION ( 'NONE',  ( 0.000000000000000000, -0.2818822000686317941, 0.9594490217226071538 ) ) ;
#163901=CARTESIAN_POINT ( 'NONE',  ( 22.49544290803790147, 31.79553970091822990, -238.8548453295647391 ) ) ;
#163942=ORIENTED_EDGE ( 'NONE', *, *, #9594, .T. ) ;
#163944=CARTESIAN_POINT ( 'NONE',  ( -18.59999999999999787, 67.75954444190071513, -227.8703747234148693 ) ) ;
#163947=ORIENTED_EDGE ( 'NONE', *, *, #198490, .F. ) ;
#163984=CARTESIAN_POINT ( 'NONE',  ( 22.39999999999999503, 31.94635157770351341, -238.7871412784868710 ) ) ;
#164008=ORIENTED_EDGE ( 'NONE', *, *, #232101, .T. ) ;
#164012=ORIENTED_EDGE ( 'NONE', *, *, #171923, .F. ) ;
#164017=EDGE_CURVE ( 'NONE', #170250, #241192, #233251, .T. ) ;
#164029=DIRECTION ( 'NONE',  ( 0.000000000000000000, 0.9126074666063780372, 0.4088369013363259419 ) ) ;
#164087=CYLINDRICAL_SURFACE ( 'NONE', #82468, 0.4999999999999944489 ) ;
#164108=CARTESIAN_POINT ( 'NONE',  ( 18.52326479938732362, 77.30136670619768324, -241.9095796805263205 ) ) ;
#164119=CYLINDRICAL_SURFACE ( 'NONE', #35239, 0.1000000000000024342 ) ;
#164145=CARTESIAN_POINT ( 'NONE',  ( 18.50000000000000000, 77.35494420175977837, -241.6200040285045532 ) ) ;
#164156=DIRECTION ( 'NONE',  ( 0.000000000000000000, -0.2868887416115947775, 0.9579639084728169829 ) ) ;
#164182=EDGE_CURVE ( 'NONE', #235820, #63414, #41461, .T. ) ;
#164193=DIRECTION ( 'NONE',  ( 0.000000000000000000, -0.9126074666064055707, -0.4088369013362648241 ) ) ;
#164197=CARTESIAN_POINT ( 'NONE',  ( 20.12500000000000355, 40.50633771312144660, -237.6829562735682657 ) ) ;
#164210=DIRECTION ( 'NONE',  ( 0.000000000000000000, -0.9126074666063545004, -0.4088369013363783999 ) ) ;
#164229=CARTESIAN_POINT ( 'NONE',  ( -21.45000000000000284, 52.80902093404626640, -233.8693558107618173 ) ) ;
#164292=AXIS2_PLACEMENT_3D ( 'NONE', #175237, #130926, #153103 ) ;
#164296=ORIENTED_EDGE ( 'NONE', *, *, #104860, .T. ) ;
#164347=DIRECTION ( 'NONE',  ( -1.000000000000000000, 0.000000000000000000, 0.000000000000000000 ) ) ;
#164371=DIRECTION ( 'NONE',  ( 0.000000000000000000, 0.9126074666063844765, 0.4088369013363114535 ) ) ;
#164381=CIRCLE ( 'NONE', #139217, 0.09999999999999939493 ) ;
#164398=EDGE_CURVE ( 'NONE', #187157, #139949, #34735, .T. ) ;
#164401=DIRECTION ( 'NONE',  ( 0.000000000000000000, -0.9126074666063660468, -0.4088369013363524762 ) ) ;
#164404=ORIENTED_EDGE ( 'NONE', *, *, #74526, .T. ) ;
#164413=( BOUNDED_SURFACE ( )  B_SPLINE_SURFACE ( 3, 2, ( 
 ( #66844, #129380, #185506 ),
 ( #6863, #146357, #10724 ),
 ( #246746, #90229, #190664 ),
 ( #30294, #225879, #47252 ),
 ( #126814, #169836, #250600 ),
 ( #68126, #210219, #27750 ) ),
 .UNSPECIFIED., .F., .F., .F. ) 
 B_SPLINE_SURFACE_WITH_KNOTS ( ( 4, 2, 4 ),
 ( 3, 3 ),
 ( 4.712388980384689674, 5.497787143782137953, 6.283185307179586232 ),
 ( 0.000000000000000000, 1.000000000000000000 ),
 .UNSPECIFIED. ) 
 GEOMETRIC_REPRESENTATION_ITEM ( )  RATIONAL_B_SPLINE_SURFACE ( (
 ( 1.000000000000000000, 0.7071067811865898722, 1.000000000000000000),
 ( 1.000000000000000000, 0.7727932973488216284, 1.000000000000000000),
 ( 1.000000000000000000, 0.8282379607654585252, 1.000000000000000000),
 ( 1.000000000000000000, 0.9038128468034328789, 1.000000000000000000),
 ( 1.000000000000000000, 0.9240297172247350366, 1.000000000000000000),
 ( 1.000000000000000000, 0.9238795325113333679, 1.000000000000000000) ) ) 
 REPRESENTATION_ITEM ( '' )  SURFACE ( )  );
#164423=DIRECTION ( 'NONE',  ( -1.000000000000000000, -1.418437941187492324E-14, 3.166243193347622926E-14 ) ) ;
#164443=EDGE_LOOP ( 'NONE', ( #3346, #96635, #189753, #205313 ) ) ;
#164461=ORIENTED_EDGE ( 'NONE', *, *, #8475, .F. ) ;
#164490=DIRECTION ( 'NONE',  ( 0.000000000000000000, 0.4088369013363345461, -0.9126074666063741514 ) ) ;
#164531=VERTEX_POINT ( 'NONE', #120692 ) ;
#164603=DIRECTION ( 'NONE',  ( 1.000000000000000000, 0.000000000000000000, 0.000000000000000000 ) ) ;
#164621=ORIENTED_EDGE ( 'NONE', *, *, #35870, .T. ) ;
#164635=EDGE_LOOP ( 'NONE', ( #55906, #143762, #221820, #123558 ) ) ;
#164658=CARTESIAN_POINT ( 'NONE',  ( 21.97500000000000497, 52.06567329910104291, -231.9654557484363409 ) ) ;
#164671=ORIENTED_EDGE ( 'NONE', *, *, #10457, .T. ) ;
#164676=CARTESIAN_POINT ( 'NONE',  ( 21.03670563405601968, 43.56349054571641233, -234.8157308747548484 ) ) ;
#164688=ORIENTED_EDGE ( 'NONE', *, *, #102012, .F. ) ;
#164697=DIRECTION ( 'NONE',  ( 1.000000000000000000, 0.000000000000000000, 0.000000000000000000 ) ) ;
#164701=CARTESIAN_POINT ( 'NONE',  ( -23.25000000000000000, 67.74990736105834799, -227.9721689390126755 ) ) ;
#164727=EDGE_LOOP ( 'NONE', ( #92115, #164461, #66653 ) ) ;
#164729=DIRECTION ( 'NONE',  ( 1.000000000000000000, 0.000000000000000000, 0.000000000000000000 ) ) ;
#164868=AXIS2_PLACEMENT_3D ( 'NONE', #234664, #55994, #30073 ) ;
#164873=ORIENTED_EDGE ( 'NONE', *, *, #9682, .F. ) ;
#164902=FACE_OUTER_BOUND ( 'NONE', #46993, .T. ) ;
#164909=LINE ( 'NONE', #979, #163828 ) ;
#164936=ORIENTED_EDGE ( 'NONE', *, *, #213074, .T. ) ;
#164949=ORIENTED_EDGE ( 'NONE', *, *, #208596, .F. ) ;
#164952=DIRECTION ( 'NONE',  ( 0.000000000000000000, 0.4088369013363281623, -0.9126074666063771490 ) ) ;
#164955=CARTESIAN_POINT ( 'NONE',  ( 20.89878130938411616, 68.09900309800710261, -224.1499508721967970 ) ) ;
#164968=DIRECTION ( 'NONE',  ( 0.000000000000000000, -0.4088369013363280513, 0.9126074666063769270 ) ) ;
#164971=DIRECTION ( 'NONE',  ( 2.694716079187274425E-16, 0.4088369013363281623, -0.9126074666063770380 ) ) ;
#165007=AXIS2_PLACEMENT_3D ( 'NONE', #69579, #126967, #149117 ) ;
#165120=FACE_OUTER_BOUND ( 'NONE', #47467, .T. ) ;
#165133=EDGE_CURVE ( 'NONE', #18074, #60562, #225696, .T. ) ;
#165165=FACE_OUTER_BOUND ( 'NONE', #91701, .T. ) ;
#165174=CIRCLE ( 'NONE', #48464, 0.9750000000000036415 ) ;
#165207=DIRECTION ( 'NONE',  ( 1.000000000000000000, 0.000000000000000000, 0.000000000000000000 ) ) ;
#165213=CARTESIAN_POINT ( 'NONE',  ( -18.50000000000000000, 67.85909929089923764, -227.8797997985275856 ) ) ;
#165240=CIRCLE ( 'NONE', #52796, 0.1000000000000024342 ) ;
#165279=DIRECTION ( 'NONE',  ( -1.000000000000000000, 1.335000415235278971E-16, -2.979993593738921214E-16 ) ) ;
#165280=ORIENTED_EDGE ( 'NONE', *, *, #131233, .T. ) ;
#165297=FACE_BOUND ( 'NONE', #53123, .T. ) ;
#165395=CIRCLE ( 'NONE', #77883, 0.1000000000000074440 ) ;
#165432=ORIENTED_EDGE ( 'NONE', *, *, #225449, .T. ) ;
#165433=ADVANCED_FACE ( 'NONE', ( #148637 ), #3971, .T. ) ;
#165443=AXIS2_PLACEMENT_3D ( 'NONE', #185115, #85978, #165567 ) ;
#165444=CARTESIAN_POINT ( 'NONE',  ( -20.54999999999999716, 68.96522873961046685, -235.0783363939394235 ) ) ;
#165455=CARTESIAN_POINT ( 'NONE',  ( -21.59142135623730852, 52.84246341164006822, -233.6994099349884380 ) ) ;
#165464=FACE_OUTER_BOUND ( 'NONE', #134140, .T. ) ;
#165468=FACE_OUTER_BOUND ( 'NONE', #84777, .T. ) ;
#165481=AXIS2_PLACEMENT_3D ( 'NONE', #138521, #182842, #100671 ) ;
#165496=AXIS2_PLACEMENT_3D ( 'NONE', #61086, #161498, #241025 ) ;
#165497=CARTESIAN_POINT ( 'NONE',  ( 20.95539060131842746, 39.30035216274485776, -236.7266179559437091 ) ) ;
#165504=B_SPLINE_CURVE_WITH_KNOTS ( 'NONE', 3,
 ( #104874, #198875, #102308, #5790 ),
 .UNSPECIFIED., .F., .F.,
 ( 4, 4 ),
 ( 7.757919228897728493E-18, 0.0001058379652594506807 ),
 .UNSPECIFIED. ) ;
#165556=EDGE_CURVE ( 'NONE', #179132, #152685, #12988, .T. ) ;
#165567=DIRECTION ( 'NONE',  ( 0.000000000000000000, -0.6324589521315897578, 0.7745938767306462802 ) ) ;
#165579=CARTESIAN_POINT ( 'NONE',  ( -21.11825140030084214, 34.01722988687274096, -243.6719807376591689 ) ) ;
#165582=ORIENTED_EDGE ( 'NONE', *, *, #209131, .T. ) ;
#165583=CYLINDRICAL_SURFACE ( 'NONE', #172018, 0.09999999999999939493 ) ;
#165584=ADVANCED_FACE ( 'NONE', ( #93770 ), #41797, .T. ) ;
#165587=CARTESIAN_POINT ( 'NONE',  ( -18.59999999999999787, 44.52640028187936849, -247.3006740988509193 ) ) ;
#165604=CARTESIAN_POINT ( 'NONE',  ( 20.94999999999999574, 44.29184115892635987, -259.0069060397277667 ) ) ;
#165618=DIRECTION ( 'NONE',  ( 0.000000000000000000, 0.9126074666063660468, 0.4088369013363524762 ) ) ;
#165663=ADVANCED_FACE ( 'NONE', ( #81878 ), #159469, .T. ) ;
#165686=ORIENTED_EDGE ( 'NONE', *, *, #252058, .F. ) ;
#165723=AXIS2_PLACEMENT_3D ( 'NONE', #28431, #3679, #6240 ) ;
#165748=CARTESIAN_POINT ( 'NONE',  ( 21.53752568622180874, 30.42476846892407139, -252.2355353702193668 ) ) ;
#165813=LINE ( 'NONE', #110951, #151767 ) ;
#165815=EDGE_CURVE ( 'NONE', #155635, #68804, #38846, .T. ) ;
#165828=AXIS2_PLACEMENT_3D ( 'NONE', #110803, #212493, #213757 ) ;
#165863=AXIS2_PLACEMENT_3D ( 'NONE', #240572, #63197, #141466 ) ;
#165904=PRODUCT_DEFINITION_SHAPE ( 'NONE', 'NONE',  #179166 ) ;
#165917=DIRECTION ( 'NONE',  ( 1.000000000000000000, 0.000000000000000000, 0.000000000000000000 ) ) ;
#165942=EDGE_LOOP ( 'NONE', ( #161594, #125204, #217136, #21602 ) ) ;
#165944=CARTESIAN_POINT ( 'NONE',  ( -21.05000000000000071, 47.95459712139159336, -246.5019368548292675 ) ) ;
#165954=CARTESIAN_POINT ( 'NONE',  ( -18.59999999999999787, 38.23914636435921466, -236.1324109481172968 ) ) ;
#165958=ADVANCED_FACE ( 'NONE', ( #115277 ), #153168, .T. ) ;
#165963=ORIENTED_EDGE ( 'NONE', *, *, #156553, .T. ) ;
#165964=DIRECTION ( 'NONE',  ( 0.000000000000000000, -0.9126074666063660468, -0.4088369013363524762 ) ) ;
#165965=CARTESIAN_POINT ( 'NONE',  ( 20.94999999999999574, 46.45388641681647357, -243.1520440498138385 ) ) ;
#165979=CARTESIAN_POINT ( 'NONE',  ( -20.94999999999999929, 46.53760404070597900, -243.0973507280067167 ) ) ;
#166042=LINE ( 'NONE', #10799, #228395 ) ;
#166048=AXIS2_PLACEMENT_3D ( 'NONE', #238053, #16474, #93409 ) ;
#166063=ORIENTED_EDGE ( 'NONE', *, *, #152773, .F. ) ;
#166079=CIRCLE ( 'NONE', #207760, 0.09999999999999950595 ) ;
#166088=DIRECTION ( 'NONE',  ( 1.000000000000000000, 0.000000000000000000, 0.000000000000000000 ) ) ;
#166091=ORIENTED_EDGE ( 'NONE', *, *, #171954, .F. ) ;
#166113=AXIS2_PLACEMENT_3D ( 'NONE', #38913, #140550, #117161 ) ;
#166119=EDGE_CURVE ( 'NONE', #66990, #158029, #230363, .T. ) ;
#166133=ORIENTED_EDGE ( 'NONE', *, *, #217062, .T. ) ;
#166145=AXIS2_PLACEMENT_3D ( 'NONE', #83773, #44706, #160818 ) ;
#166156=ORIENTED_EDGE ( 'NONE', *, *, #94560, .F. ) ;
#166172=ORIENTED_EDGE ( 'NONE', *, *, #199187, .T. ) ;
#166177=DIRECTION ( 'NONE',  ( 0.000000000000000000, -0.9126074666063771490, -0.4088369013363281623 ) ) ;
#166214=DIRECTION ( 'NONE',  ( 0.000000000000000000, -0.4088369013363280513, 0.9126074666063769270 ) ) ;
#166245=AXIS2_PLACEMENT_3D ( 'NONE', #248858, #164193, #203313 ) ;
#166263=CARTESIAN_POINT ( 'NONE',  ( 20.94999999999999929, 62.33780030268293615, -247.9091949332902516 ) ) ;
#166287=LINE ( 'NONE', #28055, #194741 ) ;
#166293=AXIS2_PLACEMENT_3D ( 'NONE', #24659, #138132, #241129 ) ;
#166308=DIRECTION ( 'NONE',  ( 0.000000000000000000, 0.4088369013363576943, -0.9126074666063638263 ) ) ;
#166319=CARTESIAN_POINT ( 'NONE',  ( 21.05000000000000071, 39.26973050389061370, -236.6309188891183055 ) ) ;
#166323=DIRECTION ( 'NONE',  ( 0.000000000000000000, -0.9656312546561486299, -0.2599159095384356855 ) ) ;
#166327=ORIENTED_EDGE ( 'NONE', *, *, #25132, .T. ) ;
#166369=ORIENTED_EDGE ( 'NONE', *, *, #166640, .T. ) ;
#166414=ORIENTED_EDGE ( 'NONE', *, *, #139095, .F. ) ;
#166431=DIRECTION ( 'NONE',  ( -0.000000000000000000, 0.4088369013363276072, -0.9126074666063772600 ) ) ;
#166437=CIRCLE ( 'NONE', #62174, 11.89999999999999858 ) ;
#166482=EDGE_LOOP ( 'NONE', ( #126517, #128900, #257237, #22314, #104649 ) ) ;
#166529=DIRECTION ( 'NONE',  ( 0.000000000000000000, -0.9126074666065445706, -0.4088369013359539617 ) ) ;
#166589=DIRECTION ( 'NONE',  ( 1.000000000000000000, 0.000000000000000000, 0.000000000000000000 ) ) ;
#166622=CARTESIAN_POINT ( 'NONE',  ( 20.85000000000000142, 74.73788286442776041, -233.7359682632885267 ) ) ;
#166640=EDGE_CURVE ( 'NONE', #57578, #223215, #92601, .T. ) ;
#166642=CARTESIAN_POINT ( 'NONE',  ( -23.25000000000000000, 56.06656052939784018, -228.0911609752645290 ) ) ;
#166657=ORIENTED_EDGE ( 'NONE', *, *, #35368, .T. ) ;
#166680=AXIS2_PLACEMENT_3D ( 'NONE', #35627, #135958, #115131 ) ;
#166703=CARTESIAN_POINT ( 'NONE',  ( 21.04999999999998650, 45.11960049378627247, -238.4740710069430349 ) ) ;
#166734=EDGE_CURVE ( 'NONE', #89898, #49355, #151072, .T. ) ;
#166736=CIRCLE ( 'NONE', #204090, 0.1000000000000024342 ) ;
#166761=CARTESIAN_POINT ( 'NONE',  ( 22.50000000000000000, 25.89490299898616854, -254.2637355452866927 ) ) ;
#166788=CARTESIAN_POINT ( 'NONE',  ( -23.15000000000000213, 41.46275801244657799, -260.2743004338703940 ) ) ;
#166798=DIRECTION ( 'NONE',  ( 1.000000000000000000, 0.000000000000000000, 0.000000000000000000 ) ) ;
#166802=CARTESIAN_POINT ( 'NONE',  ( 20.95203847575071521, 39.27146918321979996, -236.8741184434562683 ) ) ;
#166817=EDGE_LOOP ( 'NONE', ( #218702, #211540, #224818, #174396, #141930 ) ) ;
#166830=DIRECTION ( 'NONE',  ( 2.465190328815662439E-32, -0.9126074666063770380, -0.4088369013363282178 ) ) ;
#166868=ORIENTED_EDGE ( 'NONE', *, *, #135944, .T. ) ;
#166876=AXIS2_PLACEMENT_3D ( 'NONE', #84516, #3747, #83254 ) ;
#166884=CARTESIAN_POINT ( 'NONE',  ( 18.49999999999999645, 22.88260507592945814, -249.4775442468528013 ) ) ;
#166897=VERTEX_POINT ( 'NONE', #170855 ) ;
#166903=DIRECTION ( 'NONE',  ( -1.000000000000000000, -0.000000000000000000, 0.000000000000000000 ) ) ;
#166945=CARTESIAN_POINT ( 'NONE',  ( -23.25000000000000000, 41.46275801244657799, -260.2743004338703940 ) ) ;
#166946=VERTEX_POINT ( 'NONE', #220199 ) ;
#166950=CARTESIAN_POINT ( 'NONE',  ( -23.25000000000000000, 47.66483718802935954, -241.7716698398223514 ) ) ;
#166995=TOROIDAL_SURFACE ( 'NONE', #200264, 0.2000000000000000111, 0.1000000000000000056 ) ;
#167005=CIRCLE ( 'NONE', #129361, 0.09999999999999481526 ) ;
#167008=ORIENTED_EDGE ( 'NONE', *, *, #115294, .F. ) ;
#167080=DIRECTION ( 'NONE',  ( -0.000000000000000000, -0.9126074666063771490, -0.4088369013363281623 ) ) ;
#167081=SPHERICAL_SURFACE ( 'NONE', #188898, 0.1000000000000000056 ) ;
#167099=CARTESIAN_POINT ( 'NONE',  ( -18.59999999999999787, 43.57568952063339651, -245.1784935019914826 ) ) ;
#167115=AXIS2_PLACEMENT_3D ( 'NONE', #159062, #177352, #79478 ) ;
#167117=CYLINDRICAL_SURFACE ( 'NONE', #167623, 0.1000000000000024342 ) ;
#167140=SPHERICAL_SURFACE ( 'NONE', #207514, 0.1000000000000000056 ) ;
#167161=ORIENTED_EDGE ( 'NONE', *, *, #152020, .F. ) ;
#167166=DIRECTION ( 'NONE',  ( 0.000000000000000000, -0.9126074666063771490, -0.4088369013363281623 ) ) ;
#167167=EDGE_LOOP ( 'NONE', ( #218565, #83676, #127774, #156569 ) ) ;
#167182=AXIS2_PLACEMENT_3D ( 'NONE', #116671, #196210, #219612 ) ;
#167184=DIRECTION ( 'NONE',  ( 0.000000000000000000, 0.9126074666063770380, 0.4088369013363281068 ) ) ;
#167209=ORIENTED_EDGE ( 'NONE', *, *, #42533, .T. ) ;
#167275=VECTOR ( 'NONE', #6023, 1000.000000000000114 ) ;
#167302=DIRECTION ( 'NONE',  ( 0.000000000000000000, -0.9126074666063770380, -0.4088369013363281068 ) ) ;
#167309=CARTESIAN_POINT ( 'NONE',  ( -20.64999999999999858, 53.03738849591485405, -234.3791188517465400 ) ) ;
#167313=CARTESIAN_POINT ( 'NONE',  ( -2.995603634470829482E-16, 64.04979281095441479, -250.1555871257962735 ) ) ;
#167321=DIRECTION ( 'NONE',  ( 0.000000000000000000, -0.9126074666063660468, -0.4088369013363524762 ) ) ;
#167336=DIRECTION ( 'NONE',  ( -0.000000000000000000, -0.4088369013363281068, 0.9126074666063770380 ) ) ;
#167363=CARTESIAN_POINT ( 'NONE',  ( 21.05000000000000071, 44.15903683684982894, -236.5744930507153470 ) ) ;
#167377=CIRCLE ( 'NONE', #209043, 7.799999999999993605 ) ;
#167385=EDGE_LOOP ( 'NONE', ( #178281, #160169, #158785, #204852 ) ) ;
#167448=VERTEX_POINT ( 'NONE', #242006 ) ;
#167493=CARTESIAN_POINT ( 'NONE',  ( 21.05000000000000071, 55.99424519013661694, -234.9720658648265896 ) ) ;
#167504=ORIENTED_EDGE ( 'NONE', *, *, #98597, .T. ) ;
#167505=CARTESIAN_POINT ( 'NONE',  ( 18.49999999999999289, 39.24721131055453327, -235.5164460677962666 ) ) ;
#167512=CIRCLE ( 'NONE', #192434, 0.09999999999999939493 ) ;
#167529=FACE_OUTER_BOUND ( 'NONE', #71283, .T. ) ;
#167531=ORIENTED_EDGE ( 'NONE', *, *, #30136, .F. ) ;
#167540=DIRECTION ( 'NONE',  ( 0.000000000000000000, 0.9126074666064696306, 0.4088369013361213278 ) ) ;
#167542=CARTESIAN_POINT ( 'NONE',  ( -20.54999999999999716, 56.74893307810339849, -253.4262823364869064 ) ) ;
#167561=ORIENTED_EDGE ( 'NONE', *, *, #181974, .F. ) ;
#167575=ORIENTED_EDGE ( 'NONE', *, *, #104717, .F. ) ;
#167580=DIRECTION ( 'NONE',  ( 0.000000000000000000, 0.9126074666063660468, 0.4088369013363524762 ) ) ;
#167595=AXIS2_PLACEMENT_3D ( 'NONE', #117275, #57267, #238495 ) ;
#167619=AXIS2_PLACEMENT_3D ( 'NONE', #68581, #148116, #127266 ) ;
#167623=AXIS2_PLACEMENT_3D ( 'NONE', #126670, #187939, #32748 ) ;
#167651=ORIENTED_EDGE ( 'NONE', *, *, #233229, .F. ) ;
#167691=ORIENTED_EDGE ( 'NONE', *, *, #190414, .T. ) ;
#167698=TOROIDAL_SURFACE ( 'NONE', #196696, 0.2000000000000000111, 0.1000000000000000056 ) ;
#167721=CIRCLE ( 'NONE', #146825, 0.1000000000000024342 ) ;
#167744=DIRECTION ( 'NONE',  ( 0.000000000000000000, -0.9126074666063771490, -0.4088369013363281623 ) ) ;
#167745=DIRECTION ( 'NONE',  ( -0.000000000000000000, -0.8490545835447252943, -0.5283051335749947564 ) ) ;
#167779=CIRCLE ( 'NONE', #105352, 12.87499999999999645 ) ;
#167783=CARTESIAN_POINT ( 'NONE',  ( -21.05000000000000071, 30.73075574124490572, -252.3164853687435709 ) ) ;
#167803=ORIENTED_EDGE ( 'NONE', *, *, #181939, .T. ) ;
#167807=DIRECTION ( 'NONE',  ( 1.000000000000000000, 0.000000000000000000, 0.000000000000000000 ) ) ;
#167817=ADVANCED_FACE ( 'NONE', ( #48318 ), #185269, .T. ) ;
#167821=EDGE_CURVE ( 'NONE', #20356, #192641, #9193, .T. ) ;
#167849=CIRCLE ( 'NONE', #234441, 3.899999999999999023 ) ;
#167880=ORIENTED_EDGE ( 'NONE', *, *, #153026, .T. ) ;
#167891=EDGE_CURVE ( 'NONE', #167448, #14564, #250375, .T. ) ;
#167902=CARTESIAN_POINT ( 'NONE',  ( 22.50000000000000000, 36.65892442174472876, -249.5511627012454596 ) ) ;
#167929=DIRECTION ( 'NONE',  ( -2.978066053179067258E-16, -0.4088369013363278293, 0.9126074666063771490 ) ) ;
#167949=EDGE_CURVE ( 'NONE', #89549, #64826, #217757, .T. ) ;
#167990=EDGE_CURVE ( 'NONE', #44800, #206460, #250531, .T. ) ;
#168006=CIRCLE ( 'NONE', #97175, 0.09999999999999609201 ) ;
#168039=CARTESIAN_POINT ( 'NONE',  ( -20.54999999999999361, 51.38014393322265505, -230.1906178717505611 ) ) ;
#168054=EDGE_CURVE ( 'NONE', #7052, #245185, #97689, .T. ) ;
#168070=EDGE_CURVE ( 'NONE', #229370, #207268, #146834, .T. ) ;
#168092=VECTOR ( 'NONE', #19047, 1000.000000000000000 ) ;
#168098=CARTESIAN_POINT ( 'NONE',  ( 20.95420533658165141, 39.25354836604451947, -236.8330523274166808 ) ) ;
#168112=VECTOR ( 'NONE', #36066, 1000.000000000000000 ) ;
#168134=VERTEX_POINT ( 'NONE', #20773 ) ;
#168144=DIRECTION ( 'NONE',  ( 0.000000000000000000, -0.9126074666063771490, -0.4088369013363281623 ) ) ;
#168147=DIRECTION ( 'NONE',  ( 0.000000000000000000, 0.4088369013363205573, -0.9126074666063803686 ) ) ;
#168162=CARTESIAN_POINT ( 'NONE',  ( 19.99999999999998934, 51.33926024308902925, -230.0993571250899379 ) ) ;
#168182=FACE_OUTER_BOUND ( 'NONE', #6124, .T. ) ;
#168213=ORIENTED_EDGE ( 'NONE', *, *, #181101, .T. ) ;
#168243=VECTOR ( 'NONE', #101274, 1000.000000000000000 ) ;
#168257=CARTESIAN_POINT ( 'NONE',  ( -18.59999999999999787, 67.23127455305835554, -235.8551265064784559 ) ) ;
#168264=DIRECTION ( 'NONE',  ( 0.000000000000000000, 0.2716869542551192951, -0.9623856809447951521 ) ) ;
#168272=( BOUNDED_SURFACE ( )  B_SPLINE_SURFACE ( 3, 2, ( 
 ( #156290, #136675, #23184 ),
 ( #243483, #122265, #124836 ),
 ( #44003, #105211, #45291 ),
 ( #244757, #40187, #6144 ) ),
 .UNSPECIFIED., .F., .F., .T. ) 
 B_SPLINE_SURFACE_WITH_KNOTS ( ( 4, 4 ),
 ( 3, 3 ),
 ( -8.673617379884035472E-18, 0.001979672783031562362 ),
 ( 0.000000000000000000, 1.000000000000000000 ),
 .UNSPECIFIED. ) 
 GEOMETRIC_REPRESENTATION_ITEM ( )  RATIONAL_B_SPLINE_SURFACE ( (
 ( 1.000000000000000000, 0.7103081912007771503, 1.000000000000000000),
 ( 1.000000000000000000, 0.7104998333560409440, 1.000000000000000000),
 ( 1.000000000000000000, 0.7107238315753027225, 1.000000000000000000),
 ( 1.000000000000000000, 0.7110073749539924659, 1.000000000000000000) ) ) 
 REPRESENTATION_ITEM ( '' )  SURFACE ( )  );
#168314=DIRECTION ( 'NONE',  ( -1.000000000000000000, -0.000000000000000000, -0.000000000000000000 ) ) ;
#168361=ORIENTED_EDGE ( 'NONE', *, *, #40894, .F. ) ;
#168392=CARTESIAN_POINT ( 'NONE',  ( -20.64999999999999858, 52.99650480578122824, -234.2878581050858884 ) ) ;
#168420=DIRECTION ( 'NONE',  ( -0.000000000000000000, -0.9126074666063769270, -0.4088369013363283844 ) ) ;
#168429=ADVANCED_FACE ( 'NONE', ( #54427 ), #133958, .F. ) ;
#168445=CARTESIAN_POINT ( 'NONE',  ( 20.94999999999999929, 63.48958393997221350, -237.5313578019574265 ) ) ;
#168449=ORIENTED_EDGE ( 'NONE', *, *, #114229, .F. ) ;
#168463=EDGE_CURVE ( 'NONE', #105422, #255259, #221827, .T. ) ;
#168487=CARTESIAN_POINT ( 'NONE',  ( -20.64999999999999858, 48.91146289617405785, -253.9240286733484595 ) ) ;
#168498=VERTEX_POINT ( 'NONE', #136515 ) ;
#168521=EDGE_CURVE ( 'NONE', #60194, #123645, #77832, .T. ) ;
#168531=CARTESIAN_POINT ( 'NONE',  ( -20.64999999999999858, 53.03738849591485405, -234.3791188517465400 ) ) ;
#168536=LINE ( 'NONE', #32873, #2482 ) ;
#168551=VERTEX_POINT ( 'NONE', #81657 ) ;
#168576=VECTOR ( 'NONE', #232957, 1000.000000000000227 ) ;
#168627=CARTESIAN_POINT ( 'NONE',  ( -20.94999999999999929, 67.23127455305835554, -235.8551265064784559 ) ) ;
#168645=CARTESIAN_POINT ( 'NONE',  ( -22.39999999999999858, 36.65892442174472876, -249.5511627012454596 ) ) ;
#168732=CARTESIAN_POINT ( 'NONE',  ( -23.25000000000000000, 36.65892442174472876, -249.5511627012454596 ) ) ;
#168755=CARTESIAN_POINT ( 'NONE',  ( 18.39999999999999858, 47.00127771169579205, -255.4372249185379928 ) ) ;
#168759=CARTESIAN_POINT ( 'NONE',  ( 23.24999999999999645, 53.86595165227826243, -236.3638196928718855 ) ) ;
#168786=VERTEX_POINT ( 'NONE', #211930 ) ;
#168798=DIRECTION ( 'NONE',  ( 1.000000000000000000, 0.000000000000000000, 0.000000000000000000 ) ) ;
#168807=CARTESIAN_POINT ( 'NONE',  ( -23.15000000000000213, 36.65892442174472876, -249.5511627012454596 ) ) ;
#168830=CARTESIAN_POINT ( 'NONE',  ( 21.05000000000000071, 63.48958393997221350, -237.5313578019574265 ) ) ;
#168842=ORIENTED_EDGE ( 'NONE', *, *, #171828, .F. ) ;
#168843=CARTESIAN_POINT ( 'NONE',  ( 23.24999999999999645, 45.51971589178210564, -240.3486087337583399 ) ) ;
#168870=DIRECTION ( 'NONE',  ( 1.000000000000000000, 0.000000000000000000, 0.000000000000000000 ) ) ;
#168895=VERTEX_POINT ( 'NONE', #235320 ) ;
#168905=CIRCLE ( 'NONE', #143916, 0.3999999999999996891 ) ;
#168925=AXIS2_PLACEMENT_3D ( 'NONE', #84741, #143469, #120098 ) ;
#168934=CYLINDRICAL_SURFACE ( 'NONE', #160935, 0.09999999999999609201 ) ;
#168938=LINE ( 'NONE', #148050, #247680 ) ;
#168995=DIRECTION ( 'NONE',  ( 0.000000000000000000, 0.9126074666063622720, 0.4088369013363611360 ) ) ;
#169003=CARTESIAN_POINT ( 'NONE',  ( -18.59999999999999787, 67.85909929089923764, -227.8797997985275856 ) ) ;
#169045=CYLINDRICAL_SURFACE ( 'NONE', #85132, 0.09999999999999939493 ) ;
#169054=AXIS2_PLACEMENT_3D ( 'NONE', #104898, #106201, #9683 ) ;
#169081=DIRECTION ( 'NONE',  ( 1.000000000000000000, 0.000000000000000000, 0.000000000000000000 ) ) ;
#169082=DIRECTION ( 'NONE',  ( -1.000000000000000000, 2.986185139342066933E-16, -6.665775143889695732E-16 ) ) ;
#169086=DIRECTION ( 'NONE',  ( 0.000000000000000000, 0.9126074666063753726, 0.4088369013363316040 ) ) ;
#169091=ORIENTED_EDGE ( 'NONE', *, *, #16062, .T. ) ;
#169134=CARTESIAN_POINT ( 'NONE',  ( 23.14999999999999858, 45.73145985849338047, -239.4600911154851133 ) ) ;
#169147=ORIENTED_EDGE ( 'NONE', *, *, #21113, .T. ) ;
#169187=DIRECTION ( 'NONE',  ( 0.000000000000000000, -0.9126074666063771490, -0.4088369013363281623 ) ) ;
#169189=CARTESIAN_POINT ( 'NONE',  ( 23.25000000000000000, 69.09936979046463534, -247.6075824278584889 ) ) ;
#169201=CARTESIAN_POINT ( 'NONE',  ( 21.11344571971300255, 43.49375376562721840, -234.8545817895094387 ) ) ;
#169217=ORIENTED_EDGE ( 'NONE', *, *, #162500, .F. ) ;
#169266=DIRECTION ( 'NONE',  ( -0.000000000000000000, 0.9126074666063770380, 0.4088369013363281068 ) ) ;
#169268=DIRECTION ( 'NONE',  ( 1.734723475976817823E-14, 0.9126074666063771490, 0.4088369013363281623 ) ) ;
#169283=CARTESIAN_POINT ( 'NONE',  ( -18.59999999999999787, 67.76783854423860021, -227.9206834886612114 ) ) ;
#169295=CARTESIAN_POINT ( 'NONE',  ( -18.50000000000000000, 21.17283678855158513, -243.7231193059830332 ) ) ;
#169329=CARTESIAN_POINT ( 'NONE',  ( 20.85000000000000142, 78.48087866980282001, -232.8271061603568910 ) ) ;
#169363=FACE_OUTER_BOUND ( 'NONE', #110850, .T. ) ;
#169375=CARTESIAN_POINT ( 'NONE',  ( 20.02499999999999858, 52.06567329910104291, -231.9654557484363409 ) ) ;
#169405=DIRECTION ( 'NONE',  ( -1.000000000000000000, -0.000000000000000000, -0.000000000000000000 ) ) ;
#169407=CARTESIAN_POINT ( 'NONE',  ( 20.85000000000000142, 69.29728574394107454, -247.8047749431123634 ) ) ;
#169418=CIRCLE ( 'NONE', #215161, 0.09999999999999939493 ) ;
#169429=VERTEX_POINT ( 'NONE', #72633 ) ;
#169469=CARTESIAN_POINT ( 'NONE',  ( -18.59999999999999787, 47.07326788871598211, -255.0992659944397190 ) ) ;
#169504=CIRCLE ( 'NONE', #32110, 0.09999999999999609201 ) ;
#169512=DIRECTION ( 'NONE',  ( 0.000000000000000000, -0.9126074666063770380, -0.4088369013363281068 ) ) ;
#169520=DIRECTION ( 'NONE',  ( -1.000000000000000000, 0.000000000000000000, 0.000000000000000000 ) ) ;
#169522=AXIS2_PLACEMENT_3D ( 'NONE', #73369, #74665, #249416 ) ;
#169535=ORIENTED_EDGE ( 'NONE', *, *, #56272, .F. ) ;
#169551=LINE ( 'NONE', #11737, #120306 ) ;
#169557=EDGE_CURVE ( 'NONE', #123645, #210461, #255028, .T. ) ;
#169566=ORIENTED_EDGE ( 'NONE', *, *, #63995, .T. ) ;
#169591=EDGE_CURVE ( 'NONE', #24915, #175784, #68108, .T. ) ;
#169683=DIRECTION ( 'NONE',  ( 0.000000000000000000, 0.4088369013363281623, -0.9126074666063771490 ) ) ;
#169693=ORIENTED_EDGE ( 'NONE', *, *, #48951, .F. ) ;
#169719=VERTEX_POINT ( 'NONE', #104968 ) ;
#169720=CIRCLE ( 'NONE', #136514, 0.1999999999999985401 ) ;
#169784=AXIS2_PLACEMENT_3D ( 'NONE', #191127, #254858, #150691 ) ;
#169799=ORIENTED_EDGE ( 'NONE', *, *, #97789, .T. ) ;
#169836=CARTESIAN_POINT ( 'NONE',  ( 19.99999999737951484, 54.38478828167306034, -228.7349980859749223 ) ) ;
#169861=EDGE_CURVE ( 'NONE', #175048, #62010, #5722, .T. ) ;
#169892=DIRECTION ( 'NONE',  ( 1.000000000000000000, 0.000000000000000000, 0.000000000000000000 ) ) ;
#169912=DIRECTION ( 'NONE',  ( 0.000000000000000000, 0.9501938099239353175, -0.3116596277708039708 ) ) ;
#169966=DIRECTION ( 'NONE',  ( 0.000000000000000000, -0.4088369013363281068, 0.9126074666063770380 ) ) ;
#169975=CARTESIAN_POINT ( 'NONE',  ( 23.14999999999999503, 51.33926024308902214, -230.0993571250899095 ) ) ;
#170051=ORIENTED_EDGE ( 'NONE', *, *, #67402, .F. ) ;
#170096=CARTESIAN_POINT ( 'NONE',  ( 23.14999999999999503, 56.06656052939784729, -228.0911609752645290 ) ) ;
#170101=AXIS2_PLACEMENT_3D ( 'NONE', #32036, #12465, #232797 ) ;
#170103=CARTESIAN_POINT ( 'NONE',  ( -18.50000000000000000, 47.89822068137787170, -246.3100470504847692 ) ) ;
#170148=DIRECTION ( 'NONE',  ( 2.465190328815662439E-32, -0.9126074666063770380, -0.4088369013363282178 ) ) ;
#170183=AXIS2_PLACEMENT_3D ( 'NONE', #53570, #232226, #113541 ) ;
#170229=DIRECTION ( 'NONE',  ( -1.000000000000000000, -0.000000000000000000, -0.000000000000000000 ) ) ;
#170240=ORIENTED_EDGE ( 'NONE', *, *, #117861, .T. ) ;
#170249=ADVANCED_FACE ( 'NONE', ( #171154 ), #255867, .T. ) ;
#170250=VERTEX_POINT ( 'NONE', #112429 ) ;
#170290=ORIENTED_EDGE ( 'NONE', *, *, #50169, .T. ) ;
#170294=CARTESIAN_POINT ( 'NONE',  ( -21.14999999999999858, 41.46275801244657799, -260.2743004338703940 ) ) ;
#170317=DIRECTION ( 'NONE',  ( -2.940209281316622988E-16, -0.4088369013363260529, 0.9126074666063779262 ) ) ;
#170319=EDGE_CURVE ( 'NONE', #126259, #109005, #197452, .T. ) ;
#170345=DIRECTION ( 'NONE',  ( 1.000000000000000000, 0.000000000000000000, 0.000000000000000000 ) ) ;
#170362=CARTESIAN_POINT ( 'NONE',  ( 20.12500000000000000, 40.07562767317620711, -237.3368484665046765 ) ) ;
#170372=CARTESIAN_POINT ( 'NONE',  ( -21.05000000000000071, 69.38854649060172619, -247.7638912529787660 ) ) ;
#170407=CARTESIAN_POINT ( 'NONE',  ( 21.05000000000000071, 48.50000630096247534, -244.2465039064066161 ) ) ;
#170420=ADVANCED_FACE ( 'NONE', ( #238790 ), #143661, .F. ) ;
#170426=DIRECTION ( 'NONE',  ( 1.000000000000000000, 0.000000000000000000, 0.000000000000000000 ) ) ;
#170457=CARTESIAN_POINT ( 'NONE',  ( 18.59999999999999787, 47.95459712139159336, -246.5019368548292675 ) ) ;
#170481=EDGE_CURVE ( 'NONE', #219794, #119221, #120717, .T. ) ;
#170508=CARTESIAN_POINT ( 'NONE',  ( 21.04999999999999716, 43.40169206266419621, -234.8839448309778106 ) ) ;
#170530=CARTESIAN_POINT ( 'NONE',  ( -20.94999999999999929, 55.49311008795314137, -234.6486875357297492 ) ) ;
#170531=ORIENTED_EDGE ( 'NONE', *, *, #83740, .F. ) ;
#170564=ORIENTED_EDGE ( 'NONE', *, *, #208392, .T. ) ;
#170568=TOROIDAL_SURFACE ( 'NONE', #45623, 4.149999999999999467, 0.1000000000000000056 ) ;
#170646=EDGE_LOOP ( 'NONE', ( #2259, #214376, #79350, #118223 ) ) ;
#170697=FACE_OUTER_BOUND ( 'NONE', #130393, .T. ) ;
#170733=CARTESIAN_POINT ( 'NONE',  ( -23.25000000000000000, 36.65892442174472876, -249.5511627012454596 ) ) ;
#170758=CYLINDRICAL_SURFACE ( 'NONE', #130455, 0.1000000000000024342 ) ;
#170774=CARTESIAN_POINT ( 'NONE',  ( -20.54999999999999716, 67.23127455305835554, -235.8551265064784559 ) ) ;
#170783=AXIS2_PLACEMENT_3D ( 'NONE', #207431, #224394, #147439 ) ;
#170799=ORIENTED_EDGE ( 'NONE', *, *, #193644, .F. ) ;
#170805=DIRECTION ( 'NONE',  ( 1.000000000000000000, 0.000000000000000000, -0.000000000000000000 ) ) ;
#170821=AXIS2_PLACEMENT_3D ( 'NONE', #242818, #121624, #241542 ) ;
#170833=CARTESIAN_POINT ( 'NONE',  ( 21.05000000000000071, 48.98768910550767686, -253.5949463715719787 ) ) ;
#170843=EDGE_LOOP ( 'NONE', ( #185516, #92319, #240214, #236001 ) ) ;
#170853=CARTESIAN_POINT ( 'NONE',  ( 21.14999999999999858, 44.24607648097409651, -236.5241869975821487 ) ) ;
#170855=CARTESIAN_POINT ( 'NONE',  ( 18.59999999999999432, 47.92640890138473253, -246.4059919526569900 ) ) ;
#170866=DIRECTION ( 'NONE',  ( 1.000000000000000000, 0.000000000000000000, 0.000000000000000000 ) ) ;
#170873=DIRECTION ( 'NONE',  ( 0.000000000000000000, -0.9126074666063768159, -0.4088369013363282178 ) ) ;
#170885=ORIENTED_EDGE ( 'NONE', *, *, #237420, .F. ) ;
#170897=ORIENTED_EDGE ( 'NONE', *, *, #147777, .F. ) ;
#170901=DIRECTION ( 'NONE',  ( 0.000000000000000000, -0.9126074666063545004, -0.4088369013363783999 ) ) ;
#170916=ORIENTED_EDGE ( 'NONE', *, *, #108979, .F. ) ;
#170917=TOROIDAL_SURFACE ( 'NONE', #58389, 1.900000000000002576, 0.1000000000000000056 ) ;
#170935=VECTOR ( 'NONE', #118903, 1000.000000000000114 ) ;
#170944=PRODUCT_CONTEXT ( 'NONE', #235521, 'mechanical' ) ;
#170976=VERTEX_POINT ( 'NONE', #211876 ) ;
#170992=VECTOR ( 'NONE', #248069, 1000.000000000000000 ) ;
#171015=DIRECTION ( 'NONE',  ( 1.000000000000000000, 0.000000000000000000, 0.000000000000000000 ) ) ;
#171028=CIRCLE ( 'NONE', #141736, 0.1000000000000024342 ) ;
#171048=DIRECTION ( 'NONE',  ( -4.701977403289178758E-30, 0.9126074666063700436, 0.4088369013363439830 ) ) ;
#171065=CARTESIAN_POINT ( 'NONE',  ( 23.14999999999999503, 51.38014393322265505, -230.1906178717505327 ) ) ;
#171076=ORIENTED_EDGE ( 'NONE', *, *, #252747, .F. ) ;
#171099=VERTEX_POINT ( 'NONE', #216972 ) ;
#171102=VERTEX_POINT ( 'NONE', #119185 ) ;
#171124=FACE_OUTER_BOUND ( 'NONE', #249435, .T. ) ;
#171134=EDGE_LOOP ( 'NONE', ( #152783, #240094, #95555, #133817 ) ) ;
#171136=DIRECTION ( 'NONE',  ( 0.000000000000000000, 0.8490545835447238510, 0.5283051335749973099 ) ) ;
#171148=ORIENTED_EDGE ( 'NONE', *, *, #227422, .T. ) ;
#171150=CARTESIAN_POINT ( 'NONE',  ( 18.49999999999998934, 54.48300931968434213, -228.8005724072070564 ) ) ;
#171154=FACE_OUTER_BOUND ( 'NONE', #95155, .T. ) ;
#171156=DIRECTION ( 'NONE',  ( -1.000000000000000000, -0.000000000000000000, 0.000000000000000000 ) ) ;
#171163=CARTESIAN_POINT ( 'NONE',  ( 21.93642651522410247, 33.66330848088261263, -242.8643360821705528 ) ) ;
#171172=VERTEX_POINT ( 'NONE', #22671 ) ;
#171193=FACE_OUTER_BOUND ( 'NONE', #93866, .T. ) ;
#171212=ORIENTED_EDGE ( 'NONE', *, *, #188343, .T. ) ;
#171234=LINE ( 'NONE', #90349, #120221 ) ;
#171245=EDGE_CURVE ( 'NONE', #15348, #932, #162178, .T. ) ;
#171248=CARTESIAN_POINT ( 'NONE',  ( -23.25000000000000000, 36.65892442174472876, -249.5511627012454596 ) ) ;
#171254=CIRCLE ( 'NONE', #21378, 0.1999999999999976519 ) ;
#171255=EDGE_CURVE ( 'NONE', #231797, #240937, #47320, .T. ) ;
#171260=ORIENTED_EDGE ( 'NONE', *, *, #43038, .F. ) ;
#171262=ORIENTED_EDGE ( 'NONE', *, *, #69892, .F. ) ;
#171303=VECTOR ( 'NONE', #185795, 1000.000000000000000 ) ;
#171315=DIRECTION ( 'NONE',  ( 0.000000000000000000, 0.9126074666063660468, 0.4088369013363524762 ) ) ;
#171325=EDGE_CURVE ( 'NONE', #49350, #30904, #102292, .T. ) ;
#171378=CIRCLE ( 'NONE', #87916, 0.09999999999998997191 ) ;
#171380=FACE_OUTER_BOUND ( 'NONE', #124557, .T. ) ;
#171387=ORIENTED_EDGE ( 'NONE', *, *, #68303, .T. ) ;
#171391=CIRCLE ( 'NONE', #58896, 0.09999999999999609201 ) ;
#171450=ORIENTED_EDGE ( 'NONE', *, *, #108014, .F. ) ;
#171463=ORIENTED_EDGE ( 'NONE', *, *, #124960, .F. ) ;
#171471=FACE_OUTER_BOUND ( 'NONE', #154320, .T. ) ;
#171501=CARTESIAN_POINT ( 'NONE',  ( 21.05000000000000071, 55.59258605799641373, -234.6589115948038966 ) ) ;
#171507=CARTESIAN_POINT ( 'NONE',  ( -21.05000000000000426, 30.86995437684646504, -252.0366859498333554 ) ) ;
#171512=VERTEX_POINT ( 'NONE', #193290 ) ;
#171560=CARTESIAN_POINT ( 'NONE',  ( 22.48970261584622321, 31.84544391280713072, -238.9419228052725543 ) ) ;
#171562=CYLINDRICAL_SURFACE ( 'NONE', #33663, 11.80000000000000249 ) ;
#171602=DIRECTION ( 'NONE',  ( 1.000000000000000000, 0.000000000000000000, 0.000000000000000000 ) ) ;
#171617=AXIS2_PLACEMENT_3D ( 'NONE', #131241, #49133, #73876 ) ;
#171644=DIRECTION ( 'NONE',  ( -0.7071067811865389130, 0.6453109281988527179, 0.2890913453342166539 ) ) ;
#171654=DIRECTION ( 'NONE',  ( 1.000000000000000000, -1.335000415235278971E-16, 2.979993593738921214E-16 ) ) ;
#171661=CARTESIAN_POINT ( 'NONE',  ( 20.94999999999999574, 46.59314322379660922, -243.1831726892433210 ) ) ;
#171662=ORIENTED_EDGE ( 'NONE', *, *, #206842, .T. ) ;
#171737=ORIENTED_EDGE ( 'NONE', *, *, #9090, .T. ) ;
#171748=DIRECTION ( 'NONE',  ( -1.000000000000000000, 0.000000000000000000, 0.000000000000000000 ) ) ;
#171760=ORIENTED_EDGE ( 'NONE', *, *, #515, .F. ) ;
#171814=CARTESIAN_POINT ( 'NONE',  ( 23.14999999999998437, 35.00313497133259943, -245.8551024614896505 ) ) ;
#171828=EDGE_CURVE ( 'NONE', #93087, #132474, #52167, .T. ) ;
#171836=CARTESIAN_POINT ( 'NONE',  ( -18.59999999999999787, 44.43513953521873106, -247.3415577889845736 ) ) ;
#171838=EDGE_CURVE ( 'NONE', #191945, #136081, #11802, .T. ) ;
#171858=AXIS2_PLACEMENT_3D ( 'NONE', #13143, #69269, #92660 ) ;
#171869=DIRECTION ( 'NONE',  ( 0.000000000000000000, 0.2818822000686317941, -0.9594490217226071538 ) ) ;
#171880=DIRECTION ( 'NONE',  ( 0.000000000000000000, 0.9126074666062508056, 0.4088369013366094928 ) ) ;
#171881=EDGE_CURVE ( 'NONE', #197319, #78569, #198384, .T. ) ;
#171917=DIRECTION ( 'NONE',  ( 1.000000000000000000, 0.000000000000000000, 0.000000000000000000 ) ) ;
#171923=EDGE_CURVE ( 'NONE', #148712, #115637, #152810, .T. ) ;
#171929=AXIS2_PLACEMENT_3D ( 'NONE', #131340, #50497, #230448 ) ;
#171942=ADVANCED_FACE ( 'NONE', ( #237243 ), #31989, .F. ) ;
#171954=EDGE_CURVE ( 'NONE', #217616, #86618, #156458, .T. ) ;
#171962=CARTESIAN_POINT ( 'NONE',  ( 22.39999999999999858, 29.50811709945092076, -252.6450601445781103 ) ) ;
#171983=VECTOR ( 'NONE', #144347, 1000.000000000000000 ) ;
#172018=AXIS2_PLACEMENT_3D ( 'NONE', #67752, #145994, #85994 ) ;
#172027=CARTESIAN_POINT ( 'NONE',  ( 23.14999999999999858, 70.88170441948386724, -234.2197789011331679 ) ) ;
#172052=ORIENTED_EDGE ( 'NONE', *, *, #256188, .F. ) ;
#172090=ORIENTED_EDGE ( 'NONE', *, *, #27430, .T. ) ;
#172097=VERTEX_POINT ( 'NONE', #123718 ) ;
#172142=LINE ( 'NONE', #215072, #223287 ) ;
#172146=ORIENTED_EDGE ( 'NONE', *, *, #135001, .T. ) ;
#172173=DIRECTION ( 'NONE',  ( -0.000000000000000000, -0.9126074666063771490, -0.4088369013363281623 ) ) ;
#172195=EDGE_CURVE ( 'NONE', #233797, #177788, #165240, .T. ) ;
#172196=CARTESIAN_POINT ( 'NONE',  ( 19.97071067811864609, 54.36283943849028333, -228.7769250045207912 ) ) ;
#172200=CIRCLE ( 'NONE', #159672, 0.09999999999999414912 ) ;
#172212=AXIS2_PLACEMENT_3D ( 'NONE', #25737, #180966, #2299 ) ;
#172238=ADVANCED_FACE ( 'NONE', ( #127563 ), #69406, .F. ) ;
#172256=ADVANCED_FACE ( 'NONE', ( #229241 ), #130117, .T. ) ;
#172262=VERTEX_POINT ( 'NONE', #25905 ) ;
#172264=DIRECTION ( 'NONE',  ( 0.000000000000000000, -0.6936040289657786628, -0.7203564749500342979 ) ) ;
#172294=ORIENTED_EDGE ( 'NONE', *, *, #230732, .F. ) ;
#172313=ORIENTED_EDGE ( 'NONE', *, *, #210642, .T. ) ;
#172351=AXIS2_PLACEMENT_3D ( 'NONE', #103361, #64261, #61691 ) ;
#172356=CARTESIAN_POINT ( 'NONE',  ( 20.94999999999999929, 68.00366762990589109, -224.2307594727497815 ) ) ;
#172404=CARTESIAN_POINT ( 'NONE',  ( 21.05000000000000071, 40.68212387350988735, -238.0221676322813096 ) ) ;
#172413=EDGE_LOOP ( 'NONE', ( #145543, #91311, #191367, #139950 ) ) ;
#172426=AXIS2_PLACEMENT_3D ( 'NONE', #225638, #168314, #47007 ) ;
#172445=ORIENTED_EDGE ( 'NONE', *, *, #157210, .T. ) ;
#172459=ORIENTED_EDGE ( 'NONE', *, *, #167949, .F. ) ;
#172466=ADVANCED_FACE ( 'NONE', ( #199087 ), #110698, .T. ) ;
#172537=CIRCLE ( 'NONE', #93360, 0.09999999999999414912 ) ;
#172539=DIRECTION ( 'NONE',  ( 0.000000000000000000, 0.9126074666063770380, 0.4088369013363281068 ) ) ;
#172580=EDGE_LOOP ( 'NONE', ( #97975, #217948, #171463, #41268 ) ) ;
#172584=CIRCLE ( 'NONE', #118367, 12.87499999999999112 ) ;
#172587=EDGE_CURVE ( 'NONE', #121176, #62147, #128220, .T. ) ;
#172595=CARTESIAN_POINT ( 'NONE',  ( -21.05000000000000071, 47.95459712139159336, -246.5019368548292675 ) ) ;
#172606=DIRECTION ( 'NONE',  ( 0.000000000000000000, -0.4166553800442105437, 0.9090645160164456673 ) ) ;
#172616=CARTESIAN_POINT ( 'NONE',  ( -22.47071067811865319, 36.65892442174472876, -249.5511627012454596 ) ) ;
#172619=CARTESIAN_POINT ( 'NONE',  ( 21.13461538461538325, 44.29694026544699170, -236.3931290369747842 ) ) ;
#172659=ORIENTED_EDGE ( 'NONE', *, *, #188829, .F. ) ;
#172671=SPHERICAL_SURFACE ( 'NONE', #40989, 0.1000000000000000056 ) ;
#172675=VERTEX_POINT ( 'NONE', #237589 ) ;
#172691=ORIENTED_EDGE ( 'NONE', *, *, #143065, .T. ) ;
#172703=ORIENTED_EDGE ( 'NONE', *, *, #22271, .T. ) ;
#172735=VECTOR ( 'NONE', #178177, 1000.000000000000000 ) ;
#172742=FACE_OUTER_BOUND ( 'NONE', #62999, .T. ) ;
#172743=DIRECTION ( 'NONE',  ( 1.000000000000000000, 0.000000000000000000, 0.000000000000000000 ) ) ;
#172755=( BOUNDED_SURFACE ( )  B_SPLINE_SURFACE ( 3, 2, ( 
 ( #96047, #115629, #196437 ),
 ( #17793, #54364, #37394 ),
 ( #178195, #175618, #19087 ),
 ( #99877, #154783, #76487 ) ),
 .UNSPECIFIED., .F., .F., .F. ) 
 B_SPLINE_SURFACE_WITH_KNOTS ( ( 4, 4 ),
 ( 3, 3 ),
 ( 0.04058434257139457990, 0.04256401539001584966 ),
 ( 0.000000000000000000, 1.000000000000000000 ),
 .UNSPECIFIED. ) 
 GEOMETRIC_REPRESENTATION_ITEM ( )  RATIONAL_B_SPLINE_SURFACE ( (
 ( 1.000000000000000000, 0.7103081912008166743, 1.000000000000000000),
 ( 1.000000000000000000, 0.7104998333555226919, 1.000000000000000000),
 ( 1.000000000000000000, 0.7107238315754937918, 1.000000000000000000),
 ( 1.000000000000000000, 0.7110073749539386201, 1.000000000000000000) ) ) 
 REPRESENTATION_ITEM ( '' )  SURFACE ( )  );
#172760=EDGE_CURVE ( 'NONE', #111770, #218845, #172142, .T. ) ;
#172773=FACE_OUTER_BOUND ( 'NONE', #175123, .T. ) ;
#172775=ORIENTED_EDGE ( 'NONE', *, *, #26808, .F. ) ;
#172800=CARTESIAN_POINT ( 'NONE',  ( 20.94999999999999929, 51.66758181523423588, -231.0768342483179083 ) ) ;
#172807=AXIS2_PLACEMENT_3D ( 'NONE', #183630, #47949, #67521 ) ;
#172825=ADVANCED_FACE ( 'NONE', ( #131689 ), #234637, .T. ) ;
#172826=CARTESIAN_POINT ( 'NONE',  ( -21.05000000000000071, 36.65892442174472876, -249.5511627012454596 ) ) ;
#172853=DIRECTION ( 'NONE',  ( 0.000000000000000000, 0.9947597004326491632, -0.1022405907413782566 ) ) ;
#172855=FACE_OUTER_BOUND ( 'NONE', #143207, .T. ) ;
#172891=DIRECTION ( 'NONE',  ( -0.000000000000000000, 0.9126074666063772600, 0.4088369013363276072 ) ) ;
#172907=DIRECTION ( 'NONE',  ( 0.000000000000000000, -0.9126074666063764829, -0.4088369013363293281 ) ) ;
#172961=CARTESIAN_POINT ( 'NONE',  ( 20.94999999999999574, 48.05114133249968944, -246.4758750954581785 ) ) ;
#172967=AXIS2_PLACEMENT_3D ( 'NONE', #228085, #12905, #168147 ) ;
#173011=CARTESIAN_POINT ( 'NONE',  ( -20.94999999999999929, 48.05114133249968944, -246.4758750954581785 ) ) ;
#173021=SPHERICAL_SURFACE ( 'NONE', #155945, 0.1000000000000000056 ) ;
#173027=DIRECTION ( 'NONE',  ( -1.000000000000000000, -0.000000000000000000, -0.000000000000000000 ) ) ;
#173041=EDGE_CURVE ( 'NONE', #233644, #11074, #40174, .T. ) ;
#173055=DIRECTION ( 'NONE',  ( 0.000000000000000000, 0.9126074666063771490, 0.4088369013363281623 ) ) ;
#173066=CARTESIAN_POINT ( 'NONE',  ( 20.95512820512820440, 43.40368376489742275, -234.8883907171572787 ) ) ;
#173070=ORIENTED_EDGE ( 'NONE', *, *, #7509, .F. ) ;
#173080=EDGE_CURVE ( 'NONE', #5885, #221119, #27714, .T. ) ;
#173082=CARTESIAN_POINT ( 'NONE',  ( 21.12769345151713196, 43.45362607442633873, -234.7614388166508093 ) ) ;
#173099=ORIENTED_EDGE ( 'NONE', *, *, #172195, .T. ) ;
#173131=CARTESIAN_POINT ( 'NONE',  ( -23.15000000000000213, 69.16514130714681130, -247.7543978865853660 ) ) ;
#173148=DIRECTION ( 'NONE',  ( 0.7071067811864846231, 0.2890913453341779626, -0.6453109281989296564 ) ) ;
#173167=CIRCLE ( 'NONE', #244012, 0.09999999999999538425 ) ;
#173185=CARTESIAN_POINT ( 'NONE',  ( 20.94999999999999929, 48.40874555430183790, -244.2873875965402704 ) ) ;
#173218=LINE ( 'NONE', #235695, #36531 ) ;
#173226=DIRECTION ( 'NONE',  ( 1.000000000000000000, 0.000000000000000000, 0.000000000000000000 ) ) ;
#173230=CYLINDRICAL_SURFACE ( 'NONE', #66322, 0.09999999999999939493 ) ;
#173237=( BOUNDED_CURVE ( )  B_SPLINE_CURVE ( 3, ( #117074, #256510, #255237, #132805 ),
 .UNSPECIFIED., .F., .F. ) 
 B_SPLINE_CURVE_WITH_KNOTS ( ( 4, 4 ),
 ( 1.570796326794895448, 3.141592653589791784 ),
 .UNSPECIFIED. ) 
 CURVE ( )  GEOMETRIC_REPRESENTATION_ITEM ( )  RATIONAL_B_SPLINE_CURVE ( ( 1.000000000000000000, 0.8047378541243650485, 0.8047378541243650485, 1.000000000000000000 ) ) 
 REPRESENTATION_ITEM ( '' )  );
#173274=B_SPLINE_CURVE_WITH_KNOTS ( 'NONE', 3,
 ( #181280, #123861, #62599, #202109, #183821, #41771, #102983, #182560, #5152, #242509, #203395, #143409, #126411, #65149, #205949, #44326, #125147, #24782, #104263 ),
 .UNSPECIFIED., .F., .F.,
 ( 4, 3, 3, 3, 3, 3, 4 ),
 ( 0.000000000000000000, 1.655171619025856859E-05, 2.773500582849416576E-05, 5.941817267376708916E-05, 0.0001114174635873553602, 0.0001914169455916492238, 0.0002627181070750875128 ),
 .UNSPECIFIED. ) ;
#173278=CARTESIAN_POINT ( 'NONE',  ( 21.05000000000000071, 62.08591502004790641, -248.5699171172615820 ) ) ;
#173322=LINE ( 'NONE', #130277, #117988 ) ;
#173327=ORIENTED_EDGE ( 'NONE', *, *, #205645, .T. ) ;
#173368=CARTESIAN_POINT ( 'NONE',  ( -22.59999970745345976, 25.93914356428276591, -254.3637448099888445 ) ) ;
#173383=EDGE_LOOP ( 'NONE', ( #6206, #17206, #202837, #44641 ) ) ;
#173403=CARTESIAN_POINT ( 'NONE',  ( -23.15000000000000213, 62.08591502004791352, -248.5699171172615820 ) ) ;
#173404=DIRECTION ( 'NONE',  ( -1.000000000000000000, -0.000000000000000000, 0.000000000000000000 ) ) ;
#173422=ORIENTED_EDGE ( 'NONE', *, *, #125456, .T. ) ;
#173432=LINE ( 'NONE', #31336, #233096 ) ;
#173435=DIRECTION ( 'NONE',  ( -1.000000000000000000, -0.000000000000000000, 0.000000000000000000 ) ) ;
#173450=CARTESIAN_POINT ( 'NONE',  ( 23.15000000000000213, 61.88149656937974896, -248.1136133839584090 ) ) ;
#173459=CIRCLE ( 'NONE', #165007, 0.1999999999999987899 ) ;
#173468=CARTESIAN_POINT ( 'NONE',  ( -20.85000000000000142, 68.11287320386161070, -224.1382462126928488 ) ) ;
#173474=EDGE_CURVE ( 'NONE', #75249, #129055, #186075, .T. ) ;
#173476=DIRECTION ( 'NONE',  ( 1.000000000000000000, 0.000000000000000000, 0.000000000000000000 ) ) ;
#173492=AXIS2_PLACEMENT_3D ( 'NONE', #84495, #124969, #67549 ) ;
#173513=CARTESIAN_POINT ( 'NONE',  ( -22.57320508075685694, 31.85509083104292571, -238.8280249686205252 ) ) ;
#173543=CARTESIAN_POINT ( 'NONE',  ( 22.39999999999999503, 29.50811709945092076, -252.6450601445781103 ) ) ;
#173568=EDGE_CURVE ( 'NONE', #60065, #151804, #123733, .T. ) ;
#173575=ADVANCED_FACE ( 'NONE', ( #230161 ), #254928, .T. ) ;
#173598=EDGE_CURVE ( 'NONE', #118767, #111624, #23528, .T. ) ;
#173602=CARTESIAN_POINT ( 'NONE',  ( 21.14999999999999858, 45.25174493058054281, -238.5244480634700324 ) ) ;
#173606=CARTESIAN_POINT ( 'NONE',  ( 23.14999999999999503, 21.13195309841794867, -243.6318585593223816 ) ) ;
#173613=TOROIDAL_SURFACE ( 'NONE', #115289, 12.97499999999999787, 0.1000000000000000056 ) ;
#173615=CARTESIAN_POINT ( 'NONE',  ( 23.14999999999998792, 31.89597452117651244, -238.9192857152811769 ) ) ;
#173616=DIRECTION ( 'NONE',  ( 0.000000000000000000, 0.9126074666063769270, 0.4088369013363281623 ) ) ;
#173632=ORIENTED_EDGE ( 'NONE', *, *, #25985, .T. ) ;
#173652=VERTEX_POINT ( 'NONE', #221816 ) ;
#173692=ORIENTED_EDGE ( 'NONE', *, *, #251668, .T. ) ;
#173693=ORIENTED_EDGE ( 'NONE', *, *, #97213, .T. ) ;
#173715=ADVANCED_FACE ( 'NONE', ( #150035 ), #68417, .F. ) ;
#173729=DIRECTION ( 'NONE',  ( 1.000000000000000000, 0.000000000000000000, 0.000000000000000000 ) ) ;
#173735=CARTESIAN_POINT ( 'NONE',  ( 22.16821283564877021, 33.56853718381600515, -242.6527871905703932 ) ) ;
#173743=ADVANCED_FACE ( 'NONE', ( #147444 ), #86155, .F. ) ;
#173752=VECTOR ( 'NONE', #64322, 1000.000000000000114 ) ;
#173770=CARTESIAN_POINT ( 'NONE',  ( 18.40916198585723151, 77.13860745477401792, -241.8264963619319872 ) ) ;
#173788=VERTEX_POINT ( 'NONE', #250393 ) ;
#173803=ORIENTED_EDGE ( 'NONE', *, *, #46805, .T. ) ;
#173814=CARTESIAN_POINT ( 'NONE',  ( 23.24999999999999289, 45.21086124044690280, -238.4331873168094091 ) ) ;
#173819=DIRECTION ( 'NONE',  ( -1.000000000000000000, 0.000000000000000000, 0.000000000000000000 ) ) ;
#173823=DIRECTION ( 'NONE',  ( 0.000000000000000000, 0.9126074666063773710, 0.4088369013363274962 ) ) ;
#173828=ORIENTED_EDGE ( 'NONE', *, *, #67912, .T. ) ;
#173831=CARTESIAN_POINT ( 'NONE',  ( 23.14999999999998437, 38.31471387215685809, -253.2472229410012687 ) ) ;
#173834=EDGE_CURVE ( 'NONE', #41988, #94854, #200164, .T. ) ;
#173880=ORIENTED_EDGE ( 'NONE', *, *, #248339, .T. ) ;
#173891=VERTEX_POINT ( 'NONE', #213836 ) ;
#173910=DIRECTION ( 'NONE',  ( -3.265361837132812600E-16, -0.4088369013363246096, 0.9126074666063785923 ) ) ;
#173954=AXIS2_PLACEMENT_3D ( 'NONE', #28786, #250349, #27496 ) ;
#173990=DIRECTION ( 'NONE',  ( 0.000000000000000000, 0.9126074666063805907, 0.4088369013363201132 ) ) ;
#174027=AXIS2_PLACEMENT_3D ( 'NONE', #199247, #240934, #38891 ) ;
#174044=EDGE_CURVE ( 'NONE', #235986, #118225, #206339, .T. ) ;
#174102=EDGE_CURVE ( 'NONE', #176861, #243814, #48879, .T. ) ;
#174103=CARTESIAN_POINT ( 'NONE',  ( 18.57071067811864040, 51.89016398296629973, -231.5736831079530020 ) ) ;
#174173=CYLINDRICAL_SURFACE ( 'NONE', #153729, 11.79999999999999538 ) ;
#174194=AXIS2_PLACEMENT_3D ( 'NONE', #75981, #133394, #253323 ) ;
#174208=CIRCLE ( 'NONE', #199114, 11.65000000000000213 ) ;
#174212=AXIS2_PLACEMENT_3D ( 'NONE', #144463, #42827, #28436 ) ;
#174221=EDGE_CURVE ( 'NONE', #22954, #118580, #36193, .T. ) ;
#174238=AXIS2_PLACEMENT_3D ( 'NONE', #211475, #112384, #191944 ) ;
#174273=EDGE_CURVE ( 'NONE', #201532, #7052, #149052, .T. ) ;
#174319=EDGE_CURVE ( 'NONE', #143659, #96682, #212343, .T. ) ;
#174325=EDGE_CURVE ( 'NONE', #62507, #93087, #198902, .T. ) ;
#174354=CARTESIAN_POINT ( 'NONE',  ( 22.00411653962185099, 33.60306640061018868, -242.9721070132476939 ) ) ;
#174375=ADVANCED_FACE ( 'NONE', ( #158719 ), #137820, .T. ) ;
#174396=ORIENTED_EDGE ( 'NONE', *, *, #159550, .T. ) ;
#174400=CARTESIAN_POINT ( 'NONE',  ( -20.94999999999999574, 56.21213088740040575, -228.0580413555848622 ) ) ;
#174405=ORIENTED_EDGE ( 'NONE', *, *, #101296, .F. ) ;
#174430=DIRECTION ( 'NONE',  ( 0.000000000000000000, -0.4088369013363280513, 0.9126074666063769270 ) ) ;
#174436=ORIENTED_EDGE ( 'NONE', *, *, #223879, .F. ) ;
#174449=CYLINDRICAL_SURFACE ( 'NONE', #121022, 0.09999999999999950595 ) ;
#174480=ORIENTED_EDGE ( 'NONE', *, *, #245811, .F. ) ;
#174483=AXIS2_PLACEMENT_3D ( 'NONE', #198354, #100508, #19738 ) ;
#174486=CARTESIAN_POINT ( 'NONE',  ( -20.85000000000000142, 74.83909925395606422, -233.7225145625711491 ) ) ;
#174500=VERTEX_POINT ( 'NONE', #84222 ) ;
#174534=EDGE_CURVE ( 'NONE', #225362, #223565, #111613, .T. ) ;
#174536=AXIS2_PLACEMENT_3D ( 'NONE', #47538, #107527, #167540 ) ;
#174577=CIRCLE ( 'NONE', #245449, 0.1000000000000024342 ) ;
#174581=VERTEX_POINT ( 'NONE', #106387 ) ;
#174605=ORIENTED_EDGE ( 'NONE', *, *, #73466, .T. ) ;
#174639=AXIS2_PLACEMENT_3D ( 'NONE', #172595, #132134, #171315 ) ;
#174645=CIRCLE ( 'NONE', #162137, 0.1000000000000024342 ) ;
#174667=AXIS2_PLACEMENT_3D ( 'NONE', #46666, #159272, #60136 ) ;
#174674=AXIS2_PLACEMENT_3D ( 'NONE', #221761, #180113, #177571 ) ;
#174763=ADVANCED_FACE ( 'NONE', ( #172855 ), #153280, .T. ) ;
#174767=ADVANCED_FACE ( 'NONE', ( #34598 ), #3450, .T. ) ;
#174769=AXIS2_PLACEMENT_3D ( 'NONE', #154742, #16509, #73930 ) ;
#174789=ORIENTED_EDGE ( 'NONE', *, *, #29438, .T. ) ;
#174797=CARTESIAN_POINT ( 'NONE',  ( 20.94999999999999929, 69.05648948627111849, -235.0374527038057977 ) ) ;
#174805=EDGE_CURVE ( 'NONE', #241985, #91860, #17563, .T. ) ;
#174809=CYLINDRICAL_SURFACE ( 'NONE', #256532, 0.09999999999999609201 ) ;
#174848=VECTOR ( 'NONE', #21687, 1000.000000000000114 ) ;
#174862=ORIENTED_EDGE ( 'NONE', *, *, #160066, .T. ) ;
#174870=EDGE_LOOP ( 'NONE', ( #8160, #162644, #226227, #115250 ) ) ;
#174872=CARTESIAN_POINT ( 'NONE',  ( 22.57320508075688537, 31.89597452117651244, -238.9192857152811769 ) ) ;
#174891=EDGE_CURVE ( 'NONE', #239804, #143336, #199099, .T. ) ;
#174922=CARTESIAN_POINT ( 'NONE',  ( 23.14999999999999858, 69.05648948627110428, -235.0374527038057977 ) ) ;
#174950=ORIENTED_EDGE ( 'NONE', *, *, #205971, .T. ) ;
#174978=AXIS2_PLACEMENT_3D ( 'NONE', #213286, #30839, #50346 ) ;
#174981=ORIENTED_EDGE ( 'NONE', *, *, #112784, .T. ) ;
#175028=EDGE_CURVE ( 'NONE', #120409, #31046, #224748, .T. ) ;
#175048=VERTEX_POINT ( 'NONE', #169975 ) ;
#175062=DIRECTION ( 'NONE',  ( 1.000000000000000000, 0.000000000000000000, 0.000000000000000000 ) ) ;
#175065=FACE_OUTER_BOUND ( 'NONE', #87362, .T. ) ;
#175075=VECTOR ( 'NONE', #3658, 1000.000000000000114 ) ;
#175098=FILL_AREA_STYLE ('',( #95504 ) ) ;
#175114=AXIS2_PLACEMENT_3D ( 'NONE', #223222, #4178, #180267 ) ;
#175122=CARTESIAN_POINT ( 'NONE',  ( 21.05000000000000782, 30.90959765417966665, -252.1452208208993966 ) ) ;
#175123=EDGE_LOOP ( 'NONE', ( #26183, #73840, #146396, #137076 ) ) ;
#175127=VERTEX_POINT ( 'NONE', #135917 ) ;
#175158=DIRECTION ( 'NONE',  ( 1.000000000000000000, 0.000000000000000000, 0.000000000000000000 ) ) ;
#175159=CARTESIAN_POINT ( 'NONE',  ( 23.14999999999999858, 56.16603649944111254, -228.1013850343386480 ) ) ;
#175188=ORIENTED_EDGE ( 'NONE', *, *, #23486, .T. ) ;
#175205=AXIS2_PLACEMENT_3D ( 'NONE', #257700, #79102, #58264 ) ;
#175231=AXIS2_PLACEMENT_3D ( 'NONE', #79611, #198293, #17115 ) ;
#175237=CARTESIAN_POINT ( 'NONE',  ( -23.15000000000000213, 69.16514130714681130, -247.7543978865853660 ) ) ;
#175249=CARTESIAN_POINT ( 'NONE',  ( 18.39999999999999858, 77.27075167199318173, -241.8768735168259241 ) ) ;
#175263=CARTESIAN_POINT ( 'NONE',  ( 21.05000000000000071, 44.00266445878927613, -258.8505972146074896 ) ) ;
#175275=CARTESIAN_POINT ( 'NONE',  ( -21.44999999999999929, 53.12864924257549148, -234.3382351616128858 ) ) ;
#175288=CIRCLE ( 'NONE', #183636, 0.09999999999999939493 ) ;
#175291=DIRECTION ( 'NONE',  ( 0.000000000000000000, 0.9126074666063660468, 0.4088369013363524762 ) ) ;
#175306=ORIENTED_EDGE ( 'NONE', *, *, #71219, .T. ) ;
#175385=EDGE_CURVE ( 'NONE', #13609, #120046, #78810, .T. ) ;
#175409=CARTESIAN_POINT ( 'NONE',  ( 18.59999999999999787, 77.40560538581968331, -241.7331240221339783 ) ) ;
#175437=CARTESIAN_POINT ( 'NONE',  ( -21.05000000000000071, 36.65892442174472876, -249.5511627012454596 ) ) ;
#175453=EDGE_CURVE ( 'NONE', #112954, #191992, #120556, .T. ) ;
#175456=AXIS2_PLACEMENT_3D ( 'NONE', #204288, #25674, #187327 ) ;
#175499=ORIENTED_EDGE ( 'NONE', *, *, #9090, .F. ) ;
#175501=FACE_OUTER_BOUND ( 'NONE', #145759, .T. ) ;
#175572=EDGE_LOOP ( 'NONE', ( #187846, #9391, #159867, #191271, #201481 ) ) ;
#175593=ORIENTED_EDGE ( 'NONE', *, *, #20523, .F. ) ;
#175603=ORIENTED_EDGE ( 'NONE', *, *, #44357, .T. ) ;
#175618=CARTESIAN_POINT ( 'NONE',  ( -21.53699400384685703, 33.88385736502569756, -243.3566462376632842 ) ) ;
#175645=PLANE ( 'NONE',  #94117 ) ;
#175658=ADVANCED_FACE ( 'NONE', ( #94578 ), #174173, .F. ) ;
#175679=DIRECTION ( 'NONE',  ( -0.7071067811865475727, 0.2890913453342130457, -0.6453109281988448354 ) ) ;
#175681=ADVANCED_FACE ( 'NONE', ( #234088 ), #149452, .F. ) ;
#175700=CARTESIAN_POINT ( 'NONE',  ( 20.94999999999999574, 35.88801296822693843, -234.5558624753690538 ) ) ;
#175705=CARTESIAN_POINT ( 'NONE',  ( -22.48479450179659977, 26.00783696130147504, -254.2712270987252339 ) ) ;
#175759=ADVANCED_FACE ( 'NONE', ( #236658 ), #99692, .F. ) ;
#175781=DIRECTION ( 'NONE',  ( 0.000000000000000000, 0.9126074666063545004, 0.4088369013363783999 ) ) ;
#175784=VERTEX_POINT ( 'NONE', #159708 ) ;
#175785=CARTESIAN_POINT ( 'NONE',  ( 20.94999999999999929, 45.93587830916155212, -239.9163948487882863 ) ) ;
#175811=CARTESIAN_POINT ( 'NONE',  ( 20.94999999999999929, 54.23099463892082639, -236.2002849323373539 ) ) ;
#175823=ORIENTED_EDGE ( 'NONE', *, *, #206393, .F. ) ;
#175853=FACE_OUTER_BOUND ( 'NONE', #47919, .T. ) ;
#175868=ORIENTED_EDGE ( 'NONE', *, *, #161876, .F. ) ;
#175870=CIRCLE ( 'NONE', #46640, 11.74999999999999822 ) ;
#175881=CIRCLE ( 'NONE', #84219, 0.09999999999999854838 ) ;
#175923=FACE_OUTER_BOUND ( 'NONE', #58891, .T. ) ;
#176031=ORIENTED_EDGE ( 'NONE', *, *, #117071, .F. ) ;
#176036=CIRCLE ( 'NONE', #209308, 0.9750000000000036415 ) ;
#176044=ORIENTED_EDGE ( 'NONE', *, *, #12970, .T. ) ;
#176060=LINE ( 'NONE', #174797, #96138 ) ;
#176075=CARTESIAN_POINT ( 'NONE',  ( 21.14999999999999503, 30.69873658968802133, -264.9868732779115703 ) ) ;
#176121=ORIENTED_EDGE ( 'NONE', *, *, #140237, .F. ) ;
#176131=VERTEX_POINT ( 'NONE', #175159 ) ;
#176155=CARTESIAN_POINT ( 'NONE',  ( 21.14999999999999858, 45.02833974712562792, -238.5149546970766892 ) ) ;
#176169=EDGE_CURVE ( 'NONE', #242431, #13670, #212503, .T. ) ;
#176176=AXIS2_PLACEMENT_3D ( 'NONE', #256279, #217205, #257572 ) ;
#176187=CARTESIAN_POINT ( 'NONE',  ( -21.05000000000000071, 30.73075574124490572, -252.3164853687435709 ) ) ;
#176198=ORIENTED_EDGE ( 'NONE', *, *, #155678, .T. ) ;
#176200=ORIENTED_EDGE ( 'NONE', *, *, #199562, .F. ) ;
#176202=ORIENTED_EDGE ( 'NONE', *, *, #247643, .F. ) ;
#176217=EDGE_CURVE ( 'NONE', #18296, #133755, #100019, .T. ) ;
#176298=ORIENTED_EDGE ( 'NONE', *, *, #233943, .T. ) ;
#176331=CARTESIAN_POINT ( 'NONE',  ( -20.85000000000000142, 74.74783850729542678, -233.7633982527047465 ) ) ;
#176362=CARTESIAN_POINT ( 'NONE',  ( -21.05000000000000071, 46.54514716347711101, -243.1111603596801842 ) ) ;
#176374=CARTESIAN_POINT ( 'NONE',  ( -20.54999999999999716, 62.04503132991428060, -248.4786563706009588 ) ) ;
#176375=DIRECTION ( 'NONE',  ( 1.000000000000000000, 0.000000000000000000, 0.000000000000000000 ) ) ;
#176449=CARTESIAN_POINT ( 'NONE',  ( 18.59999999999999076, 46.45388641681647357, -243.1520440498138385 ) ) ;
#176467=EDGE_LOOP ( 'NONE', ( #167161, #55093, #89374, #116627 ) ) ;
#176504=ORIENTED_EDGE ( 'NONE', *, *, #5499, .T. ) ;
#176508=FACE_OUTER_BOUND ( 'NONE', #202138, .T. ) ;
#176540=DIRECTION ( 'NONE',  ( 0.000000000000000000, 0.9126074666063769270, 0.4088369013363280513 ) ) ;
#176541=EDGE_CURVE ( 'NONE', #105422, #214442, #167377, .T. ) ;
#176610=AXIS2_PLACEMENT_3D ( 'NONE', #226213, #51437, #47598 ) ;
#176681=FACE_OUTER_BOUND ( 'NONE', #148771, .T. ) ;
#176713=CARTESIAN_POINT ( 'NONE',  ( 18.49999999999998934, 53.37395138337728895, -234.8857996415767104 ) ) ;
#176755=ORIENTED_EDGE ( 'NONE', *, *, #217476, .F. ) ;
#176808=CARTESIAN_POINT ( 'NONE',  ( -20.85000000000000142, 67.23127455305835554, -235.8551265064784559 ) ) ;
#176818=EDGE_CURVE ( 'NONE', #33783, #15704, #117288, .T. ) ;
#176831=EDGE_CURVE ( 'NONE', #2697, #120409, #204928, .T. ) ;
#176840=LINE ( 'NONE', #180678, #239780 ) ;
#176861=VERTEX_POINT ( 'NONE', #97680 ) ;
#176888=AXIS2_PLACEMENT_3D ( 'NONE', #242437, #63821, #143345 ) ;
#176920=AXIS2_PLACEMENT_3D ( 'NONE', #170407, #110367, #244733 ) ;
#176925=EDGE_CURVE ( 'NONE', #246004, #228778, #142563, .T. ) ;
#176942=DIRECTION ( 'NONE',  ( 0.000000000000000000, -0.9126074666063622720, -0.4088369013363611360 ) ) ;
#176943=VERTEX_POINT ( 'NONE', #117281 ) ;
#176997=FACE_OUTER_BOUND ( 'NONE', #159705, .T. ) ;
#177037=DIRECTION ( 'NONE',  ( 0.000000000000000000, 0.9126074666063764829, 0.4088369013363290505 ) ) ;
#177064=EDGE_CURVE ( 'NONE', #21148, #224911, #189148, .T. ) ;
#177088=CARTESIAN_POINT ( 'NONE',  ( 23.24999999999999289, 31.89597452117650533, -238.9192857152811484 ) ) ;
#177114=CYLINDRICAL_SURFACE ( 'NONE', #6510, 0.1000000000000024342 ) ;
#177178=DIRECTION ( 'NONE',  ( 6.938893903907222856E-15, 0.4088369013363281068, -0.9126074666063770380 ) ) ;
#177187=EDGE_LOOP ( 'NONE', ( #140750, #78687, #155001 ) ) ;
#177188=DIRECTION ( 'NONE',  ( 0.000000000000000000, 0.4088369013363287729, -0.9126074666063767049 ) ) ;
#177197=LINE ( 'NONE', #205699, #257439 ) ;
#177212=CARTESIAN_POINT ( 'NONE',  ( 18.39999999999999858, 77.17949092533254429, -241.9177572069595783 ) ) ;
#177221=ORIENTED_EDGE ( 'NONE', *, *, #196069, .F. ) ;
#177259=LINE ( 'NONE', #136804, #111530 ) ;
#177285=ORIENTED_EDGE ( 'NONE', *, *, #225449, .F. ) ;
#177292=CARTESIAN_POINT ( 'NONE',  ( -20.85000000000000497, 56.11297552314564285, -227.9607914937810733 ) ) ;
#177341=( BOUNDED_SURFACE ( )  B_SPLINE_SURFACE ( 3, 2, ( 
 ( #139099, #137837, #879 ),
 ( #217373, #2176, #102540 ),
 ( #37490, #40073, #136552 ),
 ( #140410, #3467, #256447 ),
 ( #257744, #117013, #119600 ),
 ( #219959, #158736, #118303 ),
 ( #21774, #141697, #197819 ),
 ( #200401, #201674, #199115 ),
 ( #60874, #236957, #157458 ),
 ( #160013, #20496, #19193 ) ),
 .UNSPECIFIED., .F., .F., .F. ) 
 B_SPLINE_SURFACE_WITH_KNOTS ( ( 4, 2, 2, 2, 4 ),
 ( 3, 3 ),
 ( 0.0001836757140118967866, 0.0004000170051583450668, 0.0005081876507315692204, 0.0005622729735181812702, 0.0006163582963047933199 ),
 ( 0.000000000000000000, 1.000000000000000000 ),
 .UNSPECIFIED. ) 
 GEOMETRIC_REPRESENTATION_ITEM ( )  RATIONAL_B_SPLINE_SURFACE ( (
 ( 1.000000000000000000, 0.7071067811865475727, 1.000000000000000000),
 ( 1.000000000000000000, 0.6461995200041559251, 1.000000000000000000),
 ( 1.000000000000000000, 0.5776453529532865616, 1.000000000000000000),
 ( 1.000000000000000000, 0.4585233068360237696, 1.000000000000000000),
 ( 1.000000000000000000, 0.4154092989944294656, 1.000000000000000000),
 ( 1.000000000000000000, 0.3550093145832801111, 1.000000000000000000),
 ( 1.000000000000000000, 0.3354498651690954736, 1.000000000000000000),
 ( 1.000000000000000000, 0.3060347992252003824, 1.000000000000000000),
 ( 1.000000000000000000, 0.2963555829628572447, 1.000000000000000000),
 ( 1.000000000000000000, 0.2966190024561997651, 1.000000000000000000) ) ) 
 REPRESENTATION_ITEM ( '' )  SURFACE ( )  );
#177352=DIRECTION ( 'NONE',  ( 1.000000000000000000, 0.000000000000000000, 0.000000000000000000 ) ) ;
#177370=AXIS2_PLACEMENT_3D ( 'NONE', #40006, #119527, #199049 ) ;
#177379=CYLINDRICAL_SURFACE ( 'NONE', #147643, 0.1000000000000078187 ) ;
#177427=ORIENTED_EDGE ( 'NONE', *, *, #185841, .T. ) ;
#177428=VERTEX_POINT ( 'NONE', #85496 ) ;
#177448=CARTESIAN_POINT ( 'NONE',  ( 23.14999999999999858, 53.62064951147646497, -235.8162552129080609 ) ) ;
#177481=TOROIDAL_SURFACE ( 'NONE', #139832, 1.900000000000002576, 0.1000000000000000056 ) ;
#177536=DIRECTION ( 'NONE',  ( -1.000000000000000000, 0.000000000000000000, 0.000000000000000000 ) ) ;
#177565=VERTEX_POINT ( 'NONE', #131078 ) ;
#177571=DIRECTION ( 'NONE',  ( -1.000000000000000000, -0.000000000000000000, 0.000000000000000000 ) ) ;
#177573=LINE ( 'NONE', #154162, #224665 ) ;
#177585=ORIENTED_EDGE ( 'NONE', *, *, #178669, .F. ) ;
#177605=LINE ( 'NONE', #56320, #219457 ) ;
#177606=DIRECTION ( 'NONE',  ( -1.000000000000000000, -0.000000000000000000, 0.000000000000000000 ) ) ;
#177620=VERTEX_POINT ( 'NONE', #90660 ) ;
#177625=DIRECTION ( 'NONE',  ( -0.000000000000000000, 0.4088369013363281623, -0.9126074666063771490 ) ) ;
#177654=CIRCLE ( 'NONE', #115259, 4.000000000000002665 ) ;
#177655=CARTESIAN_POINT ( 'NONE',  ( 18.53691006697114929, 54.99043569302317280, -230.0501718883048738 ) ) ;
#177656=AXIS2_PLACEMENT_3D ( 'NONE', #145477, #46369, #202891 ) ;
#177659=DIRECTION ( 'NONE',  ( -0.000000000000000000, -0.4088369013363283844, 0.9126074666063769270 ) ) ;
#177663=CYLINDRICAL_SURFACE ( 'NONE', #60950, 0.09999999999999939493 ) ;
#177666=CIRCLE ( 'NONE', #206855, 0.09999999999999939493 ) ;
#177688=ADVANCED_FACE ( 'NONE', ( #34572, #33309 ), #112809, .T. ) ;
#177690=CARTESIAN_POINT ( 'NONE',  ( -22.49806830649814415, 31.82532512087596288, -238.9510566881495777 ) ) ;
#177705=CIRCLE ( 'NONE', #169522, 0.09999999999999939493 ) ;
#177715=DIRECTION ( 'NONE',  ( 0.000000000000000000, -0.4166553800442105437, 0.9090645160164456673 ) ) ;
#177788=VERTEX_POINT ( 'NONE', #117925 ) ;
#177796=DIRECTION ( 'NONE',  ( -1.000000000000000000, 0.000000000000000000, 0.000000000000000000 ) ) ;
#177804=CARTESIAN_POINT ( 'NONE',  ( -18.59999999999999787, 47.95459712139159336, -246.5019368548292675 ) ) ;
#177822=DIRECTION ( 'NONE',  ( 0.000000000000000000, 0.9126074666063769270, 0.4088369013363280513 ) ) ;
#177855=CARTESIAN_POINT ( 'NONE',  ( -20.94999999999999929, 67.23127455305835554, -235.8551265064784559 ) ) ;
#177864=DIRECTION ( 'NONE',  ( 0.000000000000000000, 0.9579639084728132081, 0.2868887416116073785 ) ) ;
#177865=ORIENTED_EDGE ( 'NONE', *, *, #27113, .T. ) ;
#177924=CARTESIAN_POINT ( 'NONE',  ( -23.15000000000000213, 47.70572087816298534, -241.8629305864830030 ) ) ;
#177945=AXIS2_PLACEMENT_3D ( 'NONE', #68592, #7323, #226347 ) ;
#177950=DIRECTION ( 'NONE',  ( -4.239556034732056743E-17, -0.9579639084728132081, -0.2868887416116073230 ) ) ;
#177951=TOROIDAL_SURFACE ( 'NONE', #61419, 0.2000000000000000111, 0.1000000000000000056 ) ;
#177955=EDGE_CURVE ( 'NONE', #44054, #182258, #244292, .T. ) ;
#177985=CARTESIAN_POINT ( 'NONE',  ( -20.94999999999999929, 46.50671693017397246, -243.2369495081682942 ) ) ;
#178027=CARTESIAN_POINT ( 'NONE',  ( 18.59999999999997655, 74.93036000061670165, -233.6816308724374949 ) ) ;
#178052=LINE ( 'NONE', #77618, #196000 ) ;
#178064=ORIENTED_EDGE ( 'NONE', *, *, #65821, .F. ) ;
#178075=ORIENTED_EDGE ( 'NONE', *, *, #233302, .T. ) ;
#178076=EDGE_CURVE ( 'NONE', #105460, #104983, #169418, .T. ) ;
#178101=EDGE_CURVE ( 'NONE', #180643, #112954, #11159, .T. ) ;
#178177=DIRECTION ( 'NONE',  ( 1.000000000000000000, 0.000000000000000000, 0.000000000000000000 ) ) ;
#178181=ORIENTED_EDGE ( 'NONE', *, *, #106210, .F. ) ;
#178195=CARTESIAN_POINT ( 'NONE',  ( -21.46681500593987479, 33.85532080846552816, -243.2929468148609260 ) ) ;
#178281=ORIENTED_EDGE ( 'NONE', *, *, #62555, .T. ) ;
#178290=DIRECTION ( 'NONE',  ( 0.000000000000000000, 0.9126074666063769270, 0.4088369013363280513 ) ) ;
#178300=ORIENTED_EDGE ( 'NONE', *, *, #51374, .T. ) ;
#178307=EDGE_CURVE ( 'NONE', #210461, #85043, #211073, .T. ) ;
#178314=DIRECTION ( 'NONE',  ( 0.000000000000000000, -0.9126074666063763718, -0.4088369013363293836 ) ) ;
#178320=FACE_OUTER_BOUND ( 'NONE', #107812, .T. ) ;
#178325=DIRECTION ( 'NONE',  ( -0.000000000000000000, -0.4088369013363283844, 0.9126074666063769270 ) ) ;
#178330=CARTESIAN_POINT ( 'NONE',  ( -20.85000000000000142, 74.44087353924872730, -232.6253149859214773 ) ) ;
#178349=CARTESIAN_POINT ( 'NONE',  ( 22.48660254037845263, 31.80946045771257502, -238.8484668136873381 ) ) ;
#178367=EDGE_CURVE ( 'NONE', #38559, #48342, #227806, .T. ) ;
#178370=CARTESIAN_POINT ( 'NONE',  ( -21.65000000000000213, 52.80902093404626640, -233.8693558107618173 ) ) ;
#178409=ORIENTED_EDGE ( 'NONE', *, *, #175453, .T. ) ;
#178410=AXIS2_PLACEMENT_3D ( 'NONE', #161997, #143682, #126697 ) ;
#178422=CARTESIAN_POINT ( 'NONE',  ( -23.15000000000000213, 61.88149656937975607, -248.1136133839584090 ) ) ;
#178448=DIRECTION ( 'NONE',  ( 1.000000000000000000, 1.387778780781454006E-13, 0.000000000000000000 ) ) ;
#178449=ORIENTED_EDGE ( 'NONE', *, *, #60452, .T. ) ;
#178483=EDGE_LOOP ( 'NONE', ( #172691, #133142, #175593 ) ) ;
#178487=VERTEX_POINT ( 'NONE', #38759 ) ;
#178502=CARTESIAN_POINT ( 'NONE',  ( -23.25000000000000000, 36.65892442174472876, -249.5511627012454596 ) ) ;
#178504=VERTEX_POINT ( 'NONE', #219954 ) ;
#178526=DIRECTION ( 'NONE',  ( 0.000000000000000000, -0.9579639084728132081, -0.2868887416116073785 ) ) ;
#178600=CARTESIAN_POINT ( 'NONE',  ( -23.15000000000000213, 69.09936979046463534, -247.6075824278584605 ) ) ;
#178605=CIRCLE ( 'NONE', #103704, 0.09999999999999939493 ) ;
#178655=ADVANCED_FACE ( 'NONE', ( #165120 ), #149427, .T. ) ;
#178669=EDGE_CURVE ( 'NONE', #41121, #104038, #77958, .T. ) ;
#178677=CARTESIAN_POINT ( 'NONE',  ( 21.14999999999999503, 26.06832281015329755, -254.4051978787608732 ) ) ;
#178756=DIRECTION ( 'NONE',  ( 0.000000000000000000, 0.9579639084728132081, 0.2868887416116073785 ) ) ;
#178761=EDGE_CURVE ( 'NONE', #75249, #44800, #236380, .T. ) ;
#178763=ORIENTED_EDGE ( 'NONE', *, *, #95373, .T. ) ;
#178776=AXIS2_PLACEMENT_3D ( 'NONE', #36198, #156154, #92291 ) ;
#178788=ORIENTED_EDGE ( 'NONE', *, *, #47806, .F. ) ;
#178795=VERTEX_POINT ( 'NONE', #73745 ) ;
#178800=CARTESIAN_POINT ( 'NONE',  ( -18.50000000000000000, 31.98723526783714988, -238.8784020251475511 ) ) ;
#178831=ORIENTED_EDGE ( 'NONE', *, *, #87636, .T. ) ;
#178847=DIRECTION ( 'NONE',  ( 0.000000000000000000, -0.4088369013363283289, 0.9126074666063768159 ) ) ;
#178883=ORIENTED_EDGE ( 'NONE', *, *, #99740, .F. ) ;
#178942=ORIENTED_EDGE ( 'NONE', *, *, #2091, .T. ) ;
#178944=CARTESIAN_POINT ( 'NONE',  ( 23.15000000000000213, 61.88149656937974896, -248.1136133839584090 ) ) ;
#178953=CARTESIAN_POINT ( 'NONE',  ( -20.85000000000000142, 71.99422445362657186, -246.4870034924427671 ) ) ;
#178983=CARTESIAN_POINT ( 'NONE',  ( -22.48660254037843487, 31.85034414784621148, -238.9397275603479898 ) ) ;
#178989=ADVANCED_FACE ( 'NONE', ( #205205 ), #26609, .F. ) ;
#179003=CARTESIAN_POINT ( 'NONE',  ( 21.00000000000000000, 51.97441255244040548, -232.0063394385699667 ) ) ;
#179059=CIRCLE ( 'NONE', #162461, 0.09999999999999939493 ) ;
#179062=ORIENTED_EDGE ( 'NONE', *, *, #127898, .F. ) ;
#179063=ORIENTED_EDGE ( 'NONE', *, *, #29158, .T. ) ;
#179082=DIRECTION ( 'NONE',  ( 1.000000000000000000, -1.207181226542539700E-16, 2.694675058168174199E-16 ) ) ;
#179098=CARTESIAN_POINT ( 'NONE',  ( 23.14999999999999858, 54.36558989155976462, -236.3448031251562327 ) ) ;
#179119=ORIENTED_EDGE ( 'NONE', *, *, #147731, .T. ) ;
#179124=ORIENTED_EDGE ( 'NONE', *, *, #236877, .F. ) ;
#179132=VERTEX_POINT ( 'NONE', #115115 ) ;
#179139=DIRECTION ( 'NONE',  ( 0.000000000000000000, 0.4088369013363280513, -0.9126074666063769270 ) ) ;
#179147=VECTOR ( 'NONE', #154757, 1000.000000000000114 ) ;
#179152=EDGE_CURVE ( 'NONE', #109264, #71691, #65865, .T. ) ;
#179166=PRODUCT_DEFINITION ( 'UNKNOWN', '', #119697, #238298 ) ;
#179168=AXIS2_PLACEMENT_3D ( 'NONE', #63334, #137735, #180741 ) ;
#179201=ORIENTED_EDGE ( 'NONE', *, *, #91621, .F. ) ;
#179234=EDGE_LOOP ( 'NONE', ( #68706, #180570, #156018, #27448 ) ) ;
#179256=CARTESIAN_POINT ( 'NONE',  ( 18.58719872626879877, 77.36871634755026150, -241.7964367688455241 ) ) ;
#179260=DIRECTION ( 'NONE',  ( -0.000000000000000000, -0.9126074666063771490, -0.4088369013363281623 ) ) ;
#179273=EDGE_CURVE ( 'NONE', #85043, #97414, #160694, .T. ) ;
#179306=TOROIDAL_SURFACE ( 'NONE', #175231, 11.65000000000000036, 0.1000000000000000056 ) ;
#179324=AXIS2_PLACEMENT_3D ( 'NONE', #1440, #83521, #163115 ) ;
#179334=LINE ( 'NONE', #158493, #137487 ) ;
#179356=DIRECTION ( 'NONE',  ( 0.000000000000000000, 0.9126074666063753726, 0.4088369013363320481 ) ) ;
#179408=DIRECTION ( 'NONE',  ( 1.000000000000000000, 0.000000000000000000, 0.000000000000000000 ) ) ;
#179421=B_SPLINE_CURVE_WITH_KNOTS ( 'NONE', 3,
 ( #181034, #83155, #246132, #124902, #203144, #162755 ),
 .UNSPECIFIED., .F., .F.,
 ( 4, 2, 4 ),
 ( 0.000000000000000000, 0.0001568709654583398281, 0.0003137419309166796563 ),
 .UNSPECIFIED. ) ;
#179446=AXIS2_PLACEMENT_3D ( 'NONE', #147584, #48475, #129307 ) ;
#179465=ORIENTED_EDGE ( 'NONE', *, *, #78103, .F. ) ;
#179469=DIRECTION ( 'NONE',  ( 0.000000000000000000, -0.9126074666063545004, -0.4088369013363783999 ) ) ;
#179534=VERTEX_POINT ( 'NONE', #125392 ) ;
#179538=ORIENTED_EDGE ( 'NONE', *, *, #255333, .T. ) ;
#179548=DIRECTION ( 'NONE',  ( 1.000000000000000000, 0.000000000000000000, 0.000000000000000000 ) ) ;
#179563=DIRECTION ( 'NONE',  ( 0.000000000000000000, -0.9126074666063660468, -0.4088369013363524762 ) ) ;
#179573=EDGE_CURVE ( 'NONE', #24454, #182190, #11880, .T. ) ;
#179621=ORIENTED_EDGE ( 'NONE', *, *, #235995, .F. ) ;
#179639=CARTESIAN_POINT ( 'NONE',  ( 21.10320863425824811, 34.01941935407060669, -243.7204517896670382 ) ) ;
#179660=CIRCLE ( 'NONE', #195858, 0.3999999999999970801 ) ;
#179677=ORIENTED_EDGE ( 'NONE', *, *, #133235, .T. ) ;
#179682=FACE_OUTER_BOUND ( 'NONE', #7483, .T. ) ;
#179714=CYLINDRICAL_SURFACE ( 'NONE', #72547, 0.1000000000000024342 ) ;
#179743=DIRECTION ( 'NONE',  ( 1.000000000000000000, 0.000000000000000000, 0.000000000000000000 ) ) ;
#179758=DIRECTION ( 'NONE',  ( 1.000000000000000000, 0.000000000000000000, 0.000000000000000000 ) ) ;
#179795=FACE_OUTER_BOUND ( 'NONE', #167385, .T. ) ;
#179800=DIRECTION ( 'NONE',  ( -1.836970198721029934E-16, -0.4088369013363280513, 0.9126074666063769270 ) ) ;
#179820=ORIENTED_EDGE ( 'NONE', *, *, #19361, .T. ) ;
#179824=DIRECTION ( 'NONE',  ( 0.000000000000000000, -0.9126074666063602736, -0.4088369013363654103 ) ) ;
#179843=CARTESIAN_POINT ( 'NONE',  ( 20.94999999999999929, 68.01331835486308819, -224.1288211375801609 ) ) ;
#179859=DIRECTION ( 'NONE',  ( -1.000000000000000000, -0.000000000000000000, -0.000000000000000000 ) ) ;
#179887=EDGE_LOOP ( 'NONE', ( #174981, #7337, #149921, #116951 ) ) ;
#179903=ORIENTED_EDGE ( 'NONE', *, *, #149185, .T. ) ;
#179910=VECTOR ( 'NONE', #230656, 1000.000000000000000 ) ;
#179986=DIRECTION ( 'NONE',  ( 4.377807931758639578E-15, -0.9876013379310922824, -0.1569827930593562515 ) ) ;
#180040=ORIENTED_EDGE ( 'NONE', *, *, #118738, .F. ) ;
#180048=ORIENTED_EDGE ( 'NONE', *, *, #127301, .F. ) ;
#180113=DIRECTION ( 'NONE',  ( 0.000000000000000000, 0.9126074666063770380, 0.4088369013363281068 ) ) ;
#180143=AXIS2_PLACEMENT_3D ( 'NONE', #195950, #117673, #38157 ) ;
#180144=DIRECTION ( 'NONE',  ( 0.000000000000000000, -0.9126074666063773710, -0.4088369013363271631 ) ) ;
#180201=EDGE_CURVE ( 'NONE', #40310, #143511, #237113, .T. ) ;
#180220=DIRECTION ( 'NONE',  ( 1.000000000000000000, 0.000000000000000000, 0.000000000000000000 ) ) ;
#180267=DIRECTION ( 'NONE',  ( -1.000000000000000000, 0.000000000000000000, 0.000000000000000000 ) ) ;
#180290=AXIS2_PLACEMENT_3D ( 'NONE', #167313, #244236, #125585 ) ;
#180292=ORIENTED_EDGE ( 'NONE', *, *, #251668, .F. ) ;
#180317=ORIENTED_EDGE ( 'NONE', *, *, #85972, .T. ) ;
#180326=ADVANCED_FACE ( 'NONE', ( #49895 ), #128974, .T. ) ;
#180336=ORIENTED_EDGE ( 'NONE', *, *, #25375, .T. ) ;
#180407=CARTESIAN_POINT ( 'NONE',  ( 21.05000000000001137, 33.99373157816871327, -243.8426824212976953 ) ) ;
#180412=CARTESIAN_POINT ( 'NONE',  ( 23.14999999999999503, 42.94327155031035659, -233.8606566173841372 ) ) ;
#180413=CYLINDRICAL_SURFACE ( 'NONE', #21841, 0.1000000000000065836 ) ;
#180423=ORIENTED_EDGE ( 'NONE', *, *, #220382, .F. ) ;
#180426=DIRECTION ( 'NONE',  ( -0.7071067811865475727, 0.2890913453342130457, -0.6453109281988448354 ) ) ;
#180434=CARTESIAN_POINT ( 'NONE',  ( 21.04999999999651905, 40.80806194774932294, -237.9707170097019855 ) ) ;
#180441=AXIS2_PLACEMENT_3D ( 'NONE', #20284, #66785, #27698 ) ;
#180448=CARTESIAN_POINT ( 'NONE',  ( 23.14999999999999503, 21.17283678855157802, -243.7231193059830048 ) ) ;
#180452=ADVANCED_FACE ( 'NONE', ( #197108 ), #135841, .T. ) ;
#180499=ADVANCED_FACE ( 'NONE', ( #238820 ), #4049, .F. ) ;
#180512=CARTESIAN_POINT ( 'NONE',  ( 18.59999999999999787, 74.86109765932729943, -233.8067614591677454 ) ) ;
#180533=LINE ( 'NONE', #220912, #92829 ) ;
#180543=AXIS2_PLACEMENT_3D ( 'NONE', #121960, #257551, #20304 ) ;
#180570=ORIENTED_EDGE ( 'NONE', *, *, #167990, .T. ) ;
#180590=VECTOR ( 'NONE', #155621, 1000.000000000000000 ) ;
#180595=ORIENTED_EDGE ( 'NONE', *, *, #97624, .F. ) ;
#180618=DIRECTION ( 'NONE',  ( 0.000000000000000000, 0.2868887416115947775, -0.9579639084728169829 ) ) ;
#180643=VERTEX_POINT ( 'NONE', #126575 ) ;
#180666=EDGE_CURVE ( 'NONE', #27038, #61955, #158224, .T. ) ;
#180678=CARTESIAN_POINT ( 'NONE',  ( -20.54999999999999716, 65.40605961984559258, -236.6728003091511425 ) ) ;
#180738=DIRECTION ( 'NONE',  ( 0.000000000000000000, -0.9126074666063771490, -0.4088369013363281623 ) ) ;
#180741=DIRECTION ( 'NONE',  ( 0.000000000000000000, 0.4088369013363304383, -0.9126074666063759278 ) ) ;
#180746=ORIENTED_EDGE ( 'NONE', *, *, #114081, .T. ) ;
#180791=LINE ( 'NONE', #195561, #131537 ) ;
#180797=ORIENTED_EDGE ( 'NONE', *, *, #176925, .F. ) ;
#180808=AXIS2_PLACEMENT_3D ( 'NONE', #375, #244122, #141187 ) ;
#180828=VERTEX_POINT ( 'NONE', #234661 ) ;
#180852=LINE ( 'NONE', #199123, #146781 ) ;
#180876=DIRECTION ( 'NONE',  ( -1.000000000000000000, -0.000000000000000000, 0.000000000000000000 ) ) ;
#180879=CIRCLE ( 'NONE', #55949, 0.09999999999999847899 ) ;
#180890=DIRECTION ( 'NONE',  ( 1.000000000000000000, 0.000000000000000000, 0.000000000000000000 ) ) ;
#180906=EDGE_CURVE ( 'NONE', #140623, #24438, #220725, .T. ) ;
#180910=CARTESIAN_POINT ( 'NONE',  ( 21.08198257630413508, 34.00199500830718335, -243.7980364803085820 ) ) ;
#180919=EDGE_LOOP ( 'NONE', ( #231764, #16489, #115774, #186794 ) ) ;
#180959=AXIS2_PLACEMENT_3D ( 'NONE', #40501, #179986, #102981 ) ;
#180966=DIRECTION ( 'NONE',  ( -1.000000000000000000, -0.000000000000000000, 0.000000000000000000 ) ) ;
#180974=CIRCLE ( 'NONE', #56036, 0.09999999999999939493 ) ;
#180983=DIRECTION ( 'NONE',  ( 0.000000000000000000, 0.4088369013363281068, -0.9126074666063770380 ) ) ;
#180989=VECTOR ( 'NONE', #194463, 1000.000000000000114 ) ;
#180996=AXIS2_PLACEMENT_3D ( 'NONE', #36026, #155984, #212098 ) ;
#181034=CARTESIAN_POINT ( 'NONE',  ( -22.39999999999999858, 25.97741635855165754, -254.4468634167653249 ) ) ;
#181038=ORIENTED_EDGE ( 'NONE', *, *, #53541, .F. ) ;
#181046=ORIENTED_EDGE ( 'NONE', *, *, #247643, .T. ) ;
#181055=FACE_OUTER_BOUND ( 'NONE', #159147, .T. ) ;
#181076=TOROIDAL_SURFACE ( 'NONE', #118125, 0.6000000000000013101, 0.1000000000000000056 ) ;
#181096=CARTESIAN_POINT ( 'NONE',  ( -20.94403535211772294, 68.04082873524789932, -224.1991862745062178 ) ) ;
#181101=EDGE_CURVE ( 'NONE', #218845, #55374, #120979, .T. ) ;
#181120=CARTESIAN_POINT ( 'NONE',  ( 21.30740335185486245, 33.88803232685230427, -243.6079558105722356 ) ) ;
#181163=CARTESIAN_POINT ( 'NONE',  ( 23.14999999999999503, 56.15782127605848473, -228.0502772851308748 ) ) ;
#181164=DIRECTION ( 'NONE',  ( 0.000000000000000000, -0.4088369013363783999, 0.9126074666063545004 ) ) ;
#181202=CARTESIAN_POINT ( 'NONE',  ( -20.54999999999999716, 52.99650480578122824, -234.2878581050858884 ) ) ;
#181216=ORIENTED_EDGE ( 'NONE', *, *, #68303, .F. ) ;
#181224=EDGE_CURVE ( 'NONE', #73568, #2253, #129328, .T. ) ;
#181261=DIRECTION ( 'NONE',  ( -1.000000000000000000, 0.000000000000000000, 0.000000000000000000 ) ) ;
#181280=CARTESIAN_POINT ( 'NONE',  ( -21.07928932188134041, 30.84304088367084162, -252.0482413927653340 ) ) ;
#181312=CARTESIAN_POINT ( 'NONE',  ( -23.15000000000000213, 54.18213181965657554, -236.9344197582443883 ) ) ;
#181336=VERTEX_POINT ( 'NONE', #8261 ) ;
#181346=ADVANCED_FACE ( 'NONE', ( #149066 ), #50370, .F. ) ;
#181375=DIRECTION ( 'NONE',  ( 1.000000000000000000, 0.000000000000000000, -0.000000000000000000 ) ) ;
#181377=AXIS2_PLACEMENT_3D ( 'NONE', #162099, #241614, #145069 ) ;
#181388=ORIENTED_EDGE ( 'NONE', *, *, #160028, .F. ) ;
#181472=ORIENTED_EDGE ( 'NONE', *, *, #79689, .T. ) ;
#181479=EDGE_CURVE ( 'NONE', #229370, #65743, #60203, .T. ) ;
#181507=CARTESIAN_POINT ( 'NONE',  ( 20.85000000000000142, 67.23127455305835554, -235.8551265064784559 ) ) ;
#181511=CARTESIAN_POINT ( 'NONE',  ( -20.64999999999999858, 67.23127455305835554, -235.8551265064784559 ) ) ;
#181561=DIRECTION ( 'NONE',  ( 2.952720810173289112E-16, 0.4088369013363280513, -0.9126074666063769270 ) ) ;
#181578=ORIENTED_EDGE ( 'NONE', *, *, #119169, .T. ) ;
#181594=CIRCLE ( 'NONE', #10901, 0.09999999999999609201 ) ;
#181601=CARTESIAN_POINT ( 'NONE',  ( 18.58685178364167712, 47.00654334275795776, -255.2230915614995865 ) ) ;
#181623=CARTESIAN_POINT ( 'NONE',  ( -18.59999999999999787, 21.13195309841794867, -243.6318585593224100 ) ) ;
#181624=AXIS2_PLACEMENT_3D ( 'NONE', #15625, #250351, #232093 ) ;
#181642=PLANE ( 'NONE',  #157196 ) ;
#181655=LINE ( 'NONE', #18715, #82730 ) ;
#181685=CARTESIAN_POINT ( 'NONE',  ( 21.05000000000000071, 36.65892442174472876, -249.5511627012454596 ) ) ;
#181723=CARTESIAN_POINT ( 'NONE',  ( 18.59999999999999076, 51.96945017402672562, -231.5060697639786440 ) ) ;
#181731=CARTESIAN_POINT ( 'NONE',  ( 23.14999999999999858, 45.21086124044690280, -238.4331873168094091 ) ) ;
#181733=ADVANCED_FACE ( 'NONE', ( #211286 ), #147454, .T. ) ;
#181737=DIRECTION ( 'NONE',  ( 1.000000000000000000, 0.000000000000000000, 0.000000000000000000 ) ) ;
#181785=CIRCLE ( 'NONE', #144330, 0.1000000000000024342 ) ;
#181788=EDGE_CURVE ( 'NONE', #183348, #232311, #229571, .T. ) ;
#181938=AXIS2_PLACEMENT_3D ( 'NONE', #252861, #110787, #109495 ) ;
#181939=EDGE_CURVE ( 'NONE', #66990, #112216, #203272, .T. ) ;
#181958=ADVANCED_BREP_SHAPE_REPRESENTATION ( '', ( #103691, #2425 ), #231953 ) ;
#181970=FACE_OUTER_BOUND ( 'NONE', #52445, .T. ) ;
#181974=EDGE_CURVE ( 'NONE', #219191, #212760, #42212, .T. ) ;
#181996=AXIS2_PLACEMENT_3D ( 'NONE', #137202, #198460, #19847 ) ;
#182002=VECTOR ( 'NONE', #253306, 1000.000000000000114 ) ;
#182003=DIRECTION ( 'NONE',  ( 1.000000000000000000, 0.000000000000000000, -0.000000000000000000 ) ) ;
#182027=CARTESIAN_POINT ( 'NONE',  ( 20.85000000000000142, 67.23127455305835554, -235.8551265064784559 ) ) ;
#182050=CARTESIAN_POINT ( 'NONE',  ( -21.05000000000000071, 36.73178316696986911, -249.7991537124309218 ) ) ;
#182051=CIRCLE ( 'NONE', #7240, 0.1999999999999893807 ) ;
#182055=AXIS2_PLACEMENT_3D ( 'NONE', #36181, #72755, #231810 ) ;
#182118=CARTESIAN_POINT ( 'NONE',  ( -23.25000000000000000, 67.85125148167622910, -227.9794913823769491 ) ) ;
#182160=DIRECTION ( 'NONE',  ( 0.000000000000000000, -0.9126074666063771490, -0.4088369013363276627 ) ) ;
#182171=CARTESIAN_POINT ( 'NONE',  ( -21.14999999999999858, 36.65892442174472876, -249.5511627012454596 ) ) ;
#182175=DIRECTION ( 'NONE',  ( 0.000000000000000000, -0.4088369013363280513, 0.9126074666063769270 ) ) ;
#182190=VERTEX_POINT ( 'NONE', #257745 ) ;
#182196=DIRECTION ( 'NONE',  ( 1.000000000000000000, 0.000000000000000000, 0.000000000000000000 ) ) ;
#182211=AXIS2_PLACEMENT_3D ( 'NONE', #15939, #80994, #199708 ) ;
#182258=VERTEX_POINT ( 'NONE', #238231 ) ;
#182259=DIRECTION ( 'NONE',  ( 0.000000000000000000, 0.9126074666063781482, 0.4088369013363256643 ) ) ;
#182268=ORIENTED_EDGE ( 'NONE', *, *, #254731, .F. ) ;
#182276=ORIENTED_EDGE ( 'NONE', *, *, #248339, .F. ) ;
#182291=FACE_OUTER_BOUND ( 'NONE', #131920, .T. ) ;
#182295=EDGE_LOOP ( 'NONE', ( #101337, #235589, #58771, #195777 ) ) ;
#182298=DIRECTION ( 'NONE',  ( 1.000000000000000000, 0.000000000000000000, 0.000000000000000000 ) ) ;
#182301=ORIENTED_EDGE ( 'NONE', *, *, #96319, .F. ) ;
#182319=LINE ( 'NONE', #218842, #247099 ) ;
#182367=ORIENTED_EDGE ( 'NONE', *, *, #14856, .T. ) ;
#182383=CIRCLE ( 'NONE', #103239, 0.1999999999999985401 ) ;
#182396=ORIENTED_EDGE ( 'NONE', *, *, #109769, .T. ) ;
#182399=VERTEX_POINT ( 'NONE', #161293 ) ;
#182419=DIRECTION ( 'NONE',  ( -1.000000000000000000, 1.387778780781454006E-13, 0.000000000000000000 ) ) ;
#182478=CARTESIAN_POINT ( 'NONE',  ( -20.94999999999999929, 38.25685495413521409, -235.9601135138701693 ) ) ;
#182511=ORIENTED_EDGE ( 'NONE', *, *, #109785, .F. ) ;
#182516=EDGE_CURVE ( 'NONE', #173891, #151159, #63216, .T. ) ;
#182527=CARTESIAN_POINT ( 'NONE',  ( -20.94999999999999929, 44.18518595211054389, -258.7688298343402380 ) ) ;
#182560=CARTESIAN_POINT ( 'NONE',  ( -21.08376601933334271, 30.84514200246639604, -252.0857823083072446 ) ) ;
#182580=CARTESIAN_POINT ( 'NONE',  ( -20.94999999999999929, 67.23127455305835554, -235.8551265064784559 ) ) ;
#182585=CARTESIAN_POINT ( 'NONE',  ( 18.59999999999999076, 53.42432843990430058, -234.7536552047824330 ) ) ;
#182619=ORIENTED_EDGE ( 'NONE', *, *, #139267, .T. ) ;
#182654=ORIENTED_EDGE ( 'NONE', *, *, #3102, .T. ) ;
#182707=AXIS2_PLACEMENT_3D ( 'NONE', #144311, #67376, #205581 ) ;
#182744=EDGE_CURVE ( 'NONE', #129055, #206460, #208621, .T. ) ;
#182758=ORIENTED_EDGE ( 'NONE', *, *, #36050, .F. ) ;
#182777=ORIENTED_EDGE ( 'NONE', *, *, #230660, .T. ) ;
#182798=ORIENTED_EDGE ( 'NONE', *, *, #29158, .F. ) ;
#182801=EDGE_CURVE ( 'NONE', #203994, #70783, #44875, .T. ) ;
#182821=CARTESIAN_POINT ( 'NONE',  ( 18.49999999999999645, 46.45388641681647357, -243.1520440498138385 ) ) ;
#182842=DIRECTION ( 'NONE',  ( 1.000000000000000000, -1.207181226542539700E-16, 2.694675058168174199E-16 ) ) ;
#182844=CARTESIAN_POINT ( 'NONE',  ( -20.54999999999999716, 54.14029358995846053, -238.9803212882090691 ) ) ;
#182848=DIRECTION ( 'NONE',  ( 1.000000000000000000, 0.000000000000000000, -0.000000000000000000 ) ) ;
#182857=DIRECTION ( 'NONE',  ( 0.000000000000000000, -0.9501938099239353175, 0.3116596277708039708 ) ) ;
#182861=CIRCLE ( 'NONE', #236791, 0.09999999999999939493 ) ;
#182875=CARTESIAN_POINT ( 'NONE',  ( 23.14999999999999503, 42.98415524044398950, -233.9519173640447889 ) ) ;
#182894=VERTEX_POINT ( 'NONE', #74421 ) ;
#182906=VERTEX_POINT ( 'NONE', #14437 ) ;
#182927=ORIENTED_EDGE ( 'NONE', *, *, #103325, .T. ) ;
#182937=EDGE_CURVE ( 'NONE', #41742, #139213, #206512, .T. ) ;
#182965=CARTESIAN_POINT ( 'NONE',  ( 23.24999999999999289, 53.24180694658302571, -234.8354225850497130 ) ) ;
#182970=AXIS2_PLACEMENT_3D ( 'NONE', #111547, #151987, #231505 ) ;
#182985=CARTESIAN_POINT ( 'NONE',  ( 20.94999999999999929, 43.16354019706792400, -239.5695141926698284 ) ) ;
#183001=CARTESIAN_POINT ( 'NONE',  ( 23.24999999999999289, 45.29262862071417572, -238.6157088101306556 ) ) ;
#183026=CYLINDRICAL_SURFACE ( 'NONE', #228209, 0.09999999999999939493 ) ;
#183027=DIRECTION ( 'NONE',  ( 0.000000000000000000, -0.2818822000685679008, 0.9594490217226259166 ) ) ;
#183029=CARTESIAN_POINT ( 'NONE',  ( 20.95224633520496127, 40.77109002121920156, -237.9561148901888430 ) ) ;
#183052=CARTESIAN_POINT ( 'NONE',  ( 20.04142135623730070, 21.17283678855157802, -243.7231193059830332 ) ) ;
#183056=CARTESIAN_POINT ( 'NONE',  ( -23.15000000000000213, 56.06656052939784729, -228.0911609752645290 ) ) ;
#183121=CARTESIAN_POINT ( 'NONE',  ( -21.07928932188134041, 33.98134083355423485, -243.8161431329846778 ) ) ;
#183123=CARTESIAN_POINT ( 'NONE',  ( -20.94999999999999929, 69.56804783242856161, -248.4091712263733882 ) ) ;
#183164=EDGE_CURVE ( 'NONE', #246198, #198338, #96332, .T. ) ;
#183167=CIRCLE ( 'NONE', #54145, 0.1000000000000024342 ) ;
#183172=CIRCLE ( 'NONE', #212220, 0.09999999999999609201 ) ;
#183191=VERTEX_POINT ( 'NONE', #144604 ) ;
#183202=EDGE_CURVE ( 'NONE', #221407, #144142, #237821, .T. ) ;
#183210=CARTESIAN_POINT ( 'NONE',  ( -20.64999999999999858, 54.73010456436290383, -239.3295147855486107 ) ) ;
#183214=CIRCLE ( 'NONE', #241488, 0.1999999999999921840 ) ;
#183246=ORIENTED_EDGE ( 'NONE', *, *, #122007, .F. ) ;
#183253=CARTESIAN_POINT ( 'NONE',  ( 23.14999999999999503, 42.98415524044398950, -233.9519173640447889 ) ) ;
#183292=EDGE_CURVE ( 'NONE', #71259, #206012, #33866, .T. ) ;
#183337=DIRECTION ( 'NONE',  ( 1.000000000000000000, -7.510212038922846022E-17, 1.676432719286211941E-16 ) ) ;
#183348=VERTEX_POINT ( 'NONE', #244539 ) ;
#183387=DIRECTION ( 'NONE',  ( 0.000000000000000000, -0.9126074666063660468, -0.4088369013363524762 ) ) ;
#183423=ORIENTED_EDGE ( 'NONE', *, *, #60038, .T. ) ;
#183437=CYLINDRICAL_SURFACE ( 'NONE', #245617, 0.09999999999999609201 ) ;
#183452=AXIS2_PLACEMENT_3D ( 'NONE', #35853, #134901, #192344 ) ;
#183474=VECTOR ( 'NONE', #119282, 1000.000000000000114 ) ;
#183482=AXIS2_PLACEMENT_3D ( 'NONE', #169003, #223781, #248497 ) ;
#183534=CIRCLE ( 'NONE', #117078, 0.1000000000000024342 ) ;
#183541=FACE_OUTER_BOUND ( 'NONE', #224250, .T. ) ;
#183566=ORIENTED_EDGE ( 'NONE', *, *, #116570, .T. ) ;
#183583=PLANE ( 'NONE',  #189719 ) ;
#183595=EDGE_CURVE ( 'NONE', #236709, #249163, #134481, .T. ) ;
#183601=VERTEX_POINT ( 'NONE', #234901 ) ;
#183612=VERTEX_POINT ( 'NONE', #219160 ) ;
#183622=ADVANCED_FACE ( 'NONE', ( #118806 ), #121403, .T. ) ;
#183626=EDGE_LOOP ( 'NONE', ( #147102, #10584, #64436, #158988 ) ) ;
#183630=CARTESIAN_POINT ( 'NONE',  ( 21.05000000000000071, 67.23127455305835554, -235.8551265064784559 ) ) ;
#183636=AXIS2_PLACEMENT_3D ( 'NONE', #81050, #122791, #78488 ) ;
#183670=EDGE_CURVE ( 'NONE', #154226, #169429, #237458, .T. ) ;
#183683=DIRECTION ( 'NONE',  ( -1.000000000000000000, -0.000000000000000000, 0.000000000000000000 ) ) ;
#183708=AXIS2_PLACEMENT_3D ( 'NONE', #221536, #19531, #258076 ) ;
#183732=CARTESIAN_POINT ( 'NONE',  ( -20.54999999999999716, 54.18213181965657554, -236.9344197582443883 ) ) ;
#183771=DIRECTION ( 'NONE',  ( 0.000000000000000000, -0.9126074666063622720, -0.4088369013363611360 ) ) ;
#183795=ORIENTED_EDGE ( 'NONE', *, *, #50725, .F. ) ;
#183808=VECTOR ( 'NONE', #51608, 1000.000000000000000 ) ;
#183817=CARTESIAN_POINT ( 'NONE',  ( -18.39999999999999858, 77.27075167199318173, -241.8768735168259241 ) ) ;
#183821=CARTESIAN_POINT ( 'NONE',  ( -21.08078803292166725, 30.84699535066559761, -252.0680663746180414 ) ) ;
#183824=AXIS2_PLACEMENT_3D ( 'NONE', #252674, #255196, #136573 ) ;
#183837=ORIENTED_EDGE ( 'NONE', *, *, #128526, .T. ) ;
#183855=CARTESIAN_POINT ( 'NONE',  ( 21.05000000000000071, 36.65892442174472876, -249.5511627012454596 ) ) ;
#183879=EDGE_LOOP ( 'NONE', ( #211518, #182367, #249723, #122094 ) ) ;
#183923=DIRECTION ( 'NONE',  ( 0.000000000000000000, 0.9126074666063660468, 0.4088369013363524762 ) ) ;
#183948=CARTESIAN_POINT ( 'NONE',  ( 18.59999999999999076, 55.04793976901536467, -229.8170162380219494 ) ) ;
#183973=FACE_OUTER_BOUND ( 'NONE', #52321, .T. ) ;
#184029=ORIENTED_EDGE ( 'NONE', *, *, #90839, .T. ) ;
#184032=B_SPLINE_CURVE_WITH_KNOTS ( 'NONE', 3,
 ( #139709, #237549, #138414, #39380, #118901, #79727, #60180, #40674, #74663, #122758 ),
 .UNSPECIFIED., .F., .F.,
 ( 4, 2, 2, 2, 4 ),
 ( 0.000000000000000000, 0.0001584437871625145604, 0.0002376656807437778308, 0.0002772766275344028795, 0.0003168875743250278740 ),
 .UNSPECIFIED. ) ;
#184052=CARTESIAN_POINT ( 'NONE',  ( -18.50000000000000711, 47.12013762176896847, -255.1881735838713610 ) ) ;
#184078=ORIENTED_EDGE ( 'NONE', *, *, #164017, .T. ) ;
#184085=EDGE_CURVE ( 'NONE', #67538, #176131, #198010, .T. ) ;
#184102=CARTESIAN_POINT ( 'NONE',  ( -20.64999999999999858, 62.08591502004791352, -248.5699171172615820 ) ) ;
#184138=DIRECTION ( 'NONE',  ( 0.000000000000000000, -0.4088369013363280513, 0.9126074666063769270 ) ) ;
#184145=DIRECTION ( 'NONE',  ( -1.000000000000000000, -0.000000000000000000, -0.000000000000000000 ) ) ;
#184166=ORIENTED_EDGE ( 'NONE', *, *, #184085, .F. ) ;
#184206=EDGE_LOOP ( 'NONE', ( #253433, #244817 ) ) ;
#184218=DIRECTION ( 'NONE',  ( 0.000000000000000000, -0.9126074666064812879, -0.4088369013360954596 ) ) ;
#184226=ORIENTED_EDGE ( 'NONE', *, *, #113244, .F. ) ;
#184253=CIRCLE ( 'NONE', #109233, 0.09999999999999609201 ) ;
#184281=DIRECTION ( 'NONE',  ( 1.000000000000000000, 0.000000000000000000, 0.000000000000000000 ) ) ;
#184311=CYLINDRICAL_SURFACE ( 'NONE', #136481, 0.1000000000000024342 ) ;
#184345=DIRECTION ( 'NONE',  ( 1.000000000000000000, 0.000000000000000000, 0.000000000000000000 ) ) ;
#184362=DIRECTION ( 'NONE',  ( -1.000000000000000000, 0.000000000000000000, 0.000000000000000000 ) ) ;
#184372=EDGE_LOOP ( 'NONE', ( #117575, #179063, #231465 ) ) ;
#184379=B_SPLINE_CURVE_WITH_KNOTS ( 'NONE', 3,
 ( #223608, #141520, #202782, #119406, #238052, #24168, #44999, #103659, #124547, #257563, #59384, #221052, #200223, #121969, #3279, #41175 ),
 .UNSPECIFIED., .F., .F.,
 ( 4, 3, 3, 3, 3, 4 ),
 ( 0.000000000000000000, 2.209833635978175731E-05, 5.595056164117426028E-05, 8.979992002653444747E-05, 0.0001236482757198794019, 0.0001574984039362407678 ),
 .UNSPECIFIED. ) ;
#184425=CARTESIAN_POINT ( 'NONE',  ( 21.04999999999999716, 39.15970426261371529, -236.7233909955383240 ) ) ;
#184445=FACE_OUTER_BOUND ( 'NONE', #176467, .T. ) ;
#184464=CARTESIAN_POINT ( 'NONE',  ( 23.24999999999999645, 67.23127455305835554, -235.8551265064784559 ) ) ;
#184474=EDGE_CURVE ( 'NONE', #177788, #172262, #121725, .T. ) ;
#184506=CARTESIAN_POINT ( 'NONE',  ( 20.91682497891423154, 68.08564185115264422, -224.1612363371343122 ) ) ;
#184526=EDGE_LOOP ( 'NONE', ( #149970, #247135, #210452 ) ) ;
#184528=ADVANCED_FACE ( 'NONE', ( #79977 ), #159557, .F. ) ;
#184542=CARTESIAN_POINT ( 'NONE',  ( 22.50000000000000000, 36.65892442174472876, -249.5511627012454596 ) ) ;
#184543=CARTESIAN_POINT ( 'NONE',  ( 21.05000000000000071, 39.23476235320398331, -236.9756760510740321 ) ) ;
#184585=VERTEX_POINT ( 'NONE', #65577 ) ;
#184586=AXIS2_PLACEMENT_3D ( 'NONE', #238013, #99768, #142754 ) ;
#184592=LINE ( 'NONE', #240728, #219806 ) ;
#184598=CIRCLE ( 'NONE', #55384, 3.999999999999989786 ) ;
#184616=CIRCLE ( 'NONE', #68106, 11.64999999999999680 ) ;
#184657=AXIS2_PLACEMENT_3D ( 'NONE', #73153, #76961, #56094 ) ;
#184687=EDGE_CURVE ( 'NONE', #34062, #31046, #151276, .T. ) ;
#184726=CARTESIAN_POINT ( 'NONE',  ( 18.60000000000000142, 47.07326788871598922, -255.0992659944397190 ) ) ;
#184745=CIRCLE ( 'NONE', #93168, 0.09999999999999609201 ) ;
#184749=EDGE_CURVE ( 'NONE', #74900, #70387, #167849, .T. ) ;
#184785=DIRECTION ( 'NONE',  ( 0.000000000000000000, -0.4088369013363280513, 0.9126074666063772600 ) ) ;
#184809=CYLINDRICAL_SURFACE ( 'NONE', #34810, 2.000000000000012879 ) ;
#184812=PLANE ( 'NONE',  #14425 ) ;
#184817=CYLINDRICAL_SURFACE ( 'NONE', #188513, 0.09999999999999939493 ) ;
#184820=ORIENTED_EDGE ( 'NONE', *, *, #253354, .F. ) ;
#184833=CARTESIAN_POINT ( 'NONE',  ( -23.15000000000000213, 70.79044367282321559, -234.2606625912667937 ) ) ;
#184890=CARTESIAN_POINT ( 'NONE',  ( -23.25000000000000000, 54.18213181965657554, -236.9344197582443883 ) ) ;
#184916=CARTESIAN_POINT ( 'NONE',  ( -20.54999999999999716, 67.23127455305835554, -235.8551265064784559 ) ) ;
#184924=CARTESIAN_POINT ( 'NONE',  ( 18.59999999999999076, 43.16354019706792400, -239.5695141926698284 ) ) ;
#184926=VECTOR ( 'NONE', #57407, 1000.000000000000114 ) ;
#184928=ORIENTED_EDGE ( 'NONE', *, *, #220982, .F. ) ;
#184930=CIRCLE ( 'NONE', #147523, 7.720710678118663850 ) ;
#184962=( BOUNDED_CURVE ( )  B_SPLINE_CURVE ( 3, ( #208142, #2526, #164197, #242427 ),
 .UNSPECIFIED., .F., .F. ) 
 B_SPLINE_CURVE_WITH_KNOTS ( ( 4, 4 ),
 ( 3.192897208853993529, 4.712388980384689674 ),
 .UNSPECIFIED. ) 
 CURVE ( )  GEOMETRIC_REPRESENTATION_ITEM ( )  RATIONAL_B_SPLINE_CURVE ( ( 1.000000000000000000, 0.8166740347213228279, 0.8166740347213228279, 1.000000000000000000 ) ) 
 REPRESENTATION_ITEM ( '' )  );
#184981=CIRCLE ( 'NONE', #255658, 0.09999999999999854838 ) ;
#184989=CARTESIAN_POINT ( 'NONE',  ( -23.15000000000000213, 62.08148826970418099, -247.6553521922769221 ) ) ;
#185006=DIRECTION ( 'NONE',  ( -0.000000000000000000, 0.9126074666063770380, 0.4088369013363281068 ) ) ;
#185033=DIRECTION ( 'NONE',  ( 0.000000000000000000, 0.9947597004326491632, -0.1022405907413782566 ) ) ;
#185037=DIRECTION ( 'NONE',  ( 2.659396599871503635E-15, 0.4701782451859590206, 0.8825714802517993229 ) ) ;
#185042=CARTESIAN_POINT ( 'NONE',  ( 20.95576188350343116, 39.26765041487632857, -236.7575746322726502 ) ) ;
#185073=CARTESIAN_POINT ( 'NONE',  ( 22.39999999999999503, 31.98723526783714277, -238.8784020251475511 ) ) ;
#185084=CARTESIAN_POINT ( 'NONE',  ( -22.37643362114956957, 29.65906341269005608, -252.5784446511937347 ) ) ;
#185088=DIRECTION ( 'NONE',  ( -1.000000000000000000, 0.000000000000000000, 0.000000000000000000 ) ) ;
#185091=AXIS2_PLACEMENT_3D ( 'NONE', #140835, #41758, #28641 ) ;
#185097=ORIENTED_EDGE ( 'NONE', *, *, #226465, .T. ) ;
#185111=CARTESIAN_POINT ( 'NONE',  ( -20.94999999999999929, 43.52285900727589762, -245.0935880436369985 ) ) ;
#185115=CARTESIAN_POINT ( 'NONE',  ( 20.94999999999999929, 44.05869416168422958, -258.6139110589941197 ) ) ;
#185197=EDGE_CURVE ( 'NONE', #60065, #114887, #64144, .T. ) ;
#185206=DIRECTION ( 'NONE',  ( -1.000000000000000000, 1.335000415235278971E-16, -2.979993593738921214E-16 ) ) ;
#185236=CARTESIAN_POINT ( 'NONE',  ( -23.25000000000000000, 69.20602499728043711, -247.8456586332460176 ) ) ;
#185250=VECTOR ( 'NONE', #239896, 1000.000000000000114 ) ;
#185269=SPHERICAL_SURFACE ( 'NONE', #213113, 0.1000000000000000056 ) ;
#185326=CARTESIAN_POINT ( 'NONE',  ( 20.04142135623730070, 51.38014393322265505, -230.1906178717505611 ) ) ;
#185344=CIRCLE ( 'NONE', #10386, 7.791421356237310469 ) ;
#185391=DIRECTION ( 'NONE',  ( -0.7071067811865685560, -0.2890913453344204909, 0.6453109281987288171 ) ) ;
#185429=TOROIDAL_SURFACE ( 'NONE', #210383, 12.97499999999999609, 0.1000000000000000056 ) ;
#185438=EDGE_CURVE ( 'NONE', #203994, #230665, #155747, .T. ) ;
#185439=CARTESIAN_POINT ( 'NONE',  ( 18.46921299892754931, 46.92271302580608960, -255.3731210386297050 ) ) ;
#185462=EDGE_CURVE ( 'NONE', #148383, #255010, #118315, .T. ) ;
#185506=CARTESIAN_POINT ( 'NONE',  ( 19.75857864376269291, 54.53338637621133955, -228.6684279704127789 ) ) ;
#185516=ORIENTED_EDGE ( 'NONE', *, *, #219395, .T. ) ;
#185521=ORIENTED_EDGE ( 'NONE', *, *, #225077, .F. ) ;
#185547=VECTOR ( 'NONE', #170345, 1000.000000000000000 ) ;
#185565=CARTESIAN_POINT ( 'NONE',  ( 21.05000000000000071, 40.68212387350988735, -238.0221676322813096 ) ) ;
#185581=FACE_OUTER_BOUND ( 'NONE', #25559, .T. ) ;
#185594=CARTESIAN_POINT ( 'NONE',  ( 20.94999999999999574, 43.10494791715829166, -239.6505508802563327 ) ) ;
#185598=EDGE_CURVE ( 'NONE', #95600, #246752, #227900, .T. ) ;
#185608=VECTOR ( 'NONE', #19303, 1000.000000000000000 ) ;
#185609=DIRECTION ( 'NONE',  ( 0.000000000000000000, 0.9126074666063660468, 0.4088369013363524762 ) ) ;
#185614=CARTESIAN_POINT ( 'NONE',  ( 21.05000005000965757, 44.14570381864804460, -236.4763722595682509 ) ) ;
#185654=CARTESIAN_POINT ( 'NONE',  ( 19.75857864376268935, 54.48300931968434213, -228.8005724072070564 ) ) ;
#185655=DIRECTION ( 'NONE',  ( 1.000000000000000000, 0.000000000000000000, 0.000000000000000000 ) ) ;
#185662=CARTESIAN_POINT ( 'NONE',  ( 21.14999999999999503, 26.06832281015329755, -254.4051978787608732 ) ) ;
#185669=CIRCLE ( 'NONE', #44004, 0.1000000000000024342 ) ;
#185672=VECTOR ( 'NONE', #46552, 1000.000000000000000 ) ;
#185677=CIRCLE ( 'NONE', #256515, 0.09999999999999939493 ) ;
#185699=ADVANCED_FACE ( 'NONE', ( #158663 ), #143429, .T. ) ;
#185710=CARTESIAN_POINT ( 'NONE',  ( 21.00000000000000000, 52.06567329910104291, -231.9654557484363409 ) ) ;
#185792=VECTOR ( 'NONE', #152410, 1000.000000000000114 ) ;
#185795=DIRECTION ( 'NONE',  ( -1.000000000000000000, -0.000000000000000000, -0.000000000000000000 ) ) ;
#185809=VERTEX_POINT ( 'NONE', #81621 ) ;
#185818=VERTEX_POINT ( 'NONE', #47646 ) ;
#185841=EDGE_CURVE ( 'NONE', #157652, #149628, #102470, .T. ) ;
#185847=ORIENTED_EDGE ( 'NONE', *, *, #98597, .F. ) ;
#185861=CARTESIAN_POINT ( 'NONE',  ( 20.85000000000000142, 78.48087866980282001, -232.8271061603568910 ) ) ;
#185873=CARTESIAN_POINT ( 'NONE',  ( -21.51976009735018991, 33.83367400564330296, -243.2446267297141844 ) ) ;
#185876=LINE ( 'NONE', #244562, #174848 ) ;
#185881=LINE ( 'NONE', #128484, #109855 ) ;
#185911=CARTESIAN_POINT ( 'NONE',  ( -20.64999999999999858, 54.34471204062663219, -239.4366250215122420 ) ) ;
#185950=CARTESIAN_POINT ( 'NONE',  ( 23.24999999999999645, 36.65892442174472876, -249.5511627012454596 ) ) ;
#185961=EDGE_CURVE ( 'NONE', #211199, #183348, #197769, .T. ) ;
#185971=CIRCLE ( 'NONE', #11190, 0.1000000000000024342 ) ;
#186017=ORIENTED_EDGE ( 'NONE', *, *, #127702, .F. ) ;
#186019=CARTESIAN_POINT ( 'NONE',  ( -23.25000000000000000, 21.13195309841794867, -243.6318585593224100 ) ) ;
#186057=CARTESIAN_POINT ( 'NONE',  ( -20.64999999999999858, 53.03738849591485405, -234.3791188517465400 ) ) ;
#186068=ORIENTED_EDGE ( 'NONE', *, *, #168070, .F. ) ;
#186075=CIRCLE ( 'NONE', #252698, 0.1000000000000024342 ) ;
#186079=CARTESIAN_POINT ( 'NONE',  ( -21.05000000000000071, 48.05114133249968944, -246.4758750954581785 ) ) ;
#186092=AXIS2_PLACEMENT_3D ( 'NONE', #117296, #192988, #14371 ) ;
#186129=DIRECTION ( 'NONE',  ( 0.000000000000000000, -0.9126074666063660468, -0.4088369013363524762 ) ) ;
#186164=EDGE_CURVE ( 'NONE', #110735, #180828, #152018, .T. ) ;
#186172=CIRCLE ( 'NONE', #98641, 12.87499999999999112 ) ;
#186174=EDGE_CURVE ( 'NONE', #13269, #124911, #247669, .T. ) ;
#186177=AXIS2_PLACEMENT_3D ( 'NONE', #79692, #53725, #133270 ) ;
#186215=FACE_OUTER_BOUND ( 'NONE', #12486, .T. ) ;
#186218=LINE ( 'NONE', #105347, #149174 ) ;
#186274=CARTESIAN_POINT ( 'NONE',  ( 18.45139536634709287, 77.16971529390174567, -241.7973093201318022 ) ) ;
#186342=ADVANCED_FACE ( 'NONE', ( #107003 ), #186574, .F. ) ;
#186343=CARTESIAN_POINT ( 'NONE',  ( 20.94999999999999574, 39.29335463311362275, -236.8946393634874994 ) ) ;
#186350=EDGE_LOOP ( 'NONE', ( #49423, #215967, #118484, #10984 ) ) ;
#186392=CIRCLE ( 'NONE', #194772, 0.4999999999999972800 ) ;
#186422=CARTESIAN_POINT ( 'NONE',  ( 21.14999999999999858, 26.02743912001966464, -254.3139371321002216 ) ) ;
#186423=ORIENTED_EDGE ( 'NONE', *, *, #43221, .T. ) ;
#186428=LINE ( 'NONE', #225507, #216735 ) ;
#186458=ORIENTED_EDGE ( 'NONE', *, *, #206393, .T. ) ;
#186488=DIRECTION ( 'NONE',  ( 0.000000000000000000, -0.09425075112713271475, -0.9955484899852801162 ) ) ;
#186507=ORIENTED_EDGE ( 'NONE', *, *, #248664, .F. ) ;
#186516=DIRECTION ( 'NONE',  ( 0.000000000000000000, 0.4088369013363287729, -0.9126074666063767049 ) ) ;
#186529=DIRECTION ( 'NONE',  ( 0.000000000000000000, -0.4088369013363280513, 0.9126074666063769270 ) ) ;
#186544=CIRCLE ( 'NONE', #24229, 0.1000000000000024342 ) ;
#186560=EDGE_CURVE ( 'NONE', #61043, #89516, #77152, .T. ) ;
#186574=CYLINDRICAL_SURFACE ( 'NONE', #56294, 0.1000000000000024342 ) ;
#186598=CIRCLE ( 'NONE', #190707, 0.09999999999999681366 ) ;
#186669=EDGE_CURVE ( 'NONE', #81651, #191031, #82061, .T. ) ;
#186671=DIRECTION ( 'NONE',  ( 0.000000000000000000, 0.9126074666063769270, 0.4088369013363282733 ) ) ;
#186692=CARTESIAN_POINT ( 'NONE',  ( 21.05000000000000071, 48.89266972451527948, -253.5637804087949121 ) ) ;
#186709=EDGE_LOOP ( 'NONE', ( #102175, #72017, #250649, #17978 ) ) ;
#186753=FACE_OUTER_BOUND ( 'NONE', #56020, .T. ) ;
#186756=CARTESIAN_POINT ( 'NONE',  ( -20.00857864376270001, 52.22920805963557456, -232.3304987350788906 ) ) ;
#186766=ORIENTED_EDGE ( 'NONE', *, *, #127702, .T. ) ;
#186768=VERTEX_POINT ( 'NONE', #229240 ) ;
#186794=ORIENTED_EDGE ( 'NONE', *, *, #2783, .F. ) ;
#186796=ORIENTED_EDGE ( 'NONE', *, *, #9236, .F. ) ;
#186808=ORIENTED_EDGE ( 'NONE', *, *, #201556, .F. ) ;
#186821=VECTOR ( 'NONE', #139960, 1000.000000000000114 ) ;
#186840=CARTESIAN_POINT ( 'NONE',  ( -18.59999999999999787, 44.52640028187936849, -247.3006740988509193 ) ) ;
#186849=ADVANCED_FACE ( 'NONE', ( #252627 ), #135242, .F. ) ;
#186873=VERTEX_POINT ( 'NONE', #94839 ) ;
#186875=EDGE_CURVE ( 'NONE', #249043, #142489, #10192, .T. ) ;
#186876=CARTESIAN_POINT ( 'NONE',  ( 20.94999999999999929, 65.40605961984559258, -236.6728003091511425 ) ) ;
#186888=FACE_OUTER_BOUND ( 'NONE', #128450, .T. ) ;
#186925=CARTESIAN_POINT ( 'NONE',  ( 20.95512828230157965, 44.16605519446306261, -236.4619169603685123 ) ) ;
#187037=TOROIDAL_SURFACE ( 'NONE', #124481, 12.77499999999999858, 0.1000000000000000056 ) ;
#187038=EDGE_CURVE ( 'NONE', #36016, #168895, #44512, .T. ) ;
#187050=CARTESIAN_POINT ( 'NONE',  ( -20.94999999999999929, 67.23127455305835554, -235.8551265064784559 ) ) ;
#187066=LINE ( 'NONE', #167505, #94049 ) ;
#187067=FACE_OUTER_BOUND ( 'NONE', #28790, .T. ) ;
#187072=AXIS2_PLACEMENT_3D ( 'NONE', #179003, #141130, #21205 ) ;
#187101=PLANE ( 'NONE',  #24576 ) ;
#187111=DIRECTION ( 'NONE',  ( -0.000000000000000000, 0.9969158384938637818, -0.07847809223010315804 ) ) ;
#187124=VERTEX_POINT ( 'NONE', #159524 ) ;
#187125=EDGE_CURVE ( 'NONE', #217763, #21148, #27267, .T. ) ;
#187144=AXIS2_PLACEMENT_3D ( 'NONE', #38776, #195306, #37501 ) ;
#187157=VERTEX_POINT ( 'NONE', #82507 ) ;
#187203=EDGE_CURVE ( 'NONE', #77135, #221888, #156453, .T. ) ;
#187244=ORIENTED_EDGE ( 'NONE', *, *, #180201, .T. ) ;
#187255=ORIENTED_EDGE ( 'NONE', *, *, #146937, .F. ) ;
#187281=ORIENTED_EDGE ( 'NONE', *, *, #26092, .F. ) ;
#187286=CARTESIAN_POINT ( 'NONE',  ( 21.00000000000000000, 43.94346684630428967, -235.6041041703296344 ) ) ;
#187287=AXIS2_PLACEMENT_3D ( 'NONE', #230457, #154800, #216008 ) ;
#187327=DIRECTION ( 'NONE',  ( 0.000000000000000000, -0.9126074666063768159, -0.4088369013363282178 ) ) ;
#187359=DIRECTION ( 'NONE',  ( -0.000000000000000000, 0.9126074666063771490, 0.4088369013363281623 ) ) ;
#187376=CARTESIAN_POINT ( 'NONE',  ( -21.05000000000000071, 34.07612324756792077, -243.5412266404783566 ) ) ;
#187389=CARTESIAN_POINT ( 'NONE',  ( 18.54147908293629143, 46.96077838941292981, -255.3055355240929600 ) ) ;
#187419=ADVANCED_FACE ( 'NONE', ( #253316 ), #115101, .F. ) ;
#187444=DIRECTION ( 'NONE',  ( 1.000000000000000000, 0.000000000000000000, -0.000000000000000000 ) ) ;
#187487=CYLINDRICAL_SURFACE ( 'NONE', #174212, 0.1000000000000024342 ) ;
#187492=EDGE_CURVE ( 'NONE', #174581, #41411, #52337, .T. ) ;
#187558=CARTESIAN_POINT ( 'NONE',  ( 21.05000000000000071, 67.23127455305835554, -235.8551265064784559 ) ) ;
#187563=DIRECTION ( 'NONE',  ( 0.000000000000000000, -0.8103668758649578141, 0.5859227990963212784 ) ) ;
#187570=ADVANCED_FACE ( 'NONE', ( #103215 ), #177481, .F. ) ;
#187645=CIRCLE ( 'NONE', #96022, 0.1000000000000024342 ) ;
#187684=DIRECTION ( 'NONE',  ( 1.000000000000000000, 0.000000000000000000, 0.000000000000000000 ) ) ;
#187720=CARTESIAN_POINT ( 'NONE',  ( -21.05000000000000071, 44.34387878855809362, -247.3824414791181994 ) ) ;
#187776=CIRCLE ( 'NONE', #183482, 0.09999999999999609201 ) ;
#187794=FACE_OUTER_BOUND ( 'NONE', #29885, .T. ) ;
#187796=CARTESIAN_POINT ( 'NONE',  ( 21.05000000000000071, 44.18518595211054389, -258.7688298343402380 ) ) ;
#187829=CARTESIAN_POINT ( 'NONE',  ( -20.85000000000000142, 67.23127455305835554, -235.8551265064784559 ) ) ;
#187832=EDGE_CURVE ( 'NONE', #106227, #151804, #131460, .T. ) ;
#187835=CIRCLE ( 'NONE', #212945, 0.09999999999999414912 ) ;
#187846=ORIENTED_EDGE ( 'NONE', *, *, #253487, .T. ) ;
#187848=ADVANCED_FACE ( 'NONE', ( #178320 ), #44368, .T. ) ;
#187901=CIRCLE ( 'NONE', #21322, 11.65000000000001990 ) ;
#187939=DIRECTION ( 'NONE',  ( 0.000000000000000000, 0.4088369013363276072, -0.9126074666063773710 ) ) ;
#187972=AXIS2_PLACEMENT_3D ( 'NONE', #6342, #143294, #84559 ) ;
#187981=AXIS2_PLACEMENT_3D ( 'NONE', #36627, #195694, #96538 ) ;
#188016=CYLINDRICAL_SURFACE ( 'NONE', #51120, 0.09999999999999939493 ) ;
#188055=ORIENTED_EDGE ( 'NONE', *, *, #59341, .T. ) ;
#188078=EDGE_LOOP ( 'NONE', ( #39986, #135085, #172294, #193784 ) ) ;
#188120=DIRECTION ( 'NONE',  ( 0.000000000000000000, 0.9126074666064696306, 0.4088369013361213278 ) ) ;
#188123=CARTESIAN_POINT ( 'NONE',  ( -21.44999999999999929, 52.95562111564758823, -234.1965973584252652 ) ) ;
#188133=ORIENTED_EDGE ( 'NONE', *, *, #178669, .T. ) ;
#188151=ADVANCED_FACE ( 'NONE', ( #149457 ), #92020, .F. ) ;
#188183=DIRECTION ( 'NONE',  ( 0.000000000000000000, 0.9126074666063660468, 0.4088369013363524762 ) ) ;
#188188=CARTESIAN_POINT ( 'NONE',  ( 21.06277459767418136, 44.16883162190262624, -236.4642769761964303 ) ) ;
#188189=ORIENTED_EDGE ( 'NONE', *, *, #73844, .F. ) ;
#188195=DIRECTION ( 'NONE',  ( 0.000000000000000000, -0.5283051335750404975, 0.8490545835446967615 ) ) ;
#188214=CARTESIAN_POINT ( 'NONE',  ( -22.50000000000000000, 31.85509083104287598, -238.8280249686205536 ) ) ;
#188218=AXIS2_PLACEMENT_3D ( 'NONE', #7981, #167080, #246569 ) ;
#188226=CARTESIAN_POINT ( 'NONE',  ( 23.25000000000000000, 30.73962027982165424, -265.0781340245722504 ) ) ;
#188248=ORIENTED_EDGE ( 'NONE', *, *, #53466, .F. ) ;
#188257=ORIENTED_EDGE ( 'NONE', *, *, #29027, .T. ) ;
#188279=DIRECTION ( 'NONE',  ( 1.000000000000000000, -1.335000415235278971E-16, 2.979993593738921214E-16 ) ) ;
#188289=EDGE_CURVE ( 'NONE', #43171, #158029, #198465, .T. ) ;
#188304=CYLINDRICAL_SURFACE ( 'NONE', #26618, 0.1000000000000024342 ) ;
#188329=EDGE_LOOP ( 'NONE', ( #20512, #44239, #100492, #253127 ) ) ;
#188343=EDGE_CURVE ( 'NONE', #108899, #44054, #247966, .T. ) ;
#188363=CARTESIAN_POINT ( 'NONE',  ( 23.24999999999999289, 42.94327155031035659, -233.8606566173841372 ) ) ;
#188427=ORIENTED_EDGE ( 'NONE', *, *, #9129, .F. ) ;
#188429=DIRECTION ( 'NONE',  ( 0.000000000000000000, -0.9126074666063660468, -0.4088369013363524762 ) ) ;
#188456=VERTEX_POINT ( 'NONE', #198826 ) ;
#188500=ORIENTED_EDGE ( 'NONE', *, *, #122954, .F. ) ;
#188507=EDGE_LOOP ( 'NONE', ( #120469, #64275, #44135, #108237, #51603, #161171, #229728, #233179, #224516 ) ) ;
#188513=AXIS2_PLACEMENT_3D ( 'NONE', #203102, #221363, #102692 ) ;
#188514=CARTESIAN_POINT ( 'NONE',  ( 20.85000000000000142, 67.85909929089923764, -227.8797997985275856 ) ) ;
#188524=EDGE_CURVE ( 'NONE', #222021, #161463, #140181, .T. ) ;
#188545=DIRECTION ( 'NONE',  ( 0.000000000000000000, -0.9126074666063769270, -0.4088369013363280513 ) ) ;
#188553=EDGE_LOOP ( 'NONE', ( #127454, #53886, #223892, #49767 ) ) ;
#188606=ORIENTED_EDGE ( 'NONE', *, *, #109410, .T. ) ;
#188637=DIRECTION ( 'NONE',  ( 1.000000000000000000, 0.000000000000000000, 0.000000000000000000 ) ) ;
#188653=CARTESIAN_POINT ( 'NONE',  ( 18.39999999999998437, 46.91436717984748128, -255.3877622108296066 ) ) ;
#188668=DIRECTION ( 'NONE',  ( 0.000000000000000000, -0.9126074666063545004, -0.4088369013363783999 ) ) ;
#188673=DIRECTION ( 'NONE',  ( 0.000000000000000000, -0.9126074666063770380, -0.4088369013363281068 ) ) ;
#188685=AXIS2_PLACEMENT_3D ( 'NONE', #192482, #252436, #94654 ) ;
#188701=DIRECTION ( 'NONE',  ( 0.000000000000000000, 0.9126074666063660468, 0.4088369013363524762 ) ) ;
#188720=LINE ( 'NONE', #110464, #179147 ) ;
#188721=LINE ( 'NONE', #54338, #254306 ) ;
#188727=CARTESIAN_POINT ( 'NONE',  ( 21.93340585971645851, 33.66454284798804508, -242.8670914416629500 ) ) ;
#188750=ORIENTED_EDGE ( 'NONE', *, *, #228064, .F. ) ;
#188821=AXIS2_PLACEMENT_3D ( 'NONE', #181312, #82158, #144716 ) ;
#188828=CARTESIAN_POINT ( 'NONE',  ( 18.42636655943170965, 77.14547211592135056, -241.8200727776024621 ) ) ;
#188829=EDGE_CURVE ( 'NONE', #89024, #68660, #122859, .T. ) ;
#188838=EDGE_LOOP ( 'NONE', ( #231972, #735, #99900, #210477 ) ) ;
#188895=CARTESIAN_POINT ( 'NONE',  ( -18.59999999999999787, 74.74783850729542678, -233.7633982527047465 ) ) ;
#188898=AXIS2_PLACEMENT_3D ( 'NONE', #185326, #113170, #75357 ) ;
#188909=AXIS2_PLACEMENT_3D ( 'NONE', #36346, #14220, #31239 ) ;
#188910=CIRCLE ( 'NONE', #159694, 0.09999999999999609201 ) ;
#188912=AXIS2_PLACEMENT_3D ( 'NONE', #84105, #122010, #166308 ) ;
#188930=FACE_OUTER_BOUND ( 'NONE', #9056, .T. ) ;
#188956=EDGE_LOOP ( 'NONE', ( #227130, #209222, #200369 ) ) ;
#189012=CARTESIAN_POINT ( 'NONE',  ( -20.64999999999999858, 68.96522873961046685, -235.0783363939394235 ) ) ;
#189029=CARTESIAN_POINT ( 'NONE',  ( -22.50000000000000000, 25.98655542988603173, -254.2226763854395983 ) ) ;
#189042=DIRECTION ( 'NONE',  ( -0.000000000000000000, 0.5469332180710856361, -0.8371762388950169109 ) ) ;
#189071=CIRCLE ( 'NONE', #214016, 0.09999999999999481526 ) ;
#189089=DIRECTION ( 'NONE',  ( 0.000000000000000000, 0.9126074666063771490, 0.4088369013363281623 ) ) ;
#189106=CARTESIAN_POINT ( 'NONE',  ( -18.50000000000000000, 74.74783850729544099, -233.7633982527047465 ) ) ;
#189109=DIRECTION ( 'NONE',  ( 1.000000000000000000, 0.000000000000000000, 0.000000000000000000 ) ) ;
#189115=EDGE_CURVE ( 'NONE', #2253, #185818, #239981, .T. ) ;
#189127=CARTESIAN_POINT ( 'NONE',  ( -18.59999999999999787, 43.44873802792533724, -245.1397081572968659 ) ) ;
#189148=B_SPLINE_CURVE_WITH_KNOTS ( 'NONE', 3,
 ( #199402, #98959, #59839, #63712, #3742, #222775, #201954, #83251, #181120, #24626 ),
 .UNSPECIFIED., .F., .F.,
 ( 4, 3, 3, 4 ),
 ( 0.000000000000000000, 0.0002000000000002877026, 0.001000000000045112155, 0.001967863649472104820 ),
 .UNSPECIFIED. ) ;
#189150=DIRECTION ( 'NONE',  ( 1.000000000000000000, 0.000000000000000000, 0.000000000000000000 ) ) ;
#189198=CARTESIAN_POINT ( 'NONE',  ( -18.59999999999999787, 52.17883100310857003, -232.4626431718731396 ) ) ;
#189228=CARTESIAN_POINT ( 'NONE',  ( 18.59999999999999432, 44.52640028187936849, -247.3006740988509193 ) ) ;
#189235=CARTESIAN_POINT ( 'NONE',  ( -18.50016250449483479, 68.01715840423038628, -224.2192812407666054 ) ) ;
#189344=AXIS2_PLACEMENT_3D ( 'NONE', #23294, #157691, #101470 ) ;
#189351=EDGE_LOOP ( 'NONE', ( #229467, #63290, #182927, #104272 ) ) ;
#189357=ORIENTED_EDGE ( 'NONE', *, *, #162620, .F. ) ;
#189358=AXIS2_PLACEMENT_3D ( 'NONE', #164229, #8989, #243749 ) ;
#189413=FACE_OUTER_BOUND ( 'NONE', #200129, .T. ) ;
#189425=AXIS2_PLACEMENT_3D ( 'NONE', #192799, #194096, #154974 ) ;
#189430=DIRECTION ( 'NONE',  ( 0.000000000000000000, 0.4088369013363281068, -0.9126074666063770380 ) ) ;
#189438=ORIENTED_EDGE ( 'NONE', *, *, #31096, .T. ) ;
#189498=DIRECTION ( 'NONE',  ( 0.000000000000000000, 0.9126074666063769270, 0.4088369013363280513 ) ) ;
#189548=VECTOR ( 'NONE', #168870, 1000.000000000000000 ) ;
#189562=AXIS2_PLACEMENT_3D ( 'NONE', #56720, #215810, #17615 ) ;
#189580=DIRECTION ( 'NONE',  ( -0.8660254037844744568, -0.4563037333031724763, -0.2044184506680482571 ) ) ;
#189596=CIRCLE ( 'NONE', #18705, 4.049999999999994493 ) ;
#189605=CARTESIAN_POINT ( 'NONE',  ( 20.94999999999999574, 44.52640028187936849, -247.3006740988509193 ) ) ;
#189680=VECTOR ( 'NONE', #203053, 1000.000000000000000 ) ;
#189719=AXIS2_PLACEMENT_3D ( 'NONE', #225243, #187444, #87015 ) ;
#189722=ORIENTED_EDGE ( 'NONE', *, *, #157210, .F. ) ;
#189726=DIRECTION ( 'NONE',  ( 1.000000000000000000, 0.000000000000000000, 0.000000000000000000 ) ) ;
#189753=ORIENTED_EDGE ( 'NONE', *, *, #185961, .F. ) ;
#189784=AXIS2_PLACEMENT_3D ( 'NONE', #26584, #108668, #189498 ) ;
#189799=ORIENTED_EDGE ( 'NONE', *, *, #153401, .T. ) ;
#189832=ORIENTED_EDGE ( 'NONE', *, *, #139723, .T. ) ;
#189837=CARTESIAN_POINT ( 'NONE',  ( -21.05000000000000071, 38.04609728753135300, -236.0545303518866547 ) ) ;
#189844=VERTEX_POINT ( 'NONE', #17372 ) ;
#189862=TOROIDAL_SURFACE ( 'NONE', #169054, 0.2000000000000000111, 0.1000000000000000056 ) ;
#189881=AXIS2_PLACEMENT_3D ( 'NONE', #20608, #43994, #4837 ) ;
#189893=CIRCLE ( 'NONE', #256468, 0.4999999999999944489 ) ;
#189924=EDGE_CURVE ( 'NONE', #28183, #70441, #207010, .T. ) ;
#189928=ORIENTED_EDGE ( 'NONE', *, *, #62555, .F. ) ;
#189970=DIRECTION ( 'NONE',  ( 0.000000000000000000, -0.07847809223012357227, -0.9969158384938622275 ) ) ;
#190008=DIRECTION ( 'NONE',  ( 1.836970198721030427E-16, 0.4088369013363281623, -0.9126074666063771490 ) ) ;
#190017=EDGE_CURVE ( 'NONE', #257664, #99817, #98630, .T. ) ;
#190020=CARTESIAN_POINT ( 'NONE',  ( 21.06089410995835820, 43.41001159599868231, -234.7743943900634065 ) ) ;
#190028=ORIENTED_EDGE ( 'NONE', *, *, #117554, .T. ) ;
#190039=DIRECTION ( 'NONE',  ( 0.000000000000000000, -0.9126074666063772600, -0.4088369013363276627 ) ) ;
#190044=ORIENTED_EDGE ( 'NONE', *, *, #68328, .F. ) ;
#190051=DIRECTION ( 'NONE',  ( 1.000000000000000000, 0.000000000000000000, 0.000000000000000000 ) ) ;
#190056=ORIENTED_EDGE ( 'NONE', *, *, #222553, .T. ) ;
#190067=EDGE_CURVE ( 'NONE', #84389, #136081, #128087, .T. ) ;
#190125=DIRECTION ( 'NONE',  ( -0.000000000000000000, 0.4088369013363281068, -0.9126074666063770380 ) ) ;
#190128=EDGE_LOOP ( 'NONE', ( #98622, #61283, #107946, #193735 ) ) ;
#190129=ADVANCED_FACE ( 'NONE', ( #232281 ), #53621, .F. ) ;
#190156=EDGE_CURVE ( 'NONE', #211199, #58126, #157335, .T. ) ;
#190191=AXIS2_PLACEMENT_3D ( 'NONE', #1132, #235909, #19450 ) ;
#190217=CYLINDRICAL_SURFACE ( 'NONE', #199647, 0.1000000000000200173 ) ;
#190253=AXIS2_PLACEMENT_3D ( 'NONE', #43867, #4711, #45143 ) ;
#190296=DIRECTION ( 'NONE',  ( 0.000000000000000000, 0.9126074666063770380, 0.4088369013363281068 ) ) ;
#190299=CARTESIAN_POINT ( 'NONE',  ( 18.59999999999999076, 35.94660524813656366, -234.4748257877825495 ) ) ;
#190305=DIRECTION ( 'NONE',  ( 1.000000000000000000, 0.000000000000000000, 0.000000000000000000 ) ) ;
#190316=TOROIDAL_SURFACE ( 'NONE', #136098, 2.100000000000002309, 0.1000000000000000056 ) ;
#190331=CARTESIAN_POINT ( 'NONE',  ( -22.60000000000094289, 25.89494711235942148, -254.2627752153470055 ) ) ;
#190347=B_SPLINE_CURVE_WITH_KNOTS ( 'NONE', 3,
 ( #128717, #208261, #152149, #73903, #252489, #249942, #75179, #234212, #94705, #192540 ),
 .UNSPECIFIED., .F., .F.,
 ( 4, 3, 3, 4 ),
 ( 0.000000000000000000, 0.0002000000000008530056, 0.001000000000082974230, 0.001967863649483338456 ),
 .UNSPECIFIED. ) ;
#190414=EDGE_CURVE ( 'NONE', #4366, #119120, #186544, .T. ) ;
#190446=CIRCLE ( 'NONE', #53030, 0.1999999999999961531 ) ;
#190451=ADVANCED_FACE ( 'NONE', ( #7777 ), #247662, .F. ) ;
#190463=AXIS2_PLACEMENT_3D ( 'NONE', #168392, #32722, #191784 ) ;
#190542=EDGE_LOOP ( 'NONE', ( #186796, #52656, #49071, #169147, #93405, #227780 ) ) ;
#190578=CARTESIAN_POINT ( 'NONE',  ( -20.64999999999999858, 62.04503132991428060, -248.4786563706009588 ) ) ;
#190591=ORIENTED_EDGE ( 'NONE', *, *, #66941, .T. ) ;
#190604=EDGE_LOOP ( 'NONE', ( #104623, #79575, #99991, #14555 ) ) ;
#190641=CIRCLE ( 'NONE', #252964, 0.1000000000000091788 ) ;
#190646=CIRCLE ( 'NONE', #253152, 0.09999999999999063804 ) ;
#190664=CARTESIAN_POINT ( 'NONE',  ( 19.90621891164687440, 54.51371537586219063, -228.6772403362143109 ) ) ;
#190677=ORIENTED_EDGE ( 'NONE', *, *, #214294, .F. ) ;
#190707=AXIS2_PLACEMENT_3D ( 'NONE', #192677, #136518, #217339 ) ;
#190737=ADVANCED_FACE ( 'NONE', ( #140530 ), #215379, .T. ) ;
#190747=DIRECTION ( 'NONE',  ( 0.000000000000000000, -0.4088369013363280513, 0.9126074666063769270 ) ) ;
#190756=CARTESIAN_POINT ( 'NONE',  ( 21.05000000000000071, 41.42187432231294508, -260.1830396872097140 ) ) ;
#190815=AXIS2_PLACEMENT_3D ( 'NONE', #75785, #92758, #210164 ) ;
#190832=ORIENTED_EDGE ( 'NONE', *, *, #212731, .T. ) ;
#190845=AXIS2_PLACEMENT_3D ( 'NONE', #138345, #181375, #127 ) ;
#190863=EDGE_LOOP ( 'NONE', ( #230236, #256259, #102923, #95266, #101484 ) ) ;
#190882=AXIS2_PLACEMENT_3D ( 'NONE', #2728, #41901, #62727 ) ;
#190955=DIRECTION ( 'NONE',  ( 0.000000000000000000, -0.9126074666063545004, -0.4088369013363783999 ) ) ;
#190956=EDGE_CURVE ( 'NONE', #173891, #148222, #54266, .T. ) ;
#191001=CARTESIAN_POINT ( 'NONE',  ( 23.15000000000000213, 69.25640205380743453, -247.7135141964517402 ) ) ;
#191031=VERTEX_POINT ( 'NONE', #244324 ) ;
#191056=DIRECTION ( 'NONE',  ( 0.000000000000000000, -0.4088369013363280513, 0.9126074666063771490 ) ) ;
#191063=AXIS2_PLACEMENT_3D ( 'NONE', #143305, #241149, #239856 ) ;
#191066=CARTESIAN_POINT ( 'NONE',  ( -21.07928932188134041, 30.84304088367083452, -252.0482413927653340 ) ) ;
#191098=ORIENTED_EDGE ( 'NONE', *, *, #113222, .T. ) ;
#191104=DIRECTION ( 'NONE',  ( 0.000000000000000000, 0.9126074666063771490, 0.4088369013363281623 ) ) ;
#191114=( BOUNDED_SURFACE ( )  B_SPLINE_SURFACE ( 3, 2, ( 
 ( #75231, #70097, #30976 ),
 ( #174354, #213414, #188727 ),
 ( #192586, #251256, #72659 ),
 ( #110472, #152202, #231725 ) ),
 .UNSPECIFIED., .F., .F., .F. ) 
 B_SPLINE_SURFACE_WITH_KNOTS ( ( 4, 4 ),
 ( 3, 3 ),
 ( 0.04058434257139474644, 0.04256401539001599538 ),
 ( 0.000000000000000000, 1.000000000000000000 ),
 .UNSPECIFIED. ) 
 GEOMETRIC_REPRESENTATION_ITEM ( )  RATIONAL_B_SPLINE_SURFACE ( (
 ( 1.000000000000000000, 0.7103081912007761511, 1.000000000000000000),
 ( 1.000000000000000000, 0.7104998333555769818, 1.000000000000000000),
 ( 1.000000000000000000, 0.7107238315754760283, 1.000000000000000000),
 ( 1.000000000000000000, 0.7110073749539387311, 1.000000000000000000) ) ) 
 REPRESENTATION_ITEM ( '' )  SURFACE ( )  );
#191118=FACE_OUTER_BOUND ( 'NONE', #253288, .T. ) ;
#191119=CARTESIAN_POINT ( 'NONE',  ( 22.50000000000000000, 31.80488924422933295, -238.9605610896540213 ) ) ;
#191127=CARTESIAN_POINT ( 'NONE',  ( 21.00000000000000000, 51.97441255244040548, -232.0063394385699667 ) ) ;
#191140=ORIENTED_EDGE ( 'NONE', *, *, #195401, .F. ) ;
#191143=CARTESIAN_POINT ( 'NONE',  ( -21.05000000000000071, 38.12692959845505669, -236.1422783512203125 ) ) ;
#191154=CARTESIAN_POINT ( 'NONE',  ( 21.05000000000000071, 61.88149656937974896, -248.1136133839584090 ) ) ;
#191180=AXIS2_PLACEMENT_3D ( 'NONE', #203561, #144856, #243964 ) ;
#191183=EDGE_CURVE ( 'NONE', #94854, #241978, #153634, .T. ) ;
#191201=EDGE_LOOP ( 'NONE', ( #253960, #84712, #23520, #193264 ) ) ;
#191236=ORIENTED_EDGE ( 'NONE', *, *, #196385, .T. ) ;
#191245=AXIS2_PLACEMENT_3D ( 'NONE', #12813, #67623, #28554 ) ;
#191247=DIRECTION ( 'NONE',  ( 0.000000000000000000, 0.9126074666063660468, 0.4088369013363524762 ) ) ;
#191254=ORIENTED_EDGE ( 'NONE', *, *, #33763, .F. ) ;
#191262=ORIENTED_EDGE ( 'NONE', *, *, #19344, .F. ) ;
#191271=ORIENTED_EDGE ( 'NONE', *, *, #233119, .T. ) ;
#191293=EDGE_LOOP ( 'NONE', ( #223526, #204123, #236074 ) ) ;
#191296=CIRCLE ( 'NONE', #91498, 0.1000000000000024342 ) ;
#191300=AXIS2_PLACEMENT_3D ( 'NONE', #236984, #119616, #142982 ) ;
#191305=EDGE_CURVE ( 'NONE', #210045, #217030, #169551, .T. ) ;
#191308=EDGE_CURVE ( 'NONE', #112295, #230417, #82789, .T. ) ;
#191316=CARTESIAN_POINT ( 'NONE',  ( -18.50000000000000000, 43.92448011351754644, -236.0509145372394357 ) ) ;
#191320=DIRECTION ( 'NONE',  ( 0.000000000000000000, 0.9126074666063660468, 0.4088369013363524762 ) ) ;
#191367=ORIENTED_EDGE ( 'NONE', *, *, #174273, .F. ) ;
#191401=EDGE_LOOP ( 'NONE', ( #154125, #11437, #55592, #255661 ) ) ;
#191463=CARTESIAN_POINT ( 'NONE',  ( 23.14999999999999503, 21.13195309841794867, -243.6318585593223816 ) ) ;
#191465=ORIENTED_EDGE ( 'NONE', *, *, #38925, .T. ) ;
#191512=ORIENTED_EDGE ( 'NONE', *, *, #797, .F. ) ;
#191525=CARTESIAN_POINT ( 'NONE',  ( 18.59999999999999787, 78.48087866980282001, -232.8271061603568910 ) ) ;
#191556=ORIENTED_EDGE ( 'NONE', *, *, #218829, .T. ) ;
#191557=VECTOR ( 'NONE', #64398, 1000.000000000000000 ) ;
#191576=AXIS2_PLACEMENT_3D ( 'NONE', #131205, #112941, #150779 ) ;
#191586=ADVANCED_FACE ( 'NONE', ( #117239 ), #57234, .F. ) ;
#191590=ORIENTED_EDGE ( 'NONE', *, *, #131290, .T. ) ;
#191593=DIRECTION ( 'NONE',  ( 0.000000000000000000, 0.9126074666063771490, 0.4088369013363281623 ) ) ;
#191624=EDGE_LOOP ( 'NONE', ( #215479, #196279, #153768, #59311, #15164, #99485, #65193, #55292, #169799, #31325 ) ) ;
#191635=CYLINDRICAL_SURFACE ( 'NONE', #80486, 0.09999999999999939493 ) ;
#191644=CARTESIAN_POINT ( 'NONE',  ( 18.59999999999999787, 46.62132166459547733, -243.0426574061995950 ) ) ;
#191657=CARTESIAN_POINT ( 'NONE',  ( -20.00857864376270001, 44.09750824044544970, -236.1925523404271132 ) ) ;
#191682=VERTEX_POINT ( 'NONE', #3693 ) ;
#191750=CIRCLE ( 'NONE', #237512, 0.09999999999999854838 ) ;
#191768=ADVANCED_FACE ( 'NONE', ( #11418 ), #170568, .T. ) ;
#191784=DIRECTION ( 'NONE',  ( 0.000000000000000000, -0.9126074666063660468, -0.4088369013363524762 ) ) ;
#191875=LINE ( 'NONE', #232278, #139662 ) ;
#191935=DIRECTION ( 'NONE',  ( -1.000000000000000000, 7.510212038922875604E-17, -1.676432719286210708E-16 ) ) ;
#191944=DIRECTION ( 'NONE',  ( 2.952720810173289112E-16, 0.4088369013363266635, -0.9126074666063777041 ) ) ;
#191945=VERTEX_POINT ( 'NONE', #222402 ) ;
#191992=VERTEX_POINT ( 'NONE', #80324 ) ;
#191993=AXIS2_PLACEMENT_3D ( 'NONE', #99909, #235592, #137768 ) ;
#192001=DIRECTION ( 'NONE',  ( -0.000000000000000000, -0.9126074666063770380, -0.4088369013363281068 ) ) ;
#192008=CARTESIAN_POINT ( 'NONE',  ( -22.50000000000000000, 36.65892442174472876, -249.5511627012454596 ) ) ;
#192015=ORIENTED_EDGE ( 'NONE', *, *, #133541, .T. ) ;
#192045=ORIENTED_EDGE ( 'NONE', *, *, #35870, .F. ) ;
#192048=CARTESIAN_POINT ( 'NONE',  ( 20.94999999999999574, 43.57568952063339651, -245.1784935019914826 ) ) ;
#192081=CARTESIAN_POINT ( 'NONE',  ( 18.59999999999999432, 44.52640028187936849, -247.3006740988509193 ) ) ;
#192089=EDGE_CURVE ( 'NONE', #91918, #248466, #6298, .T. ) ;
#192115=TOROIDAL_SURFACE ( 'NONE', #79633, 0.6000000000000004219, 0.1000000000000000056 ) ;
#192124=ADVANCED_FACE ( 'NONE', ( #194884 ), #231441, .T. ) ;
#192130=DIRECTION ( 'NONE',  ( 0.000000000000000000, -0.09425075112713271475, -0.9955484899852801162 ) ) ;
#192149=ORIENTED_EDGE ( 'NONE', *, *, #212566, .T. ) ;
#192161=DIRECTION ( 'NONE',  ( 1.000000000000000000, -1.335000415235278971E-16, 2.979993593738921214E-16 ) ) ;
#192168=CIRCLE ( 'NONE', #129610, 0.09999999999999939493 ) ;
#192172=EDGE_LOOP ( 'NONE', ( #176044, #17184, #200857, #179124 ) ) ;
#192185=CARTESIAN_POINT ( 'NONE',  ( -23.15000000000000213, 32.87160343532826801, -251.2478358417912148 ) ) ;
#192195=ORIENTED_EDGE ( 'NONE', *, *, #212347, .T. ) ;
#192207=ORIENTED_EDGE ( 'NONE', *, *, #140415, .F. ) ;
#192218=EDGE_LOOP ( 'NONE', ( #19465, #3399, #21674, #245578 ) ) ;
#192226=ORIENTED_EDGE ( 'NONE', *, *, #225001, .T. ) ;
#192237=TOROIDAL_SURFACE ( 'NONE', #21542, 0.4000000000000012990, 0.1000000000000000056 ) ;
#192259=CIRCLE ( 'NONE', #221256, 0.09999999999999939493 ) ;
#192265=DIRECTION ( 'NONE',  ( -2.952720810173289112E-16, -0.4088369013363281068, 0.9126074666063770380 ) ) ;
#192320=DIRECTION ( 'NONE',  ( 0.000000000000000000, -0.9947597004326491632, 0.1022405907413782566 ) ) ;
#192327=CARTESIAN_POINT ( 'NONE',  ( -21.05000000000000071, 30.73599169745032356, -252.2206231971132127 ) ) ;
#192344=DIRECTION ( 'NONE',  ( 0.000000000000000000, 0.4088369013363783999, -0.9126074666063545004 ) ) ;
#192416=CARTESIAN_POINT ( 'NONE',  ( -23.15000000000000213, 51.38014393322265505, -230.1906178717505611 ) ) ;
#192424=CARTESIAN_POINT ( 'NONE',  ( -21.64999999999999858, 44.87429835298447500, -237.9265065269792103 ) ) ;
#192434=AXIS2_PLACEMENT_3D ( 'NONE', #109946, #210351, #51235 ) ;
#192443=AXIS2_PLACEMENT_3D ( 'NONE', #64414, #184345, #21455 ) ;
#192461=FACE_OUTER_BOUND ( 'NONE', #223080, .T. ) ;
#192476=DIRECTION ( 'NONE',  ( 0.000000000000000000, 0.9126074666063632712, 0.4088369013363589710 ) ) ;
#192482=CARTESIAN_POINT ( 'NONE',  ( 20.94999999999999574, 39.23476235320398331, -236.9756760510740037 ) ) ;
#192500=ORIENTED_EDGE ( 'NONE', *, *, #25169, .F. ) ;
#192504=CYLINDRICAL_SURFACE ( 'NONE', #198133, 0.09999999999999939493 ) ;
#192507=AXIS2_PLACEMENT_3D ( 'NONE', #168039, #67606, #244958 ) ;
#192528=CARTESIAN_POINT ( 'NONE',  ( -20.94999999999999929, 44.06250559941687328, -258.7395785465160429 ) ) ;
#192540=CARTESIAN_POINT ( 'NONE',  ( -22.47071067811865319, 33.41224047107334627, -242.5462774987836383 ) ) ;
#192542=FACE_OUTER_BOUND ( 'NONE', #249220, .T. ) ;
#192545=ORIENTED_EDGE ( 'NONE', *, *, #127898, .T. ) ;
#192586=CARTESIAN_POINT ( 'NONE',  ( 21.53752568617646901, 33.79390208801449091, -243.3979355726051494 ) ) ;
#192597=VERTEX_POINT ( 'NONE', #238507 ) ;
#192627=ORIENTED_EDGE ( 'NONE', *, *, #176541, .F. ) ;
#192632=EDGE_LOOP ( 'NONE', ( #49882, #198409, #176202, #159127 ) ) ;
#192641=VERTEX_POINT ( 'NONE', #62449 ) ;
#192677=CARTESIAN_POINT ( 'NONE',  ( -20.85000000000000142, 67.65998959290219261, -227.8609496483021530 ) ) ;
#192696=FACE_OUTER_BOUND ( 'NONE', #72885, .T. ) ;
#192707=AXIS2_PLACEMENT_3D ( 'NONE', #151100, #32467, #12894 ) ;
#192726=DIRECTION ( 'NONE',  ( 0.000000000000000000, 0.9126074666063660468, 0.4088369013363524762 ) ) ;
#192757=B_SPLINE_CURVE_WITH_KNOTS ( 'NONE', 3,
 ( #135102, #214649, #36039, #115552, #104942, #82810, #164955, #219781, #184506, #46277, #21608, #223623, #142796, #65849, #102376, #239361, #201506, #5864, #85378 ),
 .UNSPECIFIED., .F., .F.,
 ( 4, 3, 3, 3, 3, 3, 4 ),
 ( 1.387778780781445521E-17, 2.646747978908830373E-05, 5.271166642130153582E-05, 9.008788829885479505E-05, 0.0001426648776561217978, 0.0001897378458660037217, 0.0001917382627806517032 ),
 .UNSPECIFIED. ) ;
#192760=CARTESIAN_POINT ( 'NONE',  ( 23.14999999999999858, 67.23127455305835554, -235.8551265064784559 ) ) ;
#192799=CARTESIAN_POINT ( 'NONE',  ( -20.64999999999999858, 47.91013932883114990, -242.3192343197862044 ) ) ;
#192829=ORIENTED_EDGE ( 'NONE', *, *, #215686, .T. ) ;
#192854=SPHERICAL_SURFACE ( 'NONE', #78381, 0.1000000000000000056 ) ;
#192863=ADVANCED_FACE ( 'NONE', ( #59527 ), #99943, .F. ) ;
#192882=EDGE_CURVE ( 'NONE', #200649, #84649, #8563, .T. ) ;
#192904=ORIENTED_EDGE ( 'NONE', *, *, #198157, .T. ) ;
#192911=LINE ( 'NONE', #232050, #90454 ) ;
#192925=AXIS2_PLACEMENT_3D ( 'NONE', #69368, #130605, #112344 ) ;
#192932=EDGE_CURVE ( 'NONE', #228315, #150739, #208497, .T. ) ;
#192934=DIRECTION ( 'NONE',  ( 1.000000000000000000, 0.000000000000000000, 0.000000000000000000 ) ) ;
#192936=VERTEX_POINT ( 'NONE', #200361 ) ;
#192950=LINE ( 'NONE', #74315, #49178 ) ;
#192955=ORIENTED_EDGE ( 'NONE', *, *, #99740, .T. ) ;
#192988=DIRECTION ( 'NONE',  ( -1.000000000000000000, -0.000000000000000000, 0.000000000000000000 ) ) ;
#192991=DIRECTION ( 'NONE',  ( 1.000000000000000000, 0.000000000000000000, 0.000000000000000000 ) ) ;
#192999=CARTESIAN_POINT ( 'NONE',  ( -20.54999999999999716, 44.87429835298446790, -237.9265065269792103 ) ) ;
#193083=FACE_OUTER_BOUND ( 'NONE', #10572, .T. ) ;
#193102=ORIENTED_EDGE ( 'NONE', *, *, #122082, .F. ) ;
#193132=VECTOR ( 'NONE', #212550, 1000.000000000000227 ) ;
#193146=ADVANCED_FACE ( 'NONE', ( #51517 ), #251011, .F. ) ;
#193156=AXIS2_PLACEMENT_3D ( 'NONE', #146835, #47735, #223810 ) ;
#193164=TOROIDAL_SURFACE ( 'NONE', #209719, 0.4000000000000009104, 0.1000000000000000056 ) ;
#193174=PLANE ( 'NONE',  #161765 ) ;
#193175=DIRECTION ( 'NONE',  ( -0.000000000000000000, 0.4088369013363286064, -0.9126074666063768159 ) ) ;
#193213=ORIENTED_EDGE ( 'NONE', *, *, #237052, .T. ) ;
#193245=CARTESIAN_POINT ( 'NONE',  ( 23.24999999999999645, 67.23127455305835554, -235.8551265064784559 ) ) ;
#193264=ORIENTED_EDGE ( 'NONE', *, *, #14122, .F. ) ;
#193290=CARTESIAN_POINT ( 'NONE',  ( -23.25000000000000000, 32.87160343532826090, -251.2478358417912148 ) ) ;
#193334=VECTOR ( 'NONE', #156855, 1000.000000000000114 ) ;
#193341=SURFACE_STYLE_USAGE ( .BOTH. , #111224 ) ;
#193350=FACE_OUTER_BOUND ( 'NONE', #120204, .T. ) ;
#193377=AXIS2_PLACEMENT_3D ( 'NONE', #252065, #89138, #31774 ) ;
#193410=CYLINDRICAL_SURFACE ( 'NONE', #174639, 0.1000000000000024342 ) ;
#193439=DIRECTION ( 'NONE',  ( -1.000000000000000000, 7.510212038922875604E-17, -1.676432719286210708E-16 ) ) ;
#193452=AXIS2_PLACEMENT_3D ( 'NONE', #249189, #127952, #70574 ) ;
#193495=ORIENTED_EDGE ( 'NONE', *, *, #24063, .F. ) ;
#193502=DIRECTION ( 'NONE',  ( 0.000000000000000000, 0.9126074666063781482, 0.4088369013363256643 ) ) ;
#193512=EDGE_CURVE ( 'NONE', #223817, #7829, #79064, .T. ) ;
#193518=CARTESIAN_POINT ( 'NONE',  ( 20.94999999999999929, 65.49732036650624423, -236.6319166190174883 ) ) ;
#193530=DIRECTION ( 'NONE',  ( -1.000000000000000000, 0.000000000000000000, 0.000000000000000000 ) ) ;
#193606=DIRECTION ( 'NONE',  ( 0.000000000000000000, -0.09425075112713271475, -0.9955484899852801162 ) ) ;
#193634=EDGE_CURVE ( 'NONE', #47998, #168551, #241764, .T. ) ;
#193641=ORIENTED_EDGE ( 'NONE', *, *, #85815, .T. ) ;
#193643=B_SPLINE_CURVE_WITH_KNOTS ( 'NONE', 3,
 ( #53731, #94135, #34204, #233666, #171163, #173735, #229796 ),
 .UNSPECIFIED., .F., .F.,
 ( 4, 3, 4 ),
 ( 0.000000000000000000, 0.0007844235214594282848, 0.001767853679404336829 ),
 .UNSPECIFIED. ) ;
#193644=EDGE_CURVE ( 'NONE', #144138, #52663, #53813, .T. ) ;
#193700=DIRECTION ( 'NONE',  ( 1.000000000000000000, 0.000000000000000000, 0.000000000000000000 ) ) ;
#193735=ORIENTED_EDGE ( 'NONE', *, *, #27222, .F. ) ;
#193757=ORIENTED_EDGE ( 'NONE', *, *, #90581, .F. ) ;
#193784=ORIENTED_EDGE ( 'NONE', *, *, #62321, .F. ) ;
#193805=AXIS2_PLACEMENT_3D ( 'NONE', #205558, #123475, #124766 ) ;
#193819=LINE ( 'NONE', #254997, #73946 ) ;
#193831=EDGE_LOOP ( 'NONE', ( #96070, #207570, #195639, #45583 ) ) ;
#193854=CARTESIAN_POINT ( 'NONE',  ( -21.52071067811865746, 52.78011179951285214, -233.8048247179419548 ) ) ;
#193862=DIRECTION ( 'NONE',  ( -1.000000000000000000, 0.000000000000000000, 0.000000000000000000 ) ) ;
#193880=VECTOR ( 'NONE', #44206, 1000.000000000000000 ) ;
#193889=CARTESIAN_POINT ( 'NONE',  ( -20.64999999999999858, 54.18117728009210055, -239.0715820348696923 ) ) ;
#193895=CARTESIAN_POINT ( 'NONE',  ( 20.74625933824008328, 40.83477453765030418, -237.9468798847826179 ) ) ;
#193927=CARTESIAN_POINT ( 'NONE',  ( -20.99142135623731065, 56.16603649944111254, -228.1013850343386196 ) ) ;
#193959=DIRECTION ( 'NONE',  ( 1.000000000000000000, 0.000000000000000000, 0.000000000000000000 ) ) ;
#193970=CARTESIAN_POINT ( 'NONE',  ( 20.94999999999999929, 67.23127455305835554, -235.8551265064784559 ) ) ;
#193971=CARTESIAN_POINT ( 'NONE',  ( -20.54999999999999716, 48.98768910550767686, -253.5949463715719787 ) ) ;
#193972=ORIENTED_EDGE ( 'NONE', *, *, #47618, .F. ) ;
#194016=ADVANCED_FACE ( 'NONE', ( #57335 ), #233679, .T. ) ;
#194067=FACE_OUTER_BOUND ( 'NONE', #96689, .T. ) ;
#194086=ORIENTED_EDGE ( 'NONE', *, *, #205652, .T. ) ;
#194090=CARTESIAN_POINT ( 'NONE',  ( -18.59999999999999787, 47.92640890138473253, -246.4059919526569900 ) ) ;
#194096=DIRECTION ( 'NONE',  ( 1.000000000000000000, 0.000000000000000000, 0.000000000000000000 ) ) ;
#194109=ORIENTED_EDGE ( 'NONE', *, *, #101625, .F. ) ;
#194174=CARTESIAN_POINT ( 'NONE',  ( 22.50927854361885139, 25.97741623539291567, -254.4468631480566501 ) ) ;
#194181=CARTESIAN_POINT ( 'NONE',  ( -21.65000000000000213, 52.90028168070691095, -233.8284721206281915 ) ) ;
#194187=CIRCLE ( 'NONE', #189881, 0.1000000000000087624 ) ;
#194208=EDGE_CURVE ( 'NONE', #108499, #198869, #37976, .T. ) ;
#194213=DIRECTION ( 'NONE',  ( 0.000000000000000000, -0.4088369013363494231, 0.9126074666063672680 ) ) ;
#194215=EDGE_LOOP ( 'NONE', ( #166657, #20983, #95198, #74324 ) ) ;
#194235=ORIENTED_EDGE ( 'NONE', *, *, #90470, .F. ) ;
#194283=CARTESIAN_POINT ( 'NONE',  ( -18.59999999999999787, 46.59314322379660922, -243.1831726892433210 ) ) ;
#194293=FACE_OUTER_BOUND ( 'NONE', #235747, .T. ) ;
#194341=EDGE_CURVE ( 'NONE', #227768, #24438, #254863, .T. ) ;
#194371=EDGE_CURVE ( 'NONE', #44800, #110771, #138786, .T. ) ;
#194374=EDGE_LOOP ( 'NONE', ( #242018, #136451, #56982, #23972 ) ) ;
#194378=VECTOR ( 'NONE', #158112, 1000.000000000000000 ) ;
#194392=DIRECTION ( 'NONE',  ( 1.000000000000000000, 0.000000000000000000, 0.000000000000000000 ) ) ;
#194401=EDGE_LOOP ( 'NONE', ( #158623, #226935, #1001, #167008, #225814 ) ) ;
#194426=AXIS2_PLACEMENT_3D ( 'NONE', #69707, #207934, #72268 ) ;
#194436=ORIENTED_EDGE ( 'NONE', *, *, #174102, .F. ) ;
#194455=AXIS2_PLACEMENT_3D ( 'NONE', #88650, #168264, #247752 ) ;
#194463=DIRECTION ( 'NONE',  ( 0.000000000000000000, -0.9126074666063770380, -0.4088369013363281068 ) ) ;
#194484=EDGE_LOOP ( 'NONE', ( #129290, #228176, #191262, #140854 ) ) ;
#194543=EDGE_LOOP ( 'NONE', ( #242040, #207340, #14763, #37269 ) ) ;
#194572=DIRECTION ( 'NONE',  ( 0.000000000000000000, 0.9126074666063773710, 0.4088369013363274962 ) ) ;
#194591=CARTESIAN_POINT ( 'NONE',  ( 18.36493879433090370, 77.43242999775311830, -241.6948683660838242 ) ) ;
#194642=( LENGTH_UNIT ( ) NAMED_UNIT ( * ) SI_UNIT ( .MILLI., .METRE. ) );
#194661=FACE_OUTER_BOUND ( 'NONE', #191201, .T. ) ;
#194670=CARTESIAN_POINT ( 'NONE',  ( 21.05000000000000071, 30.90801580390627734, -252.0203440857197279 ) ) ;
#194671=ORIENTED_EDGE ( 'NONE', *, *, #112974, .T. ) ;
#194677=DIRECTION ( 'NONE',  ( 1.000000000000000000, -1.207181226542539700E-16, 2.694675058168174199E-16 ) ) ;
#194694=AXIS2_PLACEMENT_3D ( 'NONE', #91073, #195335, #256496 ) ;
#194696=CARTESIAN_POINT ( 'NONE',  ( -23.25000000000000000, 54.92280082623103965, -239.2759596675668092 ) ) ;
#194719=DIRECTION ( 'NONE',  ( -1.000000000000000000, 2.986185139342070877E-16, -6.665775143889692774E-16 ) ) ;
#194741=VECTOR ( 'NONE', #245792, 1000.000000000000000 ) ;
#194766=ADVANCED_FACE ( 'NONE', ( #253930 ), #19187, .F. ) ;
#194772=AXIS2_PLACEMENT_3D ( 'NONE', #173450, #36475, #93846 ) ;
#194787=ORIENTED_EDGE ( 'NONE', *, *, #77577, .T. ) ;
#194794=VECTOR ( 'NONE', #228601, 1000.000000000000114 ) ;
#194798=LINE ( 'NONE', #95658, #252829 ) ;
#194800=ORIENTED_EDGE ( 'NONE', *, *, #108979, .T. ) ;
#194826=EDGE_CURVE ( 'NONE', #17340, #110197, #146615, .T. ) ;
#194862=DIRECTION ( 'NONE',  ( 1.000000000000000000, 0.000000000000000000, 0.000000000000000000 ) ) ;
#194884=FACE_OUTER_BOUND ( 'NONE', #177187, .T. ) ;
#194916=ORIENTED_EDGE ( 'NONE', *, *, #179273, .F. ) ;
#194931=ORIENTED_EDGE ( 'NONE', *, *, #163455, .T. ) ;
#194948=EDGE_CURVE ( 'NONE', #146851, #136568, #64727, .T. ) ;
#194961=ORIENTED_EDGE ( 'NONE', *, *, #200044, .F. ) ;
#194967=EDGE_CURVE ( 'NONE', #41483, #208529, #142956, .T. ) ;
#195033=ADVANCED_FACE ( 'NONE', ( #149426 ), #110266, .F. ) ;
#195049=DIRECTION ( 'NONE',  ( 1.000000000000000000, 0.000000000000000000, 0.000000000000000000 ) ) ;
#195078=CARTESIAN_POINT ( 'NONE',  ( 21.07954640115310596, 30.85578282560233987, -252.0785699441653946 ) ) ;
#195081=ORIENTED_EDGE ( 'NONE', *, *, #69706, .F. ) ;
#195105=TOROIDAL_SURFACE ( 'NONE', #82611, 12.77500000000000036, 0.1000000000000000056 ) ;
#195106=ORIENTED_EDGE ( 'NONE', *, *, #35893, .T. ) ;
#195173=DIRECTION ( 'NONE',  ( 1.000000000000000000, 0.000000000000000000, 0.000000000000000000 ) ) ;
#195185=FACE_OUTER_BOUND ( 'NONE', #253925, .T. ) ;
#195247=EDGE_LOOP ( 'NONE', ( #43536, #239902, #66544, #160476 ) ) ;
#195288=CIRCLE ( 'NONE', #166245, 0.09999999999999326095 ) ;
#195306=DIRECTION ( 'NONE',  ( 0.000000000000000000, 0.2716869542551192951, -0.9623856809447951521 ) ) ;
#195331=CARTESIAN_POINT ( 'NONE',  ( -23.15000000000000213, 47.66483718802935954, -241.7716698398223514 ) ) ;
#195335=DIRECTION ( 'NONE',  ( 0.000000000000000000, -0.4948392722769175411, -0.8689845192018386122 ) ) ;
#195336=ORIENTED_EDGE ( 'NONE', *, *, #61756, .F. ) ;
#195401=EDGE_CURVE ( 'NONE', #161463, #101099, #217728, .T. ) ;
#195427=EDGE_CURVE ( 'NONE', #105460, #33224, #180533, .T. ) ;
#195434=AXIS2_PLACEMENT_3D ( 'NONE', #154005, #134363, #70595 ) ;
#195435=ORIENTED_EDGE ( 'NONE', *, *, #254008, .F. ) ;
#195439=ADVANCED_FACE ( 'NONE', ( #203936 ), #25325, .T. ) ;
#195462=ADVANCED_FACE ( 'NONE', ( #222186 ), #219636, .T. ) ;
#195501=VERTEX_POINT ( 'NONE', #207824 ) ;
#195514=CARTESIAN_POINT ( 'NONE',  ( 18.39999999999999858, 77.13860723519891849, -241.8264964602989266 ) ) ;
#195522=DIRECTION ( 'NONE',  ( 0.000000000000000000, 0.9126074666063545004, 0.4088369013363783999 ) ) ;
#195529=ORIENTED_EDGE ( 'NONE', *, *, #5590, .T. ) ;
#195534=DIRECTION ( 'NONE',  ( 0.000000000000000000, -0.8490545835447252943, -0.5283051335749948674 ) ) ;
#195549=DIRECTION ( 'NONE',  ( -1.000000000000000000, 1.335000415235278971E-16, -2.979993593738921214E-16 ) ) ;
#195561=CARTESIAN_POINT ( 'NONE',  ( -20.64999999999999858, 54.14029358995846053, -238.9803212882090691 ) ) ;
#195569=CARTESIAN_POINT ( 'NONE',  ( 20.94999999999999929, 69.19063053712525857, -247.5666987377248631 ) ) ;
#195577=AXIS2_PLACEMENT_3D ( 'NONE', #32621, #170866, #212521 ) ;
#195594=VECTOR ( 'NONE', #113588, 1000.000000000000114 ) ;
#195639=ORIENTED_EDGE ( 'NONE', *, *, #190017, .F. ) ;
#195652=AXIS2_PLACEMENT_3D ( 'NONE', #109581, #28826, #31385 ) ;
#195670=ORIENTED_EDGE ( 'NONE', *, *, #112161, .F. ) ;
#195694=DIRECTION ( 'NONE',  ( 1.441126678808781316E-14, -0.5469332180710856361, 0.8371762388950170219 ) ) ;
#195700=AXIS2_PLACEMENT_3D ( 'NONE', #208597, #130307, #165618 ) ;
#195706=ORIENTED_EDGE ( 'NONE', *, *, #127277, .F. ) ;
#195725=ORIENTED_EDGE ( 'NONE', *, *, #107609, .T. ) ;
#195727=CARTESIAN_POINT ( 'NONE',  ( 21.05000000000000071, 44.37956953460552256, -247.4621105139464419 ) ) ;
#195740=DIRECTION ( 'NONE',  ( 1.000000000000000000, -2.986185139342066440E-16, 6.665775143889694746E-16 ) ) ;
#195742=CIRCLE ( 'NONE', #203897, 0.1999999999999987899 ) ;
#195777=ORIENTED_EDGE ( 'NONE', *, *, #173598, .T. ) ;
#195779=AXIS2_PLACEMENT_3D ( 'NONE', #153752, #14208, #209823 ) ;
#195791=DIRECTION ( 'NONE',  ( 1.000000000000000000, 0.000000000000000000, 0.000000000000000000 ) ) ;
#195804=EDGE_LOOP ( 'NONE', ( #5276, #234934, #231067, #74987 ) ) ;
#195850=ORIENTED_EDGE ( 'NONE', *, *, #18487, .T. ) ;
#195858=AXIS2_PLACEMENT_3D ( 'NONE', #150842, #173027, #231684 ) ;
#195866=DIRECTION ( 'NONE',  ( 0.000000000000000000, -0.5859227990963362664, -0.8103668758649469339 ) ) ;
#195872=DIRECTION ( 'NONE',  ( -0.000000000000000000, -0.9594490217226112616, -0.2818822000686178608 ) ) ;
#195893=DIRECTION ( 'NONE',  ( -1.000000000000000000, 8.623019343401632876E-17, 8.389849937938899189E-16 ) ) ;
#195894=VECTOR ( 'NONE', #180426, 1000.000000000000000 ) ;
#195906=DIRECTION ( 'NONE',  ( 0.000000000000000000, -0.9656312546561486299, -0.2599159095384356855 ) ) ;
#195921=CARTESIAN_POINT ( 'NONE',  ( 18.49999999999999289, 55.02897297050080994, -230.1354412432072536 ) ) ;
#195950=CARTESIAN_POINT ( 'NONE',  ( 20.94999999999999929, 49.36776662947724503, -253.7196102226803021 ) ) ;
#195951=CARTESIAN_POINT ( 'NONE',  ( -18.59999999999999787, 38.29773864426884700, -236.0513742605307925 ) ) ;
#196000=VECTOR ( 'NONE', #73829, 1000.000000000000000 ) ;
#196009=AXIS2_PLACEMENT_3D ( 'NONE', #17271, #154249, #173823 ) ;
#196022=CYLINDRICAL_SURFACE ( 'NONE', #108232, 0.1000000000000024342 ) ;
#196048=VECTOR ( 'NONE', #169266, 1000.000000000000114 ) ;
#196058=AXIS2_PLACEMENT_3D ( 'NONE', #75853, #155433, #34193 ) ;
#196060=EDGE_LOOP ( 'NONE', ( #119865, #49442 ) ) ;
#196069=EDGE_CURVE ( 'NONE', #19219, #212713, #1431, .T. ) ;
#196108=ORIENTED_EDGE ( 'NONE', *, *, #68139, .T. ) ;
#196124=DIRECTION ( 'NONE',  ( -1.000000000000000000, -0.000000000000000000, -0.000000000000000000 ) ) ;
#196139=CYLINDRICAL_SURFACE ( 'NONE', #4765, 11.74999999999999822 ) ;
#196140=VECTOR ( 'NONE', #195893, 1000.000000000000000 ) ;
#196159=AXIS2_PLACEMENT_3D ( 'NONE', #176449, #192161, #173910 ) ;
#196210=DIRECTION ( 'NONE',  ( 1.000000000000000000, 0.000000000000000000, 0.000000000000000000 ) ) ;
#196218=CARTESIAN_POINT ( 'NONE',  ( 18.59999999999999432, 77.44184265367997000, -241.6694879557322508 ) ) ;
#196276=AXIS2_PLACEMENT_3D ( 'NONE', #9883, #230221, #149425 ) ;
#196279=ORIENTED_EDGE ( 'NONE', *, *, #29813, .T. ) ;
#196300=DIRECTION ( 'NONE',  ( 0.000000000000000000, 0.4088369013363281068, -0.9126074666063770380 ) ) ;
#196333=CARTESIAN_POINT ( 'NONE',  ( 18.49999999999998934, 68.00417547777205129, -224.2303273613012209 ) ) ;
#196338=ORIENTED_EDGE ( 'NONE', *, *, #250921, .T. ) ;
#196385=EDGE_CURVE ( 'NONE', #132466, #73568, #43796, .T. ) ;
#196407=CARTESIAN_POINT ( 'NONE',  ( -20.54999999999999716, 54.18117728009210055, -239.0715820348696923 ) ) ;
#196409=LINE ( 'NONE', #214689, #23557 ) ;
#196432=ORIENTED_EDGE ( 'NONE', *, *, #67679, .T. ) ;
#196437=CARTESIAN_POINT ( 'NONE',  ( -22.47071067811865674, 33.41224047107334627, -242.5462774987836383 ) ) ;
#196446=DIRECTION ( 'NONE',  ( 0.000000000000000000, 0.4088369013363281068, -0.9126074666063770380 ) ) ;
#196462=ORIENTED_EDGE ( 'NONE', *, *, #67467, .T. ) ;
#196475=ORIENTED_EDGE ( 'NONE', *, *, #213771, .T. ) ;
#196524=AXIS2_PLACEMENT_3D ( 'NONE', #117005, #36206, #219953 ) ;
#196525=CARTESIAN_POINT ( 'NONE',  ( -21.14999999999999858, 31.89597452117651244, -238.9192857152811769 ) ) ;
#196542=AXIS2_PLACEMENT_3D ( 'NONE', #213498, #193959, #253902 ) ;
#196550=CARTESIAN_POINT ( 'NONE',  ( -23.25000000000000000, 46.05992536685982230, -240.5730681801377102 ) ) ;
#196588=ORIENTED_EDGE ( 'NONE', *, *, #244459, .F. ) ;
#196670=ORIENTED_EDGE ( 'NONE', *, *, #85404, .F. ) ;
#196696=AXIS2_PLACEMENT_3D ( 'NONE', #118552, #179800, #62411 ) ;
#196697=DIRECTION ( 'NONE',  ( 1.000000000000000000, 0.000000000000000000, 0.000000000000000000 ) ) ;
#196706=CARTESIAN_POINT ( 'NONE',  ( -18.39999999999999858, 77.26488334054519669, -241.9697969554615611 ) ) ;
#196708=CIRCLE ( 'NONE', #217542, 0.1000000000000041550 ) ;
#196721=CARTESIAN_POINT ( 'NONE',  ( -20.85000000000000142, 67.23127455305835554, -235.8551265064784559 ) ) ;
#196758=DIRECTION ( 'NONE',  ( 0.000000000000000000, 0.9126074666063660468, 0.4088369013363524762 ) ) ;
#196787=AXIS2_PLACEMENT_3D ( 'NONE', #255126, #214766, #40023 ) ;
#196848=DIRECTION ( 'NONE',  ( 0.000000000000000000, 0.4088369013363281623, -0.9126074666063771490 ) ) ;
#196879=AXIS2_PLACEMENT_3D ( 'NONE', #117329, #196848, #97729 ) ;
#196932=ORIENTED_EDGE ( 'NONE', *, *, #47618, .T. ) ;
#196933=DIRECTION ( 'NONE',  ( 1.000000000000000000, 0.000000000000000000, -0.000000000000000000 ) ) ;
#196942=ORIENTED_EDGE ( 'NONE', *, *, #38507, .T. ) ;
#196953=LINE ( 'NONE', #118733, #81522 ) ;
#196963=DIRECTION ( 'NONE',  ( 0.000000000000000000, -0.9126074666063769270, -0.4088369013363280513 ) ) ;
#197000=EDGE_CURVE ( 'NONE', #7959, #10735, #230439, .T. ) ;
#197024=DIRECTION ( 'NONE',  ( -0.000000000000000000, -0.4088369013363281068, 0.9126074666063770380 ) ) ;
#197036=AXIS2_PLACEMENT_3D ( 'NONE', #207029, #28430, #167929 ) ;
#197083=DIRECTION ( 'NONE',  ( -1.000000000000000000, 0.000000000000000000, 0.000000000000000000 ) ) ;
#197108=FACE_OUTER_BOUND ( 'NONE', #109187, .T. ) ;
#197161=DIRECTION ( 'NONE',  ( 1.000000000000000000, 0.000000000000000000, -0.000000000000000000 ) ) ;
#197172=DIRECTION ( 'NONE',  ( -1.836970198721029934E-16, -0.4088369013363280513, 0.9126074666063769270 ) ) ;
#197175=LINE ( 'NONE', #176362, #207594 ) ;
#197208=DIRECTION ( 'NONE',  ( 0.000000000000000000, 0.9126074666063660468, 0.4088369013363524762 ) ) ;
#197223=EDGE_CURVE ( 'NONE', #252869, #61629, #76676, .T. ) ;
#197236=CIRCLE ( 'NONE', #134674, 0.1000000000000024342 ) ;
#197261=CARTESIAN_POINT ( 'NONE',  ( 18.59999999999999076, 21.13195309841794867, -243.6318585593224100 ) ) ;
#197267=VECTOR ( 'NONE', #20000, 1000.000000000000114 ) ;
#197277=AXIS2_PLACEMENT_3D ( 'NONE', #122911, #184145, #39546 ) ;
#197319=VERTEX_POINT ( 'NONE', #239940 ) ;
#197349=CARTESIAN_POINT ( 'NONE',  ( -18.59999999999999787, 21.17283678855158513, -243.7231193059830332 ) ) ;
#197389=CARTESIAN_POINT ( 'NONE',  ( -18.59999999999999787, 45.53758419368699606, -241.2860287061636768 ) ) ;
#197397=ORIENTED_EDGE ( 'NONE', *, *, #145650, .T. ) ;
#197414=FACE_OUTER_BOUND ( 'NONE', #235496, .T. ) ;
#197418=VERTEX_POINT ( 'NONE', #127691 ) ;
#197450=CIRCLE ( 'NONE', #130250, 0.09999999999999939493 ) ;
#197452=CIRCLE ( 'NONE', #239158, 0.1000000000000024342 ) ;
#197522=DIRECTION ( 'NONE',  ( 0.000000000000000000, -0.9126074666063771490, -0.4088369013363278293 ) ) ;
#197595=VERTEX_POINT ( 'NONE', #106176 ) ;
#197612=CARTESIAN_POINT ( 'NONE',  ( 18.51697539158856642, 68.06642993404716435, -224.1774859612004036 ) ) ;
#197624=ADVANCED_FACE ( 'NONE', ( #146583 ), #67077, .F. ) ;
#197638=ADVANCED_FACE ( 'NONE', ( #184445 ), #199214, .F. ) ;
#197650=ORIENTED_EDGE ( 'NONE', *, *, #117776, .F. ) ;
#197656=CIRCLE ( 'NONE', #147601, 0.1000000000000024342 ) ;
#197657=ADVANCED_FACE ( 'NONE', ( #27986 ), #140495, .F. ) ;
#197678=CARTESIAN_POINT ( 'NONE',  ( -23.25000000000000000, 40.35498466150055918, -247.8953732508333587 ) ) ;
#197701=CARTESIAN_POINT ( 'NONE',  ( -21.14999999999999858, 41.46275801244657799, -260.2743004338703940 ) ) ;
#197703=EDGE_CURVE ( 'NONE', #25924, #973, #197656, .T. ) ;
#197704=ADVANCED_FACE ( 'NONE', ( #248283 ), #150480, .F. ) ;
#197740=LINE ( 'NONE', #60786, #66469 ) ;
#197769=CIRCLE ( 'NONE', #201870, 0.09999999999999771572 ) ;
#197776=DIRECTION ( 'NONE',  ( 0.000000000000000000, -0.4088369013363281068, 0.9126074666063770380 ) ) ;
#197784=DIRECTION ( 'NONE',  ( 1.000000000000000000, 0.000000000000000000, -0.000000000000000000 ) ) ;
#197798=CARTESIAN_POINT ( 'NONE',  ( 23.14999999999999858, 65.40605961984560679, -236.6728003091511425 ) ) ;
#197801=CARTESIAN_POINT ( 'NONE',  ( -21.14999999999999858, 31.89597452117651244, -238.9192857152811769 ) ) ;
#197819=CARTESIAN_POINT ( 'NONE',  ( -18.46919391072067995, 77.27558647942372261, -241.9522046346448292 ) ) ;
#197833=DIRECTION ( 'NONE',  ( -1.000000000000000000, -0.000000000000000000, 0.000000000000000000 ) ) ;
#197844=ORIENTED_EDGE ( 'NONE', *, *, #145040, .F. ) ;
#197884=DIRECTION ( 'NONE',  ( 0.000000000000000000, 0.9126074666063844765, 0.4088369013363114535 ) ) ;
#197904=ORIENTED_EDGE ( 'NONE', *, *, #47150, .T. ) ;
#197917=CARTESIAN_POINT ( 'NONE',  ( -21.05000000000000071, 47.95459712139159336, -246.5019368548292675 ) ) ;
#197931=EDGE_CURVE ( 'NONE', #228584, #168498, #216898, .T. ) ;
#197979=EDGE_CURVE ( 'NONE', #104336, #61955, #47805, .T. ) ;
#198005=EDGE_CURVE ( 'NONE', #102227, #68445, #447, .T. ) ;
#198006=CARTESIAN_POINT ( 'NONE',  ( -23.15000000000000213, 56.06656052939784729, -228.0911609752645290 ) ) ;
#198010=LINE ( 'NONE', #80614, #59078 ) ;
#198043=EDGE_CURVE ( 'NONE', #86618, #20356, #6116, .T. ) ;
#198070=CARTESIAN_POINT ( 'NONE',  ( -20.85000000000000142, 78.57213941646344324, -232.7862224702232652 ) ) ;
#198080=DIRECTION ( 'NONE',  ( 0.000000000000000000, 0.9126074666064696306, 0.4088369013361213278 ) ) ;
#198096=CARTESIAN_POINT ( 'NONE',  ( 18.59999999999999432, 77.44184265367997000, -241.6694879557322508 ) ) ;
#198115=FACE_OUTER_BOUND ( 'NONE', #110478, .T. ) ;
#198133=AXIS2_PLACEMENT_3D ( 'NONE', #152116, #234178, #251167 ) ;
#198148=VERTEX_POINT ( 'NONE', #41650 ) ;
#198157=EDGE_CURVE ( 'NONE', #246455, #97895, #231198, .T. ) ;
#198171=PLANE ( 'NONE',  #162151 ) ;
#198185=LINE ( 'NONE', #217733, #68541 ) ;
#198217=ORIENTED_EDGE ( 'NONE', *, *, #104764, .F. ) ;
#198242=DIRECTION ( 'NONE',  ( 0.000000000000000000, 0.9634813093406718876, 0.2677755899091333047 ) ) ;
#198250=ORIENTED_EDGE ( 'NONE', *, *, #209159, .F. ) ;
#198270=VECTOR ( 'NONE', #24446, 1000.000000000000114 ) ;
#198279=AXIS2_PLACEMENT_3D ( 'NONE', #63307, #103702, #142828 ) ;
#198289=CARTESIAN_POINT ( 'NONE',  ( -23.15000000000000213, 55.39363411790988323, -234.6384634766556303 ) ) ;
#198293=DIRECTION ( 'NONE',  ( 1.000000000000000000, 0.000000000000000000, 0.000000000000000000 ) ) ;
#198299=DIRECTION ( 'NONE',  ( 1.000000000000000000, 6.834672213024256725E-16, -4.941700349840508052E-16 ) ) ;
#198314=DIRECTION ( 'NONE',  ( 1.000000000000000000, 2.986185139342066440E-16, -6.665775143889693760E-16 ) ) ;
#198322=ORIENTED_EDGE ( 'NONE', *, *, #100494, .T. ) ;
#198328=VECTOR ( 'NONE', #219633, 1000.000000000000227 ) ;
#198329=DIRECTION ( 'NONE',  ( 1.000000000000000000, 0.000000000000000000, -0.000000000000000000 ) ) ;
#198338=VERTEX_POINT ( 'NONE', #40391 ) ;
#198346=AXIS2_PLACEMENT_3D ( 'NONE', #102411, #116877, #97268 ) ;
#198354=CARTESIAN_POINT ( 'NONE',  ( 19.75857864376268935, 54.57427006634497957, -228.7596887170734306 ) ) ;
#198355=ORIENTED_EDGE ( 'NONE', *, *, #60868, .F. ) ;
#198363=ORIENTED_EDGE ( 'NONE', *, *, #230682, .T. ) ;
#198384=CIRCLE ( 'NONE', #152626, 0.5999999999999968692 ) ;
#198391=ORIENTED_EDGE ( 'NONE', *, *, #68943, .F. ) ;
#198395=CYLINDRICAL_SURFACE ( 'NONE', #220019, 0.09999999999998002154 ) ;
#198409=ORIENTED_EDGE ( 'NONE', *, *, #96693, .T. ) ;
#198412=DIRECTION ( 'NONE',  ( -1.000000000000000000, -6.649824375826082804E-14, -1.991473509853015959E-14 ) ) ;
#198460=DIRECTION ( 'NONE',  ( 6.484947573744956454E-15, -0.03803313543129139412, 0.9992764785629977276 ) ) ;
#198465=CIRCLE ( 'NONE', #86010, 0.1000000000000024342 ) ;
#198468=VERTEX_POINT ( 'NONE', #70213 ) ;
#198487=DIRECTION ( 'NONE',  ( 0.000000000000000000, -0.4088369013363281623, 0.9126074666063771490 ) ) ;
#198488=DIRECTION ( 'NONE',  ( 1.000000000000000000, 0.000000000000000000, 0.000000000000000000 ) ) ;
#198490=EDGE_CURVE ( 'NONE', #215970, #247446, #25931, .T. ) ;
#198498=EDGE_CURVE ( 'NONE', #52160, #217616, #118947, .T. ) ;
#198513=EDGE_LOOP ( 'NONE', ( #37373, #50483, #62387 ) ) ;
#198535=VERTEX_POINT ( 'NONE', #165444 ) ;
#198552=LINE ( 'NONE', #19942, #180590 ) ;
#198553=EDGE_CURVE ( 'NONE', #121939, #176943, #80927, .T. ) ;
#198557=AXIS2_PLACEMENT_3D ( 'NONE', #51847, #66308, #28508 ) ;
#198558=AXIS2_PLACEMENT_3D ( 'NONE', #182580, #129017, #48173 ) ;
#198609=CARTESIAN_POINT ( 'NONE',  ( 23.14999999999999503, 51.24799949642838470, -230.1402408152235637 ) ) ;
#198624=DIRECTION ( 'NONE',  ( 1.000000000000000000, 0.000000000000000000, 0.000000000000000000 ) ) ;
#198644=ORIENTED_EDGE ( 'NONE', *, *, #201677, .T. ) ;
#198676=CARTESIAN_POINT ( 'NONE',  ( 21.13422380239047271, 34.00421293006652235, -243.6253044407205550 ) ) ;
#198681=DIRECTION ( 'NONE',  ( 2.952720810173288619E-16, 0.4088369013363239990, -0.9126074666063788143 ) ) ;
#198691=ADVANCED_FACE ( 'NONE', ( #218659 ), #177341, .T. ) ;
#198704=CARTESIAN_POINT ( 'NONE',  ( 21.14999999999999858, 47.74710514101221293, -244.5837943500090716 ) ) ;
#198744=CARTESIAN_POINT ( 'NONE',  ( 20.94999999999999929, 68.96522873961046685, -235.0783363939394235 ) ) ;
#198763=DIRECTION ( 'NONE',  ( -0.000000000000000000, -0.9126074666063770380, -0.4088369013363281068 ) ) ;
#198769=ADVANCED_FACE ( 'NONE', ( #72136 ), #150386, .F. ) ;
#198773=SPHERICAL_SURFACE ( 'NONE', #42598, 0.1000000000000000056 ) ;
#198782=CIRCLE ( 'NONE', #232140, 0.09999999999999939493 ) ;
#198802=EDGE_CURVE ( 'NONE', #57244, #133691, #147813, .T. ) ;
#198826=CARTESIAN_POINT ( 'NONE',  ( 23.14999999999999503, 45.11960049378627247, -238.4740710069430349 ) ) ;
#198841=ORIENTED_EDGE ( 'NONE', *, *, #79021, .F. ) ;
#198842=CIRCLE ( 'NONE', #86382, 0.1000000000000024342 ) ;
#198854=CARTESIAN_POINT ( 'NONE',  ( -18.50000000000000000, 47.95459712139159336, -246.5019368548292675 ) ) ;
#198869=VERTEX_POINT ( 'NONE', #53841 ) ;
#198875=CARTESIAN_POINT ( 'NONE',  ( 22.59080734064467677, 31.82702841783752845, -238.8405965839959606 ) ) ;
#198881=ORIENTED_EDGE ( 'NONE', *, *, #211335, .F. ) ;
#198902=CIRCLE ( 'NONE', #128188, 0.1000000000000024342 ) ;
#198923=VECTOR ( 'NONE', #156484, 1000.000000000000114 ) ;
#198940=DIRECTION ( 'NONE',  ( 0.000000000000000000, 0.4088369013363345461, -0.9126074666063741514 ) ) ;
#198963=AXIS2_PLACEMENT_3D ( 'NONE', #65938, #142876, #42513 ) ;
#198971=ADVANCED_FACE ( 'NONE', ( #160673 ), #114455, .T. ) ;
#198975=ORIENTED_EDGE ( 'NONE', *, *, #30786, .F. ) ;
#199006=ORIENTED_EDGE ( 'NONE', *, *, #223879, .T. ) ;
#199025=ORIENTED_EDGE ( 'NONE', *, *, #239227, .T. ) ;
#199038=CARTESIAN_POINT ( 'NONE',  ( -22.50000000000000000, 29.50811709945089945, -252.6450601445781103 ) ) ;
#199042=CIRCLE ( 'NONE', #36761, 0.09999999999999108213 ) ;
#199049=DIRECTION ( 'NONE',  ( 0.000000000000000000, -0.9126074666063660468, -0.4088369013363524762 ) ) ;
#199050=CYLINDRICAL_SURFACE ( 'NONE', #248352, 0.09999999999999609201 ) ;
#199078=DIRECTION ( 'NONE',  ( 0.000000000000000000, -0.9126074666062392593, -0.4088369013366354165 ) ) ;
#199085=EDGE_LOOP ( 'NONE', ( #114603, #900, #71649, #190028 ) ) ;
#199087=FACE_OUTER_BOUND ( 'NONE', #164635, .T. ) ;
#199099=CIRCLE ( 'NONE', #140841, 0.09999999999999063804 ) ;
#199114=AXIS2_PLACEMENT_3D ( 'NONE', #224753, #129527, #29185 ) ;
#199115=CARTESIAN_POINT ( 'NONE',  ( -18.43634282235113275, 77.26728940060307593, -241.9658523025645707 ) ) ;
#199123=CARTESIAN_POINT ( 'NONE',  ( -18.50000000000000000, 47.93499546395150190, -254.9093547331817717 ) ) ;
#199172=FACE_OUTER_BOUND ( 'NONE', #63554, .T. ) ;
#199187=EDGE_CURVE ( 'NONE', #169719, #148485, #101948, .T. ) ;
#199214=CYLINDRICAL_SURFACE ( 'NONE', #155999, 11.79999999999999538 ) ;
#199246=CIRCLE ( 'NONE', #153493, 0.6000000000000187406 ) ;
#199247=CARTESIAN_POINT ( 'NONE',  ( -23.15000000000000213, 47.91013932883114990, -242.3192343197862044 ) ) ;
#199256=CARTESIAN_POINT ( 'NONE',  ( -23.15000000000000213, 36.65892442174472876, -249.5511627012454596 ) ) ;
#199265=FACE_OUTER_BOUND ( 'NONE', #231142, .T. ) ;
#199293=DIRECTION ( 'NONE',  ( -1.000000000000000000, 1.207181226542539700E-16, -2.694675058168174199E-16 ) ) ;
#199334=DIRECTION ( 'NONE',  ( 1.000000000000000000, 0.000000000000000000, 0.000000000000000000 ) ) ;
#199382=B_SPLINE_CURVE_WITH_KNOTS ( 'NONE', 3,
 ( #160400, #237347, #79525, #138213, #3864, #61272, #83368, #222898, #44287, #217751 ),
 .UNSPECIFIED., .F., .F.,
 ( 4, 2, 2, 2, 4 ),
 ( 0.000000000000000000, 4.221631689688066147E-05, 8.443263379376132294E-05, 0.0001688652675874656168, 0.0003377305351749607782 ),
 .UNSPECIFIED. ) ;
#199402=CARTESIAN_POINT ( 'NONE',  ( 22.47071067811865319, 33.41224047107334627, -242.5462774987836667 ) ) ;
#199410=DIRECTION ( 'NONE',  ( 0.000000000000000000, 0.09425075112713271475, 0.9955484899852801162 ) ) ;
#199413=ORIENTED_EDGE ( 'NONE', *, *, #20345, .F. ) ;
#199437=CARTESIAN_POINT ( 'NONE',  ( 21.07928932188134397, 30.84304088367083097, -252.0482413927653340 ) ) ;
#199443=AXIS2_PLACEMENT_3D ( 'NONE', #142012, #122472, #247204 ) ;
#199454=VERTEX_POINT ( 'NONE', #199485 ) ;
#199464=DIRECTION ( 'NONE',  ( 1.000000000000000000, 0.000000000000000000, 0.000000000000000000 ) ) ;
#199474=DIRECTION ( 'NONE',  ( 0.000000000000000000, 0.9126074666063772600, 0.4088369013363274407 ) ) ;
#199476=CARTESIAN_POINT ( 'NONE',  ( 23.24999999999999289, 53.46521213003792639, -234.8449159514430846 ) ) ;
#199485=CARTESIAN_POINT ( 'NONE',  ( -20.54999999999999716, 53.03738849591485405, -234.3791188517465400 ) ) ;
#199504=VECTOR ( 'NONE', #93674, 1000.000000000000114 ) ;
#199511=ORIENTED_EDGE ( 'NONE', *, *, #174534, .F. ) ;
#199528=LINE ( 'NONE', #40473, #243364 ) ;
#199562=EDGE_CURVE ( 'NONE', #252869, #3898, #110630, .T. ) ;
#199572=CARTESIAN_POINT ( 'NONE',  ( 20.85000000000000142, 56.23643450586807546, -227.9054833905874204 ) ) ;
#199579=ORIENTED_EDGE ( 'NONE', *, *, #20342, .T. ) ;
#199593=CARTESIAN_POINT ( 'NONE',  ( 18.59999999999999076, 54.57427006634497957, -228.7596887170734306 ) ) ;
#199613=AXIS2_PLACEMENT_3D ( 'NONE', #152911, #210294, #15967 ) ;
#199647=AXIS2_PLACEMENT_3D ( 'NONE', #32453, #113232, #53269 ) ;
#199686=LINE ( 'NONE', #185236, #227861 ) ;
#199700=ORIENTED_EDGE ( 'NONE', *, *, #197979, .T. ) ;
#199703=ORIENTED_EDGE ( 'NONE', *, *, #5102, .T. ) ;
#199707=CARTESIAN_POINT ( 'NONE',  ( -22.39999999999999858, 29.50811709945089945, -252.6450601445781103 ) ) ;
#199708=DIRECTION ( 'NONE',  ( 0.000000000000000000, 0.9126074666063772600, 0.4088369013363277182 ) ) ;
#199731=CARTESIAN_POINT ( 'NONE',  ( 23.15000000000000213, 52.64219947837469959, -255.2660483925003803 ) ) ;
#199737=ORIENTED_EDGE ( 'NONE', *, *, #229842, .F. ) ;
#199744=LINE ( 'NONE', #240141, #230487 ) ;
#199758=AXIS2_PLACEMENT_3D ( 'NONE', #29582, #33442, #192476 ) ;
#199761=ORIENTED_EDGE ( 'NONE', *, *, #210642, .F. ) ;
#199774=AXIS2_PLACEMENT_3D ( 'NONE', #33919, #14332, #251631 ) ;
#199783=TOROIDAL_SURFACE ( 'NONE', #112296, 0.4000000000000005773, 0.1000000000000000056 ) ;
#199792=DIRECTION ( 'NONE',  ( 0.000000000000000000, 0.4088369013362170290, -0.9126074666064267760 ) ) ;
#199810=CARTESIAN_POINT ( 'NONE',  ( -22.50000000000000000, 31.81502280147385164, -238.9558108736092095 ) ) ;
#199811=AXIS2_PLACEMENT_3D ( 'NONE', #187286, #188545, #9903 ) ;
#199828=DIRECTION ( 'NONE',  ( 0.000000000000000000, 0.9126074666063767049, 0.4088369013363286619 ) ) ;
#199835=CARTESIAN_POINT ( 'NONE',  ( -23.25000000000000000, 69.16514130714681130, -247.7543978865853660 ) ) ;
#199841=CARTESIAN_POINT ( 'NONE',  ( 23.25000000000000000, 30.73962027982165424, -265.0781340245722504 ) ) ;
#199848=CARTESIAN_POINT ( 'NONE',  ( -20.64999999999999858, 48.98768910550766975, -253.5949463715719787 ) ) ;
#199893=ORIENTED_EDGE ( 'NONE', *, *, #90581, .T. ) ;
#199902=ADVANCED_FACE ( 'NONE', ( #86877 ), #8654, .F. ) ;
#199937=AXIS2_PLACEMENT_3D ( 'NONE', #220843, #202575, #183027 ) ;
#199964=EDGE_CURVE ( 'NONE', #257664, #129332, #202303, .T. ) ;
#200014=CARTESIAN_POINT ( 'NONE',  ( -21.05000000000000426, 34.10212959586274195, -243.5992781215346099 ) ) ;
#200015=DIRECTION ( 'NONE',  ( 0.000000000000000000, -0.4088369013362965210, 0.9126074666063913599 ) ) ;
#200035=EDGE_CURVE ( 'NONE', #74293, #51580, #45207, .T. ) ;
#200040=CARTESIAN_POINT ( 'NONE',  ( 18.59999999999999076, 67.75954444190071513, -227.8703747234148693 ) ) ;
#200044=EDGE_CURVE ( 'NONE', #243903, #3898, #234111, .T. ) ;
#200053=DIRECTION ( 'NONE',  ( 1.000000000000000000, 0.000000000000000000, 0.000000000000000000 ) ) ;
#200079=CARTESIAN_POINT ( 'NONE',  ( -21.14999999999999858, 36.65892442174472876, -249.5511627012454596 ) ) ;
#200086=DIRECTION ( 'NONE',  ( -1.000000000000000000, 0.000000000000000000, 0.000000000000000000 ) ) ;
#200087=DIRECTION ( 'NONE',  ( 0.000000000000000000, 0.9126074666063764829, 0.4088369013363294391 ) ) ;
#200090=VECTOR ( 'NONE', #231194, 1000.000000000000114 ) ;
#200102=EDGE_LOOP ( 'NONE', ( #2146, #217498, #149088, #101115 ) ) ;
#200103=ORIENTED_EDGE ( 'NONE', *, *, #35358, .T. ) ;
#200129=EDGE_LOOP ( 'NONE', ( #56550, #50582, #189722, #114525 ) ) ;
#200164=( BOUNDED_CURVE ( )  B_SPLINE_CURVE ( 3, ( #172196, #114742, #15670, #71785 ),
 .UNSPECIFIED., .F., .F. ) 
 B_SPLINE_CURVE_WITH_KNOTS ( ( 4, 4 ),
 ( 6.664455228996977694E-14, 1.570796326794907438 ),
 .UNSPECIFIED. ) 
 CURVE ( )  GEOMETRIC_REPRESENTATION_ITEM ( )  RATIONAL_B_SPLINE_CURVE ( ( 1.000000000000000000, 0.8047378541243781491, 0.8047378541243781491, 1.000000000000000000 ) ) 
 REPRESENTATION_ITEM ( '' )  );
#200184=DIRECTION ( 'NONE',  ( 4.504528286903032433E-15, 0.9579639084728162057, 0.2868887416115976086 ) ) ;
#200192=EDGE_LOOP ( 'NONE', ( #173099, #143726, #4777, #207536 ) ) ;
#200204=ADVANCED_FACE ( 'NONE', ( #41084 ), #42347, .T. ) ;
#200211=FACE_OUTER_BOUND ( 'NONE', #133200, .T. ) ;
#200214=DIRECTION ( 'NONE',  ( 0.000000000000000000, -0.9126074666063795915, -0.4088369013363224447 ) ) ;
#200223=CARTESIAN_POINT ( 'NONE',  ( 22.49436431346199683, 25.99973956953803622, -254.2530358866374343 ) ) ;
#200227=VECTOR ( 'NONE', #66006, 1000.000000000000114 ) ;
#200248=FACE_OUTER_BOUND ( 'NONE', #151931, .T. ) ;
#200264=AXIS2_PLACEMENT_3D ( 'NONE', #152073, #213291, #114202 ) ;
#200269=CARTESIAN_POINT ( 'NONE',  ( -23.15000000000000213, 45.96866462019919197, -240.6139518702713360 ) ) ;
#200282=ORIENTED_EDGE ( 'NONE', *, *, #9682, .T. ) ;
#200300=CARTESIAN_POINT ( 'NONE',  ( 20.12518398540832010, 39.87855921381013502, -237.1784891853482122 ) ) ;
#200304=FACE_OUTER_BOUND ( 'NONE', #228903, .T. ) ;
#200343=CIRCLE ( 'NONE', #142068, 11.74999999999999822 ) ;
#200350=DIRECTION ( 'NONE',  ( 0.000000000000000000, 0.9126074666063844765, 0.4088369013363114535 ) ) ;
#200361=CARTESIAN_POINT ( 'NONE',  ( -18.50000000000000000, 46.55954744353147134, -243.3218549665227783 ) ) ;
#200367=CARTESIAN_POINT ( 'NONE',  ( -18.50000000000000000, 74.93036000061670165, -233.6816308724374949 ) ) ;
#200369=ORIENTED_EDGE ( 'NONE', *, *, #111592, .F. ) ;
#200401=CARTESIAN_POINT ( 'NONE',  ( -18.41817142474032565, 77.14152309475025504, -241.8237690616388420 ) ) ;
#200415=TOROIDAL_SURFACE ( 'NONE', #112927, 7.800000000000000711, 0.1000000000000000056 ) ;
#200434=CARTESIAN_POINT ( 'NONE',  ( 23.24999999999999645, 67.23127455305835554, -235.8551265064784559 ) ) ;
#200446=EDGE_CURVE ( 'NONE', #198148, #227337, #227597, .T. ) ;
#200472=CARTESIAN_POINT ( 'NONE',  ( 21.08884785362045378, 34.01443675994195814, -243.7698937337987104 ) ) ;
#200490=CARTESIAN_POINT ( 'NONE',  ( 20.94999999999999574, 46.54031271043911033, -243.0982672308888368 ) ) ;
#200503=CARTESIAN_POINT ( 'NONE',  ( 18.50000000000000000, 77.35494420175977837, -241.6200040285045532 ) ) ;
#200517=DIRECTION ( 'NONE',  ( 1.000000000000000000, 0.000000000000000000, 0.000000000000000000 ) ) ;
#200519=CARTESIAN_POINT ( 'NONE',  ( 18.51565452909138543, 47.04884642058242150, -255.1451075356969795 ) ) ;
#200525=CARTESIAN_POINT ( 'NONE',  ( -18.59999999999999787, 74.83412143252222393, -233.7087995678629966 ) ) ;
#200582=ORIENTED_EDGE ( 'NONE', *, *, #217476, .T. ) ;
#200596=ORIENTED_EDGE ( 'NONE', *, *, #244456, .T. ) ;
#200629=ORIENTED_EDGE ( 'NONE', *, *, #174319, .T. ) ;
#200646=CARTESIAN_POINT ( 'NONE',  ( -20.94983749550516450, 68.01715840423028681, -224.2192812407665201 ) ) ;
#200649=VERTEX_POINT ( 'NONE', #50670 ) ;
#200655=AXIS2_PLACEMENT_3D ( 'NONE', #74346, #172173, #15650 ) ;
#200676=EDGE_CURVE ( 'NONE', #241192, #97342, #240093, .T. ) ;
#200677=CARTESIAN_POINT ( 'NONE',  ( 21.05000000000000071, 69.28189128378591022, -247.5258150475912089 ) ) ;
#200715=CIRCLE ( 'NONE', #234013, 0.09999999999999950595 ) ;
#200745=AXIS2_PLACEMENT_3D ( 'NONE', #44867, #141385, #65707 ) ;
#200804=DIRECTION ( 'NONE',  ( 0.000000000000000000, 0.9126074666063771490, 0.4088369013363281623 ) ) ;
#200812=VECTOR ( 'NONE', #214595, 1000.000000000000000 ) ;
#200814=VERTEX_POINT ( 'NONE', #83050 ) ;
#200835=CARTESIAN_POINT ( 'NONE',  ( 21.05000000000000071, 44.58277672189309015, -247.4925639031954745 ) ) ;
#200857=ORIENTED_EDGE ( 'NONE', *, *, #163245, .F. ) ;
#200864=FACE_OUTER_BOUND ( 'NONE', #226983, .T. ) ;
#200914=EDGE_LOOP ( 'NONE', ( #111840, #184166, #198975, #90294, #71426 ) ) ;
#200964=DIRECTION ( 'NONE',  ( 0.000000000000000000, -0.4088369013363281623, 0.9126074666063771490 ) ) ;
#200983=VERTEX_POINT ( 'NONE', #52943 ) ;
#201017=ORIENTED_EDGE ( 'NONE', *, *, #57498, .T. ) ;
#201035=CARTESIAN_POINT ( 'NONE',  ( 18.49999999999999289, 55.07829832934649517, -229.8847827466787521 ) ) ;
#201079=ADVANCED_FACE ( 'NONE', ( #231603 ), #254938, .T. ) ;
#201122=DIRECTION ( 'NONE',  ( 0.000000000000000000, 0.4088369013363281623, -0.9126074666063771490 ) ) ;
#201136=CARTESIAN_POINT ( 'NONE',  ( 23.14999999999999858, 53.62064951147646497, -235.8162552129080609 ) ) ;
#201149=VECTOR ( 'NONE', #87945, 1000.000000000000000 ) ;
#201189=CARTESIAN_POINT ( 'NONE',  ( -20.96077737575334865, 56.21923056145944742, -228.0513653586724558 ) ) ;
#201211=EDGE_LOOP ( 'NONE', ( #182798, #118550, #94065 ) ) ;
#201217=VERTEX_POINT ( 'NONE', #3229 ) ;
#201237=CARTESIAN_POINT ( 'NONE',  ( 21.04999999999999716, 34.01621449225257976, -243.6162460527932296 ) ) ;
#201340=DIRECTION ( 'NONE',  ( -2.978066053179068737E-16, -0.4088369013363267745, 0.9126074666063774821 ) ) ;
#201362=LINE ( 'NONE', #574, #198328 ) ;
#201481=ORIENTED_EDGE ( 'NONE', *, *, #26808, .T. ) ;
#201490=CARTESIAN_POINT ( 'NONE',  ( -21.05000000000000071, 46.45388641681647357, -243.1520440498138385 ) ) ;
#201498=ORIENTED_EDGE ( 'NONE', *, *, #227138, .F. ) ;
#201506=CARTESIAN_POINT ( 'NONE',  ( 20.94999675878240808, 68.00468331834515823, -224.2298952291173464 ) ) ;
#201512=CARTESIAN_POINT ( 'NONE',  ( -23.25000000000000000, 36.65892442174472876, -249.5511627012454596 ) ) ;
#201532=VERTEX_POINT ( 'NONE', #151329 ) ;
#201546=CYLINDRICAL_SURFACE ( 'NONE', #155952, 0.09999999999999939493 ) ;
#201556=EDGE_CURVE ( 'NONE', #203555, #58341, #235967, .T. ) ;
#201572=CARTESIAN_POINT ( 'NONE',  ( 20.21494484322108676, 40.46683321215910922, -237.6512114454242521 ) ) ;
#201591=CIRCLE ( 'NONE', #114102, 0.1000000000000024342 ) ;
#201615=ORIENTED_EDGE ( 'NONE', *, *, #175028, .T. ) ;
#201637=AXIS2_PLACEMENT_3D ( 'NONE', #163593, #142719, #27962 ) ;
#201642=DIRECTION ( 'NONE',  ( 1.000000000000000000, 0.000000000000000000, -0.000000000000000000 ) ) ;
#201656=DIRECTION ( 'NONE',  ( 0.000000000000000000, -0.9126074666063769270, -0.4088369013363280513 ) ) ;
#201667=CARTESIAN_POINT ( 'NONE',  ( -23.25000000000000000, 51.33926024308902214, -230.0993571250899379 ) ) ;
#201674=CARTESIAN_POINT ( 'NONE',  ( -18.33682934331483949, 77.42195030185330040, -241.7118189958663095 ) ) ;
#201677=EDGE_CURVE ( 'NONE', #128733, #218531, #182383, .T. ) ;
#201716=ADVANCED_FACE ( 'NONE', ( #86075 ), #99536, .F. ) ;
#201717=CARTESIAN_POINT ( 'NONE',  ( 20.94999999999999929, 54.36558989155976462, -236.3448031251562327 ) ) ;
#201726=EDGE_CURVE ( 'NONE', #214984, #232621, #74073, .T. ) ;
#201761=CARTESIAN_POINT ( 'NONE',  ( 21.14999999999999858, 21.13195309841794867, -243.6318585593223816 ) ) ;
#201781=ORIENTED_EDGE ( 'NONE', *, *, #126351, .T. ) ;
#201817=DIRECTION ( 'NONE',  ( 1.000000000000000000, 0.000000000000000000, 0.000000000000000000 ) ) ;
#201825=EDGE_CURVE ( 'NONE', #116784, #137324, #136559, .T. ) ;
#201839=DIRECTION ( 'NONE',  ( 0.000000000000000000, -0.4088369013362687654, 0.9126074666064034613 ) ) ;
#201843=LINE ( 'NONE', #81861, #54377 ) ;
#201865=CARTESIAN_POINT ( 'NONE',  ( -23.25000000000000000, 72.03510814376021187, -246.5782642391033903 ) ) ;
#201870=AXIS2_PLACEMENT_3D ( 'NONE', #171501, #227583, #192320 ) ;
#201890=ORIENTED_EDGE ( 'NONE', *, *, #87131, .F. ) ;
#201915=EDGE_CURVE ( 'NONE', #203994, #176131, #232285, .T. ) ;
#201918=EDGE_LOOP ( 'NONE', ( #130751, #173803, #79171, #202599, #2655, #11719, #49339, #249327, #12123, #179677, #85640, #39963 ) ) ;
#201929=FACE_OUTER_BOUND ( 'NONE', #190542, .T. ) ;
#201950=CARTESIAN_POINT ( 'NONE',  ( 18.31325810956139577, 77.39829188374345392, -241.7500340231811720 ) ) ;
#201954=CARTESIAN_POINT ( 'NONE',  ( 21.76363531954645936, 33.70142732455086332, -243.1915800643360512 ) ) ;
#201969=EDGE_CURVE ( 'NONE', #101051, #251464, #136742, .T. ) ;
#201994=EDGE_CURVE ( 'NONE', #136081, #84389, #28473, .T. ) ;
#202046=ADVANCED_FACE ( 'NONE', ( #85756 ), #187487, .T. ) ;
#202088=ORIENTED_EDGE ( 'NONE', *, *, #39884, .T. ) ;
#202107=CARTESIAN_POINT ( 'NONE',  ( -20.54999999999999716, 54.34471204062663219, -239.4366250215122420 ) ) ;
#202109=CARTESIAN_POINT ( 'NONE',  ( -21.08035267497491816, 30.84675532226686911, -252.0643358494183985 ) ) ;
#202125=EDGE_LOOP ( 'NONE', ( #191465, #21005, #210968, #188427 ) ) ;
#202138=EDGE_LOOP ( 'NONE', ( #253535, #170240, #54951, #119795 ) ) ;
#202147=ADVANCED_FACE ( 'NONE', ( #12708 ), #252557, .F. ) ;
#202184=CARTESIAN_POINT ( 'NONE',  ( 18.59999999999999076, 78.57744179526842743, -232.8011145694030972 ) ) ;
#202188=AXIS2_PLACEMENT_3D ( 'NONE', #157890, #219081, #78288 ) ;
#202197=CIRCLE ( 'NONE', #89753, 1.899999999999993028 ) ;
#202211=AXIS2_PLACEMENT_3D ( 'NONE', #221015, #99770, #179356 ) ;
#202303=CIRCLE ( 'NONE', #89865, 0.1000000000000024342 ) ;
#202317=CARTESIAN_POINT ( 'NONE',  ( 18.49999999999999289, 55.08862955830016261, -229.9605662146666134 ) ) ;
#202318=DIRECTION ( 'NONE',  ( -0.000000000000000000, 0.9126074666063770380, 0.4088369013363281068 ) ) ;
#202394=ORIENTED_EDGE ( 'NONE', *, *, #224465, .F. ) ;
#202409=CARTESIAN_POINT ( 'NONE',  ( -23.15000000000000213, 67.23127455305835554, -235.8551265064784559 ) ) ;
#202410=FACE_OUTER_BOUND ( 'NONE', #42264, .T. ) ;
#202431=CARTESIAN_POINT ( 'NONE',  ( 18.43565242384935132, 46.91436717984745286, -255.3877622108296066 ) ) ;
#202447=ADVANCED_FACE ( 'NONE', ( #172773 ), #112756, .F. ) ;
#202465=ORIENTED_EDGE ( 'NONE', *, *, #217818, .F. ) ;
#202475=ORIENTED_EDGE ( 'NONE', *, *, #145536, .T. ) ;
#202486=ORIENTED_EDGE ( 'NONE', *, *, #173834, .T. ) ;
#202537=CIRCLE ( 'NONE', #90098, 11.65000000000000213 ) ;
#202554=AXIS2_PLACEMENT_3D ( 'NONE', #200269, #219819, #236811 ) ;
#202560=CARTESIAN_POINT ( 'NONE',  ( 20.95429402530532315, 40.80824126842007615, -237.9661292884959778 ) ) ;
#202564=DIRECTION ( 'NONE',  ( 7.304098846218134667E-16, 0.4088369013363281068, -0.9126074666063770380 ) ) ;
#202575=DIRECTION ( 'NONE',  ( 0.000000000000000000, -0.9594490217226113726, -0.2818822000686178608 ) ) ;
#202576=CARTESIAN_POINT ( 'NONE',  ( 18.59999999999999787, 48.04585786805223080, -246.4610531646956417 ) ) ;
#202580=EDGE_CURVE ( 'NONE', #56413, #144623, #228538, .T. ) ;
#202581=CARTESIAN_POINT ( 'NONE',  ( -1.739115166359751170E-14, 54.57427006634497957, -228.7596887170734306 ) ) ;
#202594=EDGE_CURVE ( 'NONE', #9522, #49603, #57892, .T. ) ;
#202599=ORIENTED_EDGE ( 'NONE', *, *, #9129, .T. ) ;
#202606=DIRECTION ( 'NONE',  ( 0.000000000000000000, -0.4088369013363280513, 0.9126074666063769270 ) ) ;
#202613=EDGE_LOOP ( 'NONE', ( #170290, #169091, #133131, #248911, #198217, #96489, #69196, #234095, #34605, #69343, #249347, #2012 ) ) ;
#202622=DIRECTION ( 'NONE',  ( -1.000000000000000000, 1.335000415235278971E-16, -2.979993593738921214E-16 ) ) ;
#202635=CARTESIAN_POINT ( 'NONE',  ( -23.25000000000000000, 49.36776662947724503, -253.7196102226803021 ) ) ;
#202636=CARTESIAN_POINT ( 'NONE',  ( 20.85000000000000142, 67.23127455305835554, -235.8551265064784559 ) ) ;
#202655=AXIS2_PLACEMENT_3D ( 'NONE', #33954, #113439, #234672 ) ;
#202664=DIRECTION ( 'NONE',  ( 0.000000000000000000, -0.9126074666063545004, -0.4088369013363783999 ) ) ;
#202692=DIRECTION ( 'NONE',  ( 0.000000000000000000, 0.9126074666063772600, 0.4088369013363274407 ) ) ;
#202704=LINE ( 'NONE', #206564, #68371 ) ;
#202711=EDGE_LOOP ( 'NONE', ( #177285, #88662, #220076, #159449 ) ) ;
#202726=ADVANCED_FACE ( 'NONE', ( #103435 ), #142266, .F. ) ;
#202738=AXIS2_PLACEMENT_3D ( 'NONE', #142540, #205075, #146383 ) ;
#202782=CARTESIAN_POINT ( 'NONE',  ( 22.41477678272288188, 26.02708908150256661, -254.3131911847732454 ) ) ;
#202798=AXIS2_PLACEMENT_3D ( 'NONE', #73484, #76018, #115149 ) ;
#202837=ORIENTED_EDGE ( 'NONE', *, *, #256621, .F. ) ;
#202891=DIRECTION ( 'NONE',  ( -1.000000000000000000, 0.000000000000000000, 0.000000000000000000 ) ) ;
#202906=AXIS2_PLACEMENT_3D ( 'NONE', #66769, #224543, #147583 ) ;
#202926=CIRCLE ( 'NONE', #148781, 11.65000000000000213 ) ;
#202936=DIRECTION ( 'NONE',  ( 1.000000000000000000, 0.000000000000000000, 0.000000000000000000 ) ) ;
#202937=CIRCLE ( 'NONE', #48810, 0.09999999999999108213 ) ;
#202956=ADVANCED_FACE ( 'NONE', ( #36807 ), #95453, .T. ) ;
#202995=DIRECTION ( 'NONE',  ( 1.000000000000000000, -0.000000000000000000, -0.000000000000000000 ) ) ;
#203013=CIRCLE ( 'NONE', #90582, 4.149999999999993250 ) ;
#203016=ORIENTED_EDGE ( 'NONE', *, *, #156821, .F. ) ;
#203053=DIRECTION ( 'NONE',  ( -1.000000000000000000, 0.000000000000000000, 0.000000000000000000 ) ) ;
#203079=CARTESIAN_POINT ( 'NONE',  ( 18.46947024752492084, 46.92278096310428026, -255.3730018242404469 ) ) ;
#203102=CARTESIAN_POINT ( 'NONE',  ( 23.15000000000000213, 52.55093873171406216, -255.3069320826340061 ) ) ;
#203119=CARTESIAN_POINT ( 'NONE',  ( -20.64999999999999858, 54.27339256631721298, -236.8935360681107625 ) ) ;
#203134=CARTESIAN_POINT ( 'NONE',  ( -21.56666275994539816, 30.30957806568256885, -252.3955916421750203 ) ) ;
#203144=CARTESIAN_POINT ( 'NONE',  ( -22.60000000000081144, 25.91621687215759806, -254.3113673292270391 ) ) ;
#203193=CARTESIAN_POINT ( 'NONE',  ( 21.97500000000000497, 43.85220609964365224, -235.6449878604632886 ) ) ;
#203238=ORIENTED_EDGE ( 'NONE', *, *, #152237, .F. ) ;
#203245=CARTESIAN_POINT ( 'NONE',  ( 21.05000000000000071, 54.26566224370346703, -236.3486064386993633 ) ) ;
#203272=LINE ( 'NONE', #1196, #229660 ) ;
#203305=ORIENTED_EDGE ( 'NONE', *, *, #126195, .F. ) ;
#203312=CIRCLE ( 'NONE', #161639, 0.1999999999999987899 ) ;
#203313=DIRECTION ( 'NONE',  ( 0.000000000000000000, -0.4088369013363205573, 0.9126074666063803686 ) ) ;
#203318=LINE ( 'NONE', #123782, #152849 ) ;
#203389=ORIENTED_EDGE ( 'NONE', *, *, #132632, .F. ) ;
#203395=CARTESIAN_POINT ( 'NONE',  ( -21.09316766718153247, 30.82942261761470704, -252.1196843684382429 ) ) ;
#203411=ORIENTED_EDGE ( 'NONE', *, *, #19361, .F. ) ;
#203412=AXIS2_PLACEMENT_3D ( 'NONE', #36435, #41566, #121110 ) ;
#203432=ORIENTED_EDGE ( 'NONE', *, *, #135028, .F. ) ;
#203471=DIRECTION ( 'NONE',  ( -1.836970198721030427E-16, -0.4088369013363281623, 0.9126074666063771490 ) ) ;
#203481=VECTOR ( 'NONE', #177659, 1000.000000000000114 ) ;
#203518=CARTESIAN_POINT ( 'NONE',  ( 20.94999999999999929, 45.65843669757526158, -240.2045374387683410 ) ) ;
#203541=PLANE ( 'NONE',  #17014 ) ;
#203555=VERTEX_POINT ( 'NONE', #125928 ) ;
#203561=CARTESIAN_POINT ( 'NONE',  ( -21.14999999999999858, 31.98723526783714988, -238.8784020251475511 ) ) ;
#203627=LINE ( 'NONE', #25018, #21987 ) ;
#203646=AXIS2_PLACEMENT_3D ( 'NONE', #129136, #31354, #208690 ) ;
#203693=DIRECTION ( 'NONE',  ( 0.000000000000000000, 0.2818822000685679008, -0.9594490217226259166 ) ) ;
#203730=ORIENTED_EDGE ( 'NONE', *, *, #112161, .T. ) ;
#203735=CARTESIAN_POINT ( 'NONE',  ( 21.00000000000000000, 43.94346684630428967, -235.6041041703296344 ) ) ;
#203763=CARTESIAN_POINT ( 'NONE',  ( 23.24999999999999289, 51.38014393322265505, -230.1906178717505327 ) ) ;
#203801=DIRECTION ( 'NONE',  ( 0.000000000000000000, 0.9126074666063660468, 0.4088369013363524762 ) ) ;
#203829=DIRECTION ( 'NONE',  ( 1.000000000000000000, -1.207181226542539700E-16, 2.694675058168174199E-16 ) ) ;
#203836=CARTESIAN_POINT ( 'NONE',  ( 21.05000000000000071, 40.88152484246180052, -238.0427780438910759 ) ) ;
#203837=LINE ( 'NONE', #145137, #147719 ) ;
#203839=DIRECTION ( 'NONE',  ( 0.000000000000000000, -0.9126074666063771490, -0.4088369013363281623 ) ) ;
#203880=CARTESIAN_POINT ( 'NONE',  ( 23.24999999999997513, 56.02567683926420727, -227.9999002286038774 ) ) ;
#203897=AXIS2_PLACEMENT_3D ( 'NONE', #43965, #46514, #132490 ) ;
#203920=EDGE_CURVE ( 'NONE', #182190, #15852, #171234, .T. ) ;
#203936=FACE_OUTER_BOUND ( 'NONE', #50128, .T. ) ;
#203951=PLANE ( 'NONE',  #174674 ) ;
#203954=CARTESIAN_POINT ( 'NONE',  ( 20.85000000000000142, 78.55027968977005060, -232.7019340424676841 ) ) ;
#203972=CARTESIAN_POINT ( 'NONE',  ( 23.14999999999999147, 36.65892442174472876, -249.5511627012454596 ) ) ;
#203976=DIRECTION ( 'NONE',  ( 1.000000000000000000, 0.000000000000000000, 0.000000000000000000 ) ) ;
#203994=VERTEX_POINT ( 'NONE', #132057 ) ;
#203996=ADVANCED_FACE ( 'NONE', ( #211603 ), #209028, .F. ) ;
#204022=DIRECTION ( 'NONE',  ( -0.000000000000000000, 0.9579639084728051035, 0.2868887416116349121 ) ) ;
#204058=DIRECTION ( 'NONE',  ( -1.000000000000000000, 1.207181226542539700E-16, -2.694675058168174199E-16 ) ) ;
#204064=ORIENTED_EDGE ( 'NONE', *, *, #122270, .F. ) ;
#204069=FACE_OUTER_BOUND ( 'NONE', #44957, .T. ) ;
#204078=ORIENTED_EDGE ( 'NONE', *, *, #54465, .T. ) ;
#204090=AXIS2_PLACEMENT_3D ( 'NONE', #40029, #14026, #34893 ) ;
#204099=ORIENTED_EDGE ( 'NONE', *, *, #14035, .T. ) ;
#204109=CARTESIAN_POINT ( 'NONE',  ( 20.95262331984758575, 39.26456045904023284, -236.8738201967949806 ) ) ;
#204123=ORIENTED_EDGE ( 'NONE', *, *, #154390, .T. ) ;
#204169=AXIS2_PLACEMENT_3D ( 'NONE', #94237, #250743, #111244 ) ;
#204186=ORIENTED_EDGE ( 'NONE', *, *, #52927, .F. ) ;
#204201=EDGE_CURVE ( 'NONE', #120786, #60871, #220332, .T. ) ;
#204207=EDGE_LOOP ( 'NONE', ( #115734, #227409, #92815 ) ) ;
#204266=CIRCLE ( 'NONE', #41817, 7.900000000000009237 ) ;
#204268=DIRECTION ( 'NONE',  ( 0.000000000000000000, -0.9947597004326491632, 0.1022405907413782566 ) ) ;
#204288=CARTESIAN_POINT ( 'NONE',  ( -18.59999999999999787, 67.23127455305835554, -235.8551265064784559 ) ) ;
#204324=LINE ( 'NONE', #25706, #11349 ) ;
#204334=CIRCLE ( 'NONE', #54507, 0.09999999999999939493 ) ;
#204360=TOROIDAL_SURFACE ( 'NONE', #179446, 11.70000000000000107, 0.1000000000000000056 ) ;
#204371=DIRECTION ( 'NONE',  ( 0.000000000000000000, -0.1569827930593259702, 0.9876013379310970564 ) ) ;
#204403=ORIENTED_EDGE ( 'NONE', *, *, #197703, .T. ) ;
#204439=ORIENTED_EDGE ( 'NONE', *, *, #76553, .F. ) ;
#204455=VECTOR ( 'NONE', #171644, 1000.000000000000000 ) ;
#204476=CARTESIAN_POINT ( 'NONE',  ( 18.49999999999999289, 54.98105481382776816, -230.1569079895687366 ) ) ;
#204493=CARTESIAN_POINT ( 'NONE',  ( 18.43630871534895732, 77.26727690582558239, -241.9658728844706559 ) ) ;
#204531=DIRECTION ( 'NONE',  ( -0.7071067811865475727, 0.2890913453342130457, -0.6453109281988448354 ) ) ;
#204539=ORIENTED_EDGE ( 'NONE', *, *, #95071, .F. ) ;
#204541=CIRCLE ( 'NONE', #62898, 0.09999999999999609201 ) ;
#204586=DIRECTION ( 'NONE',  ( 0.000000000000000000, 0.9126074666063920260, 0.4088369013362946891 ) ) ;
#204596=CARTESIAN_POINT ( 'NONE',  ( 20.95017935633852346, 39.29138598153966910, -236.8932159614766420 ) ) ;
#204600=ORIENTED_EDGE ( 'NONE', *, *, #219609, .T. ) ;
#204608=CIRCLE ( 'NONE', #212991, 12.97499999999999254 ) ;
#204642=ORIENTED_EDGE ( 'NONE', *, *, #171245, .T. ) ;
#204656=CIRCLE ( 'NONE', #63007, 0.1000000000000024342 ) ;
#204689=DIRECTION ( 'NONE',  ( -0.000000000000000000, 0.4088369013363297166, -0.9126074666063763718 ) ) ;
#204690=ORIENTED_EDGE ( 'NONE', *, *, #183164, .F. ) ;
#204694=CARTESIAN_POINT ( 'NONE',  ( -23.15000000000000213, 69.20602499728043711, -247.8456586332460176 ) ) ;
#204696=CARTESIAN_POINT ( 'NONE',  ( -21.05000000000000071, 43.10494791715829166, -239.6505508802563327 ) ) ;
#204704=ORIENTED_EDGE ( 'NONE', *, *, #168463, .F. ) ;
#204706=ORIENTED_EDGE ( 'NONE', *, *, #198498, .F. ) ;
#204751=ORIENTED_EDGE ( 'NONE', *, *, #155700, .T. ) ;
#204752=EDGE_CURVE ( 'NONE', #222344, #197418, #71502, .T. ) ;
#204754=CARTESIAN_POINT ( 'NONE',  ( 23.14999999999999503, 53.42432843990430058, -234.7536552047824330 ) ) ;
#204798=DIRECTION ( 'NONE',  ( -1.000000000000000000, -0.000000000000000000, 0.000000000000000000 ) ) ;
#204852=ORIENTED_EDGE ( 'NONE', *, *, #63303, .F. ) ;
#204876=AXIS2_PLACEMENT_3D ( 'NONE', #251956, #231139, #73356 ) ;
#204897=ADVANCED_FACE ( 'NONE', ( #251389 ), #133199, .F. ) ;
#204899=DIRECTION ( 'NONE',  ( -0.000000000000000000, 0.9126074666063770380, 0.4088369013363281068 ) ) ;
#204911=CARTESIAN_POINT ( 'NONE',  ( -20.64999999999999858, 53.12864924257549148, -234.3382351616128858 ) ) ;
#204922=CARTESIAN_POINT ( 'NONE',  ( 18.59999999999998721, 67.84340367245323478, -228.0791829662263410 ) ) ;
#204928=CIRCLE ( 'NONE', #246629, 4.050000000000006040 ) ;
#204929=FACE_OUTER_BOUND ( 'NONE', #74407, .T. ) ;
#204934=ORIENTED_EDGE ( 'NONE', *, *, #217507, .F. ) ;
#204951=DIRECTION ( 'NONE',  ( -0.000000000000000000, 0.9594490217226120388, 0.2818822000686155849 ) ) ;
#205017=CARTESIAN_POINT ( 'NONE',  ( -20.99780126800934354, 56.17802974602408739, -228.0901074916681637 ) ) ;
#205021=DIRECTION ( 'NONE',  ( -1.000000000000000000, 0.000000000000000000, 0.000000000000000000 ) ) ;
#205040=ORIENTED_EDGE ( 'NONE', *, *, #94170, .F. ) ;
#205075=DIRECTION ( 'NONE',  ( 1.000000000000000000, -1.335000415235278971E-16, 2.979993593738921214E-16 ) ) ;
#205083=DIRECTION ( 'NONE',  ( 0.000000000000000000, -0.9955484899852801162, 0.09425075112713271475 ) ) ;
#205103=LINE ( 'NONE', #126880, #255239 ) ;
#205151=DIRECTION ( 'NONE',  ( 0.000000000000000000, -0.4088369013363280513, 0.9126074666063769270 ) ) ;
#205168=CYLINDRICAL_SURFACE ( 'NONE', #2339, 0.1000000000000024342 ) ;
#205204=DIRECTION ( 'NONE',  ( 0.000000000000000000, 0.9126074666063753726, 0.4088369013363317150 ) ) ;
#205205=FACE_OUTER_BOUND ( 'NONE', #190604, .T. ) ;
#205250=ORIENTED_EDGE ( 'NONE', *, *, #205798, .F. ) ;
#205261=DIRECTION ( 'NONE',  ( 0.000000000000000000, -0.4088369013363783999, 0.9126074666063545004 ) ) ;
#205264=ADVANCED_FACE ( 'NONE', ( #108974 ), #158526, .F. ) ;
#205278=ORIENTED_EDGE ( 'NONE', *, *, #143355, .T. ) ;
#205300=EDGE_LOOP ( 'NONE', ( #6882, #223546, #169693, #44173 ) ) ;
#205308=ADVANCED_FACE ( 'NONE', ( #32047 ), #171562, .F. ) ;
#205313=ORIENTED_EDGE ( 'NONE', *, *, #137670, .F. ) ;
#205320=CARTESIAN_POINT ( 'NONE',  ( 22.39999999999999503, 29.54900078958455367, -252.7363208912387051 ) ) ;
#205327=AXIS2_PLACEMENT_3D ( 'NONE', #67248, #226299, #100582 ) ;
#205372=EDGE_CURVE ( 'NONE', #119433, #175127, #115860, .T. ) ;
#205383=CARTESIAN_POINT ( 'NONE',  ( 20.95429693346636668, 39.24855018340224433, -236.8380961568129806 ) ) ;
#205388=ORIENTED_EDGE ( 'NONE', *, *, #124211, .F. ) ;
#205402=AXIS2_PLACEMENT_3D ( 'NONE', #196721, #170805, #250286 ) ;
#205502=AXIS2_PLACEMENT_3D ( 'NONE', #126673, #67981, #87527 ) ;
#205539=CARTESIAN_POINT ( 'NONE',  ( -23.24999999999999645, 77.17949092533254429, -241.9177572069595783 ) ) ;
#205558=CARTESIAN_POINT ( 'NONE',  ( -21.44999999999999929, 52.95562111564758823, -234.1965973584252652 ) ) ;
#205581=DIRECTION ( 'NONE',  ( 0.000000000000000000, 0.9126074666063813678, 0.4088369013363182813 ) ) ;
#205634=ORIENTED_EDGE ( 'NONE', *, *, #44341, .F. ) ;
#205640=AXIS2_PLACEMENT_3D ( 'NONE', #13622, #87989, #167580 ) ;
#205645=EDGE_CURVE ( 'NONE', #185809, #149671, #17062, .T. ) ;
#205651=DIRECTION ( 'NONE',  ( 0.000000000000000000, 0.9126074666063844765, 0.4088369013363114535 ) ) ;
#205652=EDGE_CURVE ( 'NONE', #168551, #228214, #252043, .T. ) ;
#205653=ORIENTED_EDGE ( 'NONE', *, *, #137353, .F. ) ;
#205697=CARTESIAN_POINT ( 'NONE',  ( -18.59999999999999787, 52.13794731297493712, -232.3713824252124880 ) ) ;
#205699=CARTESIAN_POINT ( 'NONE',  ( -20.54999999999999716, 69.05648948627111849, -235.0374527038057977 ) ) ;
#205702=AXIS2_PLACEMENT_3D ( 'NONE', #114436, #250098, #230540 ) ;
#205744=AXIS2_PLACEMENT_3D ( 'NONE', #53214, #228002, #171917 ) ;
#205795=AXIS2_PLACEMENT_3D ( 'NONE', #242440, #63826, #183771 ) ;
#205798=EDGE_CURVE ( 'NONE', #226069, #152713, #46899, .T. ) ;
#205825=AXIS2_PLACEMENT_3D ( 'NONE', #63978, #123961, #183923 ) ;
#205839=ADVANCED_FACE ( 'NONE', ( #36891 ), #218029, .T. ) ;
#205843=AXIS2_PLACEMENT_3D ( 'NONE', #211520, #245516, #32925 ) ;
#205878=DIRECTION ( 'NONE',  ( 2.775557561562881759E-13, 0.8825714802517645730, -0.4701782451860243017 ) ) ;
#205880=CIRCLE ( 'NONE', #235120, 11.90000000000001101 ) ;
#205881=DIRECTION ( 'NONE',  ( -0.000000000000000000, 0.4088369013363281068, -0.9126074666063770380 ) ) ;
#205887=EDGE_CURVE ( 'NONE', #144175, #130629, #159382, .T. ) ;
#205948=DIRECTION ( 'NONE',  ( 1.000000000000000000, 0.000000000000000000, 0.000000000000000000 ) ) ;
#205949=CARTESIAN_POINT ( 'NONE',  ( -21.11927991906891222, 30.77026771008070583, -252.1792548123860627 ) ) ;
#205952=EDGE_CURVE ( 'NONE', #172675, #133508, #203627, .T. ) ;
#205971=EDGE_CURVE ( 'NONE', #62684, #215984, #5195, .T. ) ;
#205984=CIRCLE ( 'NONE', #10177, 3.999999999999989786 ) ;
#206006=EDGE_CURVE ( 'NONE', #96525, #177565, #86216, .T. ) ;
#206012=VERTEX_POINT ( 'NONE', #50945 ) ;
#206037=LINE ( 'NONE', #166945, #135679 ) ;
#206038=ORIENTED_EDGE ( 'NONE', *, *, #87062, .T. ) ;
#206085=DIRECTION ( 'NONE',  ( 0.000000000000000000, 0.9126074666063660468, 0.4088369013363524762 ) ) ;
#206086=FACE_OUTER_BOUND ( 'NONE', #221120, .T. ) ;
#206129=EDGE_CURVE ( 'NONE', #32720, #179132, #50986, .T. ) ;
#206140=EDGE_CURVE ( 'NONE', #21323, #109005, #255145, .T. ) ;
#206192=EDGE_CURVE ( 'NONE', #9758, #102432, #256111, .T. ) ;
#206207=ORIENTED_EDGE ( 'NONE', *, *, #57400, .T. ) ;
#206263=VERTEX_POINT ( 'NONE', #113515 ) ;
#206309=ORIENTED_EDGE ( 'NONE', *, *, #30565, .F. ) ;
#206311=FACE_OUTER_BOUND ( 'NONE', #184372, .T. ) ;
#206318=ORIENTED_EDGE ( 'NONE', *, *, #200035, .F. ) ;
#206330=EDGE_CURVE ( 'NONE', #52663, #189844, #233846, .T. ) ;
#206339=B_SPLINE_CURVE_WITH_KNOTS ( 'NONE', 3,
 ( #164145, #243665, #87147, #224092, #89713, #186274, #144553, #188828, #8913, #45467 ),
 .UNSPECIFIED., .F., .F.,
 ( 4, 2, 2, 2, 4 ),
 ( 0.000000000000000000, 0.0001660831991682338823, 0.0002491247987523630071, 0.0002906455985444138680, 0.0003321663983364646746 ),
 .UNSPECIFIED. ) ;
#206393=EDGE_CURVE ( 'NONE', #10735, #93242, #204608, .T. ) ;
#206403=CARTESIAN_POINT ( 'NONE',  ( 20.44999100639886080, 39.47177588848037999, -236.8516082872442610 ) ) ;
#206420=CARTESIAN_POINT ( 'NONE',  ( -20.85000000000000142, 67.85909929089923764, -227.8797997985275856 ) ) ;
#206459=CARTESIAN_POINT ( 'NONE',  ( 21.12400222705945652, 44.24938628123909012, -236.5315751477832578 ) ) ;
#206460=VERTEX_POINT ( 'NONE', #169375 ) ;
#206465=VERTEX_POINT ( 'NONE', #148492 ) ;
#206476=TOROIDAL_SURFACE ( 'NONE', #123268, 0.2000000000000000111, 0.1000000000000000056 ) ;
#206512=LINE ( 'NONE', #54802, #162835 ) ;
#206521=VECTOR ( 'NONE', #177178, 1000.000000000000114 ) ;
#206524=EDGE_CURVE ( 'NONE', #189844, #255259, #217246, .T. ) ;
#206564=CARTESIAN_POINT ( 'NONE',  ( -18.50000000000000000, 21.17283678855158513, -243.7231193059830332 ) ) ;
#206565=ORIENTED_EDGE ( 'NONE', *, *, #68958, .T. ) ;
#206584=DIRECTION ( 'NONE',  ( -1.000000000000000000, 0.000000000000000000, 0.000000000000000000 ) ) ;
#206588=DIRECTION ( 'NONE',  ( 1.000000000000000000, 0.000000000000000000, 0.000000000000000000 ) ) ;
#206592=DIRECTION ( 'NONE',  ( -1.000000000000000000, -0.000000000000000000, 0.000000000000000000 ) ) ;
#206606=AXIS2_PLACEMENT_3D ( 'NONE', #159372, #216754, #38143 ) ;
#206623=ORIENTED_EDGE ( 'NONE', *, *, #233150, .T. ) ;
#206629=DIRECTION ( 'NONE',  ( 0.000000000000000000, -0.8103668758649471560, 0.5859227990963360444 ) ) ;
#206638=LINE ( 'NONE', #166263, #201149 ) ;
#206668=ORIENTED_EDGE ( 'NONE', *, *, #237721, .F. ) ;
#206686=CARTESIAN_POINT ( 'NONE',  ( 18.49999999999999645, 48.14768554360777841, -246.4498133360871179 ) ) ;
#206687=CIRCLE ( 'NONE', #152567, 0.2000000000000048683 ) ;
#206700=VERTEX_POINT ( 'NONE', #151738 ) ;
#206701=ORIENTED_EDGE ( 'NONE', *, *, #233099, .F. ) ;
#206717=FACE_OUTER_BOUND ( 'NONE', #27022, .T. ) ;
#206724=CARTESIAN_POINT ( 'NONE',  ( -22.16821283564876666, 33.56853718381600515, -242.6527871905703648 ) ) ;
#206725=EDGE_CURVE ( 'NONE', #109819, #54257, #229937, .T. ) ;
#206813=CARTESIAN_POINT ( 'NONE',  ( -23.15000000000000213, 54.36465331297785042, -236.8526523779771082 ) ) ;
#206842=EDGE_CURVE ( 'NONE', #21323, #214500, #113214, .T. ) ;
#206854=DIRECTION ( 'NONE',  ( 0.000000000000000000, -0.9126074666063660468, -0.4088369013363524762 ) ) ;
#206855=AXIS2_PLACEMENT_3D ( 'NONE', #89602, #169187, #34809 ) ;
#206877=ORIENTED_EDGE ( 'NONE', *, *, #85558, .F. ) ;
#206882=CARTESIAN_POINT ( 'NONE',  ( -20.64999999999999858, 61.88149656937975607, -248.1136133839584090 ) ) ;
#206934=FACE_OUTER_BOUND ( 'NONE', #127205, .T. ) ;
#206941=CARTESIAN_POINT ( 'NONE',  ( 18.39999999999998792, 46.93054509580814226, -255.3593361228639367 ) ) ;
#206944=EDGE_CURVE ( 'NONE', #13609, #117897, #200715, .T. ) ;
#206964=CARTESIAN_POINT ( 'NONE',  ( 21.07946286933444924, 30.85164652312839451, -252.0687244592667469 ) ) ;
#206973=CARTESIAN_POINT ( 'NONE',  ( -23.25000000000000000, 54.36465331297785042, -236.8526523779771082 ) ) ;
#206975=CIRCLE ( 'NONE', #44670, 0.1000000000000076245 ) ;
#206995=CARTESIAN_POINT ( 'NONE',  ( -21.14999999999999858, 44.10931966560507789, -259.0886734199950183 ) ) ;
#207010=CIRCLE ( 'NONE', #73762, 0.1000000000000024342 ) ;
#207029=CARTESIAN_POINT ( 'NONE',  ( 18.49999999999999645, 67.23127455305835554, -235.8551265064784559 ) ) ;
#207057=ORIENTED_EDGE ( 'NONE', *, *, #35893, .F. ) ;
#207079=FACE_OUTER_BOUND ( 'NONE', #226556, .T. ) ;
#207125=ORIENTED_EDGE ( 'NONE', *, *, #192932, .T. ) ;
#207137=DIRECTION ( 'NONE',  ( 1.000000000000000000, 0.000000000000000000, 0.000000000000000000 ) ) ;
#207139=CIRCLE ( 'NONE', #194694, 0.1000000000000041550 ) ;
#207162=EDGE_LOOP ( 'NONE', ( #94886, #240584, #97188, #172313 ) ) ;
#207220=DIRECTION ( 'NONE',  ( 0.000000000000000000, 0.9126074666063848095, 0.4088369013363106763 ) ) ;
#207226=ORIENTED_EDGE ( 'NONE', *, *, #170481, .F. ) ;
#207234=CYLINDRICAL_SURFACE ( 'NONE', #2444, 0.09999999999999939493 ) ;
#207259=ORIENTED_EDGE ( 'NONE', *, *, #38628, .F. ) ;
#207268=VERTEX_POINT ( 'NONE', #62575 ) ;
#207278=EDGE_CURVE ( 'NONE', #227337, #150102, #64975, .T. ) ;
#207290=ORIENTED_EDGE ( 'NONE', *, *, #62331, .T. ) ;
#207340=ORIENTED_EDGE ( 'NONE', *, *, #135818, .T. ) ;
#207345=ORIENTED_EDGE ( 'NONE', *, *, #62854, .T. ) ;
#207375=ORIENTED_EDGE ( 'NONE', *, *, #181479, .F. ) ;
#207396=ORIENTED_EDGE ( 'NONE', *, *, #84983, .F. ) ;
#207401=CARTESIAN_POINT ( 'NONE',  ( 20.04142135623730070, 54.39174857302370469, -228.8414560973406822 ) ) ;
#207416=EDGE_LOOP ( 'NONE', ( #138438, #62186, #56350, #106251 ) ) ;
#207417=EDGE_CURVE ( 'NONE', #60194, #782, #59378, .T. ) ;
#207420=DIRECTION ( 'NONE',  ( 0.000000000000000000, 0.9126074666063660468, 0.4088369013363524762 ) ) ;
#207431=CARTESIAN_POINT ( 'NONE',  ( -23.15000000000000213, 67.23127455305835554, -235.8551265064784559 ) ) ;
#207449=CARTESIAN_POINT ( 'NONE',  ( -21.14999999999999858, 37.99340787088039662, -236.0781345613907547 ) ) ;
#207463=CIRCLE ( 'NONE', #161676, 12.97499999999999254 ) ;
#207499=DIRECTION ( 'NONE',  ( -1.000000000000000000, -0.000000000000000000, 0.000000000000000000 ) ) ;
#207510=ORIENTED_EDGE ( 'NONE', *, *, #243476, .T. ) ;
#207513=FACE_OUTER_BOUND ( 'NONE', #18075, .T. ) ;
#207514=AXIS2_PLACEMENT_3D ( 'NONE', #70603, #66728, #150131 ) ;
#207518=DIRECTION ( 'NONE',  ( 1.000000000000000000, -0.000000000000000000, -0.000000000000000000 ) ) ;
#207524=CARTESIAN_POINT ( 'NONE',  ( -18.51024323315077424, 68.05374558910872906, -224.1882283518532120 ) ) ;
#207536=ORIENTED_EDGE ( 'NONE', *, *, #116099, .F. ) ;
#207570=ORIENTED_EDGE ( 'NONE', *, *, #210197, .F. ) ;
#207594=VECTOR ( 'NONE', #18556, 1000.000000000000000 ) ;
#207614=ORIENTED_EDGE ( 'NONE', *, *, #172760, .F. ) ;
#207621=EDGE_CURVE ( 'NONE', #72558, #70690, #167779, .T. ) ;
#207623=DIRECTION ( 'NONE',  ( -1.000000000000000000, 0.000000000000000000, 0.000000000000000000 ) ) ;
#207661=CARTESIAN_POINT ( 'NONE',  ( 20.85000000000000142, 67.85125148167622910, -227.9794913823769491 ) ) ;
#207664=CARTESIAN_POINT ( 'NONE',  ( 21.87500000000000355, 52.06567329910104291, -231.9654557484363409 ) ) ;
#207702=CARTESIAN_POINT ( 'NONE',  ( 20.96937028524355640, 39.15198068096341899, -236.7924211901758156 ) ) ;
#207719=ORIENTED_EDGE ( 'NONE', *, *, #50951, .T. ) ;
#207760=AXIS2_PLACEMENT_3D ( 'NONE', #184924, #114036, #252262 ) ;
#207768=EDGE_LOOP ( 'NONE', ( #123771, #86036, #242347, #124194 ) ) ;
#207800=CARTESIAN_POINT ( 'NONE',  ( 21.30000000000002558, 32.96286418198890544, -251.2069521516576174 ) ) ;
#207824=CARTESIAN_POINT ( 'NONE',  ( -18.59999999999999787, 77.44184265367995579, -241.6694879557322508 ) ) ;
#207893=DIRECTION ( 'NONE',  ( 0.000000000000000000, -0.07847809223012357227, -0.9969158384938622275 ) ) ;
#207923=ORIENTED_EDGE ( 'NONE', *, *, #154865, .T. ) ;
#207934=DIRECTION ( 'NONE',  ( 1.000000000000000000, 0.000000000000000000, 0.000000000000000000 ) ) ;
#207949=FACE_OUTER_BOUND ( 'NONE', #186709, .T. ) ;
#207990=CARTESIAN_POINT ( 'NONE',  ( -20.64999999999999858, 54.80101577392981937, -239.2322065708440846 ) ) ;
#208021=DIRECTION ( 'NONE',  ( 0.000000000000000000, -0.9126074666063772600, -0.4088369013363276627 ) ) ;
#208054=EDGE_CURVE ( 'NONE', #106227, #91860, #38954, .T. ) ;
#208142=CARTESIAN_POINT ( 'NONE',  ( 20.95512820512820440, 40.84069494668059264, -237.9516373772122222 ) ) ;
#208169=CARTESIAN_POINT ( 'NONE',  ( 20.94999999999999574, 47.92640890138473253, -246.4059919526569900 ) ) ;
#208185=ORIENTED_EDGE ( 'NONE', *, *, #181974, .T. ) ;
#208202=ORIENTED_EDGE ( 'NONE', *, *, #204752, .T. ) ;
#208225=DIRECTION ( 'NONE',  ( 1.000000000000000000, 0.000000000000000000, 0.000000000000000000 ) ) ;
#208235=AXIS2_PLACEMENT_3D ( 'NONE', #182027, #3362, #67208 ) ;
#208250=DIRECTION ( 'NONE',  ( 1.000000000000000000, 2.986185139342070877E-16, -6.665775143889692774E-16 ) ) ;
#208256=CARTESIAN_POINT ( 'NONE',  ( -22.39999999999999858, 29.54900078958453236, -252.7363208912387051 ) ) ;
#208260=ORIENTED_EDGE ( 'NONE', *, *, #220655, .F. ) ;
#208261=CARTESIAN_POINT ( 'NONE',  ( -21.12642695952773764, 33.96205950053516176, -243.7731231636842608 ) ) ;
#208290=DIRECTION ( 'NONE',  ( 0.000000000000000000, 0.9126074666063769270, 0.4088369013363280513 ) ) ;
#208304=ORIENTED_EDGE ( 'NONE', *, *, #136753, .F. ) ;
#208324=ORIENTED_EDGE ( 'NONE', *, *, #149868, .T. ) ;
#208349=DIRECTION ( 'NONE',  ( 0.000000000000000000, 0.9126074666063545004, 0.4088369013363783999 ) ) ;
#208351=FACE_OUTER_BOUND ( 'NONE', #225805, .T. ) ;
#208392=EDGE_CURVE ( 'NONE', #22954, #241306, #130694, .T. ) ;
#208409=VERTEX_POINT ( 'NONE', #130136 ) ;
#208423=EDGE_CURVE ( 'NONE', #189844, #84325, #222250, .T. ) ;
#208430=VECTOR ( 'NONE', #124080, 1000.000000000000114 ) ;
#208458=ORIENTED_EDGE ( 'NONE', *, *, #40261, .T. ) ;
#208494=AXIS2_PLACEMENT_3D ( 'NONE', #149739, #252642, #74059 ) ;
#208497=CIRCLE ( 'NONE', #75411, 0.1000000000000011158 ) ;
#208499=ORIENTED_EDGE ( 'NONE', *, *, #63774, .T. ) ;
#208512=DIRECTION ( 'NONE',  ( 1.000000000000000000, 0.000000000000000000, 0.000000000000000000 ) ) ;
#208529=VERTEX_POINT ( 'NONE', #256437 ) ;
#208561=FACE_OUTER_BOUND ( 'NONE', #223919, .T. ) ;
#208568=DIRECTION ( 'NONE',  ( 1.000000000000000000, 0.000000000000000000, -0.000000000000000000 ) ) ;
#208572=CARTESIAN_POINT ( 'NONE',  ( -18.58671080940898790, 47.00638226075548687, -255.2233826300025044 ) ) ;
#208582=DIRECTION ( 'NONE',  ( 1.000000000000000000, 0.000000000000000000, 0.000000000000000000 ) ) ;
#208592=CARTESIAN_POINT ( 'NONE',  ( -23.25000000000000000, 61.88149656937975607, -248.1136133839584090 ) ) ;
#208596=EDGE_CURVE ( 'NONE', #41988, #118767, #107699, .T. ) ;
#208597=CARTESIAN_POINT ( 'NONE',  ( 20.94999999999999574, 43.57568952063339651, -245.1784935019914826 ) ) ;
#208599=CARTESIAN_POINT ( 'NONE',  ( 22.49999999999999645, 25.98655542988603173, -254.2226763854395983 ) ) ;
#208621=CIRCLE ( 'NONE', #96154, 0.9750000000000036415 ) ;
#208626=EDGE_CURVE ( 'NONE', #136054, #220667, #230869, .T. ) ;
#208690=DIRECTION ( 'NONE',  ( 0.000000000000000000, -0.9654421110809058293, -0.2606175937108693996 ) ) ;
#208707=CYLINDRICAL_SURFACE ( 'NONE', #35597, 0.1000000000000024342 ) ;
#208714=TOROIDAL_SURFACE ( 'NONE', #229552, 11.89999999999999858, 0.1000000000000000056 ) ;
#208740=ORIENTED_EDGE ( 'NONE', *, *, #33816, .T. ) ;
#208771=CARTESIAN_POINT ( 'NONE',  ( -18.42609945526357862, 46.93054533616035684, -255.3593356979593239 ) ) ;
#208775=DIRECTION ( 'NONE',  ( 0.000000000000000000, 0.9126074666063844765, 0.4088369013363114535 ) ) ;
#208779=LINE ( 'NONE', #11878, #18472 ) ;
#208844=FACE_OUTER_BOUND ( 'NONE', #35936, .T. ) ;
#208898=EDGE_CURVE ( 'NONE', #27038, #86618, #35072, .T. ) ;
#208904=EDGE_LOOP ( 'NONE', ( #20335, #245470, #103322 ) ) ;
#208916=CARTESIAN_POINT ( 'NONE',  ( 18.59999999999999787, 43.57281345108133053, -239.9888335660389487 ) ) ;
#208947=ADVANCED_FACE ( 'NONE', ( #145763 ), #222622, .F. ) ;
#208948=DIRECTION ( 'NONE',  ( 0.000000000000000000, 0.9126074666063545004, 0.4088369013363783999 ) ) ;
#208979=AXIS2_PLACEMENT_3D ( 'NONE', #67302, #225070, #69899 ) ;
#208995=CARTESIAN_POINT ( 'NONE',  ( 20.95512820512820440, 43.40368376489742275, -234.8883907171572787 ) ) ;
#208998=DIRECTION ( 'NONE',  ( 0.000000000000000000, 0.9126074666063777041, 0.4088369013363267745 ) ) ;
#209020=EDGE_LOOP ( 'NONE', ( #139036, #124781, #222163, #63972 ) ) ;
#209028=CYLINDRICAL_SURFACE ( 'NONE', #224579, 0.1000000000000065836 ) ;
#209043=AXIS2_PLACEMENT_3D ( 'NONE', #90607, #137145, #78442 ) ;
#209050=ORIENTED_EDGE ( 'NONE', *, *, #30961, .T. ) ;
#209057=FACE_OUTER_BOUND ( 'NONE', #191401, .T. ) ;
#209081=DIRECTION ( 'NONE',  ( -1.000000000000000000, -0.000000000000000000, -0.000000000000000000 ) ) ;
#209102=ORIENTED_EDGE ( 'NONE', *, *, #65515, .F. ) ;
#209131=EDGE_CURVE ( 'NONE', #219794, #19019, #154792, .T. ) ;
#209152=CIRCLE ( 'NONE', #100778, 0.1999999999999893807 ) ;
#209159=EDGE_CURVE ( 'NONE', #20493, #178795, #209607, .T. ) ;
#209183=ORIENTED_EDGE ( 'NONE', *, *, #26787, .F. ) ;
#209187=DIRECTION ( 'NONE',  ( 0.000000000000000000, -0.4088369013363280513, 0.9126074666063769270 ) ) ;
#209188=ORIENTED_EDGE ( 'NONE', *, *, #187203, .F. ) ;
#209204=EDGE_CURVE ( 'NONE', #110542, #55978, #77771, .T. ) ;
#209222=ORIENTED_EDGE ( 'NONE', *, *, #187038, .T. ) ;
#209244=DIRECTION ( 'NONE',  ( 1.000000000000000000, 0.000000000000000000, 0.000000000000000000 ) ) ;
#209252=EDGE_CURVE ( 'NONE', #252130, #129596, #143134, .T. ) ;
#209276=VECTOR ( 'NONE', #77010, 1000.000000000000114 ) ;
#209284=CARTESIAN_POINT ( 'NONE',  ( -21.70464131381649509, 33.75808023539804736, -243.0758859948899726 ) ) ;
#209288=DIRECTION ( 'NONE',  ( 1.000000000000000000, -7.510212038922846022E-17, 1.676432719286211941E-16 ) ) ;
#209308=AXIS2_PLACEMENT_3D ( 'NONE', #218535, #55599, #56885 ) ;
#209353=FACE_OUTER_BOUND ( 'NONE', #223453, .T. ) ;
#209367=CARTESIAN_POINT ( 'NONE',  ( 22.48660254037844197, 31.85034414784619017, -238.9397275603479898 ) ) ;
#209377=CARTESIAN_POINT ( 'NONE',  ( 20.84999999999999432, 67.85909929089923764, -227.8797997985275856 ) ) ;
#209392=CARTESIAN_POINT ( 'NONE',  ( -20.94999999999999929, 38.23914636435921466, -236.1324109481172968 ) ) ;
#209436=CIRCLE ( 'NONE', #205327, 0.1000000000000087624 ) ;
#209478=EDGE_LOOP ( 'NONE', ( #214935, #79966, #146575, #62573 ) ) ;
#209494=VERTEX_POINT ( 'NONE', #138397 ) ;
#209524=ORIENTED_EDGE ( 'NONE', *, *, #83740, .T. ) ;
#209542=CIRCLE ( 'NONE', #30510, 2.000000000000012879 ) ;
#209571=CARTESIAN_POINT ( 'NONE',  ( -18.59999999999999787, 38.29773864426885410, -236.0513742605307925 ) ) ;
#209596=DIRECTION ( 'NONE',  ( 0.000000000000000000, 0.9126074666063771490, 0.4088369013363281623 ) ) ;
#209601=DIRECTION ( 'NONE',  ( -1.000000000000000000, -0.000000000000000000, 0.000000000000000000 ) ) ;
#209607=LINE ( 'NONE', #150917, #1866 ) ;
#209612=CARTESIAN_POINT ( 'NONE',  ( 23.15000000000000213, 69.47678708576792417, -248.4500549165069856 ) ) ;
#209622=CARTESIAN_POINT ( 'NONE',  ( -23.25000000000000000, 21.17283678855157802, -243.7231193059830332 ) ) ;
#209631=EDGE_CURVE ( 'NONE', #251832, #14729, #68145, .T. ) ;
#209693=FACE_OUTER_BOUND ( 'NONE', #247726, .T. ) ;
#209694=AXIS2_PLACEMENT_3D ( 'NONE', #107110, #124129, #82385 ) ;
#209701=( BOUNDED_SURFACE ( )  B_SPLINE_SURFACE ( 3, 2, ( 
 ( #232426, #133308, #34234 ),
 ( #173770, #194591, #15956 ),
 ( #96707, #62440, #204493 ),
 ( #222771, #201950, #3737 ),
 ( #22038, #254502, #161553 ),
 ( #24621, #243632, #164108 ),
 ( #23337, #42871, #121158 ),
 ( #116323, #224057, #141959 ),
 ( #45436, #156749, #144516 ),
 ( #64990, #44164, #102815 ) ),
 .UNSPECIFIED., .F., .F., .T. ) 
 B_SPLINE_SURFACE_WITH_KNOTS ( ( 4, 2, 2, 2, 4 ),
 ( 3, 3 ),
 ( 0.0001701955120502381136, 0.0002247052511886090949, 0.0002792149903269800491, 0.0003882344686037219575, 0.0006062734251572058286 ),
 ( 0.000000000000000000, 1.000000000000000000 ),
 .UNSPECIFIED. ) 
 GEOMETRIC_REPRESENTATION_ITEM ( )  RATIONAL_B_SPLINE_SURFACE ( (
 ( 1.000000000000000000, 0.2966190024561997651, 1.000000000000000000),
 ( 1.000000000000000000, 0.2964522492692210909, 1.000000000000000000),
 ( 1.000000000000000000, 0.3059923531906453276, 1.000000000000000000),
 ( 1.000000000000000000, 0.3355751146923415251, 1.000000000000000000),
 ( 1.000000000000000000, 0.3550672384958439287, 1.000000000000000000),
 ( 1.000000000000000000, 0.4157034672187444047, 1.000000000000000000),
 ( 1.000000000000000000, 0.4588031877661047919, 1.000000000000000000),
 ( 1.000000000000000000, 0.5771441759645236091, 1.000000000000000000),
 ( 1.000000000000000000, 0.6469377121783427276, 1.000000000000000000),
 ( 1.000000000000000000, 0.7071067811865475727, 1.000000000000000000) ) ) 
 REPRESENTATION_ITEM ( '' )  SURFACE ( )  );
#209719=AXIS2_PLACEMENT_3D ( 'NONE', #26481, #105976, #151584 ) ;
#209735=DIRECTION ( 'NONE',  ( 1.000000000000000000, 0.000000000000000000, 0.000000000000000000 ) ) ;
#209742=ORIENTED_EDGE ( 'NONE', *, *, #25169, .T. ) ;
#209776=FACE_OUTER_BOUND ( 'NONE', #130627, .T. ) ;
#209821=CARTESIAN_POINT ( 'NONE',  ( -23.15000000000000213, 56.18374508921711197, -227.9290876000915205 ) ) ;
#209823=DIRECTION ( 'NONE',  ( 0.000000000000000000, 0.9126074666063770380, 0.4088369013363281068 ) ) ;
#209827=DIRECTION ( 'NONE',  ( 1.000000000000000000, 0.000000000000000000, -0.000000000000000000 ) ) ;
#209836=CARTESIAN_POINT ( 'NONE',  ( -20.54999999999999716, 52.13794731297493712, -232.3713824252124880 ) ) ;
#209840=CARTESIAN_POINT ( 'NONE',  ( -18.52139480978225450, 46.94591656517138745, -255.3320236366652409 ) ) ;
#209846=AXIS2_PLACEMENT_3D ( 'NONE', #170372, #93343, #50343 ) ;
#209867=DIRECTION ( 'NONE',  ( 0.000000000000000000, 0.9126074666063769270, 0.4088369013363282733 ) ) ;
#209875=EDGE_LOOP ( 'NONE', ( #52783, #243972, #7402, #10921 ) ) ;
#209876=EDGE_CURVE ( 'NONE', #178487, #93087, #76692, .T. ) ;
#209879=EDGE_LOOP ( 'NONE', ( #97637, #17618, #163498, #153255 ) ) ;
#209920=CARTESIAN_POINT ( 'NONE',  ( -21.05000000000000071, 67.23127455305835554, -235.8551265064784559 ) ) ;
#209926=DIRECTION ( 'NONE',  ( -0.000000000000000000, 0.9126074666063770380, 0.4088369013363281068 ) ) ;
#209937=TOROIDAL_SURFACE ( 'NONE', #55956, 2.100000000000002309, 0.1000000000000000056 ) ;
#209956=FACE_OUTER_BOUND ( 'NONE', #106056, .T. ) ;
#209972=LINE ( 'NONE', #246508, #225071 ) ;
#210004=DIRECTION ( 'NONE',  ( 1.000000000000000000, 0.000000000000000000, 0.000000000000000000 ) ) ;
#210007=AXIS2_PLACEMENT_3D ( 'NONE', #44628, #224534, #241536 ) ;
#210009=CARTESIAN_POINT ( 'NONE',  ( 20.94999999999999929, 55.49311008795314137, -234.6486875357297492 ) ) ;
#210032=AXIS2_PLACEMENT_3D ( 'NONE', #178027, #188279, #205261 ) ;
#210037=EDGE_CURVE ( 'NONE', #242320, #95060, #164381, .T. ) ;
#210045=VERTEX_POINT ( 'NONE', #101528 ) ;
#210089=CARTESIAN_POINT ( 'NONE',  ( -18.50000324121759121, 68.00468331834514402, -224.2298952291173464 ) ) ;
#210164=DIRECTION ( 'NONE',  ( -3.265361837132813093E-16, -0.4088369013363283844, 0.9126074666063769270 ) ) ;
#210194=ORIENTED_EDGE ( 'NONE', *, *, #204201, .T. ) ;
#210197=EDGE_CURVE ( 'NONE', #99817, #110542, #205880, .T. ) ;
#210209=CARTESIAN_POINT ( 'NONE',  ( 21.05000000000000071, 61.88149656937974896, -248.1136133839584090 ) ) ;
#210212=AXIS2_PLACEMENT_3D ( 'NONE', #14152, #152380, #134057 ) ;
#210218=ADVANCED_FACE ( 'NONE', ( #68877 ), #164119, .F. ) ;
#210219=CARTESIAN_POINT ( 'NONE',  ( 20.00000000000000000, 54.35086488289007889, -228.7501953506800589 ) ) ;
#210233=CARTESIAN_POINT ( 'NONE',  ( 23.24999999999999289, 45.02833974712562792, -238.5149546970766892 ) ) ;
#210264=EDGE_LOOP ( 'NONE', ( #240338, #163680, #151816, #241098 ) ) ;
#210286=DIRECTION ( 'NONE',  ( 0.000000000000000000, -0.3116596277708331142, -0.9501938099239259916 ) ) ;
#210294=DIRECTION ( 'NONE',  ( 1.000000000000000000, 0.000000000000000000, 0.000000000000000000 ) ) ;
#210351=DIRECTION ( 'NONE',  ( 0.000000000000000000, 0.9126074666063771490, 0.4088369013363281623 ) ) ;
#210357=DIRECTION ( 'NONE',  ( 0.000000000000000000, -0.9126074666063660468, -0.4088369013363524762 ) ) ;
#210383=AXIS2_PLACEMENT_3D ( 'NONE', #218858, #122352, #161492 ) ;
#210401=DIRECTION ( 'NONE',  ( 1.000000000000000000, -1.335000415235278971E-16, 2.979993593738921214E-16 ) ) ;
#210403=ORIENTED_EDGE ( 'NONE', *, *, #233099, .T. ) ;
#210412=ORIENTED_EDGE ( 'NONE', *, *, #117155, .F. ) ;
#210452=ORIENTED_EDGE ( 'NONE', *, *, #20342, .F. ) ;
#210459=CARTESIAN_POINT ( 'NONE',  ( 20.94999999999999929, 71.99422445362657186, -246.4870034924427671 ) ) ;
#210461=VERTEX_POINT ( 'NONE', #97366 ) ;
#210477=ORIENTED_EDGE ( 'NONE', *, *, #188524, .F. ) ;
#210499=DIRECTION ( 'NONE',  ( 1.000000000000000000, 0.000000000000000000, -0.000000000000000000 ) ) ;
#210528=CIRCLE ( 'NONE', #6507, 0.1000000000000024342 ) ;
#210529=ADVANCED_FACE ( 'NONE', ( #103795 ), #248471, .T. ) ;
#210567=EDGE_LOOP ( 'NONE', ( #118772, #6246, #203432, #164688 ) ) ;
#210602=DIRECTION ( 'NONE',  ( -1.000000000000000000, 1.335000415235278971E-16, -2.979993593738921214E-16 ) ) ;
#210642=EDGE_CURVE ( 'NONE', #176131, #232311, #249754, .T. ) ;
#210675=DIRECTION ( 'NONE',  ( 1.000000000000000000, 4.095934188116521533E-15, 3.985178720521109717E-14 ) ) ;
#210677=CARTESIAN_POINT ( 'NONE',  ( -21.05000000000000071, 38.08698097766499302, -236.1457910985472779 ) ) ;
#210698=FACE_OUTER_BOUND ( 'NONE', #221881, .T. ) ;
#210705=AXIS2_PLACEMENT_3D ( 'NONE', #129071, #92497, #169520 ) ;
#210724=ADVANCED_FACE ( 'NONE', ( #138744 ), #218298, .T. ) ;
#210762=ORIENTED_EDGE ( 'NONE', *, *, #105577, .F. ) ;
#210874=CARTESIAN_POINT ( 'NONE',  ( 21.05000000000000071, 43.36285386911620776, -234.7972500504784534 ) ) ;
#210877=ORIENTED_EDGE ( 'NONE', *, *, #147658, .T. ) ;
#210892=CYLINDRICAL_SURFACE ( 'NONE', #60043, 0.09999999999999939493 ) ;
#210927=CARTESIAN_POINT ( 'NONE',  ( -21.05000000000000071, 35.94660524813657076, -234.4748257877825495 ) ) ;
#210936=ORIENTED_EDGE ( 'NONE', *, *, #215986, .T. ) ;
#210956=DIRECTION ( 'NONE',  ( 0.000000000000000000, -0.2868887416115947775, 0.9579639084728169829 ) ) ;
#210968=ORIENTED_EDGE ( 'NONE', *, *, #119904, .F. ) ;
#210983=AXIS2_PLACEMENT_3D ( 'NONE', #181723, #203839, #25231 ) ;
#210994=CARTESIAN_POINT ( 'NONE',  ( 18.59999999999999432, 43.57568952063339651, -245.1784935019914826 ) ) ;
#211009=CIRCLE ( 'NONE', #244125, 0.09999999999999609201 ) ;
#211010=ORIENTED_EDGE ( 'NONE', *, *, #95176, .F. ) ;
#211020=CARTESIAN_POINT ( 'NONE',  ( 18.49999999999999289, 67.84340367245323478, -228.0791829662263410 ) ) ;
#211061=DIRECTION ( 'NONE',  ( -0.000000000000000000, -0.9126074666063770380, -0.4088369013363281068 ) ) ;
#211066=AXIS2_PLACEMENT_3D ( 'NONE', #50179, #11073, #14941 ) ;
#211073=CIRCLE ( 'NONE', #119494, 0.09999999999999609201 ) ;
#211186=DIRECTION ( 'NONE',  ( -1.000000000000000000, -0.000000000000000000, -0.000000000000000000 ) ) ;
#211195=ORIENTED_EDGE ( 'NONE', *, *, #203920, .F. ) ;
#211199=VERTEX_POINT ( 'NONE', #68921 ) ;
#211200=CIRCLE ( 'NONE', #86275, 0.09999999999999609201 ) ;
#211215=FACE_OUTER_BOUND ( 'NONE', #231721, .T. ) ;
#211278=EDGE_CURVE ( 'NONE', #245692, #51036, #23300, .T. ) ;
#211286=FACE_OUTER_BOUND ( 'NONE', #155435, .T. ) ;
#211316=ORIENTED_EDGE ( 'NONE', *, *, #116250, .T. ) ;
#211321=FACE_OUTER_BOUND ( 'NONE', #130085, .T. ) ;
#211335=EDGE_CURVE ( 'NONE', #239535, #17340, #114444, .T. ) ;
#211338=AXIS2_PLACEMENT_3D ( 'NONE', #186840, #26478, #63012 ) ;
#211391=AXIS2_PLACEMENT_3D ( 'NONE', #57681, #33053, #95537 ) ;
#211447=EDGE_LOOP ( 'NONE', ( #19420, #51876, #39472, #146741 ) ) ;
#211453=AXIS2_PLACEMENT_3D ( 'NONE', #172826, #35854, #252295 ) ;
#211472=ORIENTED_EDGE ( 'NONE', *, *, #156023, .F. ) ;
#211475=CARTESIAN_POINT ( 'NONE',  ( 23.14999999999999147, 36.65892442174472876, -249.5511627012454596 ) ) ;
#211477=DIRECTION ( 'NONE',  ( -0.000000000000000000, -0.9126074666063770380, -0.4088369013363281068 ) ) ;
#211484=CARTESIAN_POINT ( 'NONE',  ( 21.14999999999999503, 26.06832281015329755, -254.4051978787608732 ) ) ;
#211518=ORIENTED_EDGE ( 'NONE', *, *, #174221, .T. ) ;
#211519=CARTESIAN_POINT ( 'NONE',  ( 21.05000000000000071, 36.65892442174472876, -249.5511627012454596 ) ) ;
#211520=CARTESIAN_POINT ( 'NONE',  ( -21.14999999999999858, 36.65892442174472876, -249.5511627012454596 ) ) ;
#211540=ORIENTED_EDGE ( 'NONE', *, *, #242309, .T. ) ;
#211547=ORIENTED_EDGE ( 'NONE', *, *, #101395, .F. ) ;
#211583=ORIENTED_EDGE ( 'NONE', *, *, #174044, .F. ) ;
#211599=DIRECTION ( 'NONE',  ( 1.000000000000000000, 0.000000000000000000, 0.000000000000000000 ) ) ;
#211602=LINE ( 'NONE', #49942, #112443 ) ;
#211603=FACE_OUTER_BOUND ( 'NONE', #57523, .T. ) ;
#211607=CARTESIAN_POINT ( 'NONE',  ( 20.85000000000000142, 78.48087866980282001, -232.8271061603568910 ) ) ;
#211696=ORIENTED_EDGE ( 'NONE', *, *, #180906, .T. ) ;
#211731=ORIENTED_EDGE ( 'NONE', *, *, #69892, .T. ) ;
#211748=DIRECTION ( 'NONE',  ( 0.000000000000000000, 0.2868887416116073785, -0.9579639084728132081 ) ) ;
#211750=DIRECTION ( 'NONE',  ( 0.000000000000000000, -0.9126074666063768159, -0.4088369013363282178 ) ) ;
#211785=EDGE_CURVE ( 'NONE', #60290, #123266, #140140, .T. ) ;
#211796=CARTESIAN_POINT ( 'NONE',  ( -20.94999999999999929, 70.97296516614450468, -234.1788952109995137 ) ) ;
#211807=DIRECTION ( 'NONE',  ( -1.000000000000000000, -0.000000000000000000, -0.000000000000000000 ) ) ;
#211830=TOROIDAL_SURFACE ( 'NONE', #120293, 0.2000000000000000111, 0.1000000000000000056 ) ;
#211840=CARTESIAN_POINT ( 'NONE',  ( 18.59999999999999076, 46.54514716347711101, -243.1111603596801842 ) ) ;
#211873=CARTESIAN_POINT ( 'NONE',  ( 20.94999999999999929, 45.73145985849338047, -239.4600911154851133 ) ) ;
#211876=CARTESIAN_POINT ( 'NONE',  ( -20.64999999999999858, 54.82645269529697885, -239.3027372265576957 ) ) ;
#211899=CARTESIAN_POINT ( 'NONE',  ( -18.50000000000000000, 74.93036000061670165, -233.6816308724374949 ) ) ;
#211906=DIRECTION ( 'NONE',  ( -4.448008912761047751E-16, -0.4088369013363289950, 0.9126074666063765939 ) ) ;
#211930=CARTESIAN_POINT ( 'NONE',  ( 20.94999999999999929, 62.04503132991427350, -248.4786563706009588 ) ) ;
#211990=ORIENTED_EDGE ( 'NONE', *, *, #139723, .F. ) ;
#212024=DIRECTION ( 'NONE',  ( -0.000000000000000000, 0.1022405907414166287, 0.9947597004326451664 ) ) ;
#212041=LINE ( 'NONE', #34690, #230933 ) ;
#212044=DIRECTION ( 'NONE',  ( 1.000000000000000000, 0.000000000000000000, 0.000000000000000000 ) ) ;
#212045=CARTESIAN_POINT ( 'NONE',  ( 23.24999999999999289, 31.98723526783714277, -238.8784020251475511 ) ) ;
#212056=CARTESIAN_POINT ( 'NONE',  ( 23.14999999999999503, 45.02833974712562792, -238.5149546970766892 ) ) ;
#212069=CARTESIAN_POINT ( 'NONE',  ( -22.39999999999999858, 31.89597452117651244, -238.9192857152811769 ) ) ;
#212083=CARTESIAN_POINT ( 'NONE',  ( -18.59999999999999787, 52.32046880629621199, -232.2896150449452364 ) ) ;
#212098=DIRECTION ( 'NONE',  ( 0.000000000000000000, 0.9126074666063771490, 0.4088369013363278293 ) ) ;
#212114=DIRECTION ( 'NONE',  ( 3.816391647148962481E-13, 0.8825714802517645730, -0.4701782451860243017 ) ) ;
#212116=ORIENTED_EDGE ( 'NONE', *, *, #185961, .T. ) ;
#212125=AXIS2_PLACEMENT_3D ( 'NONE', #127839, #189089, #224353 ) ;
#212158=CARTESIAN_POINT ( 'NONE',  ( 21.09793522318407355, 43.44397040381475961, -234.7599165424315402 ) ) ;
#212206=DIRECTION ( 'NONE',  ( 1.000000000000000000, 0.000000000000000000, 0.000000000000000000 ) ) ;
#212220=AXIS2_PLACEMENT_3D ( 'NONE', #124039, #21104, #23675 ) ;
#212228=AXIS2_PLACEMENT_3D ( 'NONE', #232732, #170229, #228867 ) ;
#212232=ORIENTED_EDGE ( 'NONE', *, *, #136026, .T. ) ;
#212242=AXIS2_PLACEMENT_3D ( 'NONE', #5727, #27921, #222205 ) ;
#212257=DIRECTION ( 'NONE',  ( 0.000000000000000000, 0.9623856809447771665, 0.2716869542551821892 ) ) ;
#212277=AXIS2_PLACEMENT_3D ( 'NONE', #198006, #218847, #156360 ) ;
#212290=FACE_OUTER_BOUND ( 'NONE', #178483, .T. ) ;
#212343=B_SPLINE_CURVE_WITH_KNOTS ( 'NONE', 3,
 ( #217352, #235642, #136533, #23053, #216077, #257723, #175705, #116995, #17878, #97390, #20478, #157441, #255156, #218640, #236936, #122133 ),
 .UNSPECIFIED., .F., .F.,
 ( 4, 3, 3, 3, 3, 4 ),
 ( 0.000000000000000000, 2.209075297427991918E-05, 5.594258369009683308E-05, 8.979524372340886272E-05, 0.0001236472815274528567, 0.0001574990747609496733 ),
 .UNSPECIFIED. ) ;
#212347=EDGE_CURVE ( 'NONE', #244838, #45673, #15463, .T. ) ;
#212394=ADVANCED_FACE ( 'NONE', ( #139204 ), #177951, .F. ) ;
#212395=EDGE_CURVE ( 'NONE', #197595, #147011, #204324, .T. ) ;
#212401=PLANE ( 'NONE',  #73455 ) ;
#212406=AXIS2_PLACEMENT_3D ( 'NONE', #22079, #232464, #212884 ) ;
#212410=CIRCLE ( 'NONE', #199758, 0.4000000000000033529 ) ;
#212433=AXIS2_PLACEMENT_3D ( 'NONE', #225829, #165917, #108485 ) ;
#212437=CARTESIAN_POINT ( 'NONE',  ( -20.54999999999999716, 47.57365439703043108, -242.5355162900727919 ) ) ;
#212438=DIRECTION ( 'NONE',  ( 0.000000000000000000, 0.9126074666063545004, 0.4088369013363783999 ) ) ;
#212460=CARTESIAN_POINT ( 'NONE',  ( -22.39999999999999858, 25.93539162822980160, -254.3551732743586626 ) ) ;
#212493=DIRECTION ( 'NONE',  ( 0.000000000000000000, 0.4088369013363281623, -0.9126074666063771490 ) ) ;
#212503=CIRCLE ( 'NONE', #237429, 0.8750000000000007772 ) ;
#212519=EDGE_LOOP ( 'NONE', ( #78609, #118186, #232771, #147712 ) ) ;
#212521=DIRECTION ( 'NONE',  ( 0.000000000000000000, 0.9126074666063768159, 0.4088369013363282178 ) ) ;
#212532=EDGE_LOOP ( 'NONE', ( #198250, #46620, #42408, #39618, #241625, #49172, #93328, #109296 ) ) ;
#212550=DIRECTION ( 'NONE',  ( -0.000000000000000000, 0.8490545835447252943, 0.5283051335749947564 ) ) ;
#212560=CARTESIAN_POINT ( 'NONE',  ( 18.59999999999999076, 74.83412143252222393, -233.7087995678629966 ) ) ;
#212566=EDGE_CURVE ( 'NONE', #183612, #134457, #190446, .T. ) ;
#212580=CARTESIAN_POINT ( 'NONE',  ( -23.25000000000000000, 54.35515994658447880, -237.0760575614320089 ) ) ;
#212595=CARTESIAN_POINT ( 'NONE',  ( -22.50000000000000000, 31.80488924422932584, -238.9605610896540213 ) ) ;
#212598=SHAPE_DEFINITION_REPRESENTATION ( #165904, #90142 ) ;
#212623=AXIS2_PLACEMENT_3D ( 'NONE', #248811, #28517, #71471 ) ;
#212627=CARTESIAN_POINT ( 'NONE',  ( -20.64999999999999858, 61.88149656937975607, -248.1136133839584090 ) ) ;
#212628=DIRECTION ( 'NONE',  ( 0.000000000000000000, 0.9126074666063660468, 0.4088369013363524762 ) ) ;
#212636=DIRECTION ( 'NONE',  ( 0.000000000000000000, 0.9126074666063660468, 0.4088369013363524762 ) ) ;
#212659=AXIS2_PLACEMENT_3D ( 'NONE', #102679, #119720, #45305 ) ;
#212675=B_SPLINE_CURVE_WITH_KNOTS ( 'NONE', 3,
 ( #210874, #32264, #130034, #237820, #13970, #248724, #75240, #10111, #113060, #89627, #111783, #70110, #173082, #149640, #133897, #131332 ),
 .UNSPECIFIED., .F., .F.,
 ( 4, 3, 3, 3, 3, 4 ),
 ( 0.000000000000000000, 3.357088238233183250E-05, 6.714213034886279538E-05, 0.0001007408646120870187, 0.0001343627955914160831, 0.0001573956632895967837 ),
 .UNSPECIFIED. ) ;
#212700=VERTEX_POINT ( 'NONE', #73850 ) ;
#212705=DIRECTION ( 'NONE',  ( -3.469446951953529623E-14, -0.9126074666063660468, -0.4088369013363524762 ) ) ;
#212713=VERTEX_POINT ( 'NONE', #172961 ) ;
#212731=EDGE_CURVE ( 'NONE', #15058, #104983, #17678, .T. ) ;
#212760=VERTEX_POINT ( 'NONE', #254953 ) ;
#212798=EDGE_LOOP ( 'NONE', ( #192904, #257658, #17768, #108285 ) ) ;
#212825=VERTEX_POINT ( 'NONE', #142755 ) ;
#212848=CARTESIAN_POINT ( 'NONE',  ( -23.15000000000000213, 54.89227652059045681, -239.1913228807104588 ) ) ;
#212879=DIRECTION ( 'NONE',  ( 0.000000000000000000, 0.9126074666063660468, 0.4088369013363524762 ) ) ;
#212884=DIRECTION ( 'NONE',  ( 0.000000000000000000, 0.9126074666063769270, 0.4088369013363280513 ) ) ;
#212894=ORIENTED_EDGE ( 'NONE', *, *, #68943, .T. ) ;
#212896=DIRECTION ( 'NONE',  ( -1.000000000000000000, -0.000000000000000000, -0.000000000000000000 ) ) ;
#212897=ORIENTED_EDGE ( 'NONE', *, *, #202594, .F. ) ;
#212902=AXIS2_PLACEMENT_3D ( 'NONE', #143909, #4395, #39713 ) ;
#212919=DIRECTION ( 'NONE',  ( 0.000000000000000000, 0.9126074666063769270, 0.4088369013363282733 ) ) ;
#212945=AXIS2_PLACEMENT_3D ( 'NONE', #12461, #91972, #231503 ) ;
#212985=DIRECTION ( 'NONE',  ( 0.000000000000000000, -0.5283051335750404975, 0.8490545835446967615 ) ) ;
#212988=ADVANCED_FACE ( 'NONE', ( #227438 ), #7103, .T. ) ;
#212991=AXIS2_PLACEMENT_3D ( 'NONE', #100340, #166798, #114154 ) ;
#213019=FACE_OUTER_BOUND ( 'NONE', #150262, .T. ) ;
#213033=CARTESIAN_POINT ( 'NONE',  ( 23.14999999999999858, 67.23127455305835554, -235.8551265064784559 ) ) ;
#213044=LINE ( 'NONE', #52676, #9835 ) ;
#213074=EDGE_CURVE ( 'NONE', #181336, #9664, #52647, .T. ) ;
#213100=CARTESIAN_POINT ( 'NONE',  ( 21.05000000000000071, 43.04635563724865932, -239.7315875678428370 ) ) ;
#213113=AXIS2_PLACEMENT_3D ( 'NONE', #84840, #49605, #147425 ) ;
#213215=EDGE_LOOP ( 'NONE', ( #108205, #232752, #243257, #189928 ) ) ;
#213231=CARTESIAN_POINT ( 'NONE',  ( -21.00448002041583706, 38.10493783585286565, -236.0281705111790131 ) ) ;
#213241=AXIS2_PLACEMENT_3D ( 'NONE', #113673, #114961, #97933 ) ;
#213280=VECTOR ( 'NONE', #10934, 1000.000000000000000 ) ;
#213286=CARTESIAN_POINT ( 'NONE',  ( -20.85000000000000142, 74.93036000061670165, -233.6816308724374949 ) ) ;
#213290=CARTESIAN_POINT ( 'NONE',  ( -22.50000000000000000, 31.89597452117652665, -238.9192857152812053 ) ) ;
#213291=DIRECTION ( 'NONE',  ( -1.000000000000000000, 1.207181226542539700E-16, -2.694675058168174199E-16 ) ) ;
#213314=DIRECTION ( 'NONE',  ( 1.000000000000000000, 0.000000000000000000, 0.000000000000000000 ) ) ;
#213319=CARTESIAN_POINT ( 'NONE',  ( -18.50000000000000000, 42.98415524044398950, -233.9519173640448173 ) ) ;
#213322=ADVANCED_FACE ( 'NONE', ( #186753 ), #140902, .T. ) ;
#213334=ADVANCED_FACE ( 'NONE', ( #234858 ), #193174, .F. ) ;
#213338=DIRECTION ( 'NONE',  ( 0.000000000000000000, -0.9126074666063770380, -0.4088369013363281068 ) ) ;
#213340=EDGE_LOOP ( 'NONE', ( #110672, #152752, #68621, #104776 ) ) ;
#213351=LINE ( 'NONE', #192528, #168576 ) ;
#213362=SPHERICAL_SURFACE ( 'NONE', #176176, 0.1000000000000000056 ) ;
#213366=DIRECTION ( 'NONE',  ( 0.000000000000000000, -0.4088369013363205573, 0.9126074666063803686 ) ) ;
#213377=AXIS2_PLACEMENT_3D ( 'NONE', #28907, #168420, #250464 ) ;
#213386=VERTEX_POINT ( 'NONE', #130610 ) ;
#213402=AXIS2_PLACEMENT_3D ( 'NONE', #228211, #63991, #30029 ) ;
#213412=LINE ( 'NONE', #197701, #218451 ) ;
#213414=CARTESIAN_POINT ( 'NONE',  ( 22.00356870140716126, 33.69312245271871120, -242.9308869566589237 ) ) ;
#213421=AXIS2_PLACEMENT_3D ( 'NONE', #16853, #211186, #256676 ) ;
#213432=CARTESIAN_POINT ( 'NONE',  ( 23.24999999999999289, 55.39363411790989034, -234.6384634766556303 ) ) ;
#213435=FACE_OUTER_BOUND ( 'NONE', #75433, .T. ) ;
#213498=CARTESIAN_POINT ( 'NONE',  ( 20.94999999999999929, 53.86595165227826243, -236.3638196928718855 ) ) ;
#213500=ORIENTED_EDGE ( 'NONE', *, *, #255289, .F. ) ;
#213502=CARTESIAN_POINT ( 'NONE',  ( -21.05000000000000071, 38.17611739746671873, -236.1379531878919806 ) ) ;
#213523=DIRECTION ( 'NONE',  ( -1.000000000000000000, -0.000000000000000000, -0.000000000000000000 ) ) ;
#213526=EDGE_CURVE ( 'NONE', #15852, #114879, #10516, .T. ) ;
#213537=DIRECTION ( 'NONE',  ( 0.000000000000000000, 0.9126074666063773710, 0.4088369013363272741 ) ) ;
#213542=FACE_OUTER_BOUND ( 'NONE', #101977, .T. ) ;
#213543=LINE ( 'NONE', #238244, #112144 ) ;
#213573=VECTOR ( 'NONE', #227880, 1000.000000000000000 ) ;
#213634=DIRECTION ( 'NONE',  ( 0.000000000000000000, 0.9126074666063771490, 0.4088369013363281623 ) ) ;
#213641=DIRECTION ( 'NONE',  ( 1.000000000000000000, 0.000000000000000000, 0.000000000000000000 ) ) ;
#213648=AXIS2_PLACEMENT_3D ( 'NONE', #148299, #106576, #188701 ) ;
#213658=VERTEX_POINT ( 'NONE', #165604 ) ;
#213685=CARTESIAN_POINT ( 'NONE',  ( -20.94999999999999929, 63.48958393997221350, -237.5313578019574265 ) ) ;
#213697=CYLINDRICAL_SURFACE ( 'NONE', #147280, 11.74999999999999822 ) ;
#213708=CARTESIAN_POINT ( 'NONE',  ( 22.45380639572341153, 25.93539157114272342, -254.3551731436069474 ) ) ;
#213757=DIRECTION ( 'NONE',  ( 0.000000000000000000, 0.9126074666063660468, 0.4088369013363524762 ) ) ;
#213771=EDGE_CURVE ( 'NONE', #210045, #111477, #99356, .T. ) ;
#213773=CARTESIAN_POINT ( 'NONE',  ( -23.25000000000000000, 78.48087866980282001, -232.8271061603568910 ) ) ;
#213817=CIRCLE ( 'NONE', #1408, 0.09999999999999939493 ) ;
#213819=ORIENTED_EDGE ( 'NONE', *, *, #30786, .T. ) ;
#213836=CARTESIAN_POINT ( 'NONE',  ( -18.50000000000000000, 52.21971469324220294, -232.5539039185337913 ) ) ;
#213840=VECTOR ( 'NONE', #217384, 1000.000000000000114 ) ;
#213870=EDGE_LOOP ( 'NONE', ( #112899, #200629, #23797, #100266 ) ) ;
#213896=AXIS2_PLACEMENT_3D ( 'NONE', #64028, #164423, #159297 ) ;
#213910=DIRECTION ( 'NONE',  ( 1.000000000000000000, 0.000000000000000000, 0.000000000000000000 ) ) ;
#213913=CIRCLE ( 'NONE', #159748, 0.5999999999999968692 ) ;
#213956=EDGE_LOOP ( 'NONE', ( #162887, #198841, #149976, #224593 ) ) ;
#213960=EDGE_CURVE ( 'NONE', #215121, #785, #3280, .T. ) ;
#214016=AXIS2_PLACEMENT_3D ( 'NONE', #166622, #42791, #63632 ) ;
#214029=ORIENTED_EDGE ( 'NONE', *, *, #80659, .T. ) ;
#214067=ORIENTED_EDGE ( 'NONE', *, *, #122082, .T. ) ;
#214083=ADVANCED_FACE ( 'NONE', ( #207949 ), #187101, .F. ) ;
#214087=DIRECTION ( 'NONE',  ( 0.000000000000000000, -0.9126074666063771490, -0.4088369013363276627 ) ) ;
#214164=AXIS2_PLACEMENT_3D ( 'NONE', #139024, #120816, #176942 ) ;
#214196=CIRCLE ( 'NONE', #14311, 0.1999999999999987899 ) ;
#214211=VECTOR ( 'NONE', #147846, 1000.000000000000114 ) ;
#214229=ORIENTED_EDGE ( 'NONE', *, *, #232407, .T. ) ;
#214234=SPHERICAL_SURFACE ( 'NONE', #166680, 0.1000000000000000056 ) ;
#214236=AXIS2_PLACEMENT_3D ( 'NONE', #188214, #227332, #9567 ) ;
#214294=EDGE_CURVE ( 'NONE', #103333, #167448, #138623, .T. ) ;
#214346=DIRECTION ( 'NONE',  ( 0.000000000000000000, 0.9126074666063660468, 0.4088369013363524762 ) ) ;
#214348=ORIENTED_EDGE ( 'NONE', *, *, #87131, .T. ) ;
#214363=ORIENTED_EDGE ( 'NONE', *, *, #198802, .T. ) ;
#214373=AXIS2_PLACEMENT_3D ( 'NONE', #197389, #56568, #133573 ) ;
#214375=AXIS2_PLACEMENT_3D ( 'NONE', #168257, #247744, #69131 ) ;
#214376=ORIENTED_EDGE ( 'NONE', *, *, #252058, .T. ) ;
#214421=CARTESIAN_POINT ( 'NONE',  ( 18.49999999999998934, 53.28269063671665151, -234.9266833317103647 ) ) ;
#214442=VERTEX_POINT ( 'NONE', #6852 ) ;
#214443=VECTOR ( 'NONE', #204689, 1000.000000000000227 ) ;
#214450=CARTESIAN_POINT ( 'NONE',  ( -18.52328366898031931, 77.30140549317121668, -241.9095147967482546 ) ) ;
#214500=VERTEX_POINT ( 'NONE', #165954 ) ;
#214553=VERTEX_POINT ( 'NONE', #236167 ) ;
#214572=ORIENTED_EDGE ( 'NONE', *, *, #200446, .F. ) ;
#214595=DIRECTION ( 'NONE',  ( 1.000000000000000000, 0.000000000000000000, 0.000000000000000000 ) ) ;
#214600=CARTESIAN_POINT ( 'NONE',  ( -20.00857864376270001, 52.21971469324220294, -232.5539039185337913 ) ) ;
#214602=ORIENTED_EDGE ( 'NONE', *, *, #244581, .T. ) ;
#214616=ORIENTED_EDGE ( 'NONE', *, *, #132465, .T. ) ;
#214631=AXIS2_PLACEMENT_3D ( 'NONE', #6138, #184785, #160122 ) ;
#214649=CARTESIAN_POINT ( 'NONE',  ( 20.85882249326303040, 68.11287320386161070, -224.1382462126928488 ) ) ;
#214653=AXIS2_PLACEMENT_3D ( 'NONE', #79934, #143789, #44714 ) ;
#214677=ADVANCED_FACE ( 'NONE', ( #53680 ), #99339, .T. ) ;
#214689=CARTESIAN_POINT ( 'NONE',  ( -21.05000000000000071, 55.49311008795314848, -234.6486875357297492 ) ) ;
#214719=ORIENTED_EDGE ( 'NONE', *, *, #256188, .T. ) ;
#214721=CARTESIAN_POINT ( 'NONE',  ( 20.52683494730153413, 40.74930916959595351, -237.8782020542120392 ) ) ;
#214766=DIRECTION ( 'NONE',  ( 0.000000000000000000, -0.4009882990724537022, 0.9160831752668424643 ) ) ;
#214806=ORIENTED_EDGE ( 'NONE', *, *, #226020, .T. ) ;
#214879=DIRECTION ( 'NONE',  ( 0.000000000000000000, 0.9126074666063772600, 0.4088369013363277182 ) ) ;
#214881=FACE_OUTER_BOUND ( 'NONE', #113217, .T. ) ;
#214897=DIRECTION ( 'NONE',  ( -1.000000000000000000, -0.000000000000000000, -0.000000000000000000 ) ) ;
#214907=EDGE_LOOP ( 'NONE', ( #205250, #253896, #120005, #204934, #180040 ) ) ;
#214923=VECTOR ( 'NONE', #145494, 1000.000000000000114 ) ;
#214935=ORIENTED_EDGE ( 'NONE', *, *, #41565, .F. ) ;
#214945=EDGE_LOOP ( 'NONE', ( #100738, #6320, #221419, #181388 ) ) ;
#214957=DIRECTION ( 'NONE',  ( 0.000000000000000000, 0.9126074666063660468, 0.4088369013363524762 ) ) ;
#214975=FACE_OUTER_BOUND ( 'NONE', #166482, .T. ) ;
#214984=VERTEX_POINT ( 'NONE', #74261 ) ;
#215015=DIRECTION ( 'NONE',  ( 0.000000000000000000, 0.9126074666063545004, 0.4088369013363783999 ) ) ;
#215068=CARTESIAN_POINT ( 'NONE',  ( -20.94999999999999929, 56.55376719376374695, -240.6385182521135278 ) ) ;
#215072=CARTESIAN_POINT ( 'NONE',  ( -20.05000000000000426, 44.14788529697245423, -236.0604079036328073 ) ) ;
#215075=EDGE_LOOP ( 'NONE', ( #208740, #229596, #81697, #1525 ) ) ;
#215085=DIRECTION ( 'NONE',  ( 0.000000000000000000, -0.4088369013363783999, 0.9126074666063545004 ) ) ;
#215121=VERTEX_POINT ( 'NONE', #37690 ) ;
#215122=AXIS2_PLACEMENT_3D ( 'NONE', #192185, #29287, #89204 ) ;
#215125=CARTESIAN_POINT ( 'NONE',  ( 21.05000000000000071, 69.34766280046808617, -247.6726305063181144 ) ) ;
#215136=VECTOR ( 'NONE', #96422, 1000.000000000000000 ) ;
#215161=AXIS2_PLACEMENT_3D ( 'NONE', #79761, #141058, #60214 ) ;
#215227=CARTESIAN_POINT ( 'NONE',  ( -21.05000000000000426, 30.78878838668999052, -252.2904874585705102 ) ) ;
#215246=ORIENTED_EDGE ( 'NONE', *, *, #108977, .T. ) ;
#215280=CARTESIAN_POINT ( 'NONE',  ( -20.64999999999999858, 44.87429835298446790, -237.9265065269792103 ) ) ;
#215332=ORIENTED_EDGE ( 'NONE', *, *, #158357, .T. ) ;
#215338=FACE_OUTER_BOUND ( 'NONE', #62101, .T. ) ;
#215379=( BOUNDED_SURFACE ( )  B_SPLINE_SURFACE ( 3, 2, ( 
 ( #23193, #220088, #41472 ),
 ( #121015, #200519, #21889 ),
 ( #81817, #63563, #161413 ),
 ( #240938, #141818, #187389 ),
 ( #84363, #27050, #67423 ),
 ( #7444, #25736, #203079 ),
 ( #66143, #144365, #10020 ),
 ( #106527, #206941, #188653 ) ),
 .UNSPECIFIED., .F., .F., .F. ) 
 B_SPLINE_SURFACE_WITH_KNOTS ( ( 4, 2, 2, 4 ),
 ( 3, 3 ),
 ( 0.0001704874539069812654, 0.0003809798300636641107, 0.0004862260181420055062, 0.0005914722062203469017 ),
 ( 0.000000000000000000, 1.000000000000000000 ),
 .UNSPECIFIED. ) 
 GEOMETRIC_REPRESENTATION_ITEM ( )  RATIONAL_B_SPLINE_SURFACE ( (
 ( 1.000000000000000000, 0.7071067811865259234, 1.000000000000000000),
 ( 1.000000000000000000, 0.7670648383569823592, 1.000000000000000000),
 ( 1.000000000000000000, 0.8204820770261218588, 1.000000000000000000),
 ( 1.000000000000000000, 0.8877218296109600226, 1.000000000000000000),
 ( 1.000000000000000000, 0.9080815932658325984, 1.000000000000000000),
 ( 1.000000000000000000, 0.9395541505869027255, 1.000000000000000000),
 ( 1.000000000000000000, 0.9506520335373465080, 1.000000000000000000),
 ( 1.000000000000000000, 0.9504532311154414437, 1.000000000000000000) ) ) 
 REPRESENTATION_ITEM ( '' )  SURFACE ( )  );
#215381=AXIS2_PLACEMENT_3D ( 'NONE', #78313, #211748, #178756 ) ;
#215419=EDGE_CURVE ( 'NONE', #89549, #145938, #188721, .T. ) ;
#215453=ORIENTED_EDGE ( 'NONE', *, *, #50725, .T. ) ;
#215457=CARTESIAN_POINT ( 'NONE',  ( 18.52928932188133970, 54.95214567929434679, -230.0923768967488456 ) ) ;
#215460=VERTEX_POINT ( 'NONE', #131314 ) ;
#215479=ORIENTED_EDGE ( 'NONE', *, *, #121385, .T. ) ;
#215484=( BOUNDED_SURFACE ( )  B_SPLINE_SURFACE ( 3, 2, ( 
 ( #227028, #69262, #4128 ),
 ( #67958, #208771, #144912 ),
 ( #146202, #147500, #148794 ),
 ( #228331, #129225, #109642 ),
 ( #83631, #163223, #143638 ),
 ( #223170, #124101, #104489 ),
 ( #184052, #5386, #84919 ),
 ( #34013, #152667, #75685 ) ),
 .UNSPECIFIED., .F., .F., .T. ) 
 B_SPLINE_SURFACE_WITH_KNOTS ( ( 4, 2, 2, 4 ),
 ( 3, 3 ),
 ( 0.0001723339234021436671, 0.0002782939632050007717, 0.0003842540030078578491, 0.0005961740826135720041 ),
 ( 0.000000000000000000, 1.000000000000000000 ),
 .UNSPECIFIED. ) 
 GEOMETRIC_REPRESENTATION_ITEM ( )  RATIONAL_B_SPLINE_SURFACE ( (
 ( 1.000000000000000000, 0.9504532311154467727, 1.000000000000000000),
 ( 1.000000000000000000, 0.9506023220712702670, 1.000000000000000000),
 ( 1.000000000000000000, 0.9395774818177810017, 1.000000000000000000),
 ( 1.000000000000000000, 0.9079328464651014174, 1.000000000000000000),
 ( 1.000000000000000000, 0.8875702416200158540, 1.000000000000000000),
 ( 1.000000000000000000, 0.8205919608051213121, 1.000000000000000000),
 ( 1.000000000000000000, 0.7666842783589820076, 1.000000000000000000),
 ( 1.000000000000000000, 0.7071067811865475727, 1.000000000000000000) ) ) 
 REPRESENTATION_ITEM ( '' )  SURFACE ( )  );
#215487=VERTEX_POINT ( 'NONE', #244197 ) ;
#215508=ORIENTED_EDGE ( 'NONE', *, *, #82715, .T. ) ;
#215523=CYLINDRICAL_SURFACE ( 'NONE', #202798, 0.09999999999999939493 ) ;
#215549=EDGE_CURVE ( 'NONE', #133691, #178504, #112679, .T. ) ;
#215560=EDGE_CURVE ( 'NONE', #57578, #104336, #20379, .T. ) ;
#215594=VERTEX_POINT ( 'NONE', #17766 ) ;
#215664=EDGE_CURVE ( 'NONE', #94854, #9091, #68150, .T. ) ;
#215684=ORIENTED_EDGE ( 'NONE', *, *, #66326, .F. ) ;
#215686=EDGE_CURVE ( 'NONE', #217030, #195501, #200343, .T. ) ;
#215730=DIRECTION ( 'NONE',  ( 1.000000000000000000, 0.000000000000000000, 0.000000000000000000 ) ) ;
#215735=B_SPLINE_CURVE_WITH_KNOTS ( 'NONE', 3,
 ( #153048, #93027, #68651, #109037, #94301, #172619 ),
 .UNSPECIFIED., .F., .F.,
 ( 4, 2, 4 ),
 ( 0.000000000000000000, 0.0001496588209255842611, 0.0002993176418511685221 ),
 .UNSPECIFIED. ) ;
#215810=DIRECTION ( 'NONE',  ( -1.000000000000000000, -0.000000000000000000, 0.000000000000000000 ) ) ;
#215839=AXIS2_PLACEMENT_3D ( 'NONE', #149646, #229170, #231740 ) ;
#215847=CARTESIAN_POINT ( 'NONE',  ( 20.94999999999999929, 61.88149656937974896, -248.1136133839584090 ) ) ;
#215856=ORIENTED_EDGE ( 'NONE', *, *, #36726, .T. ) ;
#215899=CARTESIAN_POINT ( 'NONE',  ( 20.94999999999999574, 47.95459712139159336, -246.5019368548292675 ) ) ;
#215967=ORIENTED_EDGE ( 'NONE', *, *, #211335, .T. ) ;
#215968=DIRECTION ( 'NONE',  ( 0.000000000000000000, 0.9126074666063772600, 0.4088369013363274407 ) ) ;
#215970=VERTEX_POINT ( 'NONE', #216237 ) ;
#215984=VERTEX_POINT ( 'NONE', #213685 ) ;
#215986=EDGE_CURVE ( 'NONE', #217030, #251464, #46205, .T. ) ;
#216008=DIRECTION ( 'NONE',  ( 0.000000000000000000, 0.9126074666063791474, 0.4088369013363231108 ) ) ;
#216051=ADVANCED_FACE ( 'NONE', ( #42749 ), #184817, .T. ) ;
#216054=DIRECTION ( 'NONE',  ( 0.000000000000000000, -0.09425075112712516523, -0.9955484899852807823 ) ) ;
#216058=CARTESIAN_POINT ( 'NONE',  ( -21.05000000000000071, 56.55376719376374695, -240.6385182521135278 ) ) ;
#216071=DIRECTION ( 'NONE',  ( 1.000000000000000000, 0.000000000000000000, 0.000000000000000000 ) ) ;
#216077=CARTESIAN_POINT ( 'NONE',  ( -22.49510344025093644, 25.99963044612954022, -254.2528391593452000 ) ) ;
#216091=CARTESIAN_POINT ( 'NONE',  ( -21.05000000000000071, 69.16514130714681130, -247.7543978865853660 ) ) ;
#216116=EDGE_LOOP ( 'NONE', ( #168449, #249014, #171737, #163459 ) ) ;
#216142=CARTESIAN_POINT ( 'NONE',  ( 20.85000000000000142, 56.23643450586806836, -227.9054833905874204 ) ) ;
#216151=CIRCLE ( 'NONE', #124418, 0.1000000000000024342 ) ;
#216161=VERTEX_POINT ( 'NONE', #208256 ) ;
#216190=ORIENTED_EDGE ( 'NONE', *, *, #57421, .F. ) ;
#216211=CIRCLE ( 'NONE', #224592, 0.09999999999999063804 ) ;
#216237=CARTESIAN_POINT ( 'NONE',  ( 18.59999999999997655, 74.44087353924872730, -232.6253149859214773 ) ) ;
#216273=FACE_OUTER_BOUND ( 'NONE', #25991, .T. ) ;
#216300=ADVANCED_FACE ( 'NONE', ( #219777 ), #121980, .F. ) ;
#216307=EDGE_LOOP ( 'NONE', ( #55576, #595, #25640 ) ) ;
#216316=CARTESIAN_POINT ( 'NONE',  ( 21.12642695952774119, 30.80001426052127300, -252.0675078730340601 ) ) ;
#216350=ADVANCED_FACE ( 'NONE', ( #204069 ), #9636, .T. ) ;
#216417=DIRECTION ( 'NONE',  ( -1.000000000000000000, 1.335000415235278971E-16, -2.979993593738921214E-16 ) ) ;
#216422=CARTESIAN_POINT ( 'NONE',  ( -23.15000000000000213, 36.65892442174472876, -249.5511627012454596 ) ) ;
#216443=EDGE_CURVE ( 'NONE', #97383, #255010, #117777, .T. ) ;
#216477=AXIS2_PLACEMENT_3D ( 'NONE', #186057, #242170, #165207 ) ;
#216528=TOROIDAL_SURFACE ( 'NONE', #199811, 0.9750000000000019762, 0.1000000000000000056 ) ;
#216573=VECTOR ( 'NONE', #110005, 1000.000000000000114 ) ;
#216577=DIRECTION ( 'NONE',  ( 0.000000000000000000, 0.9126074666063783702, 0.4088369013363252757 ) ) ;
#216589=( BOUNDED_CURVE ( )  B_SPLINE_CURVE ( 3, ( #156554, #78249, #159109, #157846 ),
 .UNSPECIFIED., .F., .F. ) 
 B_SPLINE_CURVE_WITH_KNOTS ( ( 4, 4 ),
 ( 4.712388980384689674, 6.283185307179586232 ),
 .UNSPECIFIED. ) 
 CURVE ( )  GEOMETRIC_REPRESENTATION_ITEM ( )  RATIONAL_B_SPLINE_CURVE ( ( 1.000000000000000000, 0.8047378541243649375, 0.8047378541243649375, 1.000000000000000000 ) ) 
 REPRESENTATION_ITEM ( '' )  );
#216596=EDGE_CURVE ( 'NONE', #68804, #155635, #209542, .T. ) ;
#216620=FACE_OUTER_BOUND ( 'NONE', #68447, .T. ) ;
#216647=ORIENTED_EDGE ( 'NONE', *, *, #153109, .T. ) ;
#216655=LINE ( 'NONE', #34203, #257945 ) ;
#216664=CIRCLE ( 'NONE', #141823, 11.74999999999999822 ) ;
#216671=ORIENTED_EDGE ( 'NONE', *, *, #45494, .F. ) ;
#216683=ORIENTED_EDGE ( 'NONE', *, *, #228591, .T. ) ;
#216693=DIRECTION ( 'NONE',  ( 0.000000000000000000, -0.9188841341108708871, -0.3945274997757635127 ) ) ;
#216711=DIRECTION ( 'NONE',  ( 0.000000000000000000, 0.5859227990963362664, 0.8103668758649469339 ) ) ;
#216735=VECTOR ( 'NONE', #83426, 1000.000000000000114 ) ;
#216744=LINE ( 'NONE', #159366, #194378 ) ;
#216754=DIRECTION ( 'NONE',  ( 0.000000000000000000, -0.8490545835447252943, -0.5283051335749948674 ) ) ;
#216797=EDGE_LOOP ( 'NONE', ( #188055, #142724, #23831, #123064 ) ) ;
#216819=EDGE_LOOP ( 'NONE', ( #22010, #12319, #10656, #199413, #207259 ) ) ;
#216832=AXIS2_PLACEMENT_3D ( 'NONE', #233556, #17082, #99141 ) ;
#216898=( BOUNDED_CURVE ( )  B_SPLINE_CURVE ( 3, ( #79881, #35686, #159457, #238998 ),
 .UNSPECIFIED., .F., .F. ) 
 B_SPLINE_CURVE_WITH_KNOTS ( ( 4, 4 ),
 ( 0.06456096931748382672, 3.077031684272309775 ),
 .UNSPECIFIED. ) 
 CURVE ( )  GEOMETRIC_REPRESENTATION_ITEM ( )  RATIONAL_B_SPLINE_CURVE ( ( 1.000000000000000000, 0.3763440860215097605, 0.3763440860215097605, 1.000000000000000000 ) ) 
 REPRESENTATION_ITEM ( '' )  );
#216905=DIRECTION ( 'NONE',  ( -1.000000000000000000, 0.000000000000000000, 0.000000000000000000 ) ) ;
#216909=DIRECTION ( 'NONE',  ( 0.000000000000000000, 0.9126074666063769270, 0.4088369013363280513 ) ) ;
#216936=CARTESIAN_POINT ( 'NONE',  ( -21.55000000000000071, 44.83341466285084209, -237.8352457803185871 ) ) ;
#216946=LINE ( 'NONE', #99551, #38585 ) ;
#216953=DIRECTION ( 'NONE',  ( 0.000000000000000000, 0.9126074666063772600, 0.4088369013363276627 ) ) ;
#216972=CARTESIAN_POINT ( 'NONE',  ( -23.15000000000000213, 46.05992536685982230, -240.5730681801377102 ) ) ;
#217015=CARTESIAN_POINT ( 'NONE',  ( -18.47140463609786565, 77.27494131181350667, -241.9533158081853230 ) ) ;
#217030=VERTEX_POINT ( 'NONE', #217552 ) ;
#217060=DIRECTION ( 'NONE',  ( 0.000000000000000000, -0.9126074666063770380, -0.4088369013363281068 ) ) ;
#217062=EDGE_CURVE ( 'NONE', #229414, #24913, #189071, .T. ) ;
#217073=EDGE_CURVE ( 'NONE', #106155, #200983, #179421, .T. ) ;
#217116=EDGE_LOOP ( 'NONE', ( #118631, #149094, #169535, #176200 ) ) ;
#217124=CARTESIAN_POINT ( 'NONE',  ( -20.00857864376270001, 44.14788529697245423, -236.0604079036328073 ) ) ;
#217136=ORIENTED_EDGE ( 'NONE', *, *, #70406, .F. ) ;
#217152=EDGE_CURVE ( 'NONE', #133508, #69777, #55751, .T. ) ;
#217166=CARTESIAN_POINT ( 'NONE',  ( 18.50211644919735221, 68.02921119886117651, -224.2090419302653856 ) ) ;
#217205=DIRECTION ( 'NONE',  ( 0.000000000000000000, -0.4088369013363280513, 0.9126074666063769270 ) ) ;
#217240=EDGE_CURVE ( 'NONE', #213658, #223475, #214196, .T. ) ;
#217246=CIRCLE ( 'NONE', #237935, 0.09999999999999609201 ) ;
#217247=VERTEX_POINT ( 'NONE', #11369 ) ;
#217251=ORIENTED_EDGE ( 'NONE', *, *, #208423, .F. ) ;
#217261=ORIENTED_EDGE ( 'NONE', *, *, #116274, .F. ) ;
#217266=DIRECTION ( 'NONE',  ( 0.000000000000000000, -0.4088369013363280513, 0.9126074666063772600 ) ) ;
#217284=CIRCLE ( 'NONE', #234050, 12.87499999999999822 ) ;
#217331=CARTESIAN_POINT ( 'NONE',  ( -20.94999999999999929, 44.25095746879271985, -258.9156452930671435 ) ) ;
#217339=DIRECTION ( 'NONE',  ( 0.000000000000000000, 0.9955484899852913294, -0.09425075112701486457 ) ) ;
#217345=DIRECTION ( 'NONE',  ( 0.000000000000000000, 0.4088369013363783999, -0.9126074666063545004 ) ) ;
#217352=CARTESIAN_POINT ( 'NONE',  ( -22.50000000000000000, 25.98655542988603173, -254.2226763854395983 ) ) ;
#217353=CIRCLE ( 'NONE', #9089, 0.1000000000000024342 ) ;
#217365=PLANE ( 'NONE',  #189784 ) ;
#217373=CARTESIAN_POINT ( 'NONE',  ( -18.50000000000000355, 77.31057150535087885, -241.6632115154811231 ) ) ;
#217384=DIRECTION ( 'NONE',  ( 0.000000000000000000, 0.9126074666063770380, 0.4088369013363281068 ) ) ;
#217385=LINE ( 'NONE', #196550, #66333 ) ;
#217388=CARTESIAN_POINT ( 'NONE',  ( -18.44362607810622379, 46.98013086100849733, -255.3267083682162593 ) ) ;
#217410=CARTESIAN_POINT ( 'NONE',  ( 20.94999999999999929, 67.23127455305835554, -235.8551265064784559 ) ) ;
#217439=ADVANCED_FACE ( 'NONE', ( #62059 ), #201546, .F. ) ;
#217476=EDGE_CURVE ( 'NONE', #9522, #71022, #180879, .T. ) ;
#217498=ORIENTED_EDGE ( 'NONE', *, *, #90964, .T. ) ;
#217507=EDGE_CURVE ( 'NONE', #220102, #118038, #255656, .T. ) ;
#217512=AXIS2_PLACEMENT_3D ( 'NONE', #70661, #111037, #130591 ) ;
#217542=AXIS2_PLACEMENT_3D ( 'NONE', #245843, #146709, #150599 ) ;
#217551=EDGE_CURVE ( 'NONE', #94408, #203994, #105838, .T. ) ;
#217552=CARTESIAN_POINT ( 'NONE',  ( -18.59999999999999787, 78.57744179526842743, -232.8011145694030972 ) ) ;
#217555=AXIS2_PLACEMENT_3D ( 'NONE', #200367, #201642, #256413 ) ;
#217579=AXIS2_PLACEMENT_3D ( 'NONE', #143646, #244026, #84925 ) ;
#217594=AXIS2_PLACEMENT_3D ( 'NONE', #18882, #257440, #80103 ) ;
#217612=EDGE_CURVE ( 'NONE', #124911, #174581, #250935, .T. ) ;
#217616=VERTEX_POINT ( 'NONE', #211840 ) ;
#217619=LINE ( 'NONE', #238493, #115638 ) ;
#217620=( BOUNDED_SURFACE ( )  B_SPLINE_SURFACE ( 3, 2, ( 
 ( #36106, #253839, #75246 ),
 ( #257635, #79035, #193895 ),
 ( #15263, #94774, #214721 ),
 ( #55614, #120788, #201572 ),
 ( #141601, #161178, #66889 ),
 ( #146401, #228546, #200300 ),
 ( #101142, #41255, #68175 ),
 ( #221127, #3358, #206403 ),
 ( #162472, #129432, #219852 ),
 ( #245539, #109851, #225926 ),
 ( #60771, #2077, #42497 ),
 ( #82876, #207702, #122047 ) ),
 .UNSPECIFIED., .F., .F., .F. ) 
 B_SPLINE_SURFACE_WITH_KNOTS ( ( 4, 2, 2, 2, 2, 4 ),
 ( 3, 3 ),
 ( 3.174653483277205090, 3.943930578431714018, 4.713207673586222946, 5.482484768740731873, 5.867123316317986337, 6.251761863895240801 ),
 ( 0.000000000000000000, 1.000000000000000000 ),
 .UNSPECIFIED. ) 
 GEOMETRIC_REPRESENTATION_ITEM ( )  RATIONAL_B_SPLINE_SURFACE ( (
 ( 1.000000000000000000, 0.8659465255642859738, 1.000000000000000000),
 ( 1.000000000000000000, 0.8648614068486716322, 1.000000000000000000),
 ( 1.000000000000000000, 0.8489031841325624939, 1.000000000000000000),
 ( 1.000000000000000000, 0.7927507630159957852, 1.000000000000000000),
 ( 1.000000000000000000, 0.7523013859024111349, 1.000000000000000000),
 ( 1.000000000000000000, 0.6616226951181095606, 1.000000000000000000),
 ( 1.000000000000000000, 0.6112214368682694632, 1.000000000000000000),
 ( 1.000000000000000000, 0.5507684314519089019, 1.000000000000000000),
 ( 1.000000000000000000, 0.5333267243155448423, 1.000000000000000000),
 ( 1.000000000000000000, 0.5084565446476616568, 1.000000000000000000),
 ( 1.000000000000000000, 0.5010722703453642790, 1.000000000000000000),
 ( 1.000000000000000000, 0.5001234037138547750, 1.000000000000000000) ) ) 
 REPRESENTATION_ITEM ( '' )  SURFACE ( )  );
#217681=CARTESIAN_POINT ( 'NONE',  ( -20.64999999999999858, 69.05648948627110428, -235.0374527038057977 ) ) ;
#217697=CARTESIAN_POINT ( 'NONE',  ( 20.85000000000000142, 74.44087353924872730, -232.6253149859214773 ) ) ;
#217699=AXIS2_PLACEMENT_3D ( 'NONE', #11724, #185206, #87368 ) ;
#217728=CIRCLE ( 'NONE', #105272, 12.77499999999999147 ) ;
#217731=CIRCLE ( 'NONE', #163774, 0.5000000000000001110 ) ;
#217732=EDGE_CURVE ( 'NONE', #166897, #209494, #101912, .T. ) ;
#217733=CARTESIAN_POINT ( 'NONE',  ( -20.54999999999999716, 48.89266972451527948, -253.5637804087949121 ) ) ;
#217745=CARTESIAN_POINT ( 'NONE',  ( -21.05000000000000071, 40.58313652815211015, -247.7931640254992658 ) ) ;
#217746=ORIENTED_EDGE ( 'NONE', *, *, #73844, .T. ) ;
#217751=CARTESIAN_POINT ( 'NONE',  ( -18.50000000000000000, 77.35494420175976416, -241.6200040285045532 ) ) ;
#217757=CIRCLE ( 'NONE', #200655, 0.09999999999999939493 ) ;
#217763=VERTEX_POINT ( 'NONE', #76157 ) ;
#217795=ADVANCED_FACE ( 'NONE', ( #218219 ), #119156, .T. ) ;
#217815=EDGE_CURVE ( 'NONE', #68201, #127037, #55283, .T. ) ;
#217818=EDGE_CURVE ( 'NONE', #97895, #215594, #81077, .T. ) ;
#217821=VECTOR ( 'NONE', #192934, 1000.000000000000000 ) ;
#217900=AXIS2_PLACEMENT_3D ( 'NONE', #47894, #27096, #85708 ) ;
#217929=VERTEX_POINT ( 'NONE', #162147 ) ;
#217937=FACE_OUTER_BOUND ( 'NONE', #228473, .T. ) ;
#217941=ADVANCED_FACE ( 'NONE', ( #5589 ), #181076, .T. ) ;
#217944=VERTEX_POINT ( 'NONE', #180412 ) ;
#217948=ORIENTED_EDGE ( 'NONE', *, *, #156553, .F. ) ;
#217961=CARTESIAN_POINT ( 'NONE',  ( -20.64999999999999858, 54.34471204062663219, -239.4366250215122420 ) ) ;
#217970=ADVANCED_FACE ( 'NONE', ( #21358 ), #193164, .F. ) ;
#218029=CYLINDRICAL_SURFACE ( 'NONE', #109441, 0.09999999999999108213 ) ;
#218058=DIRECTION ( 'NONE',  ( 0.000000000000000000, -0.4088369013363280513, 0.9126074666063769270 ) ) ;
#218068=DIRECTION ( 'NONE',  ( 0.000000000000000000, 0.4088369013363281068, -0.9126074666063770380 ) ) ;
#218079=DIRECTION ( 'NONE',  ( 0.7071067811865474617, 0.2890913453342131012, -0.6453109281988449464 ) ) ;
#218105=CIRCLE ( 'NONE', #197277, 0.09999999999999741040 ) ;
#218107=EDGE_CURVE ( 'NONE', #5240, #228447, #63967, .T. ) ;
#218162=AXIS2_PLACEMENT_3D ( 'NONE', #253926, #94858, #171880 ) ;
#218169=ORIENTED_EDGE ( 'NONE', *, *, #178367, .F. ) ;
#218176=ORIENTED_EDGE ( 'NONE', *, *, #116274, .T. ) ;
#218182=ORIENTED_EDGE ( 'NONE', *, *, #141707, .T. ) ;
#218219=FACE_OUTER_BOUND ( 'NONE', #255343, .T. ) ;
#218269=ORIENTED_EDGE ( 'NONE', *, *, #71044, .T. ) ;
#218298=SPHERICAL_SURFACE ( 'NONE', #114488, 0.1000000000000000056 ) ;
#218330=FACE_OUTER_BOUND ( 'NONE', #179234, .T. ) ;
#218350=AXIS2_PLACEMENT_3D ( 'NONE', #45934, #225824, #161079 ) ;
#218372=ORIENTED_EDGE ( 'NONE', *, *, #144677, .F. ) ;
#218382=CIRCLE ( 'NONE', #155892, 11.80000000000000959 ) ;
#218401=VECTOR ( 'NONE', #145937, 1000.000000000000000 ) ;
#218406=ADVANCED_FACE ( 'NONE', ( #208351 ), #210892, .T. ) ;
#218414=CARTESIAN_POINT ( 'NONE',  ( -21.05000000000000071, 34.17451268998649283, -243.7608519714916326 ) ) ;
#218420=AXIS2_PLACEMENT_3D ( 'NONE', #219360, #38186, #152036 ) ;
#218437=AXIS2_PLACEMENT_3D ( 'NONE', #81092, #64119, #144916 ) ;
#218450=AXIS2_PLACEMENT_3D ( 'NONE', #157679, #57221, #136772 ) ;
#218451=VECTOR ( 'NONE', #236827, 1000.000000000000114 ) ;
#218455=DIRECTION ( 'NONE',  ( 0.000000000000000000, -0.9126074666063771490, -0.4088369013363278293 ) ) ;
#218531=VERTEX_POINT ( 'NONE', #113083 ) ;
#218535=CARTESIAN_POINT ( 'NONE',  ( 21.00000000000000000, 43.85220609964365224, -235.6449878604632886 ) ) ;
#218565=ORIENTED_EDGE ( 'NONE', *, *, #70406, .T. ) ;
#218611=EDGE_CURVE ( 'NONE', #191682, #201217, #172537, .T. ) ;
#218612=ORIENTED_EDGE ( 'NONE', *, *, #125890, .T. ) ;
#218640=CARTESIAN_POINT ( 'NONE',  ( -22.42253884134832376, 26.02661726287391986, -254.3121879182652663 ) ) ;
#218653=EDGE_CURVE ( 'NONE', #198535, #166946, #51840, .T. ) ;
#218659=FACE_OUTER_BOUND ( 'NONE', #17577, .T. ) ;
#218675=LINE ( 'NONE', #4749, #142380 ) ;
#218702=ORIENTED_EDGE ( 'NONE', *, *, #6927, .F. ) ;
#218708=ORIENTED_EDGE ( 'NONE', *, *, #66941, .F. ) ;
#218712=CARTESIAN_POINT ( 'NONE',  ( 22.57320508075688892, 31.85509083104287598, -238.8280249686205536 ) ) ;
#218722=CARTESIAN_POINT ( 'NONE',  ( 21.12757541349815682, 34.00765740373876156, -243.6456173532155276 ) ) ;
#218756=ORIENTED_EDGE ( 'NONE', *, *, #148181, .F. ) ;
#218780=ORIENTED_EDGE ( 'NONE', *, *, #200676, .F. ) ;
#218781=DIRECTION ( 'NONE',  ( -1.000000000000000000, -0.000000000000000000, 0.000000000000000000 ) ) ;
#218784=FACE_OUTER_BOUND ( 'NONE', #228296, .T. ) ;
#218826=ORIENTED_EDGE ( 'NONE', *, *, #107499, .T. ) ;
#218829=EDGE_CURVE ( 'NONE', #9664, #241306, #168938, .T. ) ;
#218842=CARTESIAN_POINT ( 'NONE',  ( -18.59999999999999787, 67.74990736105834799, -227.9721689390126755 ) ) ;
#218845=VERTEX_POINT ( 'NONE', #227572 ) ;
#218847=DIRECTION ( 'NONE',  ( 3.469446951953728416E-14, -0.1022405907414316584, -0.9947597004326437231 ) ) ;
#218858=CARTESIAN_POINT ( 'NONE',  ( -20.64999999999999858, 36.65892442174472876, -249.5511627012454596 ) ) ;
#218872=EDGE_CURVE ( 'NONE', #1827, #89024, #254791, .T. ) ;
#218902=CARTESIAN_POINT ( 'NONE',  ( -20.90851465518105456, 68.09306500613196533, -224.1549646960459370 ) ) ;
#218948=AXIS2_PLACEMENT_3D ( 'NONE', #112256, #133091, #212636 ) ;
#218957=DIRECTION ( 'NONE',  ( 0.000000000000000000, -0.9126074666063545004, -0.4088369013363783999 ) ) ;
#219043=DIRECTION ( 'NONE',  ( 1.000000000000000000, 0.000000000000000000, 0.000000000000000000 ) ) ;
#219076=ORIENTED_EDGE ( 'NONE', *, *, #217732, .F. ) ;
#219078=ORIENTED_EDGE ( 'NONE', *, *, #156772, .T. ) ;
#219081=DIRECTION ( 'NONE',  ( 0.000000000000000000, -0.4088369013363280513, 0.9126074666063769270 ) ) ;
#219086=EDGE_CURVE ( 'NONE', #177620, #112295, #35514, .T. ) ;
#219128=ADVANCED_FACE ( 'NONE', ( #185581 ), #123050, .T. ) ;
#219140=AXIS2_PLACEMENT_3D ( 'NONE', #105462, #185037, #205878 ) ;
#219160=CARTESIAN_POINT ( 'NONE',  ( -18.50000000000000000, 67.65998959290220682, -227.8609496483021530 ) ) ;
#219168=DIRECTION ( 'NONE',  ( 0.000000000000000000, 0.9126074666063769270, 0.4088369013363280513 ) ) ;
#219191=VERTEX_POINT ( 'NONE', #51176 ) ;
#219207=CARTESIAN_POINT ( 'NONE',  ( 21.05000000000000071, 34.10212115774099573, -243.5992592859234378 ) ) ;
#219209=DIRECTION ( 'NONE',  ( -3.469446951953749873E-14, -0.4088369013363783999, 0.9126074666063545004 ) ) ;
#219294=EDGE_CURVE ( 'NONE', #217247, #12219, #241283, .T. ) ;
#219329=DIRECTION ( 'NONE',  ( 0.000000000000000000, 0.4088369013363306603, -0.9126074666063758167 ) ) ;
#219346=ORIENTED_EDGE ( 'NONE', *, *, #255090, .F. ) ;
#219351=DIRECTION ( 'NONE',  ( -1.000000000000000000, 0.000000000000000000, 0.000000000000000000 ) ) ;
#219360=CARTESIAN_POINT ( 'NONE',  ( -21.04999999999999716, 47.00127771169579916, -255.4372249185379928 ) ) ;
#219367=ORIENTED_EDGE ( 'NONE', *, *, #219503, .T. ) ;
#219369=FACE_OUTER_BOUND ( 'NONE', #202613, .T. ) ;
#219371=CARTESIAN_POINT ( 'NONE',  ( -18.59999999999999787, 38.29773864426885410, -236.0513742605307925 ) ) ;
#219386=ORIENTED_EDGE ( 'NONE', *, *, #61932, .T. ) ;
#219389=FACE_OUTER_BOUND ( 'NONE', #91587, .T. ) ;
#219395=EDGE_CURVE ( 'NONE', #229408, #56338, #227007, .T. ) ;
#219396=VERTEX_POINT ( 'NONE', #229412 ) ;
#219457=VECTOR ( 'NONE', #17232, 1000.000000000000114 ) ;
#219469=TOROIDAL_SURFACE ( 'NONE', #107046, 11.70000000000000107, 0.1000000000000000056 ) ;
#219502=DIRECTION ( 'NONE',  ( 0.000000000000000000, 0.9126074666063602736, 0.4088369013363654103 ) ) ;
#219503=EDGE_CURVE ( 'NONE', #96682, #154226, #2479, .T. ) ;
#219540=CARTESIAN_POINT ( 'NONE',  ( 20.94999999999999929, 40.74071615341952679, -237.9411309446948337 ) ) ;
#219554=DIRECTION ( 'NONE',  ( -1.000000000000000000, -4.163336342344362270E-13, 8.326672684688724540E-13 ) ) ;
#219556=VECTOR ( 'NONE', #79463, 1000.000000000000000 ) ;
#219567=EDGE_LOOP ( 'NONE', ( #16083, #1411, #220892, #253036 ) ) ;
#219581=DIRECTION ( 'NONE',  ( 0.000000000000000000, 0.5469332180710856361, -0.8371762388950170219 ) ) ;
#219609=EDGE_CURVE ( 'NONE', #137324, #60290, #145847, .T. ) ;
#219611=AXIS2_PLACEMENT_3D ( 'NONE', #206813, #50283, #128561 ) ;
#219612=DIRECTION ( 'NONE',  ( 0.000000000000000000, 0.9126074666063844765, 0.4088369013363114535 ) ) ;
#219633=DIRECTION ( 'NONE',  ( 0.000000000000000000, -0.4088369013363297166, 0.9126074666063763718 ) ) ;
#219636=CYLINDRICAL_SURFACE ( 'NONE', #17817, 0.09999999999999939493 ) ;
#219638=ORIENTED_EDGE ( 'NONE', *, *, #156023, .T. ) ;
#219690=DIRECTION ( 'NONE',  ( -1.000000000000000000, -0.000000000000000000, -0.000000000000000000 ) ) ;
#219719=ORIENTED_EDGE ( 'NONE', *, *, #240870, .F. ) ;
#219744=CARTESIAN_POINT ( 'NONE',  ( 18.55807992284871588, 68.10318897902124036, -224.1464165264002588 ) ) ;
#219777=FACE_OUTER_BOUND ( 'NONE', #132404, .T. ) ;
#219781=CARTESIAN_POINT ( 'NONE',  ( 20.90851465518105456, 68.09306500613196533, -224.1549646960459370 ) ) ;
#219794=VERTEX_POINT ( 'NONE', #137830 ) ;
#219806=VECTOR ( 'NONE', #243271, 1000.000000000000114 ) ;
#219819=DIRECTION ( 'NONE',  ( 0.000000000000000000, -0.4088369013363281068, 0.9126074666063770380 ) ) ;
#219846=CIRCLE ( 'NONE', #244789, 0.1999999999999935163 ) ;
#219852=CARTESIAN_POINT ( 'NONE',  ( 20.54374330479336308, 39.41460512620965062, -236.8056672937158567 ) ) ;
#219864=EDGE_CURVE ( 'NONE', #75688, #231797, #23407, .T. ) ;
#219899=ADVANCED_FACE ( 'NONE', ( #256440 ), #227372, .T. ) ;
#219923=AXIS2_PLACEMENT_3D ( 'NONE', #70302, #149828, #35034 ) ;
#219936=ADVANCED_FACE ( 'NONE', ( #58289 ), #217365, .T. ) ;
#219937=CARTESIAN_POINT ( 'NONE',  ( -20.64999999999999858, 46.05992536685982230, -240.5730681801377102 ) ) ;
#219941=CARTESIAN_POINT ( 'NONE',  ( -18.59999999999999787, 44.52640028187936849, -247.3006740988509193 ) ) ;
#219953=DIRECTION ( 'NONE',  ( 2.694716079187274425E-16, 0.4088369013363281623, -0.9126074666063770380 ) ) ;
#219954=CARTESIAN_POINT ( 'NONE',  ( -18.59999999999999787, 42.94327155031035659, -233.8606566173841372 ) ) ;
#219959=CARTESIAN_POINT ( 'NONE',  ( -18.44204374631832621, 77.15868121549257808, -241.8076815865107108 ) ) ;
#219991=FACE_OUTER_BOUND ( 'NONE', #12715, .T. ) ;
#220015=CARTESIAN_POINT ( 'NONE',  ( 22.49999999999999645, 31.82071903192824180, -238.9531407059547803 ) ) ;
#220019=AXIS2_PLACEMENT_3D ( 'NONE', #60153, #96687, #137142 ) ;
#220033=CARTESIAN_POINT ( 'NONE',  ( 23.24999999999999289, 23.29878867550048938, -248.4686781323362084 ) ) ;
#220039=ORIENTED_EDGE ( 'NONE', *, *, #32389, .T. ) ;
#220052=CARTESIAN_POINT ( 'NONE',  ( -23.25000000000000000, 36.65892442174472876, -249.5511627012454596 ) ) ;
#220068=AXIS2_PLACEMENT_3D ( 'NONE', #7905, #61439, #140990 ) ;
#220076=ORIENTED_EDGE ( 'NONE', *, *, #7992, .T. ) ;
#220088=CARTESIAN_POINT ( 'NONE',  ( 18.49999999999998934, 47.07326788871596790, -255.0992659944398042 ) ) ;
#220092=DIRECTION ( 'NONE',  ( 7.304098846218134667E-16, 0.4088369013363281068, -0.9126074666063770380 ) ) ;
#220102=VERTEX_POINT ( 'NONE', #173831 ) ;
#220130=VECTOR ( 'NONE', #53834, 1000.000000000000114 ) ;
#220199=CARTESIAN_POINT ( 'NONE',  ( -20.54999999999999716, 65.49732036650624423, -236.6319166190174883 ) ) ;
#220214=CIRCLE ( 'NONE', #199937, 0.1000000000000056677 ) ;
#220222=AXIS2_PLACEMENT_3D ( 'NONE', #199707, #58856, #21075 ) ;
#220228=AXIS2_PLACEMENT_3D ( 'NONE', #187829, #130390, #170873 ) ;
#220231=DIRECTION ( 'NONE',  ( 1.000000000000000000, 0.000000000000000000, -0.000000000000000000 ) ) ;
#220241=VERTEX_POINT ( 'NONE', #19856 ) ;
#220246=CARTESIAN_POINT ( 'NONE',  ( 21.14999999999999858, 42.98415524044398950, -233.9519173640447889 ) ) ;
#220265=CIRCLE ( 'NONE', #166293, 0.1000000000000056677 ) ;
#220268=ADVANCED_FACE ( 'NONE', ( #156817 ), #27696, .T. ) ;
#220273=ADVANCED_FACE ( 'NONE', ( #61539 ), #177663, .T. ) ;
#220296=FACE_OUTER_BOUND ( 'NONE', #57806, .T. ) ;
#220313=DIRECTION ( 'NONE',  ( 0.000000000000000000, -0.9876013379310930596, -0.1569827930593520049 ) ) ;
#220327=ORIENTED_EDGE ( 'NONE', *, *, #65994, .F. ) ;
#220332=CIRCLE ( 'NONE', #32915, 0.09999999999999741040 ) ;
#220356=CARTESIAN_POINT ( 'NONE',  ( -20.54999999999999716, 36.65892442174472876, -249.5511627012454596 ) ) ;
#220369=CIRCLE ( 'NONE', #195434, 0.3999999999999959699 ) ;
#220372=CARTESIAN_POINT ( 'NONE',  ( -21.95218792049438505, 30.04628837005676445, -252.4050306439679048 ) ) ;
#220379=CARTESIAN_POINT ( 'NONE',  ( 20.94999999999999574, 48.04585786805223080, -246.4610531646956417 ) ) ;
#220382=EDGE_CURVE ( 'NONE', #153695, #223817, #48493, .T. ) ;
#220422=DIRECTION ( 'NONE',  ( -0.000000000000000000, 0.9126074666063771490, 0.4088369013363281623 ) ) ;
#220460=ADVANCED_FACE ( 'NONE', ( #211321 ), #174809, .T. ) ;
#220466=EDGE_LOOP ( 'NONE', ( #114178, #2741, #121581, #57161 ) ) ;
#220471=ORIENTED_EDGE ( 'NONE', *, *, #185841, .F. ) ;
#220474=ORIENTED_EDGE ( 'NONE', *, *, #68866, .F. ) ;
#220498=ORIENTED_EDGE ( 'NONE', *, *, #137823, .F. ) ;
#220514=ORIENTED_EDGE ( 'NONE', *, *, #129148, .T. ) ;
#220521=DIRECTION ( 'NONE',  ( 0.000000000000000000, 0.9126074666064696306, 0.4088369013361213278 ) ) ;
#220527=CARTESIAN_POINT ( 'NONE',  ( -20.54999999999999716, 47.74660456829661825, -241.9541913331436263 ) ) ;
#220530=ORIENTED_EDGE ( 'NONE', *, *, #168054, .T. ) ;
#220531=ORIENTED_EDGE ( 'NONE', *, *, #5499, .F. ) ;
#220536=DIRECTION ( 'NONE',  ( 1.000000000000000000, 0.000000000000000000, 0.000000000000000000 ) ) ;
#220619=CARTESIAN_POINT ( 'NONE',  ( -21.14999999999999858, 26.06832281015329755, -254.4051978787608732 ) ) ;
#220640=ORIENTED_EDGE ( 'NONE', *, *, #33816, .F. ) ;
#220642=VECTOR ( 'NONE', #63140, 1000.000000000000000 ) ;
#220654=ORIENTED_EDGE ( 'NONE', *, *, #2191, .T. ) ;
#220655=EDGE_CURVE ( 'NONE', #70783, #94097, #119952, .T. ) ;
#220667=VERTEX_POINT ( 'NONE', #258093 ) ;
#220690=CARTESIAN_POINT ( 'NONE',  ( 18.59999999999999432, 44.52640028187936849, -247.3006740988509193 ) ) ;
#220700=CARTESIAN_POINT ( 'NONE',  ( -23.15000000000000213, 49.36776662947724503, -253.7196102226803021 ) ) ;
#220725=CIRCLE ( 'NONE', #108309, 0.09999999999999609201 ) ;
#220739=VERTEX_POINT ( 'NONE', #182478 ) ;
#220777=FACE_OUTER_BOUND ( 'NONE', #33578, .T. ) ;
#220807=CYLINDRICAL_SURFACE ( 'NONE', #57372, 4.000000000000002665 ) ;
#220843=CARTESIAN_POINT ( 'NONE',  ( -20.94999999999999929, 44.58277672189309015, -247.4925639031954745 ) ) ;
#220851=ORIENTED_EDGE ( 'NONE', *, *, #154511, .T. ) ;
#220860=AXIS2_PLACEMENT_3D ( 'NONE', #69245, #10549, #246568 ) ;
#220875=FACE_OUTER_BOUND ( 'NONE', #217116, .T. ) ;
#220884=CARTESIAN_POINT ( 'NONE',  ( -23.25000000000000000, 31.85509083104287598, -238.8280249686205536 ) ) ;
#220892=ORIENTED_EDGE ( 'NONE', *, *, #17357, .F. ) ;
#220912=CARTESIAN_POINT ( 'NONE',  ( -23.15000000000000213, 49.57218508014541669, -254.1759139559835035 ) ) ;
#220949=CARTESIAN_POINT ( 'NONE',  ( 20.94999999999999574, 43.04635563724865932, -239.7315875678428370 ) ) ;
#220955=ORIENTED_EDGE ( 'NONE', *, *, #110532, .F. ) ;
#220973=DIRECTION ( 'NONE',  ( 1.000000000000000000, 0.000000000000000000, 0.000000000000000000 ) ) ;
#220982=EDGE_CURVE ( 'NONE', #47325, #105460, #110623, .T. ) ;
#221015=CARTESIAN_POINT ( 'NONE',  ( 20.94999999999999929, 67.23127455305835554, -235.8551265064784559 ) ) ;
#221022=ORIENTED_EDGE ( 'NONE', *, *, #1862, .T. ) ;
#221052=CARTESIAN_POINT ( 'NONE',  ( 22.49066049874202022, 26.00400106736331196, -254.2626983329210475 ) ) ;
#221073=ORIENTED_EDGE ( 'NONE', *, *, #252478, .T. ) ;
#221076=ORIENTED_EDGE ( 'NONE', *, *, #211278, .T. ) ;
#221080=EDGE_CURVE ( 'NONE', #248454, #119221, #144526, .T. ) ;
#221087=ORIENTED_EDGE ( 'NONE', *, *, #148072, .T. ) ;
#221099=DIRECTION ( 'NONE',  ( 0.000000000000000000, 0.9126074666063660468, 0.4088369013363524762 ) ) ;
#221119=VERTEX_POINT ( 'NONE', #76624 ) ;
#221120=EDGE_LOOP ( 'NONE', ( #172146, #3348, #202394, #151343 ) ) ;
#221127=CARTESIAN_POINT ( 'NONE',  ( 20.51284917709620359, 39.44540980133907482, -237.0045804191218792 ) ) ;
#221165=ORIENTED_EDGE ( 'NONE', *, *, #248812, .T. ) ;
#221174=ADVANCED_FACE ( 'NONE', ( #64761 ), #67332, .T. ) ;
#221204=DIRECTION ( 'NONE',  ( -1.000000000000000000, 0.000000000000000000, 0.000000000000000000 ) ) ;
#221215=CARTESIAN_POINT ( 'NONE',  ( -21.04999999999965610, 34.03619476471878613, -243.8226196603530980 ) ) ;
#221254=DIRECTION ( 'NONE',  ( 0.000000000000000000, -0.2818822000686748708, 0.9594490217225944972 ) ) ;
#221256=AXIS2_PLACEMENT_3D ( 'NONE', #246809, #51156, #86427 ) ;
#221265=DIRECTION ( 'NONE',  ( 0.000000000000000000, 0.4088369013363783999, -0.9126074666063545004 ) ) ;
#221267=EDGE_CURVE ( 'NONE', #13290, #222515, #12520, .T. ) ;
#221302=CARTESIAN_POINT ( 'NONE',  ( 23.14999999999999858, 67.23127455305835554, -235.8551265064784559 ) ) ;
#221338=AXIS2_PLACEMENT_3D ( 'NONE', #67914, #189150, #247837 ) ;
#221356=LINE ( 'NONE', #243506, #139261 ) ;
#221363=DIRECTION ( 'NONE',  ( -2.952720810173289112E-16, -0.4088369013363280513, 0.9126074666063769270 ) ) ;
#221394=DIRECTION ( 'NONE',  ( 0.000000000000000000, 0.9126074666063660468, 0.4088369013363524762 ) ) ;
#221407=VERTEX_POINT ( 'NONE', #78867 ) ;
#221408=ORIENTED_EDGE ( 'NONE', *, *, #194371, .F. ) ;
#221419=ORIENTED_EDGE ( 'NONE', *, *, #208392, .F. ) ;
#221427=DIRECTION ( 'NONE',  ( 1.000000000000000000, -1.335000415235278971E-16, 2.979993593738921214E-16 ) ) ;
#221437=AXIS2_PLACEMENT_3D ( 'NONE', #149074, #108641, #245593 ) ;
#221440=EDGE_CURVE ( 'NONE', #57391, #84649, #99709, .T. ) ;
#221474=DIRECTION ( 'NONE',  ( 1.000000000000000000, 0.000000000000000000, 0.000000000000000000 ) ) ;
#221508=LINE ( 'NONE', #65018, #146112 ) ;
#221527=DIRECTION ( 'NONE',  ( -1.000000000000000000, -0.000000000000000000, -0.000000000000000000 ) ) ;
#221536=CARTESIAN_POINT ( 'NONE',  ( -23.15000000000000213, 42.98415524044398950, -233.9519173640447889 ) ) ;
#221607=EDGE_LOOP ( 'NONE', ( #77081, #239597, #245493, #130151 ) ) ;
#221639=VECTOR ( 'NONE', #240808, 1000.000000000000000 ) ;
#221675=DIRECTION ( 'NONE',  ( 1.000000000000000000, 0.000000000000000000, -0.000000000000000000 ) ) ;
#221681=ORIENTED_EDGE ( 'NONE', *, *, #176217, .F. ) ;
#221694=ORIENTED_EDGE ( 'NONE', *, *, #228741, .T. ) ;
#221731=EDGE_LOOP ( 'NONE', ( #105312, #213819, #85069, #244442 ) ) ;
#221751=ORIENTED_EDGE ( 'NONE', *, *, #15485, .F. ) ;
#221761=CARTESIAN_POINT ( 'NONE',  ( -21.05000000000000071, 43.44873802792533724, -245.1397081572968659 ) ) ;
#221778=FACE_OUTER_BOUND ( 'NONE', #194401, .T. ) ;
#221790=ORIENTED_EDGE ( 'NONE', *, *, #186164, .T. ) ;
#221816=CARTESIAN_POINT ( 'NONE',  ( -21.05000000000000071, 26.06832281015329755, -254.4051978787608732 ) ) ;
#221820=ORIENTED_EDGE ( 'NONE', *, *, #182516, .F. ) ;
#221827=CIRCLE ( 'NONE', #217555, 0.2000000000000053679 ) ;
#221850=DIRECTION ( 'NONE',  ( 1.000000000000000000, 0.000000000000000000, 0.000000000000000000 ) ) ;
#221852=EDGE_CURVE ( 'NONE', #93242, #256823, #207463, .T. ) ;
#221872=DIRECTION ( 'NONE',  ( 1.000000000000000000, 0.000000000000000000, 0.000000000000000000 ) ) ;
#221881=EDGE_LOOP ( 'NONE', ( #59826, #208458, #118246, #219078, #104645, #153093 ) ) ;
#221888=VERTEX_POINT ( 'NONE', #147220 ) ;
#221890=ORIENTED_EDGE ( 'NONE', *, *, #26385, .F. ) ;
#221898=CARTESIAN_POINT ( 'NONE',  ( 23.14999999999999858, 45.69057616835975466, -239.3688303688244616 ) ) ;
#221915=VERTEX_POINT ( 'NONE', #85931 ) ;
#221919=FACE_BOUND ( 'NONE', #6718, .T. ) ;
#221923=ORIENTED_EDGE ( 'NONE', *, *, #51023, .T. ) ;
#221937=DIRECTION ( 'NONE',  ( 1.000000000000000000, 0.000000000000000000, 0.000000000000000000 ) ) ;
#221949=DIRECTION ( 'NONE',  ( 0.000000000000000000, -0.9126074666063660468, -0.4088369013363524762 ) ) ;
#221977=EDGE_LOOP ( 'NONE', ( #184928, #171148, #178763, #60385, #30467, #133162 ) ) ;
#222016=EDGE_LOOP ( 'NONE', ( #4380, #124953, #195670, #117999 ) ) ;
#222021=VERTEX_POINT ( 'NONE', #151080 ) ;
#222052=DIRECTION ( 'NONE',  ( -6.938893903907222856E-15, -0.4088369013363283289, 0.9126074666063768159 ) ) ;
#222067=ORIENTED_EDGE ( 'NONE', *, *, #244269, .T. ) ;
#222096=DIRECTION ( 'NONE',  ( 0.000000000000000000, -0.9126074666063770380, -0.4088369013363281068 ) ) ;
#222123=CIRCLE ( 'NONE', #18154, 7.799999999999993605 ) ;
#222134=EDGE_CURVE ( 'NONE', #51812, #222344, #103551, .T. ) ;
#222136=DIRECTION ( 'NONE',  ( 1.000000000000000000, 0.000000000000000000, 0.000000000000000000 ) ) ;
#222140=CARTESIAN_POINT ( 'NONE',  ( -20.54999999999999716, 47.91013932883114990, -242.3192343197862044 ) ) ;
#222163=ORIENTED_EDGE ( 'NONE', *, *, #216443, .F. ) ;
#222186=FACE_OUTER_BOUND ( 'NONE', #125739, .T. ) ;
#222205=DIRECTION ( 'NONE',  ( 1.000000000000000000, 0.000000000000000000, 0.000000000000000000 ) ) ;
#222216=EDGE_LOOP ( 'NONE', ( #253331, #201498, #37860, #174436 ) ) ;
#222232=FACE_OUTER_BOUND ( 'NONE', #139779, .T. ) ;
#222250=CIRCLE ( 'NONE', #205702, 0.09999999999999609201 ) ;
#222271=ORIENTED_EDGE ( 'NONE', *, *, #117861, .F. ) ;
#222275=CARTESIAN_POINT ( 'NONE',  ( -23.15000000000000213, 49.57218508014541669, -254.1759139559835035 ) ) ;
#222276=FACE_OUTER_BOUND ( 'NONE', #42344, .T. ) ;
#222311=EDGE_LOOP ( 'NONE', ( #51755, #98387, #25262, #228358 ) ) ;
#222343=DIRECTION ( 'NONE',  ( 0.000000000000000000, 0.9594490217226113726, 0.2818822000686178608 ) ) ;
#222344=VERTEX_POINT ( 'NONE', #97482 ) ;
#222355=EDGE_CURVE ( 'NONE', #81533, #224911, #87667, .T. ) ;
#222369=VECTOR ( 'NONE', #93361, 1000.000000000000227 ) ;
#222375=EDGE_CURVE ( 'NONE', #101099, #187124, #236831, .T. ) ;
#222384=ORIENTED_EDGE ( 'NONE', *, *, #206725, .F. ) ;
#222402=CARTESIAN_POINT ( 'NONE',  ( -21.29999999999995808, 40.35498466150055918, -247.8953732508333587 ) ) ;
#222427=AXIS2_PLACEMENT_3D ( 'NONE', #202409, #66760, #65459 ) ;
#222488=CARTESIAN_POINT ( 'NONE',  ( 18.49999999999998934, 54.96412023489455834, -230.1191065505896063 ) ) ;
#222512=DIRECTION ( 'NONE',  ( 0.000000000000000000, 0.9126074666063660468, 0.4088369013363524762 ) ) ;
#222515=VERTEX_POINT ( 'NONE', #129902 ) ;
#222547=CARTESIAN_POINT ( 'NONE',  ( -20.95000000000000284, 56.06656052939784729, -228.0911609752645575 ) ) ;
#222553=EDGE_CURVE ( 'NONE', #215460, #251832, #49084, .T. ) ;
#222566=VECTOR ( 'NONE', #229908, 1000.000000000000114 ) ;
#222622=TOROIDAL_SURFACE ( 'NONE', #172807, 4.099999999999999645, 0.1000000000000000056 ) ;
#222628=VECTOR ( 'NONE', #190296, 1000.000000000000114 ) ;
#222661=CIRCLE ( 'NONE', #77117, 0.1000000000000024342 ) ;
#222701=ADVANCED_FACE ( 'NONE', ( #155923 ), #118051, .F. ) ;
#222705=EDGE_CURVE ( 'NONE', #171172, #147844, #81461, .T. ) ;
#222711=CIRCLE ( 'NONE', #189425, 0.4999999999999944489 ) ;
#222771=CARTESIAN_POINT ( 'NONE',  ( 18.43466021071402139, 77.15162984240767230, -241.8142968757794335 ) ) ;
#222775=CARTESIAN_POINT ( 'NONE',  ( 21.95218792049437795, 33.62430829188672021, -243.0194996105014411 ) ) ;
#222780=DIRECTION ( 'NONE',  ( -0.000000000000000000, -0.4088369013363281623, 0.9126074666063771490 ) ) ;
#222785=ORIENTED_EDGE ( 'NONE', *, *, #16719, .F. ) ;
#222841=CIRCLE ( 'NONE', #35447, 0.09999999999999609201 ) ;
#222876=FACE_OUTER_BOUND ( 'NONE', #24815, .T. ) ;
#222885=VERTEX_POINT ( 'NONE', #145309 ) ;
#222898=CARTESIAN_POINT ( 'NONE',  ( -18.49513951962167013, 77.27548444980108400, -241.6969386449946740 ) ) ;
#222911=ORIENTED_EDGE ( 'NONE', *, *, #223994, .F. ) ;
#223026=ORIENTED_EDGE ( 'NONE', *, *, #209204, .F. ) ;
#223030=ADVANCED_FACE ( 'NONE', ( #108767 ), #157394, .F. ) ;
#223080=EDGE_LOOP ( 'NONE', ( #99489, #52247, #5234, #2643 ) ) ;
#223115=FACE_OUTER_BOUND ( 'NONE', #188838, .T. ) ;
#223151=CARTESIAN_POINT ( 'NONE',  ( 18.50000000000000711, 54.95667902235472724, -229.8578999281555753 ) ) ;
#223170=CARTESIAN_POINT ( 'NONE',  ( -18.49346865148373098, 47.07686520425682630, -255.2314089849770937 ) ) ;
#223171=VECTOR ( 'NONE', #255172, 1000.000000000000000 ) ;
#223180=ORIENTED_EDGE ( 'NONE', *, *, #25859, .F. ) ;
#223205=DIRECTION ( 'NONE',  ( 0.000000000000000000, -0.07847809223012357227, -0.9969158384938622275 ) ) ;
#223211=DIRECTION ( 'NONE',  ( 4.408576920032447355E-17, -0.8490545835447252943, -0.5283051335749947564 ) ) ;
#223215=VERTEX_POINT ( 'NONE', #252960 ) ;
#223222=CARTESIAN_POINT ( 'NONE',  ( 23.15000000000000213, 30.69873658968802133, -264.9868732779115703 ) ) ;
#223266=FACE_OUTER_BOUND ( 'NONE', #134164, .T. ) ;
#223287=VECTOR ( 'NONE', #152571, 999.9999999999998863 ) ;
#223301=ORIENTED_EDGE ( 'NONE', *, *, #229565, .F. ) ;
#223306=CARTESIAN_POINT ( 'NONE',  ( -20.94999999999999929, 56.24810294282605128, -228.0242159533278254 ) ) ;
#223356=CARTESIAN_POINT ( 'NONE',  ( 21.05000000000000071, 43.51422117117169108, -240.0698702536254530 ) ) ;
#223361=DIRECTION ( 'NONE',  ( 1.000000000000000000, 0.000000000000000000, 0.000000000000000000 ) ) ;
#223387=FACE_OUTER_BOUND ( 'NONE', #150144, .T. ) ;
#223405=CARTESIAN_POINT ( 'NONE',  ( 20.95346350065193519, 40.79338854218204347, -237.9607482723631051 ) ) ;
#223408=DIRECTION ( 'NONE',  ( 1.000000000000000000, -2.986185139342070877E-16, 6.665775143889692774E-16 ) ) ;
#223417=EDGE_CURVE ( 'NONE', #102432, #11614, #28605, .T. ) ;
#223426=ORIENTED_EDGE ( 'NONE', *, *, #38928, .F. ) ;
#223453=EDGE_LOOP ( 'NONE', ( #179465, #199761, #119654, #230126 ) ) ;
#223467=VECTOR ( 'NONE', #86172, 1000.000000000000000 ) ;
#223475=VERTEX_POINT ( 'NONE', #4564 ) ;
#223484=EDGE_CURVE ( 'NONE', #61629, #225362, #199246, .T. ) ;
#223485=CARTESIAN_POINT ( 'NONE',  ( 18.59999999999999076, 21.17283678855157802, -243.7231193059830332 ) ) ;
#223500=DIRECTION ( 'NONE',  ( 1.000000000000000000, 0.000000000000000000, 0.000000000000000000 ) ) ;
#223525=DIRECTION ( 'NONE',  ( 0.000000000000000000, -0.9126074666063660468, -0.4088369013363524762 ) ) ;
#223526=ORIENTED_EDGE ( 'NONE', *, *, #201825, .T. ) ;
#223546=ORIENTED_EDGE ( 'NONE', *, *, #179152, .T. ) ;
#223549=ORIENTED_EDGE ( 'NONE', *, *, #25542, .T. ) ;
#223565=VERTEX_POINT ( 'NONE', #168843 ) ;
#223592=FACE_OUTER_BOUND ( 'NONE', #9978, .T. ) ;
#223602=DIRECTION ( 'NONE',  ( 0.000000000000000000, -0.5859227990963362664, -0.8103668758649469339 ) ) ;
#223608=CARTESIAN_POINT ( 'NONE',  ( 22.39999999999999503, 26.02743912001966464, -254.3139371321002216 ) ) ;
#223623=CARTESIAN_POINT ( 'NONE',  ( 20.93975676684922504, 68.05374558910872906, -224.1882283518532120 ) ) ;
#223642=ADVANCED_FACE ( 'NONE', ( #67124 ), #146639, .T. ) ;
#223750=EDGE_LOOP ( 'NONE', ( #217261, #38769, #218756, #204690 ) ) ;
#223781=DIRECTION ( 'NONE',  ( -1.000000000000000000, -0.000000000000000000, 0.000000000000000000 ) ) ;
#223810=DIRECTION ( 'NONE',  ( 0.000000000000000000, 0.9126074666063632712, 0.4088369013363589710 ) ) ;
#223817=VERTEX_POINT ( 'NONE', #43412 ) ;
#223861=CARTESIAN_POINT ( 'NONE',  ( -23.15000000000000213, 42.98415524044398950, -233.9519173640447889 ) ) ;
#223879=EDGE_CURVE ( 'NONE', #200983, #101872, #253567, .T. ) ;
#223892=ORIENTED_EDGE ( 'NONE', *, *, #154390, .F. ) ;
#223899=CARTESIAN_POINT ( 'NONE',  ( -20.85000000000000142, 71.99422445362657186, -246.4870034924427671 ) ) ;
#223919=EDGE_LOOP ( 'NONE', ( #197397, #142282, #148498, #250981 ) ) ;
#223941=VECTOR ( 'NONE', #32027, 1000.000000000000227 ) ;
#223961=CIRCLE ( 'NONE', #211338, 0.1000000000000056677 ) ;
#223970=DIRECTION ( 'NONE',  ( 1.000000000000000000, 0.000000000000000000, 0.000000000000000000 ) ) ;
#223994=EDGE_CURVE ( 'NONE', #164531, #249043, #178605, .T. ) ;
#224036=DIRECTION ( 'NONE',  ( 0.000000000000000000, -0.9126074666063769270, -0.4088369013363280513 ) ) ;
#224057=CARTESIAN_POINT ( 'NONE',  ( 18.44208962362600701, 77.38084206055300740, -241.7753309371236980 ) ) ;
#224092=CARTESIAN_POINT ( 'NONE',  ( 18.47688499308725696, 77.21655692720625552, -241.7530664668917098 ) ) ;
#224108=DIRECTION ( 'NONE',  ( -1.000000000000000000, 1.335000415235278971E-16, -2.979993593738921214E-16 ) ) ;
#224120=DIRECTION ( 'NONE',  ( 0.000000000000000000, 0.9126074666063769270, 0.4088369013363282733 ) ) ;
#224121=AXIS2_PLACEMENT_3D ( 'NONE', #184542, #244520, #65892 ) ;
#224134=CARTESIAN_POINT ( 'NONE',  ( -20.94999999999999929, 67.23127455305835554, -235.8551265064784559 ) ) ;
#224160=CARTESIAN_POINT ( 'NONE',  ( 20.95462737510932882, 39.25131534400754418, -236.8220897444442414 ) ) ;
#224231=DIRECTION ( 'NONE',  ( 1.000000000000000000, 0.000000000000000000, 0.000000000000000000 ) ) ;
#224250=EDGE_LOOP ( 'NONE', ( #104413, #6535, #178409, #180336, #111880 ) ) ;
#224270=EDGE_CURVE ( 'NONE', #61130, #186768, #80926, .T. ) ;
#224353=DIRECTION ( 'NONE',  ( -1.000000000000000000, 0.000000000000000000, 0.000000000000000000 ) ) ;
#224375=DIRECTION ( 'NONE',  ( 1.000000000000000000, 0.000000000000000000, 0.000000000000000000 ) ) ;
#224376=CARTESIAN_POINT ( 'NONE',  ( 20.94999999999999929, 67.23127455305835554, -235.8551265064784559 ) ) ;
#224384=CARTESIAN_POINT ( 'NONE',  ( -21.05000000000000071, 46.45388641681647357, -243.1520440498138385 ) ) ;
#224394=DIRECTION ( 'NONE',  ( 1.000000000000000000, 0.000000000000000000, 0.000000000000000000 ) ) ;
#224416=AXIS2_PLACEMENT_3D ( 'NONE', #12392, #129745, #188429 ) ;
#224465=EDGE_CURVE ( 'NONE', #85043, #61130, #133150, .T. ) ;
#224475=VERTEX_POINT ( 'NONE', #65226 ) ;
#224515=FACE_OUTER_BOUND ( 'NONE', #72572, .T. ) ;
#224516=ORIENTED_EDGE ( 'NONE', *, *, #94170, .T. ) ;
#224525=ORIENTED_EDGE ( 'NONE', *, *, #242309, .F. ) ;
#224534=DIRECTION ( 'NONE',  ( 1.000000000000000000, -1.207181226542539700E-16, 2.694675058168174199E-16 ) ) ;
#224543=DIRECTION ( 'NONE',  ( 0.000000000000000000, -0.2606175937107792495, 0.9654421110809303652 ) ) ;
#224569=CIRCLE ( 'NONE', #257845, 0.09999999999999939493 ) ;
#224579=AXIS2_PLACEMENT_3D ( 'NONE', #33010, #246855, #112508 ) ;
#224592=AXIS2_PLACEMENT_3D ( 'NONE', #98984, #100277, #140710 ) ;
#224593=ORIENTED_EDGE ( 'NONE', *, *, #150151, .F. ) ;
#224598=FACE_OUTER_BOUND ( 'NONE', #207416, .T. ) ;
#224602=EDGE_CURVE ( 'NONE', #258063, #74293, #237212, .T. ) ;
#224627=AXIS2_PLACEMENT_3D ( 'NONE', #84836, #64029, #45746 ) ;
#224652=CARTESIAN_POINT ( 'NONE',  ( 21.05000000000000071, 33.98486250090727623, -243.5821103306120108 ) ) ;
#224665=VECTOR ( 'NONE', #53729, 1000.000000000000000 ) ;
#224676=PLANE ( 'NONE',  #180290 ) ;
#224677=CARTESIAN_POINT ( 'NONE',  ( 20.95263205890648095, 40.76960636093260604, -237.9620195468288557 ) ) ;
#224681=CARTESIAN_POINT ( 'NONE',  ( -20.00857864376270001, 52.27009174976920747, -232.4217594817395138 ) ) ;
#224697=CARTESIAN_POINT ( 'NONE',  ( -23.15000000000000213, 69.15921093109223250, -247.4965637597669854 ) ) ;
#224714=DIRECTION ( 'NONE',  ( 0.000000000000000000, 0.4088369013363276072, -0.9126074666063773710 ) ) ;
#224722=CARTESIAN_POINT ( 'NONE',  ( 21.14999999999999858, 44.24607648097409651, -236.5241869975821771 ) ) ;
#224748=LINE ( 'NONE', #207800, #220130 ) ;
#224753=CARTESIAN_POINT ( 'NONE',  ( 20.94999999999999929, 67.23127455305835554, -235.8551265064784559 ) ) ;
#224772=CARTESIAN_POINT ( 'NONE',  ( -21.05000000000000071, 46.91436717984746707, -255.3877622108296634 ) ) ;
#224798=EDGE_CURVE ( 'NONE', #246752, #250586, #107899, .T. ) ;
#224801=ORIENTED_EDGE ( 'NONE', *, *, #206129, .T. ) ;
#224818=ORIENTED_EDGE ( 'NONE', *, *, #247256, .T. ) ;
#224837=AXIS2_PLACEMENT_3D ( 'NONE', #183056, #205151, #106044 ) ;
#224847=DIRECTION ( 'NONE',  ( 1.000000000000000000, 0.000000000000000000, 0.000000000000000000 ) ) ;
#224911=VERTEX_POINT ( 'NONE', #75224 ) ;
#224912=EDGE_CURVE ( 'NONE', #220667, #91403, #188720, .T. ) ;
#224955=ORIENTED_EDGE ( 'NONE', *, *, #201825, .F. ) ;
#224971=DIRECTION ( 'NONE',  ( 0.000000000000000000, 0.4088369013363287729, -0.9126074666063767049 ) ) ;
#224998=AXIS2_PLACEMENT_3D ( 'NONE', #171248, #212896, #107360 ) ;
#225001=EDGE_CURVE ( 'NONE', #220739, #170250, #233307, .T. ) ;
#225009=ORIENTED_EDGE ( 'NONE', *, *, #45998, .F. ) ;
#225070=DIRECTION ( 'NONE',  ( -0.000000000000000000, -0.9126074666063771490, -0.4088369013363281623 ) ) ;
#225071=VECTOR ( 'NONE', #105688, 1000.000000000000114 ) ;
#225076=CARTESIAN_POINT ( 'NONE',  ( -21.05000000000000071, 47.95459712139159336, -246.5019368548292675 ) ) ;
#225077=EDGE_CURVE ( 'NONE', #68027, #239535, #8431, .T. ) ;
#225136=DIRECTION ( 'NONE',  ( -1.000000000000000000, 0.000000000000000000, 0.000000000000000000 ) ) ;
#225141=FACE_OUTER_BOUND ( 'NONE', #103384, .T. ) ;
#225147=ORIENTED_EDGE ( 'NONE', *, *, #141465, .F. ) ;
#225155=CARTESIAN_POINT ( 'NONE',  ( 23.14999999999999858, 67.23127455305835554, -235.8551265064784559 ) ) ;
#225170=AXIS2_PLACEMENT_3D ( 'NONE', #86611, #166214, #47492 ) ;
#225178=CARTESIAN_POINT ( 'NONE',  ( 21.87500000000000355, 51.97441255244040548, -232.0063394385699667 ) ) ;
#225185=CARTESIAN_POINT ( 'NONE',  ( -23.25000000000000000, 78.57213941646344324, -232.7862224702232652 ) ) ;
#225214=CARTESIAN_POINT ( 'NONE',  ( 21.13614978966382552, 30.72779294459459720, -252.2082365290035284 ) ) ;
#225232=EDGE_CURVE ( 'NONE', #31046, #34062, #79318, .T. ) ;
#225237=ADVANCED_FACE ( 'NONE', ( #95414 ), #75279, .F. ) ;
#225242=CARTESIAN_POINT ( 'NONE',  ( 21.14999999999999858, 31.98723526783714988, -238.8784020251475511 ) ) ;
#225243=CARTESIAN_POINT ( 'NONE',  ( -23.25000000000000000, 21.13195309841794867, -243.6318585593224100 ) ) ;
#225284=FACE_OUTER_BOUND ( 'NONE', #230134, .T. ) ;
#225285=ORIENTED_EDGE ( 'NONE', *, *, #218611, .F. ) ;
#225309=EDGE_LOOP ( 'NONE', ( #225375, #219367, #46442, #44618 ) ) ;
#225356=CARTESIAN_POINT ( 'NONE',  ( -20.54999999999999716, 62.08591502004791352, -248.5699171172615820 ) ) ;
#225362=VERTEX_POINT ( 'NONE', #15910 ) ;
#225375=ORIENTED_EDGE ( 'NONE', *, *, #106100, .T. ) ;
#225395=DIRECTION ( 'NONE',  ( 0.000000000000000000, -0.9126074666063771490, -0.4088369013363281623 ) ) ;
#225397=ORIENTED_EDGE ( 'NONE', *, *, #217062, .F. ) ;
#225432=CARTESIAN_POINT ( 'NONE',  ( 20.95561247346651967, 39.25743729385360581, -236.7774612551371547 ) ) ;
#225449=EDGE_CURVE ( 'NONE', #13509, #82665, #162747, .T. ) ;
#225467=ORIENTED_EDGE ( 'NONE', *, *, #244269, .F. ) ;
#225482=EDGE_LOOP ( 'NONE', ( #18513, #188257, #148660, #137481 ) ) ;
#225506=CARTESIAN_POINT ( 'NONE',  ( -21.05000000000000071, 34.05153573962405034, -243.7669379519762174 ) ) ;
#225507=CARTESIAN_POINT ( 'NONE',  ( 21.05000000000000071, 47.74710514101221293, -244.5837943500090716 ) ) ;
#225510=CARTESIAN_POINT ( 'NONE',  ( 20.94999999999999929, 67.23127455305835554, -235.8551265064784559 ) ) ;
#225513=CARTESIAN_POINT ( 'NONE',  ( -18.54118089899629851, 46.96055236759813312, -255.3059391806394274 ) ) ;
#225514=EDGE_LOOP ( 'NONE', ( #179538, #220640, #230391, #245464 ) ) ;
#225523=FACE_OUTER_BOUND ( 'NONE', #27250, .T. ) ;
#225573=DIRECTION ( 'NONE',  ( 0.000000000000000000, -0.9126074666063770380, -0.4088369013363281068 ) ) ;
#225581=ORIENTED_EDGE ( 'NONE', *, *, #43038, .T. ) ;
#225594=EDGE_LOOP ( 'NONE', ( #222067, #227609, #175499, #91485 ) ) ;
#225601=VERTEX_POINT ( 'NONE', #45712 ) ;
#225635=CARTESIAN_POINT ( 'NONE',  ( -21.05000000000000071, 44.52640028187936849, -247.3006740988509193 ) ) ;
#225638=CARTESIAN_POINT ( 'NONE',  ( -18.59999999999999787, 44.52640028187936849, -247.3006740988509193 ) ) ;
#225641=EDGE_LOOP ( 'NONE', ( #101133, #236384, #66214, #93477, #161927 ) ) ;
#225643=DIRECTION ( 'NONE',  ( -1.000000000000000000, -0.000000000000000000, 0.000000000000000000 ) ) ;
#225644=ORIENTED_EDGE ( 'NONE', *, *, #34747, .T. ) ;
#225655=DIRECTION ( 'NONE',  ( -0.7070776581709312669, -0.6453375049857505985, -0.2891032514073097470 ) ) ;
#225657=AXIS2_PLACEMENT_3D ( 'NONE', #220690, #204951, #203693 ) ;
#225665=CARTESIAN_POINT ( 'NONE',  ( 21.93340585899775164, 29.97485316283794532, -252.5455442746994947 ) ) ;
#225692=LINE ( 'NONE', #88762, #81545 ) ;
#225696=CIRCLE ( 'NONE', #88317, 4.000000000000002665 ) ;
#225713=FACE_OUTER_BOUND ( 'NONE', #158702, .T. ) ;
#225760=ADVANCED_FACE ( 'NONE', ( #234622 ), #167698, .T. ) ;
#225777=DIRECTION ( 'NONE',  ( 0.000000000000000000, 0.8103668758649523740, -0.5859227990963290500 ) ) ;
#225787=B_SPLINE_CURVE_WITH_KNOTS ( 'NONE', 3,
 ( #183121, #100943, #1874, #160988, #25342, #123141, #237937, #64450 ),
 .UNSPECIFIED., .F., .F.,
 ( 4, 2, 2, 4 ),
 ( 0.000000000000000000, 6.534141206309673484E-05, 0.0001306828241261934697, 0.0002613656482524646225 ),
 .UNSPECIFIED. ) ;
#225805=EDGE_LOOP ( 'NONE', ( #166868, #46801, #207396, #211010 ) ) ;
#225814=ORIENTED_EDGE ( 'NONE', *, *, #3038, .F. ) ;
#225816=EDGE_LOOP ( 'NONE', ( #207345, #207057, #29574, #137950 ) ) ;
#225824=DIRECTION ( 'NONE',  ( -1.000000000000000000, 1.207181226542539700E-16, -2.694675058168174199E-16 ) ) ;
#225829=CARTESIAN_POINT ( 'NONE',  ( -21.05000000000000071, 36.65892442174472876, -249.5511627012454596 ) ) ;
#225843=DIRECTION ( 'NONE',  ( 0.000000000000000000, -0.9160831752668552319, -0.4009882990724247809 ) ) ;
#225845=CARTESIAN_POINT ( 'NONE',  ( 21.05000000000000071, 62.04503132991427350, -248.4786563706009588 ) ) ;
#225879=CARTESIAN_POINT ( 'NONE',  ( 19.96984138294275368, 54.41891991186830779, -228.7197075361649183 ) ) ;
#225898=VECTOR ( 'NONE', #146818, 1000.000000000000000 ) ;
#225926=CARTESIAN_POINT ( 'NONE',  ( 20.74897398619109978, 39.33521109263118376, -236.7418682356311876 ) ) ;
#226008=CIRCLE ( 'NONE', #59407, 1.900000000000004574 ) ;
#226018=VERTEX_POINT ( 'NONE', #203193 ) ;
#226020=EDGE_CURVE ( 'NONE', #198338, #201217, #121988, .T. ) ;
#226064=CYLINDRICAL_SURFACE ( 'NONE', #99133, 0.09999999999999939493 ) ;
#226069=VERTEX_POINT ( 'NONE', #171814 ) ;
#226093=( BOUNDED_CURVE ( )  B_SPLINE_CURVE ( 3, ( #148372, #227907, #85786, #204476 ),
 .UNSPECIFIED., .F., .T. ) 
 B_SPLINE_CURVE_WITH_KNOTS ( ( 4, 4 ),
 ( 1.570796326794977382, 3.141592653589781570 ),
 .UNSPECIFIED. ) 
 CURVE ( )  GEOMETRIC_REPRESENTATION_ITEM ( )  RATIONAL_B_SPLINE_CURVE ( ( 1.000000000000000000, 0.8047378541243868089, 0.8047378541243868089, 1.000000000000000000 ) ) 
 REPRESENTATION_ITEM ( '' )  );
#226096=DIRECTION ( 'NONE',  ( -0.4999999999999800160, 0.7903412497644920487, 0.3540631425617770112 ) ) ;
#226213=CARTESIAN_POINT ( 'NONE',  ( 23.14999999999999503, 56.06656052939784729, -228.0911609752645290 ) ) ;
#226221=FACE_OUTER_BOUND ( 'NONE', #193831, .T. ) ;
#226227=ORIENTED_EDGE ( 'NONE', *, *, #9236, .T. ) ;
#226244=CARTESIAN_POINT ( 'NONE',  ( 20.04142135623730070, 54.35086488289006468, -228.7501953506800305 ) ) ;
#226247=EDGE_LOOP ( 'NONE', ( #240687, #93187, #214067, #11351 ) ) ;
#226251=ORIENTED_EDGE ( 'NONE', *, *, #141863, .F. ) ;
#226257=CIRCLE ( 'NONE', #113871, 0.9750000000000036415 ) ;
#226259=EDGE_CURVE ( 'NONE', #120435, #15704, #122076, .T. ) ;
#226299=DIRECTION ( 'NONE',  ( -1.000000000000000000, -0.000000000000000000, -0.000000000000000000 ) ) ;
#226313=PLANE ( 'NONE',  #24577 ) ;
#226319=CARTESIAN_POINT ( 'NONE',  ( -23.25000000000000000, 78.57213941646344324, -232.7862224702232652 ) ) ;
#226347=DIRECTION ( 'NONE',  ( 1.000000000000000000, 0.000000000000000000, 0.000000000000000000 ) ) ;
#226349=DIRECTION ( 'NONE',  ( 1.000000000000000000, 0.000000000000000000, 0.000000000000000000 ) ) ;
#226357=TOROIDAL_SURFACE ( 'NONE', #93676, 0.6000000000000004219, 0.1000000000000000056 ) ;
#226359=EDGE_LOOP ( 'NONE', ( #176755, #10943, #205388, #226957 ) ) ;
#226376=DIRECTION ( 'NONE',  ( 1.000000000000000000, 0.000000000000000000, 0.000000000000000000 ) ) ;
#226435=ORIENTED_EDGE ( 'NONE', *, *, #243675, .F. ) ;
#226461=ORIENTED_EDGE ( 'NONE', *, *, #121385, .F. ) ;
#226465=EDGE_CURVE ( 'NONE', #68804, #166946, #168006, .T. ) ;
#226478=CIRCLE ( 'NONE', #114058, 2.000000000000000444 ) ;
#226491=CARTESIAN_POINT ( 'NONE',  ( -20.94999999999999929, 69.25640205380744874, -247.7135141964517402 ) ) ;
#226496=CARTESIAN_POINT ( 'NONE',  ( 21.10257677756356642, 30.80951268217205907, -252.1442870260762845 ) ) ;
#226545=CARTESIAN_POINT ( 'NONE',  ( -23.25000000000000000, 21.17283678855157802, -243.7231193059830332 ) ) ;
#226556=EDGE_LOOP ( 'NONE', ( #89625, #57000, #166414, #52668, #244917 ) ) ;
#226622=DIRECTION ( 'NONE',  ( 0.000000000000000000, 0.5859227990963212784, 0.8103668758649578141 ) ) ;
#226640=ORIENTED_EDGE ( 'NONE', *, *, #158928, .F. ) ;
#226653=CARTESIAN_POINT ( 'NONE',  ( -20.94999999999999929, 36.73178316696986911, -249.7991537124309218 ) ) ;
#226661=CIRCLE ( 'NONE', #43339, 0.1000000000000024342 ) ;
#226701=EDGE_LOOP ( 'NONE', ( #139, #166172, #220327 ) ) ;
#226721=CARTESIAN_POINT ( 'NONE',  ( -18.39999999999999858, 46.91436717984746707, -255.3877622108296634 ) ) ;
#226734=ORIENTED_EDGE ( 'NONE', *, *, #12970, .F. ) ;
#226791=EDGE_CURVE ( 'NONE', #152685, #110735, #47505, .T. ) ;
#226838=ADVANCED_FACE ( 'NONE', ( #161759 ), #39246, .F. ) ;
#226875=FACE_OUTER_BOUND ( 'NONE', #111276, .T. ) ;
#226892=ORIENTED_EDGE ( 'NONE', *, *, #95373, .F. ) ;
#226898=DIRECTION ( 'NONE',  ( 0.000000000000000000, -0.9126074666063660468, -0.4088369013363524762 ) ) ;
#226908=CIRCLE ( 'NONE', #172967, 0.09999999999999326095 ) ;
#226935=ORIENTED_EDGE ( 'NONE', *, *, #117747, .F. ) ;
#226957=ORIENTED_EDGE ( 'NONE', *, *, #29813, .F. ) ;
#226976=FACE_OUTER_BOUND ( 'NONE', #190128, .T. ) ;
#226980=CARTESIAN_POINT ( 'NONE',  ( -23.15000000000000213, 61.88149656937975607, -248.1136133839584090 ) ) ;
#226983=EDGE_LOOP ( 'NONE', ( #235638, #209183, #221165, #134059 ) ) ;
#226994=CARTESIAN_POINT ( 'NONE',  ( -18.50000000000000000, 25.52560498759422103, -248.6860249505299407 ) ) ;
#227007=CIRCLE ( 'NONE', #114588, 0.09999999999999939493 ) ;
#227028=CARTESIAN_POINT ( 'NONE',  ( -18.40000000000000213, 46.96039402156215914, -255.3459641718773128 ) ) ;
#227076=DIRECTION ( 'NONE',  ( -4.391705002472924160E-16, -0.4088369013363268301, 0.9126074666063775931 ) ) ;
#227090=ORIENTED_EDGE ( 'NONE', *, *, #218653, .T. ) ;
#227093=FACE_OUTER_BOUND ( 'NONE', #61085, .T. ) ;
#227095=DIRECTION ( 'NONE',  ( 0.000000000000000000, 0.9126074666063772600, 0.4088369013363276627 ) ) ;
#227102=CARTESIAN_POINT ( 'NONE',  ( 21.14999999999999858, 31.94635157770351341, -238.7871412784868710 ) ) ;
#227105=DIRECTION ( 'NONE',  ( -1.000000000000000000, -0.000000000000000000, -0.000000000000000000 ) ) ;
#227107=AXIS2_PLACEMENT_3D ( 'NONE', #106928, #186488, #7858 ) ;
#227112=DIRECTION ( 'NONE',  ( 1.000000000000000000, 0.000000000000000000, 0.000000000000000000 ) ) ;
#227114=CARTESIAN_POINT ( 'NONE',  ( 23.24999999999999289, 38.35559756229049100, -253.3384836876619204 ) ) ;
#227121=VECTOR ( 'NONE', #257194, 1000.000000000000000 ) ;
#227130=ORIENTED_EDGE ( 'NONE', *, *, #136219, .F. ) ;
#227138=EDGE_CURVE ( 'NONE', #177565, #143659, #118460, .T. ) ;
#227168=AXIS2_PLACEMENT_3D ( 'NONE', #163650, #102348, #43699 ) ;
#227199=ORIENTED_EDGE ( 'NONE', *, *, #187125, .F. ) ;
#227208=ORIENTED_EDGE ( 'NONE', *, *, #96609, .T. ) ;
#227231=EDGE_LOOP ( 'NONE', ( #214616, #229374, #229819 ) ) ;
#227303=DIRECTION ( 'NONE',  ( -0.000000000000000000, 0.9126074666063770380, 0.4088369013363281068 ) ) ;
#227332=DIRECTION ( 'NONE',  ( -0.000000000000000000, 0.9126074666063772600, 0.4088369013363276072 ) ) ;
#227337=VERTEX_POINT ( 'NONE', #100121 ) ;
#227347=CARTESIAN_POINT ( 'NONE',  ( -20.94999999999999929, 43.51422117117169108, -240.0698702536254530 ) ) ;
#227348=EDGE_CURVE ( 'NONE', #140623, #121176, #80555, .T. ) ;
#227350=LINE ( 'NONE', #224772, #59565 ) ;
#227368=EDGE_CURVE ( 'NONE', #256883, #101237, #221356, .T. ) ;
#227372=TOROIDAL_SURFACE ( 'NONE', #60757, 0.2000000000000000111, 0.1000000000000000056 ) ;
#227395=ORIENTED_EDGE ( 'NONE', *, *, #215686, .F. ) ;
#227400=EDGE_LOOP ( 'NONE', ( #254383, #186423, #190044, #137055 ) ) ;
#227404=CARTESIAN_POINT ( 'NONE',  ( 21.05000000000000071, 39.26973050389061370, -236.6309188891183055 ) ) ;
#227409=ORIENTED_EDGE ( 'NONE', *, *, #129472, .T. ) ;
#227422=EDGE_CURVE ( 'NONE', #47325, #182399, #1892, .T. ) ;
#227438=FACE_OUTER_BOUND ( 'NONE', #110353, .T. ) ;
#227441=ADVANCED_FACE ( 'NONE', ( #124854 ), #151974, .T. ) ;
#227466=ORIENTED_EDGE ( 'NONE', *, *, #181224, .T. ) ;
#227489=ORIENTED_EDGE ( 'NONE', *, *, #134124, .F. ) ;
#227490=AXIS2_PLACEMENT_3D ( 'NONE', #50163, #172743, #110147 ) ;
#227497=EDGE_CURVE ( 'NONE', #123645, #97414, #22969, .T. ) ;
#227498=ORIENTED_EDGE ( 'NONE', *, *, #174325, .T. ) ;
#227500=VERTEX_POINT ( 'NONE', #249932 ) ;
#227572=CARTESIAN_POINT ( 'NONE',  ( -20.07928932188135107, 44.15985985257265867, -236.0871375574735680 ) ) ;
#227576=AXIS2_PLACEMENT_3D ( 'NONE', #16418, #18950, #95914 ) ;
#227583=DIRECTION ( 'NONE',  ( 0.000000000000000000, 0.1022405907414230264, 0.9947597004326447223 ) ) ;
#227590=DIRECTION ( 'NONE',  ( 0.000000000000000000, 0.4088369013363281623, -0.9126074666063771490 ) ) ;
#227597=CIRCLE ( 'NONE', #248458, 7.720710678118682502 ) ;
#227609=ORIENTED_EDGE ( 'NONE', *, *, #49358, .F. ) ;
#227625=AXIS2_PLACEMENT_3D ( 'NONE', #53178, #15357, #153618 ) ;
#227629=CIRCLE ( 'NONE', #115209, 0.09999999999999939493 ) ;
#227631=DIRECTION ( 'NONE',  ( 1.000000000000000000, -1.207181226542539700E-16, 2.694675058168174199E-16 ) ) ;
#227640=DIRECTION ( 'NONE',  ( 0.000000000000000000, 0.9126074666063771490, 0.4088369013363281623 ) ) ;
#227644=CYLINDRICAL_SURFACE ( 'NONE', #196276, 0.09999999999999939493 ) ;
#227645=DIRECTION ( 'NONE',  ( 1.000000000000000000, 0.000000000000000000, 0.000000000000000000 ) ) ;
#227684=DIRECTION ( 'NONE',  ( 1.000000000000000000, 0.000000000000000000, 0.000000000000000000 ) ) ;
#227687=DIRECTION ( 'NONE',  ( 0.000000000000000000, 0.9126074666063751506, 0.4088369013363318816 ) ) ;
#227724=DIRECTION ( 'NONE',  ( 1.000000000000000000, 0.000000000000000000, 0.000000000000000000 ) ) ;
#227733=FACE_OUTER_BOUND ( 'NONE', #41839, .T. ) ;
#227756=AXIS2_PLACEMENT_3D ( 'NONE', #249732, #210602, #211906 ) ;
#227768=VERTEX_POINT ( 'NONE', #249636 ) ;
#227780=ORIENTED_EDGE ( 'NONE', *, *, #67402, .T. ) ;
#227806=CIRCLE ( 'NONE', #227625, 0.2000000000000048683 ) ;
#227861=VECTOR ( 'NONE', #163122, 1000.000000000000114 ) ;
#227876=EDGE_CURVE ( 'NONE', #166946, #198535, #202197, .T. ) ;
#227880=DIRECTION ( 'NONE',  ( 1.000000000000000000, 0.000000000000000000, 0.000000000000000000 ) ) ;
#227900=LINE ( 'NONE', #209622, #85121 ) ;
#227907=CARTESIAN_POINT ( 'NONE',  ( 18.49999999999999289, 55.11567808474818975, -229.9682219939384140 ) ) ;
#227934=AXIS2_PLACEMENT_3D ( 'NONE', #160045, #98717, #257777 ) ;
#227943=ORIENTED_EDGE ( 'NONE', *, *, #88591, .T. ) ;
#227945=DIRECTION ( 'NONE',  ( 0.000000000000000000, -0.9126074666063769270, -0.4088369013363281623 ) ) ;
#227972=ORIENTED_EDGE ( 'NONE', *, *, #152773, .T. ) ;
#227981=VERTEX_POINT ( 'NONE', #17428 ) ;
#228002=DIRECTION ( 'NONE',  ( 0.000000000000000000, -0.9126074666063771490, -0.4088369013363281623 ) ) ;
#228019=CIRCLE ( 'NONE', #252952, 0.09999999999999609201 ) ;
#228039=TOROIDAL_SURFACE ( 'NONE', #78000, 0.2000000000000000111, 0.1000000000000000056 ) ;
#228064=EDGE_CURVE ( 'NONE', #46950, #25924, #68944, .T. ) ;
#228079=AXIS2_PLACEMENT_3D ( 'NONE', #94816, #114388, #230490 ) ;
#228082=DIRECTION ( 'NONE',  ( 1.000000000000000000, 0.000000000000000000, 0.000000000000000000 ) ) ;
#228085=CARTESIAN_POINT ( 'NONE',  ( 23.14999999999999858, 45.21086124044690280, -238.4331873168094091 ) ) ;
#228103=AXIS2_PLACEMENT_3D ( 'NONE', #62458, #105386, #101537 ) ;
#228108=DIRECTION ( 'NONE',  ( 1.000000000000000000, 0.000000000000000000, -0.000000000000000000 ) ) ;
#228111=DIRECTION ( 'NONE',  ( -1.000000000000000000, -0.000000000000000000, -0.000000000000000000 ) ) ;
#228116=CIRCLE ( 'NONE', #132426, 2.000000000000001776 ) ;
#228118=CARTESIAN_POINT ( 'NONE',  ( -21.05000000000000071, 34.11489510919708579, -243.6630126800748428 ) ) ;
#228123=DIRECTION ( 'NONE',  ( 0.000000000000000000, -0.4088369013363280513, 0.9126074666063769270 ) ) ;
#228169=ORIENTED_EDGE ( 'NONE', *, *, #92649, .F. ) ;
#228170=VERTEX_POINT ( 'NONE', #128096 ) ;
#228176=ORIENTED_EDGE ( 'NONE', *, *, #119899, .F. ) ;
#228209=AXIS2_PLACEMENT_3D ( 'NONE', #180448, #159604, #239133 ) ;
#228211=CARTESIAN_POINT ( 'NONE',  ( 21.05000000000000071, 43.16354019706792400, -239.5695141926698284 ) ) ;
#228214=VERTEX_POINT ( 'NONE', #249337 ) ;
#228217=ORIENTED_EDGE ( 'NONE', *, *, #135693, .T. ) ;
#228296=EDGE_LOOP ( 'NONE', ( #102972, #149951, #95178, #195081 ) ) ;
#228301=ADVANCED_FACE ( 'NONE', ( #216273 ), #206476, .T. ) ;
#228303=ORIENTED_EDGE ( 'NONE', *, *, #45182, .F. ) ;
#228315=VERTEX_POINT ( 'NONE', #239708 ) ;
#228331=CARTESIAN_POINT ( 'NONE',  ( -18.46093223321744858, 47.00039116560562036, -255.3068790871464557 ) ) ;
#228332=CARTESIAN_POINT ( 'NONE',  ( -23.25000000000000000, 67.85125148167622910, -227.9794913823769491 ) ) ;
#228350=ORIENTED_EDGE ( 'NONE', *, *, #246861, .T. ) ;
#228358=ORIENTED_EDGE ( 'NONE', *, *, #87636, .F. ) ;
#228360=ADVANCED_FACE ( 'NONE', ( #165297, #146999, #24528 ), #183583, .F. ) ;
#228363=CARTESIAN_POINT ( 'NONE',  ( -18.50000000000000000, 68.00417547777209393, -224.2303273613012777 ) ) ;
#228383=CARTESIAN_POINT ( 'NONE',  ( -20.85000000000000142, 67.76783854423860021, -227.9206834886612114 ) ) ;
#228395=VECTOR ( 'NONE', #245563, 1000.000000000000114 ) ;
#228411=VECTOR ( 'NONE', #50930, 1000.000000000000114 ) ;
#228417=VERTEX_POINT ( 'NONE', #206995 ) ;
#228435=CARTESIAN_POINT ( 'NONE',  ( -18.59999999999999787, 74.98773774893902555, -233.8732236541320333 ) ) ;
#228447=VERTEX_POINT ( 'NONE', #193854 ) ;
#228473=EDGE_LOOP ( 'NONE', ( #221923, #27097, #184820, #82630, #199511 ) ) ;
#228493=DIRECTION ( 'NONE',  ( 1.000000000000000000, 0.000000000000000000, 0.000000000000000000 ) ) ;
#228500=ORIENTED_EDGE ( 'NONE', *, *, #255090, .T. ) ;
#228527=CARTESIAN_POINT ( 'NONE',  ( -23.15000000000000213, 62.42906104934358069, -247.8683112431566258 ) ) ;
#228536=DIRECTION ( 'NONE',  ( -0.7071067811865475727, 0.2890913453342130457, -0.6453109281988448354 ) ) ;
#228538=CIRCLE ( 'NONE', #57812, 0.09999999999999609201 ) ;
#228546=CARTESIAN_POINT ( 'NONE',  ( 20.11144452913953273, 39.79843846208498093, -237.2598321417979150 ) ) ;
#228584=VERTEX_POINT ( 'NONE', #71352 ) ;
#228591=EDGE_CURVE ( 'NONE', #171099, #250586, #148408, .T. ) ;
#228597=CIRCLE ( 'NONE', #203646, 0.1000000000000028227 ) ;
#228598=CARTESIAN_POINT ( 'NONE',  ( 18.49999999999999645, 28.08990005499213538, -254.8141779806076670 ) ) ;
#228601=DIRECTION ( 'NONE',  ( -2.952720810173289112E-16, -0.4088369013363281068, 0.9126074666063770380 ) ) ;
#228622=FACE_OUTER_BOUND ( 'NONE', #209478, .T. ) ;
#228644=DIRECTION ( 'NONE',  ( 0.000000000000000000, -0.9126074666063780372, -0.4088369013363258309 ) ) ;
#228689=ADVANCED_FACE ( 'NONE', ( #55578 ), #35984, .T. ) ;
#228691=DIRECTION ( 'NONE',  ( 0.000000000000000000, 0.9126074666064696306, 0.4088369013361213278 ) ) ;
#228694=DIRECTION ( 'NONE',  ( 0.000000000000000000, 0.9090645160164306793, 0.4166553800442435729 ) ) ;
#228696=LINE ( 'NONE', #70920, #216573 ) ;
#228720=CARTESIAN_POINT ( 'NONE',  ( -18.59999999999999787, 46.55954744353147134, -243.3218549665227783 ) ) ;
#228723=AXIS2_PLACEMENT_3D ( 'NONE', #192999, #36510, #116035 ) ;
#228741=EDGE_CURVE ( 'NONE', #57244, #148222, #44362, .T. ) ;
#228755=DIRECTION ( 'NONE',  ( 0.000000000000000000, -0.4088369013363280513, 0.9126074666063769270 ) ) ;
#228778=VERTEX_POINT ( 'NONE', #206686 ) ;
#228780=TOROIDAL_SURFACE ( 'NONE', #116355, 1.900000000000002576, 0.1000000000000000056 ) ;
#228801=CIRCLE ( 'NONE', #212242, 0.09999999999999939493 ) ;
#228828=AXIS2_PLACEMENT_3D ( 'NONE', #132757, #106734, #246272 ) ;
#228835=CARTESIAN_POINT ( 'NONE',  ( -23.25000000000000000, 78.57744179526842743, -232.8011145694030972 ) ) ;
#228837=LINE ( 'NONE', #52744, #88448 ) ;
#228867=DIRECTION ( 'NONE',  ( 0.000000000000000000, 0.9126074666063757057, 0.4088369013363311044 ) ) ;
#228893=EDGE_LOOP ( 'NONE', ( #108928, #134999, #188248, #153329 ) ) ;
#228895=DIRECTION ( 'NONE',  ( 1.000000000000000000, 0.000000000000000000, 0.000000000000000000 ) ) ;
#228903=EDGE_LOOP ( 'NONE', ( #130760, #182758, #82815, #111045 ) ) ;
#228922=DIRECTION ( 'NONE',  ( 1.000000000000000000, 0.000000000000000000, 0.000000000000000000 ) ) ;
#228926=EDGE_CURVE ( 'NONE', #85846, #230417, #139988, .T. ) ;
#228937=DIRECTION ( 'NONE',  ( -1.000000000000000000, -0.000000000000000000, 0.000000000000000000 ) ) ;
#228939=CARTESIAN_POINT ( 'NONE',  ( 22.49999999999999645, 31.81502280147385164, -238.9558108736092095 ) ) ;
#228965=CARTESIAN_POINT ( 'NONE',  ( -22.39999999999999858, 36.56766367508408422, -249.5920463913791139 ) ) ;
#228972=EDGE_CURVE ( 'NONE', #150106, #178795, #81713, .T. ) ;
#228974=DIRECTION ( 'NONE',  ( 0.000000000000000000, -0.4088369013363280513, 0.9126074666063769270 ) ) ;
#228977=ORIENTED_EDGE ( 'NONE', *, *, #189924, .T. ) ;
#229024=ORIENTED_EDGE ( 'NONE', *, *, #114968, .F. ) ;
#229029=DIRECTION ( 'NONE',  ( 0.000000000000000000, 0.9126074666064696306, 0.4088369013361213278 ) ) ;
#229067=ORIENTED_EDGE ( 'NONE', *, *, #213074, .F. ) ;
#229081=EDGE_CURVE ( 'NONE', #60562, #18074, #177654, .T. ) ;
#229098=CARTESIAN_POINT ( 'NONE',  ( -20.85000000000000142, 67.84340367245323478, -228.0791829662263410 ) ) ;
#229134=DIRECTION ( 'NONE',  ( 0.000000000000000000, 0.4088369013363345461, -0.9126074666063741514 ) ) ;
#229151=CARTESIAN_POINT ( 'NONE',  ( 21.05000000000000071, 43.38680032004197784, -234.7865223221098745 ) ) ;
#229170=DIRECTION ( 'NONE',  ( 0.000000000000000000, 0.9126074666063770380, 0.4088369013363281068 ) ) ;
#229174=ORIENTED_EDGE ( 'NONE', *, *, #171255, .T. ) ;
#229207=ADVANCED_FACE ( 'NONE', ( #245520 ), #136077, .T. ) ;
#229240=CARTESIAN_POINT ( 'NONE',  ( -20.94999999999999929, 69.28189128378591022, -247.5258150475912089 ) ) ;
#229241=FACE_OUTER_BOUND ( 'NONE', #111280, .T. ) ;
#229286=ORIENTED_EDGE ( 'NONE', *, *, #153026, .F. ) ;
#229303=CARTESIAN_POINT ( 'NONE',  ( 23.24999999999999289, 34.96225128119897363, -245.7638417148289989 ) ) ;
#229307=CARTESIAN_POINT ( 'NONE',  ( 23.15000000000000213, 62.08591502004790641, -248.5699171172615820 ) ) ;
#229308=CARTESIAN_POINT ( 'NONE',  ( -20.94999999999999929, 36.65892442174472876, -249.5511627012454596 ) ) ;
#229326=ORIENTED_EDGE ( 'NONE', *, *, #219864, .F. ) ;
#229370=VERTEX_POINT ( 'NONE', #57561 ) ;
#229374=ORIENTED_EDGE ( 'NONE', *, *, #95071, .T. ) ;
#229407=CARTESIAN_POINT ( 'NONE',  ( -18.46902351632716943, 46.92263674392135187, -255.3732559572131606 ) ) ;
#229408=VERTEX_POINT ( 'NONE', #253204 ) ;
#229412=CARTESIAN_POINT ( 'NONE',  ( 21.05000000000000071, 69.05648948627111849, -235.0374527038057977 ) ) ;
#229414=VERTEX_POINT ( 'NONE', #58835 ) ;
#229415=DIRECTION ( 'NONE',  ( 0.000000000000000000, -0.9126074666063622720, -0.4088369013363611360 ) ) ;
#229423=ORIENTED_EDGE ( 'NONE', *, *, #230660, .F. ) ;
#229431=ORIENTED_EDGE ( 'NONE', *, *, #136219, .T. ) ;
#229467=ORIENTED_EDGE ( 'NONE', *, *, #105792, .F. ) ;
#229488=DIRECTION ( 'NONE',  ( -3.787827842127535236E-15, -0.9165223833629844163, 0.3999834006488702243 ) ) ;
#229515=VECTOR ( 'NONE', #166431, 1000.000000000000114 ) ;
#229517=EDGE_CURVE ( 'NONE', #228315, #2789, #40477, .T. ) ;
#229524=EDGE_CURVE ( 'NONE', #220102, #3155, #240359, .T. ) ;
#229552=AXIS2_PLACEMENT_3D ( 'NONE', #243523, #166589, #144396 ) ;
#229565=EDGE_CURVE ( 'NONE', #231005, #40222, #199686, .T. ) ;
#229570=FACE_OUTER_BOUND ( 'NONE', #225482, .T. ) ;
#229571=LINE ( 'NONE', #210009, #54671 ) ;
#229572=CIRCLE ( 'NONE', #100354, 0.09999999999999681366 ) ;
#229582=ORIENTED_EDGE ( 'NONE', *, *, #234234, .T. ) ;
#229583=LINE ( 'NONE', #92611, #42387 ) ;
#229592=ORIENTED_EDGE ( 'NONE', *, *, #185598, .F. ) ;
#229596=ORIENTED_EDGE ( 'NONE', *, *, #208596, .T. ) ;
#229600=DIRECTION ( 'NONE',  ( 0.000000000000000000, -0.4088369013363783999, 0.9126074666063545004 ) ) ;
#229660=VECTOR ( 'NONE', #142007, 1000.000000000000000 ) ;
#229675=VECTOR ( 'NONE', #89849, 1000.000000000000000 ) ;
#229706=FACE_OUTER_BOUND ( 'NONE', #66740, .T. ) ;
#229728=ORIENTED_EDGE ( 'NONE', *, *, #18121, .T. ) ;
#229732=DIRECTION ( 'NONE',  ( 0.000000000000000000, -0.4009882990724537022, 0.9160831752668424643 ) ) ;
#229736=CARTESIAN_POINT ( 'NONE',  ( -20.94999999999999929, 67.23127455305835554, -235.8551265064784559 ) ) ;
#229737=ADVANCED_FACE ( 'NONE', ( #206086 ), #27491, .F. ) ;
#229738=ORIENTED_EDGE ( 'NONE', *, *, #1983, .F. ) ;
#229740=ORIENTED_EDGE ( 'NONE', *, *, #227348, .F. ) ;
#229752=CARTESIAN_POINT ( 'NONE',  ( 21.05000000000000071, 41.42187432231295219, -260.1830396872097140 ) ) ;
#229753=ORIENTED_EDGE ( 'NONE', *, *, #198005, .F. ) ;
#229796=CARTESIAN_POINT ( 'NONE',  ( 22.39999999999999503, 33.47376623175147614, -242.4412390690852988 ) ) ;
#229807=AXIS2_PLACEMENT_3D ( 'NONE', #138328, #114, #195791 ) ;
#229814=ORIENTED_EDGE ( 'NONE', *, *, #199964, .T. ) ;
#229819=ORIENTED_EDGE ( 'NONE', *, *, #51170, .F. ) ;
#229832=EDGE_CURVE ( 'NONE', #191992, #235775, #144836, .T. ) ;
#229837=CIRCLE ( 'NONE', #204876, 2.099999999999990763 ) ;
#229842=EDGE_CURVE ( 'NONE', #192936, #169719, #177259, .T. ) ;
#229908=DIRECTION ( 'NONE',  ( 0.000000000000000000, -0.4088369013363283844, 0.9126074666063769270 ) ) ;
#229919=CARTESIAN_POINT ( 'NONE',  ( -23.25000000000000000, 67.23127455305835554, -235.8551265064784559 ) ) ;
#229937=CIRCLE ( 'NONE', #92367, 0.1000000000000023231 ) ;
#229938=CARTESIAN_POINT ( 'NONE',  ( 23.15000000000000213, 62.33780030268294325, -247.9091949332902516 ) ) ;
#229944=CIRCLE ( 'NONE', #238304, 0.09999999999999939493 ) ;
#229960=ORIENTED_EDGE ( 'NONE', *, *, #111407, .T. ) ;
#229970=DIRECTION ( 'NONE',  ( 1.000000000000000000, 0.000000000000000000, 0.000000000000000000 ) ) ;
#229973=AXIS2_PLACEMENT_3D ( 'NONE', #195951, #254592, #197208 ) ;
#230027=AXIS2_PLACEMENT_3D ( 'NONE', #54143, #227645, #29495 ) ;
#230107=TOROIDAL_SURFACE ( 'NONE', #117691, 0.4000000000000012990, 0.1000000000000000056 ) ;
#230126=ORIENTED_EDGE ( 'NONE', *, *, #16062, .F. ) ;
#230134=EDGE_LOOP ( 'NONE', ( #84080, #108664, #251891 ) ) ;
#230161=FACE_OUTER_BOUND ( 'NONE', #75801, .T. ) ;
#230182=VERTEX_POINT ( 'NONE', #55317 ) ;
#230198=CARTESIAN_POINT ( 'NONE',  ( -21.05000000000000071, 70.88170441948386724, -234.2197789011331679 ) ) ;
#230203=CARTESIAN_POINT ( 'NONE',  ( 23.14999999999999503, 56.35580082907249277, -225.2769695492280277 ) ) ;
#230221=DIRECTION ( 'NONE',  ( -3.265361837132813093E-16, -0.4088369013363280513, 0.9126074666063769270 ) ) ;
#230236=ORIENTED_EDGE ( 'NONE', *, *, #156845, .T. ) ;
#230274=CARTESIAN_POINT ( 'NONE',  ( 20.94999999999999929, 69.08367151115869831, -247.5088222940653679 ) ) ;
#230315=TOROIDAL_SURFACE ( 'NONE', #180441, 11.90000000000000391, 0.1000000000000000056 ) ;
#230322=ORIENTED_EDGE ( 'NONE', *, *, #71002, .F. ) ;
#230354=EDGE_CURVE ( 'NONE', #151159, #231797, #99584, .T. ) ;
#230363=CIRCLE ( 'NONE', #55362, 0.1000000000000024342 ) ;
#230375=DIRECTION ( 'NONE',  ( 0.000000000000000000, -0.4088369013363280513, 0.9126074666063769270 ) ) ;
#230391=ORIENTED_EDGE ( 'NONE', *, *, #46394, .F. ) ;
#230392=LINE ( 'NONE', #72625, #232388 ) ;
#230403=ORIENTED_EDGE ( 'NONE', *, *, #52992, .F. ) ;
#230417=VERTEX_POINT ( 'NONE', #8235 ) ;
#230439=CIRCLE ( 'NONE', #238823, 0.09999999999999854838 ) ;
#230448=DIRECTION ( 'NONE',  ( 1.000000000000000000, 0.000000000000000000, 0.000000000000000000 ) ) ;
#230453=DIRECTION ( 'NONE',  ( 1.000000000000000000, 0.000000000000000000, 0.000000000000000000 ) ) ;
#230454=CARTESIAN_POINT ( 'NONE',  ( 23.14999999999999147, 36.65892442174472876, -249.5511627012454596 ) ) ;
#230457=CARTESIAN_POINT ( 'NONE',  ( -23.25000000000000000, 67.23127455305835554, -235.8551265064784559 ) ) ;
#230486=ORIENTED_EDGE ( 'NONE', *, *, #61756, .T. ) ;
#230487=VECTOR ( 'NONE', #61499, 1000.000000000000114 ) ;
#230490=DIRECTION ( 'NONE',  ( 0.000000000000000000, 0.9126074666063545004, 0.4088369013363783999 ) ) ;
#230495=PLANE ( 'NONE',  #90785 ) ;
#230527=DIRECTION ( 'NONE',  ( 0.000000000000000000, 0.9126074666064005747, 0.4088369013362753712 ) ) ;
#230540=DIRECTION ( 'NONE',  ( 0.000000000000000000, -0.9126074666063545004, -0.4088369013363783999 ) ) ;
#230584=DIRECTION ( 'NONE',  ( -1.000000000000000000, -0.000000000000000000, 0.000000000000000000 ) ) ;
#230603=ADVANCED_FACE ( 'NONE', ( #69505 ), #149039, .F. ) ;
#230653=AXIS2_PLACEMENT_3D ( 'NONE', #14546, #193175, #19669 ) ;
#230656=DIRECTION ( 'NONE',  ( -0.7071067811865475727, 0.2890913453342132122, -0.6453109281988448354 ) ) ;
#230660=EDGE_CURVE ( 'NONE', #25924, #182906, #177605, .T. ) ;
#230665=VERTEX_POINT ( 'NONE', #99292 ) ;
#230673=DIRECTION ( 'NONE',  ( -0.000000000000000000, 0.1022405907414166287, 0.9947597004326451664 ) ) ;
#230682=EDGE_CURVE ( 'NONE', #150102, #105021, #56941, .T. ) ;
#230695=VECTOR ( 'NONE', #124905, 1000.000000000000000 ) ;
#230701=CARTESIAN_POINT ( 'NONE',  ( -18.50000000000000000, 67.67657779757796277, -227.9615671787948372 ) ) ;
#230704=EDGE_CURVE ( 'NONE', #41742, #973, #107033, .T. ) ;
#230712=AXIS2_PLACEMENT_3D ( 'NONE', #191154, #171602, #248533 ) ;
#230727=ORIENTED_EDGE ( 'NONE', *, *, #71044, .F. ) ;
#230732=EDGE_CURVE ( 'NONE', #246004, #49603, #184032, .T. ) ;
#230768=CARTESIAN_POINT ( 'NONE',  ( -23.15000000000000213, 69.08367151115869831, -247.5088222940653679 ) ) ;
#230791=CIRCLE ( 'NONE', #39077, 12.77499999999999503 ) ;
#230869=CIRCLE ( 'NONE', #10081, 0.09999999999999939493 ) ;
#230910=DIRECTION ( 'NONE',  ( 0.000000000000000000, 0.5283051335750404975, -0.8490545835446967615 ) ) ;
#230933=VECTOR ( 'NONE', #196300, 1000.000000000000114 ) ;
#230961=CARTESIAN_POINT ( 'NONE',  ( -23.25000000000000000, 74.93036000061670165, -233.6816308724374949 ) ) ;
#230970=ORIENTED_EDGE ( 'NONE', *, *, #105792, .T. ) ;
#230976=CIRCLE ( 'NONE', #218450, 0.09999999999999939493 ) ;
#231005=VERTEX_POINT ( 'NONE', #56256 ) ;
#231040=ORIENTED_EDGE ( 'NONE', *, *, #173474, .T. ) ;
#231043=ADVANCED_FACE ( 'NONE', ( #187794 ), #228039, .T. ) ;
#231067=ORIENTED_EDGE ( 'NONE', *, *, #147739, .F. ) ;
#231121=AXIS2_PLACEMENT_3D ( 'NONE', #238828, #198412, #58874 ) ;
#231139=DIRECTION ( 'NONE',  ( -1.000000000000000000, 1.207181226542539700E-16, -2.694675058168174199E-16 ) ) ;
#231142=EDGE_LOOP ( 'NONE', ( #2702, #100416, #27002, #208260 ) ) ;
#231148=DIRECTION ( 'NONE',  ( 0.000000000000000000, -0.9126074666063545004, -0.4088369013363783999 ) ) ;
#231150=DIRECTION ( 'NONE',  ( 1.000000000000000000, 0.000000000000000000, 0.000000000000000000 ) ) ;
#231194=DIRECTION ( 'NONE',  ( -0.000000000000000000, 0.4088369013363281068, -0.9126074666063770380 ) ) ;
#231198=CIRCLE ( 'NONE', #6307, 0.09999999999999609201 ) ;
#231199=PLANE ( 'NONE',  #30517 ) ;
#231212=CIRCLE ( 'NONE', #27225, 4.049999999999994493 ) ;
#231243=CARTESIAN_POINT ( 'NONE',  ( 18.59999999999999076, 53.37395138337728895, -234.8857996415767104 ) ) ;
#231249=VECTOR ( 'NONE', #194719, 1000.000000000000000 ) ;
#231268=LINE ( 'NONE', #69618, #49972 ) ;
#231270=VECTOR ( 'NONE', #67343, 1000.000000000000000 ) ;
#231437=VECTOR ( 'NONE', #84892, 1000.000000000000114 ) ;
#231441=SPHERICAL_SURFACE ( 'NONE', #70766, 0.1000000000000000056 ) ;
#231465=ORIENTED_EDGE ( 'NONE', *, *, #66800, .T. ) ;
#231503=DIRECTION ( 'NONE',  ( 0.000000000000000000, -0.3999834006488773852, -0.9165223833629813077 ) ) ;
#231505=DIRECTION ( 'NONE',  ( 1.000000000000000000, 0.000000000000000000, 0.000000000000000000 ) ) ;
#231564=AXIS2_PLACEMENT_3D ( 'NONE', #186019, #43940, #148171 ) ;
#231579=CARTESIAN_POINT ( 'NONE',  ( -18.50000000000000000, 62.46832465249013921, -225.2232495205141731 ) ) ;
#231582=TOROIDAL_SURFACE ( 'NONE', #244041, 0.2000000000000000111, 0.1000000000000000056 ) ;
#231603=FACE_OUTER_BOUND ( 'NONE', #144155, .T. ) ;
#231627=CARTESIAN_POINT ( 'NONE',  ( 21.07928932188134041, 30.84304088366581453, -252.0482413927673235 ) ) ;
#231659=CARTESIAN_POINT ( 'NONE',  ( 20.94999999999999929, 69.09936979046463534, -247.6075824278584889 ) ) ;
#231684=DIRECTION ( 'NONE',  ( 0.000000000000000000, 0.9126074666063602736, 0.4088369013363654103 ) ) ;
#231695=ADVANCED_FACE ( 'NONE', ( #213435 ), #172755, .F. ) ;
#231721=EDGE_LOOP ( 'NONE', ( #215332, #45922, #233890, #35418 ) ) ;
#231725=CARTESIAN_POINT ( 'NONE',  ( 21.00023020733439338, 34.04610124266385185, -243.7188077099090719 ) ) ;
#231740=DIRECTION ( 'NONE',  ( -1.000000000000000000, -0.000000000000000000, 0.000000000000000000 ) ) ;
#231741=LINE ( 'NONE', #170530, #39236 ) ;
#231764=ORIENTED_EDGE ( 'NONE', *, *, #117155, .T. ) ;
#231768=ADVANCED_FACE ( 'NONE', ( #136445 ), #217620, .T. ) ;
#231787=CARTESIAN_POINT ( 'NONE',  ( 21.14999999999999858, 45.11960049378627247, -238.4740710069430349 ) ) ;
#231797=VERTEX_POINT ( 'NONE', #47298 ) ;
#231810=DIRECTION ( 'NONE',  ( 1.000000000000000000, -2.986185139342070877E-16, 6.665775143889692774E-16 ) ) ;
#231812=EDGE_LOOP ( 'NONE', ( #37619, #111996, #119648, #60751 ) ) ;
#231818=CARTESIAN_POINT ( 'NONE',  ( -20.94999999999999929, 44.18518595211054389, -258.7688298343402380 ) ) ;
#231821=CYLINDRICAL_SURFACE ( 'NONE', #21247, 0.09999999999999939493 ) ;
#231843=ADVANCED_FACE ( 'NONE', ( #189413 ), #132544, .F. ) ;
#231856=ADVANCED_FACE ( 'NONE', ( #159909 ), #195105, .T. ) ;
#231891=TOROIDAL_SURFACE ( 'NONE', #227576, 0.4000000000000012990, 0.1000000000000000056 ) ;
#231906=AXIS2_PLACEMENT_3D ( 'NONE', #33038, #13434, #17289 ) ;
#231953=( GEOMETRIC_REPRESENTATION_CONTEXT ( 3 ) GLOBAL_UNCERTAINTY_ASSIGNED_CONTEXT ( ( #118375 ) ) GLOBAL_UNIT_ASSIGNED_CONTEXT ( ( #194642, #133361, #35566 ) ) REPRESENTATION_CONTEXT ( 'NONE', 'WORKASPACE' ) );
#231963=CARTESIAN_POINT ( 'NONE',  ( -23.15000000000000213, 36.65892442174472876, -249.5511627012454596 ) ) ;
#231972=ORIENTED_EDGE ( 'NONE', *, *, #130251, .F. ) ;
#232000=DIRECTION ( 'NONE',  ( 0.000000000000000000, -0.9126074666063753726, -0.4088369013363320481 ) ) ;
#232011=CARTESIAN_POINT ( 'NONE',  ( 22.40000000000010516, 26.02743912001976767, -254.3139371321012163 ) ) ;
#232025=ADVANCED_FACE ( 'NONE', ( #141006 ), #198395, .T. ) ;
#232046=CIRCLE ( 'NONE', #94648, 0.4999999999999944489 ) ;
#232050=CARTESIAN_POINT ( 'NONE',  ( -20.54999999999999716, 57.22075589414561136, -237.7098882646457128 ) ) ;
#232093=DIRECTION ( 'NONE',  ( 0.000000000000000000, -0.9955484899852913294, 0.09425075112701486457 ) ) ;
#232101=EDGE_CURVE ( 'NONE', #86809, #227337, #11949, .T. ) ;
#232106=DIRECTION ( 'NONE',  ( -2.915501640297154283E-16, -0.4088369013363279403, 0.9126074666063770380 ) ) ;
#232139=ADVANCED_FACE ( 'NONE', ( #221778 ), #257556, .T. ) ;
#232140=AXIS2_PLACEMENT_3D ( 'NONE', #157019, #74922, #194862 ) ;
#232153=EDGE_LOOP ( 'NONE', ( #212232, #48640, #137080, #151174, #141480, #219638, #67403, #26862, #147942, #161571, #163942, #88290, #238483, #204704, #244576, #211547, #37985, #67505, #101586, #153456, #48703, #95906, #246454, #125433, #214363 ) ) ;
#232155=AXIS2_PLACEMENT_3D ( 'NONE', #96569, #131870, #94013 ) ;
#232167=EDGE_CURVE ( 'NONE', #70441, #99245, #79709, .T. ) ;
#232199=FACE_OUTER_BOUND ( 'NONE', #18024, .T. ) ;
#232213=CIRCLE ( 'NONE', #228103, 0.09999999999999939493 ) ;
#232223=ORIENTED_EDGE ( 'NONE', *, *, #90764, .F. ) ;
#232226=DIRECTION ( 'NONE',  ( -1.000000000000000000, -0.000000000000000000, -0.000000000000000000 ) ) ;
#232278=CARTESIAN_POINT ( 'NONE',  ( -21.05000000000000071, 44.43513953521873106, -247.3415577889845736 ) ) ;
#232281=FACE_OUTER_BOUND ( 'NONE', #158528, .T. ) ;
#232285=CIRCLE ( 'NONE', #82382, 0.09999999999999771572 ) ;
#232311=VERTEX_POINT ( 'NONE', #30059 ) ;
#232314=EDGE_CURVE ( 'NONE', #228778, #100153, #228597, .T. ) ;
#232388=VECTOR ( 'NONE', #152169, 1000.000000000000000 ) ;
#232407=EDGE_CURVE ( 'NONE', #166897, #145909, #124721, .T. ) ;
#232426=CARTESIAN_POINT ( 'NONE',  ( 18.39999999999999858, 77.13860723519891849, -241.8264964602989266 ) ) ;
#232430=FACE_OUTER_BOUND ( 'NONE', #212798, .T. ) ;
#232464=DIRECTION ( 'NONE',  ( 1.000000000000000000, 0.000000000000000000, 0.000000000000000000 ) ) ;
#232494=CARTESIAN_POINT ( 'NONE',  ( 23.14999999999999858, 65.59592694771303911, -232.2046966400529584 ) ) ;
#232498=AXIS2_PLACEMENT_3D ( 'NONE', #31675, #29122, #128178 ) ;
#232503=CARTESIAN_POINT ( 'NONE',  ( 20.85000000000000142, 67.23127455305835554, -235.8551265064784559 ) ) ;
#232513=ORIENTED_EDGE ( 'NONE', *, *, #229517, .F. ) ;
#232549=VECTOR ( 'NONE', #188673, 1000.000000000000114 ) ;
#232578=FACE_OUTER_BOUND ( 'NONE', #138992, .T. ) ;
#232621=VERTEX_POINT ( 'NONE', #231787 ) ;
#232633=CARTESIAN_POINT ( 'NONE',  ( -18.59999999999999787, 21.17283678855158513, -243.7231193059830332 ) ) ;
#232661=CARTESIAN_POINT ( 'NONE',  ( -22.39999999999999858, 31.80471377451587500, -238.9601694054148027 ) ) ;
#232664=CARTESIAN_POINT ( 'NONE',  ( -21.05000000000000071, 44.09392520544991356, -258.8097135244738638 ) ) ;
#232680=DIRECTION ( 'NONE',  ( 0.000000000000000000, 0.9126074666063773710, 0.4088369013363274962 ) ) ;
#232713=CIRCLE ( 'NONE', #99404, 0.1000000000000024342 ) ;
#232732=CARTESIAN_POINT ( 'NONE',  ( 20.85000000000000142, 67.23127455305835554, -235.8551265064784559 ) ) ;
#232737=DIRECTION ( 'NONE',  ( 1.000000000000000000, 0.000000000000000000, 0.000000000000000000 ) ) ;
#232749=EDGE_LOOP ( 'NONE', ( #181472, #198322, #4919, #156769 ) ) ;
#232751=CARTESIAN_POINT ( 'NONE',  ( -21.05000000000000071, 30.68987205111127636, -252.2252246220829193 ) ) ;
#232752=ORIENTED_EDGE ( 'NONE', *, *, #206524, .T. ) ;
#232768=EDGE_CURVE ( 'NONE', #11074, #105460, #124903, .T. ) ;
#232771=ORIENTED_EDGE ( 'NONE', *, *, #117934, .T. ) ;
#232773=VECTOR ( 'NONE', #169082, 1000.000000000000000 ) ;
#232787=ADVANCED_FACE ( 'NONE', ( #244596 ), #63386, .F. ) ;
#232797=DIRECTION ( 'NONE',  ( 0.000000000000000000, 0.9126074666063660468, 0.4088369013363524762 ) ) ;
#232798=AXIS2_PLACEMENT_3D ( 'NONE', #228527, #49867, #208948 ) ;
#232832=CARTESIAN_POINT ( 'NONE',  ( -21.05000000000000071, 69.19063053712525857, -247.5666987377248631 ) ) ;
#232833=CARTESIAN_POINT ( 'NONE',  ( -21.05439746398122836, 38.23414080847646801, -235.9702891712775852 ) ) ;
#232907=DIRECTION ( 'NONE',  ( 0.000000000000000000, 0.9126074666063772600, 0.4088369013363276627 ) ) ;
#232956=( BOUNDED_SURFACE ( )  B_SPLINE_SURFACE ( 3, 2, ( 
 ( #166319, #25496, #87997 ),
 ( #104975, #146684, #26797 ),
 ( #48893, #144123, #127153 ),
 ( #145420, #45045, #205383 ),
 ( #106278, #63311, #204109 ),
 ( #184543, #65893, #5899 ) ),
 .UNSPECIFIED., .F., .F., .F. ) 
 B_SPLINE_SURFACE_WITH_KNOTS ( ( 4, 2, 4 ),
 ( 3, 3 ),
 ( 6.719893378900350768E-05, 0.0002757154632485721507, 0.0004842319927081408480 ),
 ( 0.000000000000000000, 1.000000000000000000 ),
 .UNSPECIFIED. ) 
 GEOMETRIC_REPRESENTATION_ITEM ( )  RATIONAL_B_SPLINE_SURFACE ( (
 ( 1.000000000000000000, 0.7250110520818935367, 1.000000000000000000),
 ( 1.000000000000000000, 0.7277932058356478828, 1.000000000000000000),
 ( 1.000000000000000000, 0.7278452872621734571, 1.000000000000000000),
 ( 1.000000000000000000, 0.7221445671545261291, 1.000000000000000000),
 ( 1.000000000000000000, 0.7163662143782721925, 1.000000000000000000),
 ( 1.000000000000000000, 0.7071067811865475727, 1.000000000000000000) ) ) 
 REPRESENTATION_ITEM ( '' )  SURFACE ( )  );
#232957=DIRECTION ( 'NONE',  ( -0.000000000000000000, 0.4088369013363297166, -0.9126074666063763718 ) ) ;
#232982=AXIS2_PLACEMENT_3D ( 'NONE', #90723, #228974, #54168 ) ;
#233018=CARTESIAN_POINT ( 'NONE',  ( 21.13461538461538325, 43.49873268050095021, -234.8559629938181388 ) ) ;
#233081=CIRCLE ( 'NONE', #212228, 7.899999999999994138 ) ;
#233096=VECTOR ( 'NONE', #112141, 1000.000000000000227 ) ;
#233099=EDGE_CURVE ( 'NONE', #241027, #252869, #94505, .T. ) ;
#233119=EDGE_CURVE ( 'NONE', #61601, #28183, #37135, .T. ) ;
#233134=EDGE_CURVE ( 'NONE', #116074, #195501, #55072, .T. ) ;
#233150=EDGE_CURVE ( 'NONE', #230665, #126059, #124363, .T. ) ;
#233170=DIRECTION ( 'NONE',  ( 0.000000000000000000, 0.9126074666063775931, 0.4088369013363268301 ) ) ;
#233179=ORIENTED_EDGE ( 'NONE', *, *, #82268, .T. ) ;
#233180=ADVANCED_FACE ( 'NONE', ( #61818 ), #64385, .T. ) ;
#233190=ADVANCED_FACE ( 'NONE', ( #103480 ), #162222, .T. ) ;
#233206=DIRECTION ( 'NONE',  ( -0.000000000000000000, 0.9072850278296915594, 0.4205162045344698618 ) ) ;
#233226=CARTESIAN_POINT ( 'NONE',  ( -21.05000000000000071, 26.06793112591406825, -254.4053733484743418 ) ) ;
#233229=EDGE_CURVE ( 'NONE', #48558, #26849, #233265, .T. ) ;
#233251=LINE ( 'NONE', #93707, #100257 ) ;
#233265=CIRCLE ( 'NONE', #104216, 0.4999999999999944489 ) ;
#233302=EDGE_CURVE ( 'NONE', #221915, #168895, #211602, .T. ) ;
#233307=CIRCLE ( 'NONE', #108399, 0.1000000000000024342 ) ;
#233319=EDGE_LOOP ( 'NONE', ( #193641, #125095, #126177, #141721 ) ) ;
#233352=DIRECTION ( 'NONE',  ( 0.000000000000000000, -0.9126074666063772600, -0.4088369013363274407 ) ) ;
#233399=VERTEX_POINT ( 'NONE', #199437 ) ;
#233435=FACE_OUTER_BOUND ( 'NONE', #40079, .T. ) ;
#233437=ADVANCED_FACE ( 'NONE', ( #118616 ), #241604, .F. ) ;
#233474=FACE_OUTER_BOUND ( 'NONE', #54431, .T. ) ;
#233479=CARTESIAN_POINT ( 'NONE',  ( -23.25000000000000000, 54.09940989982483472, -238.8890605415484174 ) ) ;
#233492=EDGE_LOOP ( 'NONE', ( #96850, #23026, #41471, #104324 ) ) ;
#233524=CARTESIAN_POINT ( 'NONE',  ( -21.05000000000000071, 30.93333081445676314, -252.0793046437616454 ) ) ;
#233556=CARTESIAN_POINT ( 'NONE',  ( -20.94999999999999929, 43.51422117117169819, -240.0698702536254530 ) ) ;
#233598=CIRCLE ( 'NONE', #91926, 0.1000000000000024342 ) ;
#233599=EDGE_CURVE ( 'NONE', #119433, #124911, #150227, .T. ) ;
#233609=VECTOR ( 'NONE', #54884, 1000.000000000000114 ) ;
#233644=VERTEX_POINT ( 'NONE', #184989 ) ;
#233666=CARTESIAN_POINT ( 'NONE',  ( 21.70464131381650219, 33.75808023539804736, -243.0758859948899726 ) ) ;
#233679=( BOUNDED_SURFACE ( )  B_SPLINE_SURFACE ( 3, 2, ( 
 ( #212595, #234717, #35264 ),
 ( #114766, #135591, #153942 ),
 ( #54777, #36549, #134305 ),
 ( #136891, #15698, #173513 ) ),
 .UNSPECIFIED., .F., .F., .F. ) 
 B_SPLINE_SURFACE_WITH_KNOTS ( ( 4, 4 ),
 ( 3, 3 ),
 ( 0.0006461284895273954445, 0.0007503702773986383346 ),
 ( 0.000000000000000000, 1.000000000000000000 ),
 .UNSPECIFIED. ) 
 GEOMETRIC_REPRESENTATION_ITEM ( )  RATIONAL_B_SPLINE_SURFACE ( (
 ( 1.000000000000000000, 0.7071067811865576758, 1.000000000000000000),
 ( 1.000000000000000000, 0.7076476444649448805, 1.000000000000000000),
 ( 1.000000000000000000, 0.7075727925190935519, 1.000000000000000000),
 ( 1.000000000000000000, 0.7071067811866011965, 1.000000000000000000) ) ) 
 REPRESENTATION_ITEM ( '' )  SURFACE ( )  );
#233682=CARTESIAN_POINT ( 'NONE',  ( -22.39999999999999858, 30.95512775545487472, -252.1063933345974988 ) ) ;
#233720=ADVANCED_FACE ( 'NONE', ( #89723 ), #14068, .F. ) ;
#233749=ADVANCED_FACE ( 'NONE', ( #192696 ), #37808, .T. ) ;
#233751=CYLINDRICAL_SURFACE ( 'NONE', #196009, 7.899999999999995914 ) ;
#233759=FACE_OUTER_BOUND ( 'NONE', #194215, .T. ) ;
#233786=ORIENTED_EDGE ( 'NONE', *, *, #49592, .T. ) ;
#233797=VERTEX_POINT ( 'NONE', #60866 ) ;
#233798=EDGE_CURVE ( 'NONE', #125226, #32455, #129359, .T. ) ;
#233818=EDGE_LOOP ( 'NONE', ( #26833, #114932, #98815, #201890 ) ) ;
#233827=EDGE_LOOP ( 'NONE', ( #142523, #33169, #214029, #192149 ) ) ;
#233846=CIRCLE ( 'NONE', #96450, 0.09999999999999609201 ) ;
#233856=CARTESIAN_POINT ( 'NONE',  ( -20.94999999999999929, 43.57281345108133053, -239.9888335660389487 ) ) ;
#233869=CARTESIAN_POINT ( 'NONE',  ( -18.59999999999999787, 67.23127455305835554, -235.8551265064784559 ) ) ;
#233890=ORIENTED_EDGE ( 'NONE', *, *, #43795, .F. ) ;
#233904=VECTOR ( 'NONE', #211477, 1000.000000000000114 ) ;
#233905=CARTESIAN_POINT ( 'NONE',  ( 20.94999999999999929, 47.95459712139159336, -246.5019368548292675 ) ) ;
#233943=EDGE_CURVE ( 'NONE', #109819, #217763, #103830, .T. ) ;
#233956=DIRECTION ( 'NONE',  ( -0.000000000000000000, -0.9126074666063770380, -0.4088369013363281068 ) ) ;
#234013=AXIS2_PLACEMENT_3D ( 'NONE', #87555, #225777, #103261 ) ;
#234050=AXIS2_PLACEMENT_3D ( 'NONE', #235343, #115404, #78827 ) ;
#234088=FACE_OUTER_BOUND ( 'NONE', #83674, .T. ) ;
#234095=ORIENTED_EDGE ( 'NONE', *, *, #93828, .T. ) ;
#234097=DIRECTION ( 'NONE',  ( 0.000000000000000000, 0.9126074666063545004, 0.4088369013363783999 ) ) ;
#234111=LINE ( 'NONE', #111609, #185547 ) ;
#234153=LINE ( 'NONE', #171661, #222369 ) ;
#234154=ORIENTED_EDGE ( 'NONE', *, *, #44357, .F. ) ;
#234170=CARTESIAN_POINT ( 'NONE',  ( 18.49999999999999289, 68.00366762990589109, -224.2307594727497815 ) ) ;
#234178=DIRECTION ( 'NONE',  ( 0.000000000000000000, 0.9126074666063769270, 0.4088369013363280513 ) ) ;
#234209=ORIENTED_EDGE ( 'NONE', *, *, #176925, .T. ) ;
#234212=CARTESIAN_POINT ( 'NONE',  ( -22.01447462590973103, 33.59883294982306978, -242.9626543818881430 ) ) ;
#234234=EDGE_CURVE ( 'NONE', #183191, #57327, #92119, .T. ) ;
#234266=CIRCLE ( 'NONE', #113486, 0.1000000000000024342 ) ;
#234277=ORIENTED_EDGE ( 'NONE', *, *, #127277, .T. ) ;
#234322=ORIENTED_EDGE ( 'NONE', *, *, #179273, .T. ) ;
#234327=DIRECTION ( 'NONE',  ( 0.000000000000000000, 0.9126074666063844765, 0.4088369013363113980 ) ) ;
#234332=PLANE ( 'NONE',  #141556 ) ;
#234335=ORIENTED_EDGE ( 'NONE', *, *, #102992, .F. ) ;
#234339=DIRECTION ( 'NONE',  ( 1.000000000000000000, 0.000000000000000000, 0.000000000000000000 ) ) ;
#234384=CARTESIAN_POINT ( 'NONE',  ( 20.94999999999999574, 36.65892442174472876, -249.5511627012454596 ) ) ;
#234400=DIRECTION ( 'NONE',  ( 1.000000000000000000, 0.000000000000000000, 0.000000000000000000 ) ) ;
#234435=DIRECTION ( 'NONE',  ( 0.000000000000000000, 0.9126074666063769270, 0.4088369013363282733 ) ) ;
#234441=AXIS2_PLACEMENT_3D ( 'NONE', #193245, #56273, #251920 ) ;
#234448=CARTESIAN_POINT ( 'NONE',  ( -22.39999999999999858, 33.38250548509083160, -242.4821227592188961 ) ) ;
#234507=EDGE_LOOP ( 'NONE', ( #99078, #147605, #33628 ) ) ;
#234551=ORIENTED_EDGE ( 'NONE', *, *, #224602, .T. ) ;
#234568=FACE_OUTER_BOUND ( 'NONE', #134919, .T. ) ;
#234569=CARTESIAN_POINT ( 'NONE',  ( -22.50000000000089173, 26.00803755075855150, -254.2729232455174326 ) ) ;
#234617=CARTESIAN_POINT ( 'NONE',  ( 20.94999999999999929, 53.66153320161009788, -235.9075159595686841 ) ) ;
#234622=FACE_OUTER_BOUND ( 'NONE', #162625, .T. ) ;
#234637=CYLINDRICAL_SURFACE ( 'NONE', #181624, 0.09999999999999681366 ) ;
#234661=CARTESIAN_POINT ( 'NONE',  ( 20.94999999999999929, 48.50000630096247534, -244.2465039064066161 ) ) ;
#234664=CARTESIAN_POINT ( 'NONE',  ( 20.94999999999999574, 47.95459712139159336, -246.5019368548292675 ) ) ;
#234672=DIRECTION ( 'NONE',  ( 0.000000000000000000, 0.9126074666063632712, 0.4088369013363589710 ) ) ;
#234717=CARTESIAN_POINT ( 'NONE',  ( -22.50000000000000355, 31.76322370622490254, -238.8696546380523955 ) ) ;
#234728=ORIENTED_EDGE ( 'NONE', *, *, #210037, .F. ) ;
#234792=ORIENTED_EDGE ( 'NONE', *, *, #225232, .F. ) ;
#234806=DIRECTION ( 'NONE',  ( 1.000000000000000000, 0.000000000000000000, 0.000000000000000000 ) ) ;
#234824=DIRECTION ( 'NONE',  ( 1.000000000000000000, 0.000000000000000000, 0.000000000000000000 ) ) ;
#234858=FACE_OUTER_BOUND ( 'NONE', #130541, .T. ) ;
#234863=DIRECTION ( 'NONE',  ( 0.000000000000000000, 0.9126074666064696306, 0.4088369013361213278 ) ) ;
#234901=CARTESIAN_POINT ( 'NONE',  ( -20.94999999999999929, 71.99422445362657186, -246.4870034924427671 ) ) ;
#234923=CARTESIAN_POINT ( 'NONE',  ( -23.25000000000000000, 62.12679871018154643, -248.6611778639222337 ) ) ;
#234934=ORIENTED_EDGE ( 'NONE', *, *, #20973, .F. ) ;
#234947=DIRECTION ( 'NONE',  ( 0.000000000000000000, -0.9126074666063781482, -0.4088369013363255533 ) ) ;
#234986=CARTESIAN_POINT ( 'NONE',  ( -21.14999999999999858, 30.90801580390628800, -252.0203440857197279 ) ) ;
#234989=DIRECTION ( 'NONE',  ( 0.000000000000000000, 0.9126074666063545004, 0.4088369013363783999 ) ) ;
#235009=AXIS2_PLACEMENT_3D ( 'NONE', #106472, #89491, #169086 ) ;
#235093=CARTESIAN_POINT ( 'NONE',  ( -22.39999999999999858, 31.98723526783714988, -238.8784020251475511 ) ) ;
#235102=AXIS2_PLACEMENT_3D ( 'NONE', #200490, #145310, #25399 ) ;
#235120=AXIS2_PLACEMENT_3D ( 'NONE', #87122, #183683, #144527 ) ;
#235137=FACE_OUTER_BOUND ( 'NONE', #65414, .T. ) ;
#235156=ADVANCED_FACE ( 'NONE', ( #34379 ), #4605, .T. ) ;
#235176=DIRECTION ( 'NONE',  ( -1.000000000000000000, 1.207181226542539700E-16, -2.694675058168174199E-16 ) ) ;
#235206=DIRECTION ( 'NONE',  ( 1.000000000000000000, 0.000000000000000000, 0.000000000000000000 ) ) ;
#235240=DIRECTION ( 'NONE',  ( 0.7071067811864846231, 0.2890913453341779626, -0.6453109281989296564 ) ) ;
#235247=CARTESIAN_POINT ( 'NONE',  ( -20.94999999999999929, 70.88170441948386724, -234.2197789011331679 ) ) ;
#235255=CARTESIAN_POINT ( 'NONE',  ( -23.25000000000000000, 67.23127455305835554, -235.8551265064784559 ) ) ;
#235320=CARTESIAN_POINT ( 'NONE',  ( 18.49999999999999289, 43.16354019706792400, -239.5695141926698284 ) ) ;
#235321=ORIENTED_EDGE ( 'NONE', *, *, #23875, .F. ) ;
#235343=CARTESIAN_POINT ( 'NONE',  ( 21.05000000000000071, 36.65892442174472876, -249.5511627012454596 ) ) ;
#235352=CARTESIAN_POINT ( 'NONE',  ( 21.00000000000000000, 52.06567329910104291, -231.9654557484363409 ) ) ;
#235353=AXIS2_PLACEMENT_3D ( 'NONE', #215899, #138910, #17705 ) ;
#235377=CARTESIAN_POINT ( 'NONE',  ( 21.05000000000000071, 45.93587830916155212, -239.9163948487882863 ) ) ;
#235386=ADVANCED_FACE ( 'NONE', ( #227093 ), #68030, .F. ) ;
#235395=AXIS2_PLACEMENT_3D ( 'NONE', #103574, #83986, #141437 ) ;
#235396=ORIENTED_EDGE ( 'NONE', *, *, #153889, .F. ) ;
#235429=DIRECTION ( 'NONE',  ( -1.000000000000000000, -0.000000000000000000, 0.000000000000000000 ) ) ;
#235446=CARTESIAN_POINT ( 'NONE',  ( 21.04999999999999716, 30.73564429423252164, -252.2206578267995383 ) ) ;
#235492=DIRECTION ( 'NONE',  ( 0.000000000000000000, 0.9654421110809058293, 0.2606175937108693996 ) ) ;
#235496=EDGE_LOOP ( 'NONE', ( #8992, #153957, #41025, #31898 ) ) ;
#235521=APPLICATION_CONTEXT ( 'automotive_design' ) ;
#235543=ORIENTED_EDGE ( 'NONE', *, *, #117094, .F. ) ;
#235570=DIRECTION ( 'NONE',  ( 0.000000000000000000, 0.9126074666063770380, 0.4088369013363281068 ) ) ;
#235589=ORIENTED_EDGE ( 'NONE', *, *, #73852, .T. ) ;
#235592=DIRECTION ( 'NONE',  ( 1.000000000000000000, 0.000000000000000000, 0.000000000000000000 ) ) ;
#235597=EDGE_CURVE ( 'NONE', #175048, #230665, #52294, .T. ) ;
#235598=ORIENTED_EDGE ( 'NONE', *, *, #40651, .F. ) ;
#235638=ORIENTED_EDGE ( 'NONE', *, *, #25132, .F. ) ;
#235642=CARTESIAN_POINT ( 'NONE',  ( -22.50000000000000000, 25.98945013819915673, -254.2294471341345456 ) ) ;
#235671=DIRECTION ( 'NONE',  ( 0.000000000000000000, -0.2868887416115947775, 0.9579639084728169829 ) ) ;
#235695=CARTESIAN_POINT ( 'NONE',  ( 20.94999999999999929, 74.88978653348847558, -233.9025578500150004 ) ) ;
#235706=CARTESIAN_POINT ( 'NONE',  ( 20.87155475150661132, 56.12642167632806434, -227.9547677828175551 ) ) ;
#235726=CYLINDRICAL_SURFACE ( 'NONE', #72855, 0.4999999999999944489 ) ;
#235747=EDGE_LOOP ( 'NONE', ( #63206, #34513, #148012, #173692 ) ) ;
#235775=VERTEX_POINT ( 'NONE', #29907 ) ;
#235778=CARTESIAN_POINT ( 'NONE',  ( -23.24999999999999645, 77.27075167199318173, -241.8768735168259241 ) ) ;
#235784=ORIENTED_EDGE ( 'NONE', *, *, #174221, .F. ) ;
#235786=DIRECTION ( 'NONE',  ( 0.000000000000000000, -0.9126074666063767049, -0.4088369013363286619 ) ) ;
#235820=VERTEX_POINT ( 'NONE', #183817 ) ;
#235822=EDGE_CURVE ( 'NONE', #123266, #222515, #21856, .T. ) ;
#235831=CARTESIAN_POINT ( 'NONE',  ( 22.40000000000010161, 25.93539162822990818, -254.3551732743596574 ) ) ;
#235839=CARTESIAN_POINT ( 'NONE',  ( -18.59999999999999787, 52.27009174976920747, -232.4217594817395138 ) ) ;
#235856=CARTESIAN_POINT ( 'NONE',  ( 23.14999999999999858, 67.23127455305835554, -235.8551265064784559 ) ) ;
#235885=VECTOR ( 'NONE', #193862, 1000.000000000000000 ) ;
#235896=DIRECTION ( 'NONE',  ( -1.000000000000000000, 1.335000415235278971E-16, -2.979993593738921214E-16 ) ) ;
#235909=DIRECTION ( 'NONE',  ( -1.000000000000000000, -0.000000000000000000, -0.000000000000000000 ) ) ;
#235927=AXIS2_PLACEMENT_3D ( 'NONE', #188226, #9578, #30454 ) ;
#235967=LINE ( 'NONE', #212580, #198923 ) ;
#235986=VERTEX_POINT ( 'NONE', #200503 ) ;
#235995=EDGE_CURVE ( 'NONE', #84325, #61043, #101342, .T. ) ;
#236001=ORIENTED_EDGE ( 'NONE', *, *, #148072, .F. ) ;
#236021=ORIENTED_EDGE ( 'NONE', *, *, #125859, .F. ) ;
#236036=EDGE_LOOP ( 'NONE', ( #94258, #54549 ) ) ;
#236038=AXIS2_PLACEMENT_3D ( 'NONE', #236312, #17286, #39435 ) ;
#236061=CARTESIAN_POINT ( 'NONE',  ( -21.05000000000000071, 67.23127455305835554, -235.8551265064784559 ) ) ;
#236074=ORIENTED_EDGE ( 'NONE', *, *, #57400, .F. ) ;
#236084=CARTESIAN_POINT ( 'NONE',  ( -21.14999999999999858, 25.97741635855165754, -254.4468634167653249 ) ) ;
#236128=DIRECTION ( 'NONE',  ( 0.000000000000000000, 0.9126074666063772600, 0.4088369013363276627 ) ) ;
#236151=ORIENTED_EDGE ( 'NONE', *, *, #217073, .T. ) ;
#236167=CARTESIAN_POINT ( 'NONE',  ( 23.24999999999999289, 53.32357432685029153, -235.0179440783709879 ) ) ;
#236176=EDGE_LOOP ( 'NONE', ( #196475, #124263, #139088, #254479 ) ) ;
#236204=VECTOR ( 'NONE', #149717, 1000.000000000000114 ) ;
#236291=CARTESIAN_POINT ( 'NONE',  ( 23.14999999999999858, 67.23127455305835554, -235.8551265064784559 ) ) ;
#236303=AXIS2_PLACEMENT_3D ( 'NONE', #66735, #242784, #185391 ) ;
#236312=CARTESIAN_POINT ( 'NONE',  ( -20.94999999999999929, 67.23127455305835554, -235.8551265064784559 ) ) ;
#236313=CARTESIAN_POINT ( 'NONE',  ( 18.59999999999999076, 74.93036000061670165, -233.6816308724374949 ) ) ;
#236320=AXIS2_PLACEMENT_3D ( 'NONE', #118916, #102836, #182419 ) ;
#236344=CARTESIAN_POINT ( 'NONE',  ( -22.49231231312463208, 31.84026337202741530, -238.9442601656825786 ) ) ;
#236364=CARTESIAN_POINT ( 'NONE',  ( -20.94999999999999929, 56.46250644710310951, -240.6794019422471251 ) ) ;
#236380=CIRCLE ( 'NONE', #169784, 0.8750000000000007772 ) ;
#236384=ORIENTED_EDGE ( 'NONE', *, *, #47150, .F. ) ;
#236387=EDGE_CURVE ( 'NONE', #249181, #147011, #140943, .T. ) ;
#236400=CARTESIAN_POINT ( 'NONE',  ( -18.50000000000000711, 38.25685495413521409, -235.9601135138701693 ) ) ;
#236412=DIRECTION ( 'NONE',  ( 0.000000000000000000, -0.4088369013363280513, 0.9126074666063769270 ) ) ;
#236434=ADVANCED_FACE ( 'NONE', ( #128049 ), #239220, .T. ) ;
#236435=AXIS2_PLACEMENT_3D ( 'NONE', #92544, #156419, #251633 ) ;
#236436=DIRECTION ( 'NONE',  ( -0.7071067811865475727, 0.2890913453342130457, -0.6453109281988448354 ) ) ;
#236453=ORIENTED_EDGE ( 'NONE', *, *, #219503, .F. ) ;
#236470=DIRECTION ( 'NONE',  ( -1.000000000000000000, -0.000000000000000000, 0.000000000000000000 ) ) ;
#236472=DIRECTION ( 'NONE',  ( -0.000000000000000000, 0.9072850278296915594, 0.4205162045344698618 ) ) ;
#236486=FACE_OUTER_BOUND ( 'NONE', #94712, .T. ) ;
#236487=ORIENTED_EDGE ( 'NONE', *, *, #221080, .T. ) ;
#236492=ORIENTED_EDGE ( 'NONE', *, *, #5873, .T. ) ;
#236518=CARTESIAN_POINT ( 'NONE',  ( 21.07199075132371746, 44.21756374323442174, -236.5497397326664384 ) ) ;
#236531=ORIENTED_EDGE ( 'NONE', *, *, #36050, .T. ) ;
#236567=AXIS2_PLACEMENT_3D ( 'NONE', #156861, #175158, #199828 ) ;
#236572=CARTESIAN_POINT ( 'NONE',  ( -21.55000000000000071, 53.12864924257549148, -234.3382351616128858 ) ) ;
#236582=ORIENTED_EDGE ( 'NONE', *, *, #113222, .F. ) ;
#236632=ORIENTED_EDGE ( 'NONE', *, *, #137316, .F. ) ;
#236658=FACE_OUTER_BOUND ( 'NONE', #17982, .T. ) ;
#236704=DIRECTION ( 'NONE',  ( 0.000000000000000000, 0.9126074666063751506, 0.4088369013363318816 ) ) ;
#236709=VERTEX_POINT ( 'NONE', #3942 ) ;
#236725=DIRECTION ( 'NONE',  ( 0.000000000000000000, -0.9126074666063770380, -0.4088369013363281068 ) ) ;
#236739=ORIENTED_EDGE ( 'NONE', *, *, #40833, .F. ) ;
#236784=VERTEX_POINT ( 'NONE', #143445 ) ;
#236789=AXIS2_PLACEMENT_3D ( 'NONE', #183052, #82613, #210004 ) ;
#236791=AXIS2_PLACEMENT_3D ( 'NONE', #182875, #6777, #246662 ) ;
#236803=CARTESIAN_POINT ( 'NONE',  ( 22.57856590037848576, 25.93742114931687581, -254.3587877384877345 ) ) ;
#236811=DIRECTION ( 'NONE',  ( 0.000000000000000000, 0.9126074666063660468, 0.4088369013363524762 ) ) ;
#236816=CYLINDRICAL_SURFACE ( 'NONE', #167619, 12.87499999999999112 ) ;
#236821=ORIENTED_EDGE ( 'NONE', *, *, #89012, .T. ) ;
#236827=DIRECTION ( 'NONE',  ( -0.000000000000000000, -0.9126074666063770380, -0.4088369013363281068 ) ) ;
#236831=CIRCLE ( 'NONE', #182707, 0.5999999999999968692 ) ;
#236877=EDGE_CURVE ( 'NONE', #128733, #236709, #248987, .T. ) ;
#236885=CIRCLE ( 'NONE', #86844, 0.1000000000000024342 ) ;
#236914=ADVANCED_FACE ( 'NONE', ( #225523 ), #139428, .T. ) ;
#236921=FACE_OUTER_BOUND ( 'NONE', #129995, .T. ) ;
#236922=EDGE_CURVE ( 'NONE', #173652, #132976, #156039, .T. ) ;
#236923=ORIENTED_EDGE ( 'NONE', *, *, #124735, .T. ) ;
#236936=CARTESIAN_POINT ( 'NONE',  ( -22.41119224318417125, 26.02743912001966464, -254.3139371321002216 ) ) ;
#236957=CARTESIAN_POINT ( 'NONE',  ( -18.36527282682039441, 77.43243019102997948, -241.6948680535597020 ) ) ;
#236984=CARTESIAN_POINT ( 'NONE',  ( 23.14999999999999858, 67.23127455305835554, -235.8551265064784559 ) ) ;
#237008=DIRECTION ( 'NONE',  ( -1.000000000000000000, 0.000000000000000000, 0.000000000000000000 ) ) ;
#237020=ORIENTED_EDGE ( 'NONE', *, *, #165556, .F. ) ;
#237033=CARTESIAN_POINT ( 'NONE',  ( -23.25000000000000000, 78.45218979564165807, -232.7313097695096076 ) ) ;
#237052=EDGE_CURVE ( 'NONE', #112216, #164531, #155033, .T. ) ;
#237084=ORIENTED_EDGE ( 'NONE', *, *, #132722, .T. ) ;
#237102=ORIENTED_EDGE ( 'NONE', *, *, #123473, .F. ) ;
#237113=CIRCLE ( 'NONE', #16543, 4.099999999999998757 ) ;
#237174=ORIENTED_EDGE ( 'NONE', *, *, #119643, .T. ) ;
#237183=CARTESIAN_POINT ( 'NONE',  ( 22.47071067811865319, 29.57301391503007082, -252.6169816238249552 ) ) ;
#237193=AXIS2_PLACEMENT_3D ( 'NONE', #31677, #175062, #69509 ) ;
#237212=CIRCLE ( 'NONE', #212277, 0.09999999999999771572 ) ;
#237231=DIRECTION ( 'NONE',  ( -1.000000000000000000, 0.000000000000000000, 0.000000000000000000 ) ) ;
#237243=FACE_OUTER_BOUND ( 'NONE', #26107, .T. ) ;
#237272=AXIS2_PLACEMENT_3D ( 'NONE', #167493, #253085, #36653 ) ;
#237295=CARTESIAN_POINT ( 'NONE',  ( -18.59999999999999787, 67.67657779757796277, -227.9615671787948372 ) ) ;
#237347=CARTESIAN_POINT ( 'NONE',  ( -18.41418431465368855, 77.13860723519847795, -241.8264964602994098 ) ) ;
#237354=DIRECTION ( 'NONE',  ( -0.000000000000000000, -0.09425075112713271475, -0.9955484899852801162 ) ) ;
#237366=CARTESIAN_POINT ( 'NONE',  ( 21.05000000000000071, 69.34766280046808617, -247.6726305063181144 ) ) ;
#237381=DIRECTION ( 'NONE',  ( -1.000000000000000000, -0.000000000000000000, 0.000000000000000000 ) ) ;
#237390=CARTESIAN_POINT ( 'NONE',  ( 20.93284271247462414, 56.02567683926421438, -227.9999002286038774 ) ) ;
#237394=DIRECTION ( 'NONE',  ( 1.000000000000000000, 0.000000000000000000, 0.000000000000000000 ) ) ;
#237420=EDGE_CURVE ( 'NONE', #114879, #233399, #68879, .T. ) ;
#237427=EDGE_CURVE ( 'NONE', #57757, #198148, #190347, .T. ) ;
#237429=AXIS2_PLACEMENT_3D ( 'NONE', #39487, #255876, #119000 ) ;
#237433=AXIS2_PLACEMENT_3D ( 'NONE', #234384, #34951, #213537 ) ;
#237448=DIRECTION ( 'NONE',  ( 0.000000000000000000, -0.4088369013363783999, 0.9126074666063545004 ) ) ;
#237449=DIRECTION ( 'NONE',  ( 0.000000000000000000, 0.9126074666063753726, 0.4088369013363320481 ) ) ;
#237458=LINE ( 'NONE', #1392, #71434 ) ;
#237494=EDGE_CURVE ( 'NONE', #48558, #254767, #113000, .T. ) ;
#237504=EDGE_CURVE ( 'NONE', #182894, #146851, #118987, .T. ) ;
#237512=AXIS2_PLACEMENT_3D ( 'NONE', #6423, #48118, #87231 ) ;
#237529=EDGE_LOOP ( 'NONE', ( #46832, #77963 ) ) ;
#237536=VECTOR ( 'NONE', #225573, 1000.000000000000114 ) ;
#237549=CARTESIAN_POINT ( 'NONE',  ( 18.50000000000000711, 47.12421348240935259, -255.1840482521099318 ) ) ;
#237552=CARTESIAN_POINT ( 'NONE',  ( -23.25000000000000000, 78.48087866980282001, -232.8271061603568910 ) ) ;
#237553=EDGE_CURVE ( 'NONE', #110197, #252869, #6530, .T. ) ;
#237582=DIRECTION ( 'NONE',  ( 0.000000000000000000, -0.9126074666063545004, -0.4088369013363783999 ) ) ;
#237589=CARTESIAN_POINT ( 'NONE',  ( 21.05000000000000071, 54.32225538558145672, -236.1594012422037281 ) ) ;
#237596=CIRCLE ( 'NONE', #120910, 0.09999999999999609201 ) ;
#237627=DIRECTION ( 'NONE',  ( 2.952720810173289112E-16, 0.4088369013363281068, -0.9126074666063770380 ) ) ;
#237632=LINE ( 'NONE', #55101, #129983 ) ;
#237646=ORIENTED_EDGE ( 'NONE', *, *, #64697, .F. ) ;
#237675=CARTESIAN_POINT ( 'NONE',  ( 23.14999999999999147, 34.96225128119897363, -245.7638417148289989 ) ) ;
#237687=AXIS2_PLACEMENT_3D ( 'NONE', #18543, #115073, #173819 ) ;
#237713=CARTESIAN_POINT ( 'NONE',  ( -20.64999999999999858, 54.22301550979020845, -237.0256805049050115 ) ) ;
#237721=EDGE_CURVE ( 'NONE', #68804, #87416, #176840, .T. ) ;
#237742=AXIS2_PLACEMENT_3D ( 'NONE', #73321, #137114, #135807 ) ;
#237760=DIRECTION ( 'NONE',  ( -4.163336342344447088E-13, 0.4205162045344795763, -0.9072850278296868964 ) ) ;
#237763=DIRECTION ( 'NONE',  ( -0.000000000000000000, 0.4088369013363281068, -0.9126074666063770380 ) ) ;
#237765=DIRECTION ( 'NONE',  ( -1.000000000000000000, -0.000000000000000000, -0.000000000000000000 ) ) ;
#237785=ORIENTED_EDGE ( 'NONE', *, *, #95572, .F. ) ;
#237798=ADVANCED_FACE ( 'NONE', ( #132252 ), #231582, .T. ) ;
#237808=CARTESIAN_POINT ( 'NONE',  ( -21.07928932188134041, 33.98134083355423485, -243.8161431329846778 ) ) ;
#237815=CARTESIAN_POINT ( 'NONE',  ( 21.05000000000000071, 44.15903683684981473, -236.5744930507153185 ) ) ;
#237820=CARTESIAN_POINT ( 'NONE',  ( 21.05563370358598263, 43.39284295883493314, -234.7832529069957559 ) ) ;
#237821=CIRCLE ( 'NONE', #108809, 0.3999999999999983569 ) ;
#237832=DIRECTION ( 'NONE',  ( 0.000000000000000000, 0.9126074666063783702, 0.4088369013363252757 ) ) ;
#237836=DIRECTION ( 'NONE',  ( 0.000000000000000000, -0.4088369013363280513, 0.9126074666063771490 ) ) ;
#237848=CARTESIAN_POINT ( 'NONE',  ( 20.95083306685154056, 40.74986006426208718, -237.9477423030747616 ) ) ;
#237871=CIRCLE ( 'NONE', #125464, 0.09999999999999939493 ) ;
#237896=CARTESIAN_POINT ( 'NONE',  ( 21.14999999999999503, 30.95512775545487472, -252.1063933345974988 ) ) ;
#237910=DIRECTION ( 'NONE',  ( -1.000000000000000000, -0.000000000000000000, 0.000000000000000000 ) ) ;
#237935=AXIS2_PLACEMENT_3D ( 'NONE', #188895, #205881, #234097 ) ;
#237937=CARTESIAN_POINT ( 'NONE',  ( -21.13614978966382196, 34.00185059398663867, -243.6200312240952712 ) ) ;
#237939=CARTESIAN_POINT ( 'NONE',  ( 18.39999999999999858, 29.77885356168128439, -262.9335064780472635 ) ) ;
#237945=EDGE_LOOP ( 'NONE', ( #24307, #109541, #227943, #176504 ) ) ;
#237976=ADVANCED_FACE ( 'NONE', ( #193083 ), #151397, .T. ) ;
#237982=CARTESIAN_POINT ( 'NONE',  ( 18.49999999999999289, 62.46832465249013921, -225.2232495205141731 ) ) ;
#237989=DIRECTION ( 'NONE',  ( 0.000000000000000000, 0.9126074666063844765, 0.4088369013363114535 ) ) ;
#238013=CARTESIAN_POINT ( 'NONE',  ( 21.05000000000000071, 36.65892442174472876, -249.5511627012454596 ) ) ;
#238023=EDGE_LOOP ( 'NONE', ( #215856, #27455, #70105, #205040 ) ) ;
#238041=DIRECTION ( 'NONE',  ( -1.000000000000000000, -0.000000000000000000, -0.000000000000000000 ) ) ;
#238052=CARTESIAN_POINT ( 'NONE',  ( 22.43288208788031213, 26.02536192431362139, -254.3094986185249127 ) ) ;
#238053=CARTESIAN_POINT ( 'NONE',  ( -20.85000000000000142, 78.48087866980282001, -232.8271061603568910 ) ) ;
#238092=DIRECTION ( 'NONE',  ( -1.000000000000000000, -0.000000000000000000, 0.000000000000000000 ) ) ;
#238120=VERTEX_POINT ( 'NONE', #22737 ) ;
#238191=CIRCLE ( 'NONE', #21738, 0.09999999999999939493 ) ;
#238208=CARTESIAN_POINT ( 'NONE',  ( -23.15000000000000213, 69.19063053712525857, -247.5666987377248631 ) ) ;
#238211=DIRECTION ( 'NONE',  ( 0.000000000000000000, 0.4088369013363281623, -0.9126074666063771490 ) ) ;
#238231=CARTESIAN_POINT ( 'NONE',  ( 21.05000000000000071, 53.66153320161009788, -235.9075159595686841 ) ) ;
#238244=CARTESIAN_POINT ( 'NONE',  ( -20.54999999999999716, 54.82645269529697885, -239.3027372265576957 ) ) ;
#238270=CARTESIAN_POINT ( 'NONE',  ( 21.05000000000000071, 56.16603649944111254, -228.1013850343386480 ) ) ;
#238298=PRODUCT_DEFINITION_CONTEXT ( 'detailed design', #55765, 'design' ) ;
#238304=AXIS2_PLACEMENT_3D ( 'NONE', #209571, #173055, #131308 ) ;
#238340=DIRECTION ( 'NONE',  ( 0.000000000000000000, -0.1022405907414166287, -0.9947597004326451664 ) ) ;
#238395=CIRCLE ( 'NONE', #118261, 12.87499999999999112 ) ;
#238402=ORIENTED_EDGE ( 'NONE', *, *, #115012, .F. ) ;
#238420=EDGE_CURVE ( 'NONE', #71691, #215984, #127723, .T. ) ;
#238427=CARTESIAN_POINT ( 'NONE',  ( 21.05000000000000071, 40.88152484246180052, -238.0427780438910474 ) ) ;
#238445=ORIENTED_EDGE ( 'NONE', *, *, #125816, .F. ) ;
#238456=DIRECTION ( 'NONE',  ( 0.000000000000000000, -0.9947597004326491632, 0.1022405907413782566 ) ) ;
#238458=CARTESIAN_POINT ( 'NONE',  ( 21.78635804494511419, 30.19765029368026887, -252.3372479796726680 ) ) ;
#238464=EDGE_LOOP ( 'NONE', ( #192545, #126705, #226734, #198644 ) ) ;
#238465=CARTESIAN_POINT ( 'NONE',  ( 23.14999999999999858, 67.23127455305835554, -235.8551265064784559 ) ) ;
#238472=EDGE_CURVE ( 'NONE', #111624, #94854, #216744, .T. ) ;
#238483=ORIENTED_EDGE ( 'NONE', *, *, #108035, .F. ) ;
#238493=CARTESIAN_POINT ( 'NONE',  ( 18.49999999999998934, 43.12265650693429819, -239.4782534460092052 ) ) ;
#238495=DIRECTION ( 'NONE',  ( 0.000000000000000000, 0.9126074666063769270, 0.4088369013363282733 ) ) ;
#238500=VERTEX_POINT ( 'NONE', #14731 ) ;
#238507=CARTESIAN_POINT ( 'NONE',  ( -23.25000000000000000, 70.79044367282321559, -234.2606625912667937 ) ) ;
#238528=EDGE_CURVE ( 'NONE', #51580, #229370, #185971, .T. ) ;
#238638=ORIENTED_EDGE ( 'NONE', *, *, #140237, .T. ) ;
#238655=CIRCLE ( 'NONE', #84671, 0.2000000000000090317 ) ;
#238711=ADVANCED_FACE ( 'NONE', ( #225713 ), #9259, .F. ) ;
#238773=ORIENTED_EDGE ( 'NONE', *, *, #141766, .F. ) ;
#238790=FACE_OUTER_BOUND ( 'NONE', #75233, .T. ) ;
#238820=FACE_OUTER_BOUND ( 'NONE', #46579, .T. ) ;
#238823=AXIS2_PLACEMENT_3D ( 'NONE', #199848, #103266, #182857 ) ;
#238828=CARTESIAN_POINT ( 'NONE',  ( 18.59999999999999787, 78.48087866980282001, -232.8271061603568910 ) ) ;
#238886=CARTESIAN_POINT ( 'NONE',  ( -23.15000000000000213, 54.34471204062663219, -239.4366250215122420 ) ) ;
#238888=ORIENTED_EDGE ( 'NONE', *, *, #106782, .T. ) ;
#238905=DIRECTION ( 'NONE',  ( 0.000000000000000000, 0.9126074666063751506, 0.4088369013363318816 ) ) ;
#238909=CARTESIAN_POINT ( 'NONE',  ( 23.15000000000000213, 69.56804783242856161, -248.4091712263733882 ) ) ;
#238986=VECTOR ( 'NONE', #61641, 1000.000000000000114 ) ;
#238998=CARTESIAN_POINT ( 'NONE',  ( 20.94999999999999574, 40.74071615341952679, -237.9411309446948337 ) ) ;
#239024=ORIENTED_EDGE ( 'NONE', *, *, #119685, .F. ) ;
#239064=ORIENTED_EDGE ( 'NONE', *, *, #67467, .F. ) ;
#239066=ORIENTED_EDGE ( 'NONE', *, *, #244459, .T. ) ;
#239068=AXIS2_PLACEMENT_3D ( 'NONE', #103459, #83871, #163460 ) ;
#239075=EDGE_CURVE ( 'NONE', #58126, #7171, #190641, .T. ) ;
#239098=CARTESIAN_POINT ( 'NONE',  ( 21.05000000000000071, 65.40605961984560679, -236.6728003091511425 ) ) ;
#239113=TOROIDAL_SURFACE ( 'NONE', #47546, 0.2000000000000000111, 0.1000000000000000056 ) ;
#239133=DIRECTION ( 'NONE',  ( -1.000000000000000000, 0.000000000000000000, 0.000000000000000000 ) ) ;
#239158=AXIS2_PLACEMENT_3D ( 'NONE', #35482, #173729, #57556 ) ;
#239168=FACE_OUTER_BOUND ( 'NONE', #117672, .T. ) ;
#239204=CARTESIAN_POINT ( 'NONE',  ( 18.47149038651510367, 77.27495776109610404, -241.9532892334652274 ) ) ;
#239220=TOROIDAL_SURFACE ( 'NONE', #218350, 0.6000000000000013101, 0.1000000000000000056 ) ;
#239227=EDGE_CURVE ( 'NONE', #176943, #212760, #173218, .T. ) ;
#239278=ADVANCED_FACE ( 'NONE', ( #53218 ), #114472, .T. ) ;
#239281=VECTOR ( 'NONE', #147278, 1000.000000000000000 ) ;
#239294=LINE ( 'NONE', #60631, #135205 ) ;
#239296=AXIS2_PLACEMENT_3D ( 'NONE', #4642, #248415, #208021 ) ;
#239342=AXIS2_PLACEMENT_3D ( 'NONE', #241366, #80973, #178847 ) ;
#239361=CARTESIAN_POINT ( 'NONE',  ( 20.94999027547553894, 68.00519115550238780, -224.2294631537215821 ) ) ;
#239405=DIRECTION ( 'NONE',  ( 0.000000000000000000, -0.9126074666063769270, -0.4088369013363280513 ) ) ;
#239432=EDGE_LOOP ( 'NONE', ( #239785, #150257, #203305, #105789, #97580 ) ) ;
#239436=CARTESIAN_POINT ( 'NONE',  ( -20.05000000000000426, 52.27009174976920747, -232.4217594817395138 ) ) ;
#239470=CIRCLE ( 'NONE', #52189, 3.899999999999993694 ) ;
#239472=ORIENTED_EDGE ( 'NONE', *, *, #20438, .F. ) ;
#239535=VERTEX_POINT ( 'NONE', #249523 ) ;
#239538=DIRECTION ( 'NONE',  ( 0.000000000000000000, 0.4088369013363281068, -0.9126074666063770380 ) ) ;
#239563=CARTESIAN_POINT ( 'NONE',  ( 20.94999999999999929, 69.09936979046463534, -247.6075824278584889 ) ) ;
#239564=LINE ( 'NONE', #2211, #168243 ) ;
#239576=CARTESIAN_POINT ( 'NONE',  ( 21.04999999999999716, 56.18374508921710486, -227.9290876000915489 ) ) ;
#239581=ADVANCED_FACE ( 'NONE', ( #117695 ), #103289, .F. ) ;
#239597=ORIENTED_EDGE ( 'NONE', *, *, #86128, .F. ) ;
#239622=DIRECTION ( 'NONE',  ( 1.000000000000000000, 0.000000000000000000, 0.000000000000000000 ) ) ;
#239658=CARTESIAN_POINT ( 'NONE',  ( 22.39999999999999503, 31.76383008438224564, -238.8689086587541510 ) ) ;
#239689=CARTESIAN_POINT ( 'NONE',  ( -21.05000000000000071, 35.94660524813657076, -234.4748257877825495 ) ) ;
#239708=CARTESIAN_POINT ( 'NONE',  ( -20.94999999999999929, 44.15969672213208952, -258.9565289832007693 ) ) ;
#239746=DIRECTION ( 'NONE',  ( 0.000000000000000000, -0.4088369013363783999, 0.9126074666063545004 ) ) ;
#239760=CYLINDRICAL_SURFACE ( 'NONE', #134609, 0.09999999999999854838 ) ;
#239780=VECTOR ( 'NONE', #2011, 1000.000000000000000 ) ;
#239785=ORIENTED_EDGE ( 'NONE', *, *, #239817, .T. ) ;
#239804=VERTEX_POINT ( 'NONE', #1590 ) ;
#239817=EDGE_CURVE ( 'NONE', #60065, #217929, #103468, .T. ) ;
#239856=DIRECTION ( 'NONE',  ( 0.000000000000000000, 0.9126074666063660468, 0.4088369013363524762 ) ) ;
#239867=EDGE_CURVE ( 'NONE', #241241, #244854, #73989, .T. ) ;
#239876=CARTESIAN_POINT ( 'NONE',  ( -23.15000000000000213, 67.23127455305835554, -235.8551265064784559 ) ) ;
#239881=DIRECTION ( 'NONE',  ( 0.000000000000000000, 0.9126074666063769270, 0.4088369013363280513 ) ) ;
#239896=DIRECTION ( 'NONE',  ( 0.000000000000000000, -0.4088369013363276072, 0.9126074666063772600 ) ) ;
#239902=ORIENTED_EDGE ( 'NONE', *, *, #68328, .T. ) ;
#239912=EDGE_CURVE ( 'NONE', #206465, #7959, #3525, .T. ) ;
#239935=LINE ( 'NONE', #19602, #90724 ) ;
#239940=CARTESIAN_POINT ( 'NONE',  ( -23.25000000000000000, 47.66483718802935954, -241.7716698398223514 ) ) ;
#239945=SPHERICAL_SURFACE ( 'NONE', #185091, 0.1000000000000000056 ) ;
#239981=CIRCLE ( 'NONE', #156622, 11.80000000000000071 ) ;
#239985=DIRECTION ( 'NONE',  ( -1.000000000000000000, 1.335000415235278971E-16, -2.979993593738921214E-16 ) ) ;
#239996=AXIS2_PLACEMENT_3D ( 'NONE', #148146, #50310, #126006 ) ;
#240026=AXIS2_PLACEMENT_3D ( 'NONE', #123, #139624, #177536 ) ;
#240038=CIRCLE ( 'NONE', #10909, 7.791421356237341556 ) ;
#240068=EDGE_CURVE ( 'NONE', #221119, #67538, #216589, .T. ) ;
#240093=CIRCLE ( 'NONE', #40201, 11.79999999999999893 ) ;
#240094=ORIENTED_EDGE ( 'NONE', *, *, #233302, .F. ) ;
#240099=DIRECTION ( 'NONE',  ( -1.000000000000000000, 1.207181226542539700E-16, -2.694675058168174199E-16 ) ) ;
#240136=ORIENTED_EDGE ( 'NONE', *, *, #25859, .T. ) ;
#240141=CARTESIAN_POINT ( 'NONE',  ( -20.94999999999999929, 56.28322105926037722, -227.9393116591656963 ) ) ;
#240209=CARTESIAN_POINT ( 'NONE',  ( -23.25000000000000000, 69.25640205380744874, -247.7135141964517402 ) ) ;
#240214=ORIENTED_EDGE ( 'NONE', *, *, #107499, .F. ) ;
#240225=LINE ( 'NONE', #143664, #64530 ) ;
#240304=CIRCLE ( 'NONE', #82040, 7.900000000000009237 ) ;
#240307=AXIS2_PLACEMENT_3D ( 'NONE', #141273, #138666, #39640 ) ;
#240330=CARTESIAN_POINT ( 'NONE',  ( -20.85000000000000142, 56.23643450586806836, -227.9054833905874489 ) ) ;
#240338=ORIENTED_EDGE ( 'NONE', *, *, #113195, .T. ) ;
#240359=CIRCLE ( 'NONE', #186177, 4.050000000000022915 ) ;
#240389=AXIS2_PLACEMENT_3D ( 'NONE', #153514, #109181, #72665 ) ;
#240420=DIRECTION ( 'NONE',  ( 0.000000000000000000, 0.9126074666063660468, 0.4088369013363524762 ) ) ;
#240442=DIRECTION ( 'NONE',  ( -0.000000000000000000, 0.4088369013363281623, -0.9126074666063771490 ) ) ;
#240478=AXIS2_PLACEMENT_3D ( 'NONE', #10129, #251286, #149658 ) ;
#240512=DIRECTION ( 'NONE',  ( 1.000000000000000000, 0.000000000000000000, -0.000000000000000000 ) ) ;
#240532=CARTESIAN_POINT ( 'NONE',  ( 21.05000000000000071, 56.16603649944111254, -228.1013850343386480 ) ) ;
#240555=CARTESIAN_POINT ( 'NONE',  ( -21.05000000000000071, 46.45388641681647357, -243.1520440498138385 ) ) ;
#240572=CARTESIAN_POINT ( 'NONE',  ( 18.59999999999999432, 46.55954744353147134, -243.3218549665227783 ) ) ;
#240584=ORIENTED_EDGE ( 'NONE', *, *, #249062, .T. ) ;
#240597=SURFACE_STYLE_FILL_AREA ( #257528 ) ;
#240621=ORIENTED_EDGE ( 'NONE', *, *, #70303, .F. ) ;
#240682=EDGE_CURVE ( 'NONE', #9026, #91403, #111490, .T. ) ;
#240687=ORIENTED_EDGE ( 'NONE', *, *, #21113, .F. ) ;
#240728=CARTESIAN_POINT ( 'NONE',  ( -21.52071067811865746, 52.87137254617348958, -233.7639410278083005 ) ) ;
#240764=CARTESIAN_POINT ( 'NONE',  ( -20.54999999999999716, 48.50000630096246823, -244.2465039064066161 ) ) ;
#240774=ORIENTED_EDGE ( 'NONE', *, *, #136034, .F. ) ;
#240798=AXIS2_PLACEMENT_3D ( 'NONE', #188514, #89404, #168995 ) ;
#240808=DIRECTION ( 'NONE',  ( -1.000000000000000000, -0.000000000000000000, -0.000000000000000000 ) ) ;
#240860=CARTESIAN_POINT ( 'NONE',  ( 21.05315837706675453, 56.18370558019869776, -227.9291052909716200 ) ) ;
#240870=EDGE_CURVE ( 'NONE', #192641, #53900, #65691, .T. ) ;
#240887=DIRECTION ( 'NONE',  ( 0.000000000000000000, -0.9126074666063770380, -0.4088369013363281068 ) ) ;
#240907=VECTOR ( 'NONE', #228895, 1000.000000000000000 ) ;
#240908=AXIS2_PLACEMENT_3D ( 'NONE', #102154, #143872, #146432 ) ;
#240924=DIRECTION ( 'NONE',  ( 1.000000000000000000, 0.000000000000000000, 0.000000000000000000 ) ) ;
#240934=DIRECTION ( 'NONE',  ( 1.000000000000000000, 0.000000000000000000, 0.000000000000000000 ) ) ;
#240937=VERTEX_POINT ( 'NONE', #217124 ) ;
#240938=CARTESIAN_POINT ( 'NONE',  ( 18.47073956224761204, 47.01875662081600638, -255.2888406289864918 ) ) ;
#240953=DIRECTION ( 'NONE',  ( 0.000000000000000000, -0.9126074666063769270, -0.4088369013363280513 ) ) ;
#241025=DIRECTION ( 'NONE',  ( 0.000000000000000000, -0.6324589521315897578, 0.7745938767306462802 ) ) ;
#241027=VERTEX_POINT ( 'NONE', #7087 ) ;
#241061=DIRECTION ( 'NONE',  ( 0.000000000000000000, -0.4088369013363205573, 0.9126074666063803686 ) ) ;
#241066=CARTESIAN_POINT ( 'NONE',  ( -20.85882249326303040, 68.11287320386161070, -224.1382462126928488 ) ) ;
#241098=ORIENTED_EDGE ( 'NONE', *, *, #226791, .F. ) ;
#241126=VECTOR ( 'NONE', #35819, 1000.000000000000000 ) ;
#241129=DIRECTION ( 'NONE',  ( 0.000000000000000000, 0.2818822000685679008, -0.9594490217226259166 ) ) ;
#241134=DIRECTION ( 'NONE',  ( 1.000000000000000000, -0.000000000000000000, -0.000000000000000000 ) ) ;
#241148=CARTESIAN_POINT ( 'NONE',  ( 21.05000000000000071, 53.86595165227826243, -236.3638196928718855 ) ) ;
#241149=DIRECTION ( 'NONE',  ( 0.000000000000000000, 0.4088369013363281623, -0.9126074666063771490 ) ) ;
#241192=VERTEX_POINT ( 'NONE', #233856 ) ;
#241211=FACE_OUTER_BOUND ( 'NONE', #86022, .T. ) ;
#241241=VERTEX_POINT ( 'NONE', #96867 ) ;
#241283=LINE ( 'NONE', #104297, #23035 ) ;
#241287=EDGE_LOOP ( 'NONE', ( #121518, #91824, #204186 ) ) ;
#241306=VERTEX_POINT ( 'NONE', #185111 ) ;
#241307=ORIENTED_EDGE ( 'NONE', *, *, #174319, .F. ) ;
#241366=CARTESIAN_POINT ( 'NONE',  ( -20.00857864376270001, 44.18876898710608003, -236.1516686502934590 ) ) ;
#241398=VERTEX_POINT ( 'NONE', #148561 ) ;
#241404=AXIS2_PLACEMENT_3D ( 'NONE', #253228, #99282, #57591 ) ;
#241488=AXIS2_PLACEMENT_3D ( 'NONE', #138798, #240512, #202664 ) ;
#241508=CARTESIAN_POINT ( 'NONE',  ( 18.59999999999999076, 46.59314322379660922, -243.1831726892433210 ) ) ;
#241510=EDGE_LOOP ( 'NONE', ( #149954, #192015, #244174, #124784 ) ) ;
#241535=DIRECTION ( 'NONE',  ( 1.000000000000000000, 0.000000000000000000, 0.000000000000000000 ) ) ;
#241536=DIRECTION ( 'NONE',  ( 0.000000000000000000, 0.4088369013363306603, -0.9126074666063758167 ) ) ;
#241542=DIRECTION ( 'NONE',  ( 0.000000000000000000, 0.9126074666063660468, 0.4088369013363524762 ) ) ;
#241545=ORIENTED_EDGE ( 'NONE', *, *, #37480, .F. ) ;
#241547=DIRECTION ( 'NONE',  ( 1.000000000000000000, 0.000000000000000000, -0.000000000000000000 ) ) ;
#241556=CARTESIAN_POINT ( 'NONE',  ( 20.94999999999999574, 46.45388641681647357, -243.1520440498138385 ) ) ;
#241604=TOROIDAL_SURFACE ( 'NONE', #212406, 12.97499999999999609, 0.1000000000000000056 ) ;
#241614=DIRECTION ( 'NONE',  ( -1.000000000000000000, -0.000000000000000000, 0.000000000000000000 ) ) ;
#241625=ORIENTED_EDGE ( 'NONE', *, *, #194967, .T. ) ;
#241657=CARTESIAN_POINT ( 'NONE',  ( 21.05000000000000071, 34.10192277420338058, -243.5988165382224508 ) ) ;
#241682=ORIENTED_EDGE ( 'NONE', *, *, #230704, .F. ) ;
#241687=CARTESIAN_POINT ( 'NONE',  ( 21.05000000000000071, 40.84268664891381917, -237.9560832633917187 ) ) ;
#241733=ORIENTED_EDGE ( 'NONE', *, *, #37667, .T. ) ;
#241747=AXIS2_PLACEMENT_3D ( 'NONE', #251334, #175679, #173148 ) ;
#241764=CIRCLE ( 'NONE', #237687, 0.09999999999999939493 ) ;
#241768=CARTESIAN_POINT ( 'NONE',  ( -22.50000000000000000, 36.65892442174472876, -249.5511627012454596 ) ) ;
#241775=ADVANCED_FACE ( 'NONE', ( #32035 ), #114099, .T. ) ;
#241792=CARTESIAN_POINT ( 'NONE',  ( 20.94999999999999929, 62.08148826970417389, -247.6553521922769221 ) ) ;
#241813=ORIENTED_EDGE ( 'NONE', *, *, #175453, .F. ) ;
#241861=CARTESIAN_POINT ( 'NONE',  ( -20.54999999999999716, 47.91013932883114990, -242.3192343197862044 ) ) ;
#241876=( NAMED_UNIT ( * ) SI_UNIT ( $, .STERADIAN. ) SOLID_ANGLE_UNIT ( ) );
#241889=SPHERICAL_SURFACE ( 'NONE', #163771, 0.1000000000000000056 ) ;
#241938=VECTOR ( 'NONE', #131862, 1000.000000000000000 ) ;
#241957=DIRECTION ( 'NONE',  ( 0.000000000000000000, -0.9126074666063770380, -0.4088369013363281068 ) ) ;
#241970=EDGE_LOOP ( 'NONE', ( #141558, #179903, #77056, #99241 ) ) ;
#241978=VERTEX_POINT ( 'NONE', #77253 ) ;
#241985=VERTEX_POINT ( 'NONE', #116406 ) ;
#242001=DIRECTION ( 'NONE',  ( -1.000000000000000000, -0.000000000000000000, -0.000000000000000000 ) ) ;
#242006=CARTESIAN_POINT ( 'NONE',  ( -20.85000000000000142, 67.75954444190071513, -227.8703747234148693 ) ) ;
#242018=ORIENTED_EDGE ( 'NONE', *, *, #71953, .T. ) ;
#242033=DIRECTION ( 'NONE',  ( -3.265361837132813586E-16, -0.4088369013363280513, 0.9126074666063769270 ) ) ;
#242040=ORIENTED_EDGE ( 'NONE', *, *, #239075, .T. ) ;
#242114=AXIS2_PLACEMENT_3D ( 'NONE', #13650, #112752, #237832 ) ;
#242117=CARTESIAN_POINT ( 'NONE',  ( -20.85000000000000142, 56.18374508921710486, -227.9290876000915489 ) ) ;
#242142=AXIS2_PLACEMENT_3D ( 'NONE', #49054, #9936, #245986 ) ;
#242147=DIRECTION ( 'NONE',  ( 1.000000000000000000, 0.000000000000000000, 0.000000000000000000 ) ) ;
#242164=CYLINDRICAL_SURFACE ( 'NONE', #18875, 0.1000000000000024342 ) ;
#242170=DIRECTION ( 'NONE',  ( -0.000000000000000000, 0.9126074666063771490, 0.4088369013363281623 ) ) ;
#242217=CIRCLE ( 'NONE', #33994, 0.09999999999999939493 ) ;
#242309=EDGE_CURVE ( 'NONE', #144623, #219396, #257909, .T. ) ;
#242320=VERTEX_POINT ( 'NONE', #114806 ) ;
#242347=ORIENTED_EDGE ( 'NONE', *, *, #115513, .F. ) ;
#242356=DIRECTION ( 'NONE',  ( 0.000000000000000000, 0.9126074666063545004, 0.4088369013363783999 ) ) ;
#242382=CARTESIAN_POINT ( 'NONE',  ( -22.50000000000000000, 26.02743912001966464, -254.3139371321002216 ) ) ;
#242422=CARTESIAN_POINT ( 'NONE',  ( -20.94999999999999929, 47.92640890138473253, -246.4059919526569900 ) ) ;
#242427=CARTESIAN_POINT ( 'NONE',  ( 20.12500000000000000, 40.07562767317620711, -237.3368484665046765 ) ) ;
#242431=VERTEX_POINT ( 'NONE', #99060 ) ;
#242437=CARTESIAN_POINT ( 'NONE',  ( -23.25000000000000000, 67.85909929089923764, -227.8797997985275856 ) ) ;
#242440=CARTESIAN_POINT ( 'NONE',  ( -21.05000000000000071, 69.09936979046463534, -247.6075824278584889 ) ) ;
#242492=CIRCLE ( 'NONE', #125962, 0.09999999999999939493 ) ;
#242503=DIRECTION ( 'NONE',  ( 0.000000000000000000, 0.9126074666063769270, 0.4088369013363283844 ) ) ;
#242509=CARTESIAN_POINT ( 'NONE',  ( -21.08884785362073089, 30.83694912164556357, -252.1047855145109224 ) ) ;
#242530=ORIENTED_EDGE ( 'NONE', *, *, #252434, .T. ) ;
#242633=DIRECTION ( 'NONE',  ( 0.000000000000000000, -0.9126074666063770380, -0.4088369013363281068 ) ) ;
#242640=ORIENTED_EDGE ( 'NONE', *, *, #100367, .T. ) ;
#242675=CIRCLE ( 'NONE', #196879, 0.1000000000000024342 ) ;
#242713=CARTESIAN_POINT ( 'NONE',  ( 21.07928932188134397, 36.65892442174472876, -249.5511627012454596 ) ) ;
#242782=ADVANCED_FACE ( 'NONE', ( #132795 ), #162490, .T. ) ;
#242784=DIRECTION ( 'NONE',  ( -0.7071067811865475727, 0.2890913453342130457, -0.6453109281988448354 ) ) ;
#242795=ORIENTED_EDGE ( 'NONE', *, *, #64697, .T. ) ;
#242797=AXIS2_PLACEMENT_3D ( 'NONE', #149803, #126360, #127651 ) ;
#242818=CARTESIAN_POINT ( 'NONE',  ( 18.49999999999998934, 43.16354019706792400, -239.5695141926698284 ) ) ;
#242821=VERTEX_POINT ( 'NONE', #36265 ) ;
#242823=CARTESIAN_POINT ( 'NONE',  ( -20.85000000000000142, 72.03510814376021187, -246.5782642391033903 ) ) ;
#242834=DIRECTION ( 'NONE',  ( -1.000000000000000000, 0.000000000000000000, 0.000000000000000000 ) ) ;
#242852=CARTESIAN_POINT ( 'NONE',  ( -21.44999999999999929, 44.91518204311810081, -238.0177672736398620 ) ) ;
#242885=CIRCLE ( 'NONE', #188909, 0.1000000000000024342 ) ;
#242923=EDGE_LOOP ( 'NONE', ( #16836, #126968, #39134, #53440 ) ) ;
#242946=ADVANCED_FACE ( 'NONE', ( #81741 ), #64777, .T. ) ;
#242956=SPHERICAL_SURFACE ( 'NONE', #59014, 0.1000000000000000056 ) ;
#242981=ORIENTED_EDGE ( 'NONE', *, *, #224798, .F. ) ;
#242991=AXIS2_PLACEMENT_3D ( 'NONE', #47115, #87533, #186671 ) ;
#243006=CYLINDRICAL_SURFACE ( 'NONE', #221437, 0.1000000000000024342 ) ;
#243037=AXIS2_PLACEMENT_3D ( 'NONE', #90896, #89603, #229134 ) ;
#243114=CARTESIAN_POINT ( 'NONE',  ( -20.54999999999999716, 46.15118611352045974, -240.5321844900040844 ) ) ;
#243142=CIRCLE ( 'NONE', #55670, 0.09999999999999741040 ) ;
#243180=CARTESIAN_POINT ( 'NONE',  ( 20.94999999999999929, 40.68212387350988735, -238.0221676322813096 ) ) ;
#243181=ORIENTED_EDGE ( 'NONE', *, *, #44341, .T. ) ;
#243197=ORIENTED_EDGE ( 'NONE', *, *, #252434, .F. ) ;
#243207=SPHERICAL_SURFACE ( 'NONE', #54744, 0.1000000000000000056 ) ;
#243218=ORIENTED_EDGE ( 'NONE', *, *, #249071, .F. ) ;
#243257=ORIENTED_EDGE ( 'NONE', *, *, #108035, .T. ) ;
#243271=DIRECTION ( 'NONE',  ( 0.000000000000000000, -0.9126074666063770380, -0.4088369013363281068 ) ) ;
#243275=CARTESIAN_POINT ( 'NONE',  ( -20.54999999999999716, 67.23127455305835554, -235.8551265064784559 ) ) ;
#243327=CARTESIAN_POINT ( 'NONE',  ( -21.14999999999999858, 38.04609728753136011, -236.0545303518866547 ) ) ;
#243345=AXIS2_PLACEMENT_3D ( 'NONE', #250202, #187684, #9024 ) ;
#243364=VECTOR ( 'NONE', #237354, 1000.000000000000000 ) ;
#243384=DIRECTION ( 'NONE',  ( 0.000000000000000000, 0.9126074666063844765, 0.4088369013363113980 ) ) ;
#243424=CARTESIAN_POINT ( 'NONE',  ( 22.49533356619865643, 31.83654316555196928, -238.9459102234743284 ) ) ;
#243461=DIRECTION ( 'NONE',  ( 0.000000000000000000, -0.4088369013363283289, 0.9126074666063768159 ) ) ;
#243476=EDGE_CURVE ( 'NONE', #93920, #20493, #117057, .T. ) ;
#243483=CARTESIAN_POINT ( 'NONE',  ( -22.00411653889226571, 29.99888786984131173, -252.4262548924342013 ) ) ;
#243498=DIRECTION ( 'NONE',  ( -1.000000000000000000, -0.000000000000000000, -0.000000000000000000 ) ) ;
#243506=CARTESIAN_POINT ( 'NONE',  ( -20.64999999999999858, 53.08776555244186568, -234.2469744149522626 ) ) ;
#243515=ORIENTED_EDGE ( 'NONE', *, *, #209631, .F. ) ;
#243517=AXIS2_PLACEMENT_3D ( 'NONE', #66158, #46574, #27063 ) ;
#243523=CARTESIAN_POINT ( 'NONE',  ( -23.15000000000000213, 67.23127455305835554, -235.8551265064784559 ) ) ;
#243524=VECTOR ( 'NONE', #35428, 1000.000000000000114 ) ;
#243529=ORIENTED_EDGE ( 'NONE', *, *, #26385, .T. ) ;
#243555=ORIENTED_EDGE ( 'NONE', *, *, #8537, .T. ) ;
#243632=CARTESIAN_POINT ( 'NONE',  ( 18.33996824403515191, 77.36682667616904041, -241.8005656296788572 ) ) ;
#243665=CARTESIAN_POINT ( 'NONE',  ( 18.50000000000000000, 77.31518212004206703, -241.6587219750726092 ) ) ;
#243675=EDGE_CURVE ( 'NONE', #97342, #1847, #125602, .T. ) ;
#243709=ORIENTED_EDGE ( 'NONE', *, *, #25985, .F. ) ;
#243727=FACE_OUTER_BOUND ( 'NONE', #164443, .T. ) ;
#243749=DIRECTION ( 'NONE',  ( 1.000000000000000000, 0.000000000000000000, 0.000000000000000000 ) ) ;
#243774=CARTESIAN_POINT ( 'NONE',  ( -22.47071067811865319, 29.57301391503006016, -252.6169816238249552 ) ) ;
#243814=VERTEX_POINT ( 'NONE', #35037 ) ;
#243817=FACE_OUTER_BOUND ( 'NONE', #72980, .T. ) ;
#243827=CARTESIAN_POINT ( 'NONE',  ( -20.85000000000000142, 74.93036000061670165, -233.6816308724374949 ) ) ;
#243903=VERTEX_POINT ( 'NONE', #173278 ) ;
#243915=CARTESIAN_POINT ( 'NONE',  ( -21.14999999999999858, 26.06832281015329755, -254.4051978787608732 ) ) ;
#243964=DIRECTION ( 'NONE',  ( -1.000000000000000000, 0.000000000000000000, 0.000000000000000000 ) ) ;
#243966=CARTESIAN_POINT ( 'NONE',  ( -18.59999999999999787, 51.33926024308902925, -230.0993571250899379 ) ) ;
#243972=ORIENTED_EDGE ( 'NONE', *, *, #1108, .T. ) ;
#244012=AXIS2_PLACEMENT_3D ( 'NONE', #191644, #189042, #10413 ) ;
#244026=DIRECTION ( 'NONE',  ( -0.000000000000000000, 0.4088369013363281623, -0.9126074666063771490 ) ) ;
#244041=AXIS2_PLACEMENT_3D ( 'NONE', #232661, #73597, #34472 ) ;
#244122=DIRECTION ( 'NONE',  ( -0.000000000000000000, 0.9126074666063771490, 0.4088369013363281623 ) ) ;
#244125=AXIS2_PLACEMENT_3D ( 'NONE', #148001, #244516, #8497 ) ;
#244174=ORIENTED_EDGE ( 'NONE', *, *, #201994, .F. ) ;
#244182=CARTESIAN_POINT ( 'NONE',  ( 22.50497660315936344, 25.96815610755211523, -254.4267512576819286 ) ) ;
#244188=EDGE_LOOP ( 'NONE', ( #118004, #53423, #60288, #204064, #182268 ) ) ;
#244197=CARTESIAN_POINT ( 'NONE',  ( -18.59999999999999787, 44.01574086017817677, -236.0100308471058099 ) ) ;
#244208=CARTESIAN_POINT ( 'NONE',  ( 23.14999999999999858, 45.93587830916155212, -239.9163948487882863 ) ) ;
#244215=ORIENTED_EDGE ( 'NONE', *, *, #114081, .F. ) ;
#244224=FACE_OUTER_BOUND ( 'NONE', #19698, .T. ) ;
#244234=EDGE_CURVE ( 'NONE', #188456, #253877, #67523, .T. ) ;
#244236=DIRECTION ( 'NONE',  ( 0.000000000000000000, -0.9126074666063770380, -0.4088369013363281068 ) ) ;
#244251=DIRECTION ( 'NONE',  ( -1.000000000000000000, 1.207181226542539700E-16, -2.694675058168174199E-16 ) ) ;
#244254=DIRECTION ( 'NONE',  ( -7.304098846218443309E-16, -0.4088369013363783999, 0.9126074666063545004 ) ) ;
#244269=EDGE_CURVE ( 'NONE', #26849, #55598, #242492, .T. ) ;
#244287=CARTESIAN_POINT ( 'NONE',  ( 21.04999999999999716, 44.12019864330184049, -236.4877982702160182 ) ) ;
#244292=LINE ( 'NONE', #47368, #107394 ) ;
#244315=CARTESIAN_POINT ( 'NONE',  ( -18.59999999999999787, 51.38014393322265505, -230.1906178717505611 ) ) ;
#244324=CARTESIAN_POINT ( 'NONE',  ( 21.05000000000000071, 70.88170441948386724, -234.2197789011331679 ) ) ;
#244338=DIRECTION ( 'NONE',  ( 0.000000000000000000, -0.5859227990963362664, -0.8103668758649469339 ) ) ;
#244343=AXIS2_PLACEMENT_3D ( 'NONE', #136190, #32020, #114084 ) ;
#244350=DIRECTION ( 'NONE',  ( 0.000000000000000000, -0.9126074666063770380, -0.4088369013363281068 ) ) ;
#244357=DIRECTION ( 'NONE',  ( 1.000000000000000000, 0.000000000000000000, 0.000000000000000000 ) ) ;
#244369=ORIENTED_EDGE ( 'NONE', *, *, #27133, .T. ) ;
#244389=( BOUNDED_SURFACE ( )  B_SPLINE_SURFACE ( 3, 2, ( 
 ( #45966, #121679, #240330 ),
 ( #223306, #43404, #125505 ),
 ( #201189, #22568, #162088 ),
 ( #205017, #23870, #103356 ),
 ( #4258, #83767, #163361 ),
 ( #6843, #64252, #143775 ) ),
 .UNSPECIFIED., .F., .F., .F. ) 
 B_SPLINE_SURFACE_WITH_KNOTS ( ( 4, 2, 4 ),
 ( 3, 3 ),
 ( 1.570796326794897668, 2.356194490192346169, 3.141592653589794448 ),
 ( 0.000000000000000000, 1.000000000000000000 ),
 .UNSPECIFIED. ) 
 GEOMETRIC_REPRESENTATION_ITEM ( )  RATIONAL_B_SPLINE_SURFACE ( (
 ( 1.000000000000000000, 0.7071067811864701902, 1.000000000000000000),
 ( 1.000000000000000000, 0.6611148371806441215, 1.000000000000000000),
 ( 1.000000000000000000, 0.6092287576661893356, 1.000000000000000000),
 ( 1.000000000000000000, 0.5278258667090959255, 1.000000000000000000),
 ( 1.000000000000000000, 0.4993418825306182307, 1.000000000000000000),
 ( 1.000000000000000000, 0.5000000000001614264, 1.000000000000000000) ) ) 
 REPRESENTATION_ITEM ( '' )  SURFACE ( )  );
#244420=DIRECTION ( 'NONE',  ( 0.000000000000000000, -0.9126074666063774821, -0.4088369013363273297 ) ) ;
#244428=ORIENTED_EDGE ( 'NONE', *, *, #12273, .F. ) ;
#244442=ORIENTED_EDGE ( 'NONE', *, *, #173080, .F. ) ;
#244443=CARTESIAN_POINT ( 'NONE',  ( 20.94999999999999929, 69.28189128378591022, -247.5258150475912089 ) ) ;
#244455=CIRCLE ( 'NONE', #132043, 0.09999999999999108213 ) ;
#244456=EDGE_CURVE ( 'NONE', #125186, #129332, #17674, .T. ) ;
#244459=EDGE_CURVE ( 'NONE', #239804, #7829, #158511, .T. ) ;
#244516=DIRECTION ( 'NONE',  ( 1.000000000000000000, 0.000000000000000000, 0.000000000000000000 ) ) ;
#244520=DIRECTION ( 'NONE',  ( -1.000000000000000000, -0.000000000000000000, -0.000000000000000000 ) ) ;
#244539=CARTESIAN_POINT ( 'NONE',  ( 21.05000000000000071, 55.49311008795314137, -234.6486875357297492 ) ) ;
#244545=CARTESIAN_POINT ( 'NONE',  ( -23.15000000000000213, 49.36776662947724503, -253.7196102226803021 ) ) ;
#244562=CARTESIAN_POINT ( 'NONE',  ( 21.14999999999999503, 30.73962027982165424, -265.0781340245722504 ) ) ;
#244576=ORIENTED_EDGE ( 'NONE', *, *, #176541, .T. ) ;
#244581=EDGE_CURVE ( 'NONE', #4597, #241985, #175881, .T. ) ;
#244596=FACE_OUTER_BOUND ( 'NONE', #68802, .T. ) ;
#244611=ORIENTED_EDGE ( 'NONE', *, *, #128876, .F. ) ;
#244635=ORIENTED_EDGE ( 'NONE', *, *, #149185, .F. ) ;
#244637=CARTESIAN_POINT ( 'NONE',  ( -21.07928932188134041, 33.98134083355181190, -243.8161431329798461 ) ) ;
#244651=EDGE_CURVE ( 'NONE', #30904, #114526, #238395, .T. ) ;
#244654=CIRCLE ( 'NONE', #240389, 0.1000000000000024342 ) ;
#244722=EDGE_LOOP ( 'NONE', ( #63559, #57869, #125493, #70315 ) ) ;
#244733=DIRECTION ( 'NONE',  ( 0.000000000000000000, 0.9126074666063660468, 0.4088369013363524762 ) ) ;
#244735=ORIENTED_EDGE ( 'NONE', *, *, #17752, .T. ) ;
#244747=FACE_OUTER_BOUND ( 'NONE', #103631, .T. ) ;
#244757=CARTESIAN_POINT ( 'NONE',  ( -21.07094088545368038, 30.85066122990915716, -252.0448291528320510 ) ) ;
#244789=AXIS2_PLACEMENT_3D ( 'NONE', #184890, #88327, #24561 ) ;
#244804=CIRCLE ( 'NONE', #236435, 0.1000000000000024342 ) ;
#244817=ORIENTED_EDGE ( 'NONE', *, *, #85404, .T. ) ;
#244835=CARTESIAN_POINT ( 'NONE',  ( -23.25000000000000000, 46.00954831033281778, -240.7052126169319877 ) ) ;
#244838=VERTEX_POINT ( 'NONE', #14846 ) ;
#244854=VERTEX_POINT ( 'NONE', #56488 ) ;
#244902=AXIS2_PLACEMENT_3D ( 'NONE', #130358, #173404, #131654 ) ;
#244905=EDGE_CURVE ( 'NONE', #65749, #39261, #51575, .T. ) ;
#244908=DIRECTION ( 'NONE',  ( 0.000000000000000000, 0.9126074666063613838, 0.4088369013363628013 ) ) ;
#244917=ORIENTED_EDGE ( 'NONE', *, *, #217732, .T. ) ;
#244940=CARTESIAN_POINT ( 'NONE',  ( 23.24999999999999645, 45.69057616835975466, -239.3688303688244616 ) ) ;
#244953=ORIENTED_EDGE ( 'NONE', *, *, #135818, .F. ) ;
#244958=DIRECTION ( 'NONE',  ( 0.000000000000000000, -0.4088369013363783999, 0.9126074666063545004 ) ) ;
#244981=CARTESIAN_POINT ( 'NONE',  ( -23.25000000000000000, 78.48087866980282001, -232.8271061603568910 ) ) ;
#244986=CIRCLE ( 'NONE', #120130, 0.1000000000000024342 ) ;
#245012=CARTESIAN_POINT ( 'NONE',  ( -18.59999999999999787, 74.93036000061670165, -233.6816308724374949 ) ) ;
#245019=CIRCLE ( 'NONE', #178410, 11.74999999999999822 ) ;
#245023=AXIS2_PLACEMENT_3D ( 'NONE', #59215, #202622, #201340 ) ;
#245051=LINE ( 'NONE', #46828, #218401 ) ;
#245085=CYLINDRICAL_SURFACE ( 'NONE', #100451, 0.09999999999999939493 ) ;
#245106=PLANE ( 'NONE',  #11385 ) ;
#245111=ORIENTED_EDGE ( 'NONE', *, *, #17849, .T. ) ;
#245153=ORIENTED_EDGE ( 'NONE', *, *, #40219, .F. ) ;
#245185=VERTEX_POINT ( 'NONE', #172356 ) ;
#245187=DIRECTION ( 'NONE',  ( 0.000000000000000000, 0.3116596277708317264, 0.9501938099239264357 ) ) ;
#245208=EDGE_CURVE ( 'NONE', #172097, #137324, #17104, .T. ) ;
#245274=CARTESIAN_POINT ( 'NONE',  ( -20.94999999999999929, 67.23127455305835554, -235.8551265064784559 ) ) ;
#245371=AXIS2_PLACEMENT_3D ( 'NONE', #224134, #121238, #142032 ) ;
#245406=AXIS2_PLACEMENT_3D ( 'NONE', #244545, #65924, #46339 ) ;
#245437=EDGE_CURVE ( 'NONE', #65298, #175048, #57013, .T. ) ;
#245440=VERTEX_POINT ( 'NONE', #97419 ) ;
#245441=DIRECTION ( 'NONE',  ( 1.000000000000000000, 0.000000000000000000, 0.000000000000000000 ) ) ;
#245449=AXIS2_PLACEMENT_3D ( 'NONE', #84831, #200964, #5297 ) ;
#245464=ORIENTED_EDGE ( 'NONE', *, *, #78286, .F. ) ;
#245470=ORIENTED_EDGE ( 'NONE', *, *, #13267, .T. ) ;
#245487=DIRECTION ( 'NONE',  ( 0.000000000000000000, 0.5283051335750404975, -0.8490545835446967615 ) ) ;
#245493=ORIENTED_EDGE ( 'NONE', *, *, #126176, .F. ) ;
#245494=EDGE_LOOP ( 'NONE', ( #87514, #204078, #41424, #246444, #183246 ) ) ;
#245516=DIRECTION ( 'NONE',  ( 1.000000000000000000, 0.000000000000000000, 0.000000000000000000 ) ) ;
#245520=FACE_OUTER_BOUND ( 'NONE', #209875, .T. ) ;
#245537=CARTESIAN_POINT ( 'NONE',  ( 23.14999999999999858, 48.40874555430184500, -244.2873875965402704 ) ) ;
#245538=CARTESIAN_POINT ( 'NONE',  ( -23.15000000000000213, 48.91146289617405785, -253.9240286733484595 ) ) ;
#245539=CARTESIAN_POINT ( 'NONE',  ( 20.77766267348356166, 39.31613315723080149, -236.9111090107639939 ) ) ;
#245542=ADVANCED_FACE ( 'NONE', ( #175065 ), #251313, .F. ) ;
#245563=DIRECTION ( 'NONE',  ( 0.000000000000000000, -0.9126074666063770380, -0.4088369013363281068 ) ) ;
#245575=ORIENTED_EDGE ( 'NONE', *, *, #135944, .F. ) ;
#245578=ORIENTED_EDGE ( 'NONE', *, *, #84668, .F. ) ;
#245593=DIRECTION ( 'NONE',  ( 0.000000000000000000, 0.9126074666063660468, 0.4088369013363524762 ) ) ;
#245606=VECTOR ( 'NONE', #227112, 1000.000000000000000 ) ;
#245617=AXIS2_PLACEMENT_3D ( 'NONE', #205539, #28240, #8644 ) ;
#245654=DIRECTION ( 'NONE',  ( -1.000000000000000000, 0.000000000000000000, 0.000000000000000000 ) ) ;
#245668=ORIENTED_EDGE ( 'NONE', *, *, #70900, .F. ) ;
#245679=ORIENTED_EDGE ( 'NONE', *, *, #79135, .T. ) ;
#245692=VERTEX_POINT ( 'NONE', #100574 ) ;
#245740=AXIS2_PLACEMENT_3D ( 'NONE', #29967, #89897, #65206 ) ;
#245741=ORIENTED_EDGE ( 'NONE', *, *, #239912, .F. ) ;
#245742=ADVANCED_FACE ( 'NONE', ( #223115 ), #226357, .T. ) ;
#245757=DIRECTION ( 'NONE',  ( 0.000000000000000000, -0.4088369013363280513, 0.9126074666063771490 ) ) ;
#245792=DIRECTION ( 'NONE',  ( 1.000000000000000000, -7.510212038922875604E-17, 1.676432719286210708E-16 ) ) ;
#245811=EDGE_CURVE ( 'NONE', #171172, #19155, #62112, .T. ) ;
#245843=CARTESIAN_POINT ( 'NONE',  ( -18.59999999999999787, 77.35494420175976416, -241.6200040285045532 ) ) ;
#245848=CYLINDRICAL_SURFACE ( 'NONE', #239296, 12.87499999999999112 ) ;
#245894=CARTESIAN_POINT ( 'NONE',  ( -18.50000000000000000, 48.14768554360777841, -246.4498133360871179 ) ) ;
#245926=VECTOR ( 'NONE', #83452, 1000.000000000000000 ) ;
#245946=CARTESIAN_POINT ( 'NONE',  ( -23.25000000000000000, 25.97741635855165754, -254.4468634167653249 ) ) ;
#245949=DIRECTION ( 'NONE',  ( 0.000000000000000000, 0.9126074666063545004, 0.4088369013363783999 ) ) ;
#245963=CARTESIAN_POINT ( 'NONE',  ( -20.94999999999999929, 46.45388641681647357, -243.1520440498138385 ) ) ;
#245964=FACE_OUTER_BOUND ( 'NONE', #112022, .T. ) ;
#245982=CARTESIAN_POINT ( 'NONE',  ( 20.95512820512820440, 39.31056039967181448, -236.7220595557971023 ) ) ;
#245986=DIRECTION ( 'NONE',  ( 0.000000000000000000, 0.9126074666063660468, 0.4088369013363524762 ) ) ;
#245999=CARTESIAN_POINT ( 'NONE',  ( -21.65000000000000213, 44.68681448124952027, -237.5080042326551393 ) ) ;
#246002=ADVANCED_FACE ( 'NONE', ( #52179 ), #133027, .T. ) ;
#246004=VERTEX_POINT ( 'NONE', #130442 ) ;
#246013=DIRECTION ( 'NONE',  ( 1.000000000000000000, 0.000000000000000000, 0.000000000000000000 ) ) ;
#246016=CARTESIAN_POINT ( 'NONE',  ( 21.07933241753356768, 33.98632151110914634, -243.8137701776410040 ) ) ;
#246071=EDGE_CURVE ( 'NONE', #9664, #1847, #216211, .T. ) ;
#246091=CARTESIAN_POINT ( 'NONE',  ( -18.50000000000000000, 21.13195309841794867, -243.6318585593224100 ) ) ;
#246094=ORIENTED_EDGE ( 'NONE', *, *, #166734, .F. ) ;
#246124=ORIENTED_EDGE ( 'NONE', *, *, #253354, .T. ) ;
#246132=CARTESIAN_POINT ( 'NONE',  ( -22.50485643085239928, 25.96818459189811890, -254.4268134568224298 ) ) ;
#246160=CYLINDRICAL_SURFACE ( 'NONE', #101527, 12.87499999999999112 ) ;
#246170=CIRCLE ( 'NONE', #4719, 0.1000000000000054595 ) ;
#246186=DIRECTION ( 'NONE',  ( 1.000000000000000000, 0.000000000000000000, 0.000000000000000000 ) ) ;
#246198=VERTEX_POINT ( 'NONE', #126278 ) ;
#246211=ORIENTED_EDGE ( 'NONE', *, *, #195427, .T. ) ;
#246215=DIRECTION ( 'NONE',  ( 0.000000000000000000, -0.8103668758649578141, 0.5859227990963212784 ) ) ;
#246234=ORIENTED_EDGE ( 'NONE', *, *, #40261, .F. ) ;
#246262=AXIS2_PLACEMENT_3D ( 'NONE', #40050, #122130, #183387 ) ;
#246272=DIRECTION ( 'NONE',  ( -0.1538461538461613487, -0.4039696218774022629, 0.9017427047373168802 ) ) ;
#246302=DIRECTION ( 'NONE',  ( 0.000000000000000000, -0.9126074666063660468, -0.4088369013363524762 ) ) ;
#246331=DIRECTION ( 'NONE',  ( 0.000000000000000000, 0.4088369013363783999, -0.9126074666063545004 ) ) ;
#246387=CARTESIAN_POINT ( 'NONE',  ( -21.04999999999999716, 34.01597830783489940, -243.6159889436117965 ) ) ;
#246416=AXIS2_PLACEMENT_3D ( 'NONE', #212056, #72548, #68685 ) ;
#246440=ORIENTED_EDGE ( 'NONE', *, *, #235597, .F. ) ;
#246444=ORIENTED_EDGE ( 'NONE', *, *, #97213, .F. ) ;
#246454=ORIENTED_EDGE ( 'NONE', *, *, #190956, .T. ) ;
#246455=VERTEX_POINT ( 'NONE', #238208 ) ;
#246508=CARTESIAN_POINT ( 'NONE',  ( 23.14999999999999503, 53.37395138337728895, -234.8857996415767104 ) ) ;
#246521=CARTESIAN_POINT ( 'NONE',  ( 20.94999999999999574, 43.35747728126469980, -245.1805918474304917 ) ) ;
#246524=ORIENTED_EDGE ( 'NONE', *, *, #62845, .F. ) ;
#246526=DIRECTION ( 'NONE',  ( 0.7071359030027870585, -0.6452843503173838480, -0.2890794387705646895 ) ) ;
#246536=CARTESIAN_POINT ( 'NONE',  ( 22.47007471830799474, 29.61294623328926789, -252.7076741202934613 ) ) ;
#246568=DIRECTION ( 'NONE',  ( 0.000000000000000000, 0.9126074666063660468, 0.4088369013363524762 ) ) ;
#246569=DIRECTION ( 'NONE',  ( -1.000000000000000000, 0.000000000000000000, 0.000000000000000000 ) ) ;
#246570=AXIS2_PLACEMENT_3D ( 'NONE', #54311, #34798, #184218 ) ;
#246571=SPHERICAL_SURFACE ( 'NONE', #97261, 0.1000000000000000056 ) ;
#246581=DIRECTION ( 'NONE',  ( 0.000000000000000000, 0.9126074666063660468, 0.4088369013363524762 ) ) ;
#246584=DIRECTION ( 'NONE',  ( 0.000000000000000000, -0.9126074666063770380, -0.4088369013363281068 ) ) ;
#246588=TOROIDAL_SURFACE ( 'NONE', #67527, 11.65000000000000036, 0.1000000000000000056 ) ;
#246629=AXIS2_PLACEMENT_3D ( 'NONE', #106989, #31359, #150008 ) ;
#246641=ORIENTED_EDGE ( 'NONE', *, *, #80089, .T. ) ;
#246651=( BOUNDED_SURFACE ( )  B_SPLINE_SURFACE ( 3, 2, ( 
 ( #210677, #189837, #16354 ),
 ( #191143, #153313, #11202 ),
 ( #92010, #213231, #251074 ),
 ( #253636, #132431, #232833 ),
 ( #72470, #51567, #55420 ),
 ( #209392, #111585, #90719 ) ),
 .UNSPECIFIED., .F., .F., .F. ) 
 B_SPLINE_SURFACE_WITH_KNOTS ( ( 4, 2, 4 ),
 ( 3, 3 ),
 ( 1.570796326794895448, 2.356194490192343505, 3.141592653589791784 ),
 ( 0.000000000000000000, 1.000000000000000000 ),
 .UNSPECIFIED. ) 
 GEOMETRIC_REPRESENTATION_ITEM ( )  RATIONAL_B_SPLINE_SURFACE ( (
 ( 1.000000000000000000, 0.7071067811865475727, 1.000000000000000000),
 ( 1.000000000000000000, 0.6611148371782917810, 1.000000000000000000),
 ( 1.000000000000000000, 0.6092287576690524897, 1.000000000000000000),
 ( 1.000000000000000000, 0.5278258667062201148, 1.000000000000000000),
 ( 1.000000000000000000, 0.4993418825330976363, 1.000000000000000000),
 ( 1.000000000000000000, 0.5000000000000339728, 1.000000000000000000) ) ) 
 REPRESENTATION_ITEM ( '' )  SURFACE ( )  );
#246662=DIRECTION ( 'NONE',  ( -1.000000000000000000, 0.000000000000000000, 0.000000000000000000 ) ) ;
#246727=ORIENTED_EDGE ( 'NONE', *, *, #206524, .F. ) ;
#246746=CARTESIAN_POINT ( 'NONE',  ( 19.86930884467603065, 54.45808362210101450, -228.7712941873963928 ) ) ;
#246749=AXIS2_PLACEMENT_3D ( 'NONE', #228965, #75985, #49030 ) ;
#246752=VERTEX_POINT ( 'NONE', #30750 ) ;
#246796=ORIENTED_EDGE ( 'NONE', *, *, #176217, .T. ) ;
#246798=LINE ( 'NONE', #107293, #173752 ) ;
#246801=DIRECTION ( 'NONE',  ( 0.000000000000000000, 0.9126074666063772600, 0.4088369013363274407 ) ) ;
#246809=CARTESIAN_POINT ( 'NONE',  ( 20.94999999999999929, 45.02833974712562792, -238.5149546970766892 ) ) ;
#246811=ADVANCED_FACE ( 'NONE', ( #209353 ), #150675, .T. ) ;
#246821=DIRECTION ( 'NONE',  ( 0.000000000000000000, -0.9126074666063545004, -0.4088369013363783999 ) ) ;
#246826=FACE_OUTER_BOUND ( 'NONE', #232749, .T. ) ;
#246827=DIRECTION ( 'NONE',  ( -0.000000000000000000, -0.4088369013363281623, 0.9126074666063771490 ) ) ;
#246855=DIRECTION ( 'NONE',  ( 0.7071067811865475727, -0.2890913453342132122, 0.6453109281988448354 ) ) ;
#246861=EDGE_CURVE ( 'NONE', #33783, #208409, #142330, .T. ) ;
#246875=ORIENTED_EDGE ( 'NONE', *, *, #77097, .F. ) ;
#246878=EDGE_CURVE ( 'NONE', #224911, #233399, #137637, .T. ) ;
#246965=ORIENTED_EDGE ( 'NONE', *, *, #181479, .T. ) ;
#247005=EDGE_CURVE ( 'NONE', #232621, #102676, #66929, .T. ) ;
#247084=DIRECTION ( 'NONE',  ( 1.000000000000000000, 0.000000000000000000, 0.000000000000000000 ) ) ;
#247099=VECTOR ( 'NONE', #157647, 1000.000000000000000 ) ;
#247104=ORIENTED_EDGE ( 'NONE', *, *, #112659, .T. ) ;
#247135=ORIENTED_EDGE ( 'NONE', *, *, #42462, .T. ) ;
#247144=CARTESIAN_POINT ( 'NONE',  ( -21.13422380239062548, 30.73306616121944046, -252.2058741929238295 ) ) ;
#247178=ADVANCED_FACE ( 'NONE', ( #16975 ), #14419, .T. ) ;
#247193=DIRECTION ( 'NONE',  ( 2.715809747126111577E-16, 0.4088369013363273852, -0.9126074666063772600 ) ) ;
#247204=DIRECTION ( 'NONE',  ( 0.000000000000000000, 0.9126074666063769270, 0.4088369013363280513 ) ) ;
#247256=EDGE_CURVE ( 'NONE', #219396, #62719, #176060, .T. ) ;
#247257=ORIENTED_EDGE ( 'NONE', *, *, #223417, .T. ) ;
#247260=CARTESIAN_POINT ( 'NONE',  ( 18.59999999999999076, 78.57213941646344324, -232.7862224702232652 ) ) ;
#247261=FACE_BOUND ( 'NONE', #3758, .T. ) ;
#247282=CYLINDRICAL_SURFACE ( 'NONE', #1749, 0.09999999999999108213 ) ;
#247327=EDGE_CURVE ( 'NONE', #24913, #212760, #92049, .T. ) ;
#247393=PLANE ( 'NONE',  #52536 ) ;
#247440=B_SPLINE_CURVE_WITH_KNOTS ( 'NONE', 3,
 ( #93804, #216316, #15591, #113381, #35167, #95097, #238458, #33891, #136779, #237183 ),
 .UNSPECIFIED., .F., .F.,
 ( 4, 3, 3, 4 ),
 ( 0.000000000000000000, 0.0002000000000008589688, 0.001000000000082969676, 0.001967863649483315904 ),
 .UNSPECIFIED. ) ;
#247446=VERTEX_POINT ( 'NONE', #217697 ) ;
#247482=DIRECTION ( 'NONE',  ( 0.000000000000000000, -0.8103668758649578141, 0.5859227990963212784 ) ) ;
#247499=CIRCLE ( 'NONE', #68436, 0.09999999999999326095 ) ;
#247521=DIRECTION ( 'NONE',  ( 0.7071067811864846231, 0.2890913453341779626, -0.6453109281989296564 ) ) ;
#247563=DIRECTION ( 'NONE',  ( 2.710505431213777848E-16, 0.4088369013363281623, -0.9126074666063771490 ) ) ;
#247586=CARTESIAN_POINT ( 'NONE',  ( 20.95496329884391784, 39.25093957328100913, -236.8105868520244996 ) ) ;
#247590=EDGE_LOOP ( 'NONE', ( #154205, #242530, #59804, #53737, #217746, #185847, #69266, #150759, #86082, #206623 ) ) ;
#247593=ORIENTED_EDGE ( 'NONE', *, *, #67323, .T. ) ;
#247643=EDGE_CURVE ( 'NONE', #153695, #182906, #204656, .T. ) ;
#247649=EDGE_CURVE ( 'NONE', #24454, #130019, #163000, .T. ) ;
#247658=ORIENTED_EDGE ( 'NONE', *, *, #25375, .F. ) ;
#247662=CYLINDRICAL_SURFACE ( 'NONE', #111694, 0.4999999999999944489 ) ;
#247669=CIRCLE ( 'NONE', #231121, 0.09999999999999609201 ) ;
#247680=VECTOR ( 'NONE', #250976, 1000.000000000000227 ) ;
#247695=FACE_OUTER_BOUND ( 'NONE', #97237, .T. ) ;
#247709=EDGE_LOOP ( 'NONE', ( #204600, #159840, #9619, #38831 ) ) ;
#247726=EDGE_LOOP ( 'NONE', ( #120283, #158083, #47058, #97063 ) ) ;
#247737=AXIS2_PLACEMENT_3D ( 'NONE', #241556, #242834, #26372 ) ;
#247744=DIRECTION ( 'NONE',  ( -1.000000000000000000, -0.000000000000000000, 0.000000000000000000 ) ) ;
#247752=DIRECTION ( 'NONE',  ( 0.000000000000000000, 0.9623856809447771665, 0.2716869542551821892 ) ) ;
#247760=AXIS2_PLACEMENT_3D ( 'NONE', #65980, #163809, #127242 ) ;
#247767=ORIENTED_EDGE ( 'NONE', *, *, #119904, .T. ) ;
#247804=EDGE_CURVE ( 'NONE', #183191, #116722, #171391, .T. ) ;
#247826=CARTESIAN_POINT ( 'NONE',  ( -21.14999999999999858, 31.98723526783714988, -238.8784020251475511 ) ) ;
#247836=CIRCLE ( 'NONE', #52187, 0.09999999999999950595 ) ;
#247837=DIRECTION ( 'NONE',  ( 0.000000000000000000, 0.9126074666063777041, 0.4088369013363265525 ) ) ;
#247841=ORIENTED_EDGE ( 'NONE', *, *, #122137, .F. ) ;
#247874=CARTESIAN_POINT ( 'NONE',  ( -20.64999999999999858, 62.08591502004791352, -248.5699171172615820 ) ) ;
#247893=CARTESIAN_POINT ( 'NONE',  ( -22.50000000000000000, 26.02743912001966464, -254.3139371321002216 ) ) ;
#247908=CARTESIAN_POINT ( 'NONE',  ( -18.57399277249657032, 68.10911674539558192, -224.1414149070238864 ) ) ;
#247911=DIRECTION ( 'NONE',  ( 1.000000000000000000, 0.000000000000000000, 0.000000000000000000 ) ) ;
#247933=AXIS2_PLACEMENT_3D ( 'NONE', #125826, #170148, #147973 ) ;
#247938=CIRCLE ( 'NONE', #252206, 0.09999999999999939493 ) ;
#247960=AXIS2_PLACEMENT_3D ( 'NONE', #223899, #121001, #62278 ) ;
#247966=CIRCLE ( 'NONE', #81901, 0.5000000000000071054 ) ;
#247967=ADVANCED_FACE ( 'NONE', ( #46457 ), #88288, .F. ) ;
#248059=EDGE_LOOP ( 'NONE', ( #134509, #23481, #189438, #201781 ) ) ;
#248069=DIRECTION ( 'NONE',  ( -1.000000000000000000, 2.986185139342070877E-16, -6.665775143889692774E-16 ) ) ;
#248084=EDGE_LOOP ( 'NONE', ( #43889, #114042 ) ) ;
#248117=ADVANCED_FACE ( 'NONE', ( #34639 ), #253641, .F. ) ;
#248119=AXIS2_PLACEMENT_3D ( 'NONE', #124771, #24402, #85593 ) ;
#248141=DIRECTION ( 'NONE',  ( 1.000000000000000000, 0.000000000000000000, 0.000000000000000000 ) ) ;
#248201=FACE_OUTER_BOUND ( 'NONE', #92495, .T. ) ;
#248211=DIRECTION ( 'NONE',  ( -1.000000000000000000, -0.000000000000000000, 0.000000000000000000 ) ) ;
#248223=DIRECTION ( 'NONE',  ( 0.000000000000000000, 0.9126074666063501706, 0.4088369013363880589 ) ) ;
#248241=DIRECTION ( 'NONE',  ( -1.000000000000000000, 1.207181226542539700E-16, -2.694675058168174199E-16 ) ) ;
#248261=DIRECTION ( 'NONE',  ( 0.7071359030027302151, -0.2890794387707354418, 0.6452843503173697481 ) ) ;
#248283=FACE_OUTER_BOUND ( 'NONE', #199085, .T. ) ;
#248291=EDGE_CURVE ( 'NONE', #173652, #244838, #17053, .T. ) ;
#248300=LINE ( 'NONE', #147928, #31379 ) ;
#248339=EDGE_CURVE ( 'NONE', #219191, #121939, #146530, .T. ) ;
#248352=AXIS2_PLACEMENT_3D ( 'NONE', #98617, #76520, #156103 ) ;
#248353=AXIS2_PLACEMENT_3D ( 'NONE', #79170, #234400, #177037 ) ;
#248415=DIRECTION ( 'NONE',  ( -1.000000000000000000, -0.000000000000000000, 0.000000000000000000 ) ) ;
#248422=EDGE_CURVE ( 'NONE', #161112, #20995, #116992, .T. ) ;
#248454=VERTEX_POINT ( 'NONE', #139816 ) ;
#248458=AXIS2_PLACEMENT_3D ( 'NONE', #172616, #229970, #252096 ) ;
#248466=VERTEX_POINT ( 'NONE', #61580 ) ;
#248471=CYLINDRICAL_SURFACE ( 'NONE', #247760, 0.09999999999999609201 ) ;
#248491=ADVANCED_FACE ( 'NONE', ( #307 ), #257152, .T. ) ;
#248497=DIRECTION ( 'NONE',  ( 0.000000000000000000, -0.9126074666063545004, -0.4088369013363783999 ) ) ;
#248506=ORIENTED_EDGE ( 'NONE', *, *, #226465, .F. ) ;
#248533=DIRECTION ( 'NONE',  ( 0.000000000000000000, 0.9126074666063844765, 0.4088369013363113980 ) ) ;
#248580=CARTESIAN_POINT ( 'NONE',  ( -20.00857864376270001, 44.01574086017817677, -236.0100308471058099 ) ) ;
#248584=CARTESIAN_POINT ( 'NONE',  ( 21.14999999999999858, 42.98415524044398950, -233.9519173640447889 ) ) ;
#248612=DIRECTION ( 'NONE',  ( 0.7071067811865489050, -0.6453109281988438362, -0.2890913453342124906 ) ) ;
#248649=VECTOR ( 'NONE', #57880, 1000.000000000000000 ) ;
#248654=CARTESIAN_POINT ( 'NONE',  ( -20.54999999999999716, 48.91146289617405785, -253.9240286733484595 ) ) ;
#248664=EDGE_CURVE ( 'NONE', #161112, #220739, #173237, .T. ) ;
#248694=LINE ( 'NONE', #114311, #235885 ) ;
#248718=CARTESIAN_POINT ( 'NONE',  ( -23.25000000000000000, 74.86109765932731364, -233.8067614591677454 ) ) ;
#248724=CARTESIAN_POINT ( 'NONE',  ( 21.06490991615909536, 43.41139117757177246, -234.7742192443139118 ) ) ;
#248725=CARTESIAN_POINT ( 'NONE',  ( 23.15000000000000213, 62.12679871018153932, -248.6611778639222337 ) ) ;
#248726=CARTESIAN_POINT ( 'NONE',  ( -21.44999999999999929, 53.04688186230822566, -234.1557136682916394 ) ) ;
#248744=EDGE_CURVE ( 'NONE', #74878, #83103, #171378, .T. ) ;
#248751=EDGE_CURVE ( 'NONE', #180828, #148712, #104658, .T. ) ;
#248756=DIRECTION ( 'NONE',  ( 0.000000000000000000, 0.9126074666063770380, 0.4088369013363281068 ) ) ;
#248771=EDGE_LOOP ( 'NONE', ( #156650, #52634, #87508, #64812 ) ) ;
#248773=ORIENTED_EDGE ( 'NONE', *, *, #63166, .F. ) ;
#248789=VECTOR ( 'NONE', #8646, 1000.000000000000114 ) ;
#248790=CARTESIAN_POINT ( 'NONE',  ( -20.94999999999999929, 39.30548607490320734, -248.3655356873701123 ) ) ;
#248811=CARTESIAN_POINT ( 'NONE',  ( -20.64999999999999858, 46.15118611352045974, -240.5321844900040844 ) ) ;
#248812=EDGE_CURVE ( 'NONE', #78569, #200649, #246170, .T. ) ;
#248858=CARTESIAN_POINT ( 'NONE',  ( -23.15000000000000213, 56.06656052939784018, -228.0911609752645290 ) ) ;
#248911=ORIENTED_EDGE ( 'NONE', *, *, #220655, .T. ) ;
#248951=DIRECTION ( 'NONE',  ( 1.000000000000000000, 0.000000000000000000, 0.000000000000000000 ) ) ;
#248954=LINE ( 'NONE', #209821, #255805 ) ;
#248965=ADVANCED_FACE ( 'NONE', ( #67363 ), #29720, .T. ) ;
#248980=CARTESIAN_POINT ( 'NONE',  ( -20.85000000000000142, 62.46832465249013921, -225.2232495205141731 ) ) ;
#248987=LINE ( 'NONE', #109440, #214443 ) ;
#248994=ORIENTED_EDGE ( 'NONE', *, *, #222375, .T. ) ;
#248996=VECTOR ( 'NONE', #198763, 1000.000000000000114 ) ;
#249000=AXIS2_PLACEMENT_3D ( 'NONE', #197801, #19174, #119581 ) ;
#249008=CARTESIAN_POINT ( 'NONE',  ( 22.59999954896768770, 25.93893177648351056, -254.3632609673429101 ) ) ;
#249014=ORIENTED_EDGE ( 'NONE', *, *, #227422, .F. ) ;
#249038=FACE_OUTER_BOUND ( 'NONE', #24840, .T. ) ;
#249039=CIRCLE ( 'NONE', #124141, 11.74999999999999822 ) ;
#249043=VERTEX_POINT ( 'NONE', #231579 ) ;
#249062=EDGE_CURVE ( 'NONE', #183348, #67538, #34675, .T. ) ;
#249066=EDGE_CURVE ( 'NONE', #110771, #89549, #146513, .T. ) ;
#249071=EDGE_CURVE ( 'NONE', #120786, #7171, #16394, .T. ) ;
#249093=ORIENTED_EDGE ( 'NONE', *, *, #83353, .F. ) ;
#249117=DIRECTION ( 'NONE',  ( -1.000000000000000000, -0.000000000000000000, 0.000000000000000000 ) ) ;
#249121=ORIENTED_EDGE ( 'NONE', *, *, #113195, .F. ) ;
#249132=AXIS2_PLACEMENT_3D ( 'NONE', #212627, #34019, #208775 ) ;
#249163=VERTEX_POINT ( 'NONE', #190756 ) ;
#249181=VERTEX_POINT ( 'NONE', #249426 ) ;
#249189=CARTESIAN_POINT ( 'NONE',  ( 18.49999999999999645, 36.65892442174472876, -249.5511627012454596 ) ) ;
#249203=AXIS2_PLACEMENT_3D ( 'NONE', #4943, #64941, #87057 ) ;
#249220=EDGE_LOOP ( 'NONE', ( #225581, #122642, #152210 ) ) ;
#249280=EDGE_LOOP ( 'NONE', ( #14905, #27198, #209102, #155373 ) ) ;
#249327=ORIENTED_EDGE ( 'NONE', *, *, #119899, .T. ) ;
#249337=CARTESIAN_POINT ( 'NONE',  ( 20.84999999999998721, 62.42744096235649920, -225.1319887738535499 ) ) ;
#249347=ORIENTED_EDGE ( 'NONE', *, *, #213960, .T. ) ;
#249416=DIRECTION ( 'NONE',  ( -1.000000000000000000, 0.000000000000000000, 0.000000000000000000 ) ) ;
#249419=FACE_OUTER_BOUND ( 'NONE', #244188, .T. ) ;
#249424=VECTOR ( 'NONE', #82798, 1000.000000000000114 ) ;
#249426=CARTESIAN_POINT ( 'NONE',  ( 18.49999999999999289, 68.00366762990589109, -224.2307594727497815 ) ) ;
#249435=EDGE_LOOP ( 'NONE', ( #114119, #138308, #81550, #167504 ) ) ;
#249455=EDGE_LOOP ( 'NONE', ( #85738, #229286, #226435, #218780 ) ) ;
#249516=CARTESIAN_POINT ( 'NONE',  ( 23.24999999999999645, 54.46551753941606222, -236.3409998116131021 ) ) ;
#249523=CARTESIAN_POINT ( 'NONE',  ( 21.05000000000000071, 48.40874555430184500, -244.2873875965402704 ) ) ;
#249533=ORIENTED_EDGE ( 'NONE', *, *, #84027, .T. ) ;
#249576=EDGE_LOOP ( 'NONE', ( #156866, #159234, #107864, #47900 ) ) ;
#249636=CARTESIAN_POINT ( 'NONE',  ( 21.05000000000000071, 69.25640205380743453, -247.7135141964517402 ) ) ;
#249672=CARTESIAN_POINT ( 'NONE',  ( 23.14999999999998437, 36.65892442174472876, -249.5511627012454596 ) ) ;
#249696=DIRECTION ( 'NONE',  ( 0.000000000000000000, -0.9126074666063660468, -0.4088369013363524762 ) ) ;
#249697=ORIENTED_EDGE ( 'NONE', *, *, #96693, .F. ) ;
#249712=TOROIDAL_SURFACE ( 'NONE', #195577, 11.65000000000000036, 0.1000000000000000056 ) ;
#249723=ORIENTED_EDGE ( 'NONE', *, *, #171828, .T. ) ;
#249731=AXIS2_PLACEMENT_3D ( 'NONE', #241861, #206592, #63209 ) ;
#249732=CARTESIAN_POINT ( 'NONE',  ( 18.49999999999999645, 67.23127455305835554, -235.8551265064784559 ) ) ;
#249754=LINE ( 'NONE', #149396, #251846 ) ;
#249756=EDGE_LOOP ( 'NONE', ( #212116, #192500, #251451, #96943 ) ) ;
#249811=CIRCLE ( 'NONE', #187287, 2.099999999999998312 ) ;
#249817=DIRECTION ( 'NONE',  ( 0.000000000000000000, -0.4088369013363276072, 0.9126074666063772600 ) ) ;
#249834=LINE ( 'NONE', #47755, #149684 ) ;
#249837=CARTESIAN_POINT ( 'NONE',  ( -20.94999999999999929, 56.16603649944111254, -228.1013850343386764 ) ) ;
#249853=CARTESIAN_POINT ( 'NONE',  ( -20.94999999999999929, 67.85909929089923764, -227.8797997985275856 ) ) ;
#249858=ORIENTED_EDGE ( 'NONE', *, *, #117747, .T. ) ;
#249869=DIRECTION ( 'NONE',  ( 0.000000000000000000, -0.4088369013363783999, 0.9126074666063545004 ) ) ;
#249872=AXIS2_PLACEMENT_3D ( 'NONE', #248584, #128652, #212044 ) ;
#249882=DIRECTION ( 'NONE',  ( 0.000000000000000000, -0.9126074666063771490, -0.4088369013363281623 ) ) ;
#249911=DIRECTION ( 'NONE',  ( 0.000000000000000000, 0.9126074666063545004, 0.4088369013363783999 ) ) ;
#249932=CARTESIAN_POINT ( 'NONE',  ( 23.14999999999999503, 45.25174493058054281, -238.5244480634700324 ) ) ;
#249942=CARTESIAN_POINT ( 'NONE',  ( -21.59780538579341069, 33.76925247340353309, -243.3429228916662623 ) ) ;
#249985=AXIS2_PLACEMENT_3D ( 'NONE', #237552, #254511, #234989 ) ;
#249993=CARTESIAN_POINT ( 'NONE',  ( 21.05000000000000071, 43.36285386911620776, -234.7972500504784534 ) ) ;
#250084=DIRECTION ( 'NONE',  ( 1.000000000000000000, 0.000000000000000000, 0.000000000000000000 ) ) ;
#250095=AXIS2_PLACEMENT_3D ( 'NONE', #15040, #251050, #55392 ) ;
#250098=DIRECTION ( 'NONE',  ( -1.000000000000000000, -0.000000000000000000, 0.000000000000000000 ) ) ;
#250099=CARTESIAN_POINT ( 'NONE',  ( -23.25000000000000000, 36.65892442174472876, -249.5511627012454596 ) ) ;
#250107=CARTESIAN_POINT ( 'NONE',  ( -23.15000000000000213, 69.14775023293175593, -234.9965690136722003 ) ) ;
#250129=EDGE_CURVE ( 'NONE', #111770, #155744, #250969, .T. ) ;
#250155=ADVANCED_FACE ( 'NONE', ( #207513 ), #167117, .T. ) ;
#250161=EDGE_CURVE ( 'NONE', #110735, #108899, #142637, .T. ) ;
#250202=CARTESIAN_POINT ( 'NONE',  ( 20.94999999999999929, 36.65892442174472876, -249.5511627012454596 ) ) ;
#250286=DIRECTION ( 'NONE',  ( 0.000000000000000000, -0.9126074666063773710, -0.4088369013363274962 ) ) ;
#250308=DIRECTION ( 'NONE',  ( 0.000000000000000000, -0.4088369013363280513, 0.9126074666063769270 ) ) ;
#250331=ORIENTED_EDGE ( 'NONE', *, *, #212395, .F. ) ;
#250349=DIRECTION ( 'NONE',  ( -1.000000000000000000, -0.000000000000000000, 0.000000000000000000 ) ) ;
#250351=DIRECTION ( 'NONE',  ( 0.000000000000000000, 0.09425075112713271475, 0.9955484899852801162 ) ) ;
#250375=LINE ( 'NONE', #173468, #21593 ) ;
#250384=CARTESIAN_POINT ( 'NONE',  ( 21.05000000000000071, 53.86595165227826243, -236.3638196928718855 ) ) ;
#250393=CARTESIAN_POINT ( 'NONE',  ( -21.29999999999995808, 32.96286418198891255, -251.2069521516576174 ) ) ;
#250396=CARTESIAN_POINT ( 'NONE',  ( 22.39999999999999503, 31.76383008438224564, -238.8689086587541510 ) ) ;
#250421=DIRECTION ( 'NONE',  ( 0.000000000000000000, -0.9126074666063769270, -0.4088369013363280513 ) ) ;
#250431=VERTEX_POINT ( 'NONE', #104212 ) ;
#250464=DIRECTION ( 'NONE',  ( 2.428612866367624848E-13, -0.4088369013363783999, 0.9126074666063545004 ) ) ;
#250518=DIRECTION ( 'NONE',  ( 0.000000000000000000, -0.4088369013363783999, 0.9126074666063545004 ) ) ;
#250528=ADVANCED_FACE ( 'NONE', ( #131492 ), #55316, .T. ) ;
#250531=CIRCLE ( 'NONE', #25680, 0.1000000000000024342 ) ;
#250541=DIRECTION ( 'NONE',  ( 0.000000000000000000, -0.9126074666063771490, -0.4088369013363281623 ) ) ;
#250556=DIRECTION ( 'NONE',  ( 1.000000000000000000, 0.000000000000000000, 0.000000000000000000 ) ) ;
#250573=DIRECTION ( 'NONE',  ( -1.000000000000000000, -0.000000000000000000, 0.000000000000000000 ) ) ;
#250586=VERTEX_POINT ( 'NONE', #117072 ) ;
#250600=CARTESIAN_POINT ( 'NONE',  ( 20.04142135391667168, 54.39878304051241997, -228.7287286064368743 ) ) ;
#250628=CARTESIAN_POINT ( 'NONE',  ( -18.59999999999999787, 36.65892442174472876, -249.5511627012454596 ) ) ;
#250649=ORIENTED_EDGE ( 'NONE', *, *, #37597, .T. ) ;
#250661=CIRCLE ( 'NONE', #109185, 0.5999999999999934275 ) ;
#250669=CARTESIAN_POINT ( 'NONE',  ( 20.94999999999999929, 67.65998959290219261, -227.8609496483021530 ) ) ;
#250743=DIRECTION ( 'NONE',  ( 1.000000000000000000, 0.000000000000000000, 0.000000000000000000 ) ) ;
#250847=DIRECTION ( 'NONE',  ( -1.000000000000000000, -0.000000000000000000, 0.000000000000000000 ) ) ;
#250902=ORIENTED_EDGE ( 'NONE', *, *, #164398, .F. ) ;
#250907=VECTOR ( 'NONE', #154285, 1000.000000000000114 ) ;
#250921=EDGE_CURVE ( 'NONE', #21519, #13670, #215735, .T. ) ;
#250935=LINE ( 'NONE', #228835, #51658 ) ;
#250950=ORIENTED_EDGE ( 'NONE', *, *, #135693, .F. ) ;
#250969=CIRCLE ( 'NONE', #213377, 0.09999999999999609201 ) ;
#250976=DIRECTION ( 'NONE',  ( -0.000000000000000000, -0.8490545835447252943, -0.5283051335749947564 ) ) ;
#250980=DIRECTION ( 'NONE',  ( 0.000000000000000000, -0.9126074666063545004, -0.4088369013363783999 ) ) ;
#250981=ORIENTED_EDGE ( 'NONE', *, *, #6082, .T. ) ;
#250985=DIRECTION ( 'NONE',  ( 0.000000000000000000, -0.9126074666063660468, -0.4088369013363524762 ) ) ;
#250988=CARTESIAN_POINT ( 'NONE',  ( -21.05000000000000071, 30.90801580390628089, -252.0203440857197279 ) ) ;
#251011=SPHERICAL_SURFACE ( 'NONE', #62908, 0.1000000000000000056 ) ;
#251050=DIRECTION ( 'NONE',  ( 1.000000000000000000, 0.000000000000000000, 0.000000000000000000 ) ) ;
#251074=CARTESIAN_POINT ( 'NONE',  ( -21.12844524849339223, 38.15611011707152755, -236.0052459596564063 ) ) ;
#251087=CARTESIAN_POINT ( 'NONE',  ( 21.05000000000000071, 43.39590751456783835, -245.0548026989423818 ) ) ;
#251128=DIRECTION ( 'NONE',  ( 0.000000000000000000, -0.4088369013363783999, 0.9126074666063545004 ) ) ;
#251136=CARTESIAN_POINT ( 'NONE',  ( -18.59999999999999787, 67.23127455305835554, -235.8551265064784559 ) ) ;
#251154=CARTESIAN_POINT ( 'NONE',  ( 21.04999999999999716, 30.78822319289724163, -252.2004468398836536 ) ) ;
#251167=DIRECTION ( 'NONE',  ( -1.000000000000000000, 0.000000000000000000, 0.000000000000000000 ) ) ;
#251168=CYLINDRICAL_SURFACE ( 'NONE', #171617, 0.09999999999999854838 ) ;
#251179=ORIENTED_EDGE ( 'NONE', *, *, #91808, .F. ) ;
#251227=CIRCLE ( 'NONE', #84799, 0.1000000000000024342 ) ;
#251256=CARTESIAN_POINT ( 'NONE',  ( 21.53699400381148621, 33.88385736505378532, -243.3566462376118693 ) ) ;
#251268=CARTESIAN_POINT ( 'NONE',  ( 22.57320508075687115, 31.85509083104287598, -238.8280249686205536 ) ) ;
#251286=DIRECTION ( 'NONE',  ( 0.000000000000000000, 0.9947597004326452774, -0.1022405907414166287 ) ) ;
#251291=CARTESIAN_POINT ( 'NONE',  ( 20.94999999999999929, 45.58907629467868361, -240.2765730862633404 ) ) ;
#251313=TOROIDAL_SURFACE ( 'NONE', #72867, 11.70000000000000462, 0.1000000000000000056 ) ;
#251314=ORIENTED_EDGE ( 'NONE', *, *, #159369, .T. ) ;
#251317=DIRECTION ( 'NONE',  ( -1.000000000000000000, 0.000000000000000000, 0.000000000000000000 ) ) ;
#251334=CARTESIAN_POINT ( 'NONE',  ( -20.15000000000000568, 44.13095071803924441, -236.0226064646537054 ) ) ;
#251371=DIRECTION ( 'NONE',  ( 0.000000000000000000, 0.9126074666063783702, 0.4088369013363252757 ) ) ;
#251389=FACE_OUTER_BOUND ( 'NONE', #1429, .T. ) ;
#251401=ORIENTED_EDGE ( 'NONE', *, *, #146937, .T. ) ;
#251417=CARTESIAN_POINT ( 'NONE',  ( -23.15000000000000213, 59.59835781587673154, -226.3993831679961488 ) ) ;
#251444=DIRECTION ( 'NONE',  ( 0.000000000000000000, 0.9126074666063660468, 0.4088369013363524762 ) ) ;
#251447=CIRCLE ( 'NONE', #180543, 0.1000000000000024342 ) ;
#251451=ORIENTED_EDGE ( 'NONE', *, *, #239075, .F. ) ;
#251464=VERTEX_POINT ( 'NONE', #57425 ) ;
#251470=DIRECTION ( 'NONE',  ( 1.000000000000000000, 0.000000000000000000, 0.000000000000000000 ) ) ;
#251478=CIRCLE ( 'NONE', #80774, 0.09999999999999771572 ) ;
#251496=ORIENTED_EDGE ( 'NONE', *, *, #237553, .T. ) ;
#251529=LINE ( 'NONE', #115884, #43320 ) ;
#251535=EDGE_CURVE ( 'NONE', #119120, #117897, #218382, .T. ) ;
#251539=FACE_OUTER_BOUND ( 'NONE', #34949, .T. ) ;
#251540=CARTESIAN_POINT ( 'NONE',  ( 20.94999999999999929, 62.08591502004790641, -248.5699171172615820 ) ) ;
#251569=AXIS2_PLACEMENT_3D ( 'NONE', #23311, #162812, #63680 ) ;
#251595=ADVANCED_FACE ( 'NONE', ( #61298 ), #239945, .F. ) ;
#251624=ADVANCED_FACE ( 'NONE', ( #108128 ), #148543, .T. ) ;
#251629=CARTESIAN_POINT ( 'NONE',  ( -18.59999999999999787, 51.28888318656202472, -230.2315015618842153 ) ) ;
#251631=DIRECTION ( 'NONE',  ( 1.000000000000000000, 0.000000000000000000, 0.000000000000000000 ) ) ;
#251633=DIRECTION ( 'NONE',  ( 0.000000000000000000, -0.9126074666063660468, -0.4088369013363524762 ) ) ;
#251644=CARTESIAN_POINT ( 'NONE',  ( -20.00857864376270001, 44.10700160683882132, -235.9691471569722125 ) ) ;
#251668=EDGE_CURVE ( 'NONE', #182258, #179132, #147680, .T. ) ;
#251674=EDGE_CURVE ( 'NONE', #7052, #255010, #43442, .T. ) ;
#251695=DIRECTION ( 'NONE',  ( -0.000000000000000000, 0.9126074666063770380, 0.4088369013363281068 ) ) ;
#251760=ORIENTED_EDGE ( 'NONE', *, *, #72508, .F. ) ;
#251777=DIRECTION ( 'NONE',  ( 1.000000000000000000, 0.000000000000000000, -0.000000000000000000 ) ) ;
#251780=FACE_OUTER_BOUND ( 'NONE', #126079, .T. ) ;
#251832=VERTEX_POINT ( 'NONE', #35043 ) ;
#251835=FACE_OUTER_BOUND ( 'NONE', #88709, .T. ) ;
#251846=VECTOR ( 'NONE', #30735, 1000.000000000000114 ) ;
#251891=ORIENTED_EDGE ( 'NONE', *, *, #166119, .F. ) ;
#251903=DIRECTION ( 'NONE',  ( 0.000000000000000000, -0.9126074666063770380, -0.4088369013363281068 ) ) ;
#251907=VERTEX_POINT ( 'NONE', #45269 ) ;
#251920=DIRECTION ( 'NONE',  ( 0.000000000000000000, 0.4088369013363304383, -0.9126074666063759278 ) ) ;
#251956=CARTESIAN_POINT ( 'NONE',  ( 23.24999999999999645, 67.23127455305835554, -235.8551265064784559 ) ) ;
#251962=CARTESIAN_POINT ( 'NONE',  ( 21.05000000000000071, 69.08367151115869831, -247.5088222940653679 ) ) ;
#251987=ORIENTED_EDGE ( 'NONE', *, *, #97929, .F. ) ;
#251998=VECTOR ( 'NONE', #29842, 1000.000000000000114 ) ;
#252043=LINE ( 'NONE', #10879, #158721 ) ;
#252058=EDGE_CURVE ( 'NONE', #239535, #180828, #31197, .T. ) ;
#252065=CARTESIAN_POINT ( 'NONE',  ( -20.85000000000000142, 56.27731819600170837, -227.9967441372480721 ) ) ;
#252096=DIRECTION ( 'NONE',  ( 0.000000000000000000, 0.9126074666063770380, 0.4088369013363281068 ) ) ;
#252097=DIRECTION ( 'NONE',  ( -0.000000000000000000, -0.9126074666063770380, -0.4088369013363281068 ) ) ;
#252107=CARTESIAN_POINT ( 'NONE',  ( -22.57320508075687115, 31.85509083104287598, -238.8280249686205536 ) ) ;
#252108=TOROIDAL_SURFACE ( 'NONE', #14821, 0.2000000000000000111, 0.1000000000000000056 ) ;
#252130=VERTEX_POINT ( 'NONE', #148219 ) ;
#252150=ORIENTED_EDGE ( 'NONE', *, *, #23772, .T. ) ;
#252162=EDGE_LOOP ( 'NONE', ( #238402, #238445, #84296, #255516 ) ) ;
#252206=AXIS2_PLACEMENT_3D ( 'NONE', #161788, #62673, #142193 ) ;
#252215=CARTESIAN_POINT ( 'NONE',  ( 18.59999999999999432, 28.08990005499213538, -254.8141779806076670 ) ) ;
#252217=ADVANCED_FACE ( 'NONE', ( #116794 ), #148038, .F. ) ;
#252226=AXIS2_PLACEMENT_3D ( 'NONE', #92145, #39905, #198940 ) ;
#252255=DIRECTION ( 'NONE',  ( 1.000000000000000000, 0.000000000000000000, 0.000000000000000000 ) ) ;
#252262=DIRECTION ( 'NONE',  ( 0.000000000000000000, -0.5859227990963362664, -0.8103668758649469339 ) ) ;
#252275=CIRCLE ( 'NONE', #69167, 0.1999999999999935163 ) ;
#252291=CARTESIAN_POINT ( 'NONE',  ( -18.59999999999999787, 46.54514716347711101, -243.1111603596801842 ) ) ;
#252295=DIRECTION ( 'NONE',  ( 0.000000000000000000, 0.9126074666063769270, 0.4088369013363280513 ) ) ;
#252310=CARTESIAN_POINT ( 'NONE',  ( 21.14999999999999858, 42.98415524044398950, -233.9519173640447889 ) ) ;
#252311=DIRECTION ( 'NONE',  ( 0.000000000000000000, -0.5469332180710735347, 0.8371762388950247935 ) ) ;
#252319=ADVANCED_FACE ( 'NONE', ( #665 ), #119374, .F. ) ;
#252322=CIRCLE ( 'NONE', #164868, 0.1000000000000024342 ) ;
#252429=AXIS2_PLACEMENT_3D ( 'NONE', #211899, #128495, #250985 ) ;
#252434=EDGE_CURVE ( 'NONE', #5885, #228214, #248300, .T. ) ;
#252436=DIRECTION ( 'NONE',  ( -0.000000000000000000, -0.8103668758649471560, 0.5859227990963360444 ) ) ;
#252441=CARTESIAN_POINT ( 'NONE',  ( 21.05000000000000071, 30.68987205111126215, -252.2252246220829193 ) ) ;
#252465=ORIENTED_EDGE ( 'NONE', *, *, #240870, .T. ) ;
#252478=EDGE_CURVE ( 'NONE', #19042, #235775, #39737, .T. ) ;
#252489=CARTESIAN_POINT ( 'NONE',  ( -21.40925344232282512, 33.84637352282563683, -243.5150031621282665 ) ) ;
#252511=EDGE_CURVE ( 'NONE', #99525, #143336, #187066, .T. ) ;
#252529=CARTESIAN_POINT ( 'NONE',  ( 20.94999999999999574, 44.10931966560507789, -259.0886734199950183 ) ) ;
#252557=PLANE ( 'NONE',  #215839 ) ;
#252566=CARTESIAN_POINT ( 'NONE',  ( 21.05000000000000071, 36.75018516840536620, -249.5102790111118338 ) ) ;
#252579=EDGE_LOOP ( 'NONE', ( #81868, #247841, #113614, #93143, #127533 ) ) ;
#252627=FACE_OUTER_BOUND ( 'NONE', #247590, .T. ) ;
#252639=EDGE_CURVE ( 'NONE', #9598, #85043, #5365, .T. ) ;
#252642=DIRECTION ( 'NONE',  ( -1.000000000000000000, 1.207181226542539700E-16, -2.694675058168174199E-16 ) ) ;
#252653=AXIS2_PLACEMENT_3D ( 'NONE', #225845, #27723, #207623 ) ;
#252674=CARTESIAN_POINT ( 'NONE',  ( 21.14999999999999858, 26.06832281015329755, -254.4051978787608732 ) ) ;
#252695=AXIS2_PLACEMENT_3D ( 'NONE', #85166, #4374, #63064 ) ;
#252698=AXIS2_PLACEMENT_3D ( 'NONE', #71111, #227590, #149372 ) ;
#252705=ADVANCED_FACE ( 'NONE', ( #127921 ), #9243, .T. ) ;
#252745=CARTESIAN_POINT ( 'NONE',  ( -20.54999999999999716, 52.22920805963557456, -232.3304987350788906 ) ) ;
#252747=EDGE_CURVE ( 'NONE', #23132, #144138, #225692, .T. ) ;
#252766=AXIS2_PLACEMENT_3D ( 'NONE', #187558, #8898, #125004 ) ;
#252773=LINE ( 'NONE', #168162, #229675 ) ;
#252801=AXIS2_PLACEMENT_3D ( 'NONE', #134528, #97960, #158012 ) ;
#252805=CIRCLE ( 'NONE', #32260, 4.000000000000002665 ) ;
#252829=VECTOR ( 'NONE', #115231, 1000.000000000000114 ) ;
#252832=ORIENTED_EDGE ( 'NONE', *, *, #32878, .T. ) ;
#252854=EDGE_CURVE ( 'NONE', #142489, #186873, #156503, .T. ) ;
#252861=CARTESIAN_POINT ( 'NONE',  ( -23.25000000000000000, 67.23127455305835554, -235.8551265064784559 ) ) ;
#252869=VERTEX_POINT ( 'NONE', #95207 ) ;
#252890=AXIS2_PLACEMENT_3D ( 'NONE', #158218, #56485, #77338 ) ;
#252899=ORIENTED_EDGE ( 'NONE', *, *, #57498, .F. ) ;
#252909=AXIS2_PLACEMENT_3D ( 'NONE', #24711, #104195, #185033 ) ;
#252952=AXIS2_PLACEMENT_3D ( 'NONE', #113081, #33588, #208349 ) ;
#252957=FACE_OUTER_BOUND ( 'NONE', #29372, .T. ) ;
#252960=CARTESIAN_POINT ( 'NONE',  ( 21.05000000000000071, 43.08177281680065818, -239.3869926993485535 ) ) ;
#252964=AXIS2_PLACEMENT_3D ( 'NONE', #140764, #220313, #41682 ) ;
#252991=DIRECTION ( 'NONE',  ( -0.000000000000000000, 0.4088369013363281068, -0.9126074666063770380 ) ) ;
#253016=DIRECTION ( 'NONE',  ( 2.715809747126116508E-16, 0.4088369013363282178, -0.9126074666063770380 ) ) ;
#253034=DIRECTION ( 'NONE',  ( 0.000000000000000000, 0.9126074666063660468, 0.4088369013363524762 ) ) ;
#253036=ORIENTED_EDGE ( 'NONE', *, *, #179573, .F. ) ;
#253068=CYLINDRICAL_SURFACE ( 'NONE', #97881, 0.09999999999999939493 ) ;
#253080=CARTESIAN_POINT ( 'NONE',  ( -20.94999999999999929, 69.19063053712525857, -247.5666987377248631 ) ) ;
#253082=CARTESIAN_POINT ( 'NONE',  ( 23.15000000000000213, 69.16514130714681130, -247.7543978865853660 ) ) ;
#253085=DIRECTION ( 'NONE',  ( 0.000000000000000000, -0.9126074666063769270, -0.4088369013363280513 ) ) ;
#253092=ORIENTED_EDGE ( 'NONE', *, *, #50951, .F. ) ;
#253113=DIRECTION ( 'NONE',  ( 0.000000000000000000, 0.9947597004326491632, -0.1022405907413782566 ) ) ;
#253116=FACE_OUTER_BOUND ( 'NONE', #13840, .T. ) ;
#253127=ORIENTED_EDGE ( 'NONE', *, *, #25293, .F. ) ;
#253152=AXIS2_PLACEMENT_3D ( 'NONE', #165965, #9419, #245487 ) ;
#253158=ORIENTED_EDGE ( 'NONE', *, *, #116143, .T. ) ;
#253170=AXIS2_PLACEMENT_3D ( 'NONE', #254674, #236436, #119071 ) ;
#253177=ORIENTED_EDGE ( 'NONE', *, *, #143355, .F. ) ;
#253191=CIRCLE ( 'NONE', #28384, 0.1000000000000024342 ) ;
#253204=CARTESIAN_POINT ( 'NONE',  ( -20.94999999999999929, 62.46832465249013921, -225.2232495205141731 ) ) ;
#253228=CARTESIAN_POINT ( 'NONE',  ( 20.85000000000000142, 62.46832465249013921, -225.2232495205141731 ) ) ;
#253288=EDGE_LOOP ( 'NONE', ( #158329, #12171, #62274, #254319 ) ) ;
#253289=AXIS2_PLACEMENT_3D ( 'NONE', #109244, #53131, #128834 ) ;
#253306=DIRECTION ( 'NONE',  ( -0.000000000000000000, -0.9126074666063770380, -0.4088369013363282178 ) ) ;
#253313=CARTESIAN_POINT ( 'NONE',  ( 21.05000000000000071, 30.89539159176859684, -252.1742849677607978 ) ) ;
#253316=FACE_OUTER_BOUND ( 'NONE', #207162, .T. ) ;
#253323=DIRECTION ( 'NONE',  ( 0.000000000000000000, 0.9955484899852913294, -0.09425075112701486457 ) ) ;
#253331=ORIENTED_EDGE ( 'NONE', *, *, #255744, .T. ) ;
#253354=EDGE_CURVE ( 'NONE', #175784, #17340, #131262, .T. ) ;
#253400=CIRCLE ( 'NONE', #107471, 0.1000000000000074440 ) ;
#253433=ORIENTED_EDGE ( 'NONE', *, *, #106727, .T. ) ;
#253446=AXIS2_PLACEMENT_3D ( 'NONE', #185073, #6431, #26014 ) ;
#253456=CARTESIAN_POINT ( 'NONE',  ( -20.85000000000000142, 67.85909929089923764, -227.8797997985275856 ) ) ;
#253487=EDGE_CURVE ( 'NONE', #116722, #149671, #112708, .T. ) ;
#253494=LINE ( 'NONE', #129706, #160055 ) ;
#253535=ORIENTED_EDGE ( 'NONE', *, *, #80089, .F. ) ;
#253552=CIRCLE ( 'NONE', #12173, 0.1000000000000054595 ) ;
#253567=CIRCLE ( 'NONE', #166145, 11.75000000000000355 ) ;
#253624=AXIS2_PLACEMENT_3D ( 'NONE', #247826, #6638, #147441 ) ;
#253636=CARTESIAN_POINT ( 'NONE',  ( -21.00219873199050724, 38.22274692886851000, -236.1338529772052084 ) ) ;
#253641=PLANE ( 'NONE',  #154995 ) ;
#253666=DIRECTION ( 'NONE',  ( 1.000000000000000000, -8.623019343401624248E-17, -8.389849937938898203E-16 ) ) ;
#253696=DIRECTION ( 'NONE',  ( 1.000000000000000000, 0.000000000000000000, 0.000000000000000000 ) ) ;
#253755=DIRECTION ( 'NONE',  ( 1.000000000000000000, 0.000000000000000000, 0.000000000000000000 ) ) ;
#253809=DIRECTION ( 'NONE',  ( 0.000000000000000000, 0.4088369013363281623, -0.9126074666063771490 ) ) ;
#253816=CARTESIAN_POINT ( 'NONE',  ( -20.94999999999999929, 38.29773864426885410, -236.0513742605307925 ) ) ;
#253821=LINE ( 'NONE', #256333, #172735 ) ;
#253823=CARTESIAN_POINT ( 'NONE',  ( 21.08804281139605408, 43.58702878209024334, -234.8084616901626873 ) ) ;
#253832=EDGE_LOOP ( 'NONE', ( #31570, #223426, #73712, #112353 ) ) ;
#253839=CARTESIAN_POINT ( 'NONE',  ( 20.97217846901851956, 40.78860018870523163, -237.9757527299901199 ) ) ;
#253849=ORIENTED_EDGE ( 'NONE', *, *, #106210, .T. ) ;
#253877=VERTEX_POINT ( 'NONE', #210233 ) ;
#253896=ORIENTED_EDGE ( 'NONE', *, *, #61182, .T. ) ;
#253902=DIRECTION ( 'NONE',  ( 0.000000000000000000, 0.9126074666063844765, 0.4088369013363114535 ) ) ;
#253925=EDGE_LOOP ( 'NONE', ( #250950, #63360, #35624, #192829, #66197, #42805, #120357, #118782, #81541, #124460 ) ) ;
#253926=CARTESIAN_POINT ( 'NONE',  ( -20.94999999999999929, 43.57568952063339651, -245.1784935019914826 ) ) ;
#253930=FACE_OUTER_BOUND ( 'NONE', #52605, .T. ) ;
#253932=EDGE_LOOP ( 'NONE', ( #148946, #180746, #246234, #138077 ) ) ;
#253953=ORIENTED_EDGE ( 'NONE', *, *, #5178, .T. ) ;
#253960=ORIENTED_EDGE ( 'NONE', *, *, #23875, .T. ) ;
#253993=ORIENTED_EDGE ( 'NONE', *, *, #59058, .F. ) ;
#254008=EDGE_CURVE ( 'NONE', #172675, #177620, #189893, .T. ) ;
#254018=ORIENTED_EDGE ( 'NONE', *, *, #159800, .T. ) ;
#254019=ORIENTED_EDGE ( 'NONE', *, *, #43647, .F. ) ;
#254032=LINE ( 'NONE', #201761, #198270 ) ;
#254061=ORIENTED_EDGE ( 'NONE', *, *, #219609, .F. ) ;
#254096=ORIENTED_EDGE ( 'NONE', *, *, #147658, .F. ) ;
#254135=AXIS2_PLACEMENT_3D ( 'NONE', #62074, #43793, #2074 ) ;
#254185=ORIENTED_EDGE ( 'NONE', *, *, #120823, .T. ) ;
#254190=DIRECTION ( 'NONE',  ( 0.000000000000000000, 0.9126074666063769270, 0.4088369013363280513 ) ) ;
#254210=AXIS2_PLACEMENT_3D ( 'NONE', #216058, #240442, #37455 ) ;
#254261=DIRECTION ( 'NONE',  ( 1.000000000000000000, 0.000000000000000000, 0.000000000000000000 ) ) ;
#254301=DIRECTION ( 'NONE',  ( 0.000000000000000000, 0.4166553800442402977, -0.9090645160164321226 ) ) ;
#254306=VECTOR ( 'NONE', #72654, 1000.000000000000114 ) ;
#254317=CIRCLE ( 'NONE', #100181, 4.050000000000006040 ) ;
#254319=ORIENTED_EDGE ( 'NONE', *, *, #237553, .F. ) ;
#254336=CARTESIAN_POINT ( 'NONE',  ( 23.24999999999999645, 36.65892442174472876, -249.5511627012454596 ) ) ;
#254356=EDGE_LOOP ( 'NONE', ( #104359, #2859, #91687, #162115 ) ) ;
#254358=FACE_OUTER_BOUND ( 'NONE', #228893, .T. ) ;
#254383=ORIENTED_EDGE ( 'NONE', *, *, #164182, .F. ) ;
#254386=EDGE_LOOP ( 'NONE', ( #196432, #229753, #230322, #105595 ) ) ;
#254409=ORIENTED_EDGE ( 'NONE', *, *, #195401, .T. ) ;
#254414=AXIS2_PLACEMENT_3D ( 'NONE', #140085, #179260, #200086 ) ;
#254479=ORIENTED_EDGE ( 'NONE', *, *, #191305, .F. ) ;
#254500=ORIENTED_EDGE ( 'NONE', *, *, #82646, .T. ) ;
#254502=CARTESIAN_POINT ( 'NONE',  ( 18.31572054635686797, 77.38692514556900903, -241.7683706053347805 ) ) ;
#254510=CARTESIAN_POINT ( 'NONE',  ( 21.13461538461538325, 44.29694026544699170, -236.3931290369747842 ) ) ;
#254511=DIRECTION ( 'NONE',  ( 1.000000000000000000, 0.000000000000000000, 0.000000000000000000 ) ) ;
#254588=VECTOR ( 'NONE', #57987, 1000.000000000000114 ) ;
#254592=DIRECTION ( 'NONE',  ( 1.000000000000000000, 0.000000000000000000, 0.000000000000000000 ) ) ;
#254637=DIRECTION ( 'NONE',  ( 1.000000000000000000, 0.000000000000000000, 0.000000000000000000 ) ) ;
#254674=CARTESIAN_POINT ( 'NONE',  ( 20.04142135623730070, 51.38014393322265505, -230.1906178717505611 ) ) ;
#254686=AXIS2_PLACEMENT_3D ( 'NONE', #128583, #28231, #243384 ) ;
#254731=EDGE_CURVE ( 'NONE', #191682, #217247, #186172, .T. ) ;
#254736=EDGE_CURVE ( 'NONE', #5729, #64826, #246798, .T. ) ;
#254757=AXIS2_PLACEMENT_3D ( 'NONE', #122169, #60892, #2192 ) ;
#254767=VERTEX_POINT ( 'NONE', #245538 ) ;
#254779=LINE ( 'NONE', #211873, #160214 ) ;
#254789=CARTESIAN_POINT ( 'NONE',  ( -22.39999999999999858, 29.50811709945089945, -252.6450601445781103 ) ) ;
#254791=LINE ( 'NONE', #14969, #101901 ) ;
#254799=LINE ( 'NONE', #17515, #115166 ) ;
#254830=CARTESIAN_POINT ( 'NONE',  ( -23.25000000000000000, 62.12148660976906456, -247.5636999539406133 ) ) ;
#254858=DIRECTION ( 'NONE',  ( 0.000000000000000000, -0.9126074666063771490, -0.4088369013363281623 ) ) ;
#254863=LINE ( 'NONE', #115409, #254588 ) ;
#254882=CIRCLE ( 'NONE', #246570, 0.09999999999999741040 ) ;
#254928=( BOUNDED_SURFACE ( )  B_SPLINE_SURFACE ( 3, 2, ( 
 ( #191066, #171507, #250988 ),
 ( #72394, #151939, #34553 ),
 ( #52795, #132340, #33290 ),
 ( #114053, #112789, #14987 ),
 ( #247144, #192327, #13679 ),
 ( #73689, #232751, #54089 ) ),
 .UNSPECIFIED., .F., .F., .F. ) 
 B_SPLINE_SURFACE_WITH_KNOTS ( ( 4, 2, 4 ),
 ( 3, 3 ),
 ( 0.0001792624049599850797, 0.0003686986002125220850, 0.0005581347954650591175 ),
 ( 0.000000000000000000, 1.000000000000000000 ),
 .UNSPECIFIED. ) 
 GEOMETRIC_REPRESENTATION_ITEM ( )  RATIONAL_B_SPLINE_SURFACE ( (
 ( 1.000000000000000000, 0.9238795325112888479, 1.000000000000000000),
 ( 1.000000000000000000, 0.9229318695235336767, 1.000000000000000000),
 ( 1.000000000000000000, 0.8926288119235017415, 1.000000000000000000),
 ( 1.000000000000000000, 0.8123777807266672202, 1.000000000000000000),
 ( 1.000000000000000000, 0.7629087100935024734, 1.000000000000000000),
 ( 1.000000000000000000, 0.7071067811865475727, 1.000000000000000000) ) ) 
 REPRESENTATION_ITEM ( '' )  SURFACE ( )  );
#254936=CARTESIAN_POINT ( 'NONE',  ( 21.05000000000000071, 36.65892442174472876, -249.5511627012454596 ) ) ;
#254938=CYLINDRICAL_SURFACE ( 'NONE', #73696, 0.09999999999999609201 ) ;
#254953=CARTESIAN_POINT ( 'NONE',  ( 20.94999999999999929, 74.98773774893902555, -233.8732236541320333 ) ) ;
#254997=CARTESIAN_POINT ( 'NONE',  ( -20.54999999999999716, 54.14029358995846053, -238.9803212882090691 ) ) ;
#254999=ORIENTED_EDGE ( 'NONE', *, *, #246071, .T. ) ;
#255010=VERTEX_POINT ( 'NONE', #79708 ) ;
#255012=ORIENTED_EDGE ( 'NONE', *, *, #205887, .T. ) ;
#255028=LINE ( 'NONE', #136400, #168112 ) ;
#255036=DIRECTION ( 'NONE',  ( 0.000000000000000000, -0.1022405907414166287, -0.9947597004326451664 ) ) ;
#255045=ADVANCED_FACE ( 'NONE', ( #141004 ), #219469, .F. ) ;
#255090=EDGE_CURVE ( 'NONE', #75688, #176861, #32932, .T. ) ;
#255092=ORIENTED_EDGE ( 'NONE', *, *, #124898, .F. ) ;
#255119=VECTOR ( 'NONE', #141664, 1000.000000000000114 ) ;
#255126=CARTESIAN_POINT ( 'NONE',  ( -22.59999999999999787, 25.98655542988603173, -254.2226763854395983 ) ) ;
#255145=CIRCLE ( 'NONE', #88590, 0.1000000000000024342 ) ;
#255154=DIRECTION ( 'NONE',  ( 0.000000000000000000, 0.8103668758649577031, -0.5859227990963212784 ) ) ;
#255156=CARTESIAN_POINT ( 'NONE',  ( -22.43310005002225438, 26.02505119112246490, -254.3088301514316925 ) ) ;
#255172=DIRECTION ( 'NONE',  ( 1.000000000000000000, 0.000000000000000000, 0.000000000000000000 ) ) ;
#255195=CIRCLE ( 'NONE', #1161, 0.09999999999999609201 ) ;
#255196=DIRECTION ( 'NONE',  ( 0.000000000000000000, -0.9126074666063771490, -0.4088369013363281623 ) ) ;
#255222=DIRECTION ( 'NONE',  ( 0.000000000000000000, 0.4088369013363279403, -0.9126074666063771490 ) ) ;
#255225=DIRECTION ( 'NONE',  ( -6.938893903907222856E-15, -0.4088369013363280513, 0.9126074666063769270 ) ) ;
#255237=CARTESIAN_POINT ( 'NONE',  ( -21.06715728752538652, 38.25685495413522119, -235.9601135138701409 ) ) ;
#255238=CYLINDRICAL_SURFACE ( 'NONE', #134926, 0.09999999999999063804 ) ;
#255239=VECTOR ( 'NONE', #26506, 1000.000000000000114 ) ;
#255251=LINE ( 'NONE', #237033, #34946 ) ;
#255259=VERTEX_POINT ( 'NONE', #189106 ) ;
#255289=EDGE_CURVE ( 'NONE', #240937, #90768, #236885, .T. ) ;
#255318=DIRECTION ( 'NONE',  ( 1.000000000000000000, -7.667232114526941871E-17, 1.711482807214921537E-16 ) ) ;
#255322=CYLINDRICAL_SURFACE ( 'NONE', #166113, 0.09999999999999939493 ) ;
#255332=CARTESIAN_POINT ( 'NONE',  ( 22.39999999999999503, 31.80471377451587500, -238.9601694054147742 ) ) ;
#255333=EDGE_CURVE ( 'NONE', #245440, #41988, #12063, .T. ) ;
#255343=EDGE_LOOP ( 'NONE', ( #237785, #171662, #54927, #53069 ) ) ;
#255419=CARTESIAN_POINT ( 'NONE',  ( 18.49999999999999289, 67.85909929089923764, -227.8797997985275856 ) ) ;
#255426=CARTESIAN_POINT ( 'NONE',  ( -23.15000000000000213, 54.82645269529697885, -239.3027372265576957 ) ) ;
#255428=DIRECTION ( 'NONE',  ( -1.000000000000000000, -2.986185139342071370E-16, 6.665775143889693760E-16 ) ) ;
#255430=EDGE_CURVE ( 'NONE', #208529, #2024, #151021, .T. ) ;
#255493=AXIS2_PLACEMENT_3D ( 'NONE', #41164, #690, #200214 ) ;
#255516=ORIENTED_EDGE ( 'NONE', *, *, #100024, .F. ) ;
#255551=FACE_OUTER_BOUND ( 'NONE', #143838, .T. ) ;
#255602=DIRECTION ( 'NONE',  ( 1.296989514748957922E-15, 0.2677755899090746849, -0.9634813093406884299 ) ) ;
#255614=CYLINDRICAL_SURFACE ( 'NONE', #237272, 0.09999999999999939493 ) ;
#255649=CARTESIAN_POINT ( 'NONE',  ( 21.98333005346336577, 29.92928821712973786, -252.5659568089976403 ) ) ;
#255656=CIRCLE ( 'NONE', #30874, 0.1000000000000214190 ) ;
#255658=AXIS2_PLACEMENT_3D ( 'NONE', #170833, #245187, #30012 ) ;
#255661=ORIENTED_EDGE ( 'NONE', *, *, #98241, .F. ) ;
#255744=EDGE_CURVE ( 'NONE', #200983, #143659, #130153, .T. ) ;
#255756=ADVANCED_FACE ( 'NONE', ( #97354 ), #230107, .F. ) ;
#255758=CARTESIAN_POINT ( 'NONE',  ( 18.49999999999999645, 74.98773774893902555, -233.8732236541320333 ) ) ;
#255793=ORIENTED_EDGE ( 'NONE', *, *, #8930, .T. ) ;
#255797=TOROIDAL_SURFACE ( 'NONE', #43458, 7.800000000000000711, 0.1000000000000000056 ) ;
#255805=VECTOR ( 'NONE', #230673, 1000.000000000000114 ) ;
#255822=ORIENTED_EDGE ( 'NONE', *, *, #43221, .F. ) ;
#255828=ORIENTED_EDGE ( 'NONE', *, *, #183164, .T. ) ;
#255867=TOROIDAL_SURFACE ( 'NONE', #205843, 6.258578643762700899, 0.1000000000000000056 ) ;
#255876=DIRECTION ( 'NONE',  ( -0.000000000000000000, 0.9126074666063771490, 0.4088369013363281623 ) ) ;
#255893=LINE ( 'NONE', #35655, #231249 ) ;
#255900=AXIS2_PLACEMENT_3D ( 'NONE', #255332, #156324, #178448 ) ;
#256006=EDGE_LOOP ( 'NONE', ( #246727, #131051, #236492, #141144 ) ) ;
#256030=DIRECTION ( 'NONE',  ( -0.7071067811865475727, 0.2890913453342130457, -0.6453109281988448354 ) ) ;
#256084=DIRECTION ( 'NONE',  ( -1.000000000000000000, -0.000000000000000000, 0.000000000000000000 ) ) ;
#256097=ORIENTED_EDGE ( 'NONE', *, *, #2277, .T. ) ;
#256098=CARTESIAN_POINT ( 'NONE',  ( 23.15000000000000213, 69.16514130714681130, -247.7543978865853660 ) ) ;
#256111=CIRCLE ( 'NONE', #75652, 12.77500000000000036 ) ;
#256119=EDGE_CURVE ( 'NONE', #162201, #174581, #209436, .T. ) ;
#256152=CARTESIAN_POINT ( 'NONE',  ( -18.39999999999999858, 46.96039402156217335, -255.3459641718773128 ) ) ;
#256188=EDGE_CURVE ( 'NONE', #177428, #34297, #199744, .T. ) ;
#256196=EDGE_CURVE ( 'NONE', #142241, #221915, #67986, .T. ) ;
#256208=CARTESIAN_POINT ( 'NONE',  ( -20.64999999999999858, 67.23127455305835554, -235.8551265064784559 ) ) ;
#256209=EDGE_CURVE ( 'NONE', #77135, #26148, #9709, .T. ) ;
#256237=CARTESIAN_POINT ( 'NONE',  ( 18.50000324121758055, 68.00468331834500191, -224.2298952291171474 ) ) ;
#256244=EDGE_CURVE ( 'NONE', #21519, #131079, #226, .T. ) ;
#256259=ORIENTED_EDGE ( 'NONE', *, *, #249066, .F. ) ;
#256262=DIRECTION ( 'NONE',  ( 0.000000000000000000, 0.9126074666063660468, 0.4088369013363524762 ) ) ;
#256273=ORIENTED_EDGE ( 'NONE', *, *, #62321, .T. ) ;
#256275=CARTESIAN_POINT ( 'NONE',  ( 22.47071067811865319, 33.41224047107334627, -242.5462774987836667 ) ) ;
#256279=CARTESIAN_POINT ( 'NONE',  ( 18.59999999999999076, 43.16354019706792400, -239.5695141926698284 ) ) ;
#256306=CARTESIAN_POINT ( 'NONE',  ( 22.60000000000000142, 25.89494711235935043, -254.2627752153468350 ) ) ;
#256317=DIRECTION ( 'NONE',  ( 0.000000000000000000, -0.8103668758649578141, 0.5859227990963212784 ) ) ;
#256333=CARTESIAN_POINT ( 'NONE',  ( 20.94999999999999929, 63.58084468663284383, -237.4904741118237723 ) ) ;
#256370=DIRECTION ( 'NONE',  ( 9.044546369203339308E-15, 0.9165223833629894123, -0.3999834006488590110 ) ) ;
#256393=CARTESIAN_POINT ( 'NONE',  ( -22.39999999999999858, 31.94635157770351341, -238.7871412784868994 ) ) ;
#256413=DIRECTION ( 'NONE',  ( 0.000000000000000000, -0.9126074666069882158, -0.4088369013349636427 ) ) ;
#256416=CARTESIAN_POINT ( 'NONE',  ( -21.05000000000000071, 38.08698097766499302, -236.1457910985472779 ) ) ;
#256429=CARTESIAN_POINT ( 'NONE',  ( 20.85000000000000142, 67.65998959290219261, -227.8609496483021530 ) ) ;
#256437=CARTESIAN_POINT ( 'NONE',  ( 21.14999999999999503, 25.97741635855165754, -254.4468634167653249 ) ) ;
#256440=FACE_OUTER_BOUND ( 'NONE', #18114, .T. ) ;
#256447=CARTESIAN_POINT ( 'NONE',  ( -18.54260524012568823, 77.31769039854688685, -241.8823842174727474 ) ) ;
#256468=AXIS2_PLACEMENT_3D ( 'NONE', #122691, #26149, #164371 ) ;
#256491=CARTESIAN_POINT ( 'NONE',  ( -20.94999999999999929, 43.48442877397276618, -245.2193771921251084 ) ) ;
#256496=DIRECTION ( 'NONE',  ( 0.000000000000000000, 0.8689845192018014197, -0.4948392722769828778 ) ) ;
#256503=CARTESIAN_POINT ( 'NONE',  ( 20.94999999999999929, 44.15903683684981473, -236.5744930507153185 ) ) ;
#256510=CARTESIAN_POINT ( 'NONE',  ( -21.14999999999999503, 38.16955627025379982, -235.9992222486930302 ) ) ;
#256515=AXIS2_PLACEMENT_3D ( 'NONE', #40231, #257907, #95035 ) ;
#256532=AXIS2_PLACEMENT_3D ( 'NONE', #151364, #74413, #229600 ) ;
#256569=CARTESIAN_POINT ( 'NONE',  ( -23.25000000000000000, 74.83412143252222393, -233.7087995678629966 ) ) ;
#256581=CARTESIAN_POINT ( 'NONE',  ( -23.25000000000000000, 67.23127455305835554, -235.8551265064784559 ) ) ;
#256600=CARTESIAN_POINT ( 'NONE',  ( 20.94999999999999929, 64.58471289989986985, -237.0407535203538316 ) ) ;
#256621=EDGE_CURVE ( 'NONE', #104983, #222021, #213913, .T. ) ;
#256629=DIRECTION ( 'NONE',  ( 0.000000000000000000, -0.9126074666063660468, -0.4088369013363524762 ) ) ;
#256639=DIRECTION ( 'NONE',  ( 0.000000000000000000, 0.9061079809440786281, 0.4230464831072883181 ) ) ;
#256645=VECTOR ( 'NONE', #156941, 1000.000000000000114 ) ;
#256655=DIRECTION ( 'NONE',  ( 1.000000000000000000, 8.623019343401618085E-17, 8.389849937938898203E-16 ) ) ;
#256664=DIRECTION ( 'NONE',  ( 0.000000000000000000, -0.8103668758649578141, 0.5859227990963212784 ) ) ;
#256670=ORIENTED_EDGE ( 'NONE', *, *, #44948, .F. ) ;
#256671=DIRECTION ( 'NONE',  ( 0.000000000000000000, 0.9126074666063769270, 0.4088369013363282733 ) ) ;
#256676=DIRECTION ( 'NONE',  ( 0.000000000000000000, 0.9126074666063844765, 0.4088369013363114535 ) ) ;
#256689=DIRECTION ( 'NONE',  ( 0.000000000000000000, 0.9126074666063660468, 0.4088369013363524762 ) ) ;
#256695=DIRECTION ( 'NONE',  ( 1.000000000000000000, -1.207181226542539700E-16, 2.694675058168174199E-16 ) ) ;
#256709=CARTESIAN_POINT ( 'NONE',  ( -20.94999999999999929, 68.00366762990589109, -224.2307594727497815 ) ) ;
#256756=ADVANCED_FACE ( 'NONE', ( #251539 ), #213697, .T. ) ;
#256775=CARTESIAN_POINT ( 'NONE',  ( -23.25000000000000000, 77.26488334054519669, -241.9697969554615611 ) ) ;
#256791=AXIS2_PLACEMENT_3D ( 'NONE', #20711, #140629, #239746 ) ;
#256818=( GEOMETRIC_REPRESENTATION_CONTEXT ( 3 ) GLOBAL_UNCERTAINTY_ASSIGNED_CONTEXT ( ( #53263 ) ) GLOBAL_UNIT_ASSIGNED_CONTEXT ( ( #55069, #151665, #75952 ) ) REPRESENTATION_CONTEXT ( 'NONE', 'WORKASPACE' ) );
#256823=VERTEX_POINT ( 'NONE', #212437 ) ;
#256866=CARTESIAN_POINT ( 'NONE',  ( -21.05000000000000071, 43.52285900727589762, -245.0935880436369985 ) ) ;
#256867=ORIENTED_EDGE ( 'NONE', *, *, #104417, .F. ) ;
#256883=VERTEX_POINT ( 'NONE', #203119 ) ;
#256885=ADVANCED_FACE ( 'NONE', ( #182291 ), #40230, .F. ) ;
#256889=ADVANCED_FACE ( 'NONE', ( #45331 ), #83132, .T. ) ;
#256900=CARTESIAN_POINT ( 'NONE',  ( -23.15000000000000213, 42.98415524044399660, -233.9519173640447889 ) ) ;
#256978=ORIENTED_EDGE ( 'NONE', *, *, #12817, .F. ) ;
#256982=ORIENTED_EDGE ( 'NONE', *, *, #117250, .F. ) ;
#257024=ORIENTED_EDGE ( 'NONE', *, *, #252511, .F. ) ;
#257055=DIRECTION ( 'NONE',  ( 0.000000000000000000, -0.9126074666063773710, -0.4088369013363274962 ) ) ;
#257061=AXIS2_PLACEMENT_3D ( 'NONE', #137130, #197083, #234947 ) ;
#257079=AXIS2_PLACEMENT_3D ( 'NONE', #215847, #39832, #237989 ) ;
#257112=DIRECTION ( 'NONE',  ( 1.000000000000000000, -1.335000415235278971E-16, 2.979993593738921214E-16 ) ) ;
#257133=CYLINDRICAL_SURFACE ( 'NONE', #246749, 0.1000000000000024342 ) ;
#257152=SPHERICAL_SURFACE ( 'NONE', #138375, 0.1000000000000000056 ) ;
#257194=DIRECTION ( 'NONE',  ( 1.000000000000000000, 6.834672213024256725E-16, -4.941700349840507066E-16 ) ) ;
#257214=CIRCLE ( 'NONE', #82450, 0.2000000000000048683 ) ;
#257237=ORIENTED_EDGE ( 'NONE', *, *, #70675, .F. ) ;
#257261=DIRECTION ( 'NONE',  ( 1.000000000000000000, 0.000000000000000000, -0.000000000000000000 ) ) ;
#257264=ORIENTED_EDGE ( 'NONE', *, *, #256244, .F. ) ;
#257297=VECTOR ( 'NONE', #190125, 1000.000000000000114 ) ;
#257316=CARTESIAN_POINT ( 'NONE',  ( 18.57071067811864040, 51.98142472962693716, -231.5327994178193762 ) ) ;
#257343=LINE ( 'NONE', #81301, #119407 ) ;
#257377=CARTESIAN_POINT ( 'NONE',  ( 20.94999999999999929, 49.57218508014540959, -254.1759139559835035 ) ) ;
#257415=DIRECTION ( 'NONE',  ( 0.000000000000000000, -0.9126074666063660468, -0.4088369013363524762 ) ) ;
#257439=VECTOR ( 'NONE', #66207, 1000.000000000000000 ) ;
#257440=DIRECTION ( 'NONE',  ( 0.000000000000000000, -0.7203564749500950271, 0.6936040289657154911 ) ) ;
#257490=AXIS2_PLACEMENT_3D ( 'NONE', #1599, #141133, #2876 ) ;
#257528=FILL_AREA_STYLE ('',( #41140 ) ) ;
#257548=ORIENTED_EDGE ( 'NONE', *, *, #211785, .F. ) ;
#257551=DIRECTION ( 'NONE',  ( 0.000000000000000000, 0.4088369013363281068, -0.9126074666063770380 ) ) ;
#257556=TOROIDAL_SURFACE ( 'NONE', #57870, 3.899999999999999467, 0.1000000000000000056 ) ;
#257563=CARTESIAN_POINT ( 'NONE',  ( 22.47809213839789066, 26.01172523223769417, -254.2798450918986646 ) ) ;
#257572=DIRECTION ( 'NONE',  ( 1.000000000000000000, 0.000000000000000000, 0.000000000000000000 ) ) ;
#257635=CARTESIAN_POINT ( 'NONE',  ( 20.77526135991786660, 40.73566841623622281, -237.9374812591170780 ) ) ;
#257658=ORIENTED_EDGE ( 'NONE', *, *, #72392, .F. ) ;
#257664=VERTEX_POINT ( 'NONE', #3985 ) ;
#257700=CARTESIAN_POINT ( 'NONE',  ( -23.15000000000000213, 47.91013932883114990, -242.3192343197862044 ) ) ;
#257708=ORIENTED_EDGE ( 'NONE', *, *, #247649, .F. ) ;
#257723=CARTESIAN_POINT ( 'NONE',  ( -22.49072729836730389, 26.00394800917974436, -254.2625701408315990 ) ) ;
#257744=CARTESIAN_POINT ( 'NONE',  ( -18.46154800491015990, 77.18277205392021756, -241.7850219657576076 ) ) ;
#257745=CARTESIAN_POINT ( 'NONE',  ( 22.39999999999999503, 26.02743912001966464, -254.3139371321002216 ) ) ;
#257746=ADVANCED_FACE ( 'NONE', ( #152521 ), #53385, .T. ) ;
#257752=ORIENTED_EDGE ( 'NONE', *, *, #32853, .F. ) ;
#257772=EDGE_CURVE ( 'NONE', #168498, #228584, #96339, .T. ) ;
#257777=DIRECTION ( 'NONE',  ( 0.000000000000000000, 0.9126074666063777041, 0.4088369013363267190 ) ) ;
#257791=ADVANCED_FACE ( 'NONE', ( #158930 ), #55925, .F. ) ;
#257808=CIRCLE ( 'NONE', #245406, 0.4999999999999944489 ) ;
#257822=DIRECTION ( 'NONE',  ( 0.000000000000000000, 0.4088369013363281623, -0.9126074666063771490 ) ) ;
#257830=DIRECTION ( 'NONE',  ( 0.000000000000000000, 0.4088369013363345461, -0.9126074666063741514 ) ) ;
#257832=ORIENTED_EDGE ( 'NONE', *, *, #228064, .T. ) ;
#257845=AXIS2_PLACEMENT_3D ( 'NONE', #85566, #167744, #226376 ) ;
#257907=DIRECTION ( 'NONE',  ( 0.000000000000000000, -0.9126074666063771490, -0.4088369013363281623 ) ) ;
#257909=CIRCLE ( 'NONE', #20660, 2.000000000000001776 ) ;
#257927=DIRECTION ( 'NONE',  ( 0.000000000000000000, -0.9126074666063770380, -0.4088369013363281068 ) ) ;
#257945=VECTOR ( 'NONE', #156720, 1000.000000000000000 ) ;
#257967=CARTESIAN_POINT ( 'NONE',  ( 23.14999999999999503, 56.06656052939784729, -228.0911609752645290 ) ) ;
#257973=ADVANCED_FACE ( 'NONE', ( #181055 ), #185429, .F. ) ;
#257976=AXIS2_PLACEMENT_3D ( 'NONE', #168627, #128166, #70785 ) ;
#257977=ORIENTED_EDGE ( 'NONE', *, *, #254736, .F. ) ;
#257992=CIRCLE ( 'NONE', #87332, 11.65000000000000213 ) ;
#258041=DIRECTION ( 'NONE',  ( 0.000000000000000000, 0.8490545835447252943, 0.5283051335749948674 ) ) ;
#258063=VERTEX_POINT ( 'NONE', #166642 ) ;
#258070=ORIENTED_EDGE ( 'NONE', *, *, #169557, .F. ) ;
#258072=CARTESIAN_POINT ( 'NONE',  ( -20.85000000000000142, 67.23127455305835554, -235.8551265064784559 ) ) ;
#258076=DIRECTION ( 'NONE',  ( 0.000000000000000000, -0.9126074666063660468, -0.4088369013363524762 ) ) ;
#258081=EDGE_LOOP ( 'NONE', ( #27715, #30260, #3320, #84804 ) ) ;
#258093=CARTESIAN_POINT ( 'NONE',  ( -20.64999999999999858, 46.19206980365409265, -240.6234452366647076 ) ) ;
ENDSEC;
END-ISO-10303-21;
